ISO-10303-21;
HEADER;
/* Generated by software containing ST-Developer
 * from STEP Tools, Inc. (www.steptools.com) 
 */

FILE_DESCRIPTION(
/* description */ ('Independent30mm screw-fed quill/spindle unit with16mm straight tool s
ocket, radial set screw, native reusable open ball bearings, retained 
inner/outer race stacks, keyed quill guide and M12x1.75 fine feed. Ext
ernal moving drive and tool not included. Ideal cage orbital links; in
dividual ball spin, force and preload not simulated. No drilling capac
ity, runout, speed, torque, load, life or machine safety rating.'),
/* implementation_level */ '2;1');

FILE_NAME(
/* name */ 'Feed screw.step',
/* time_stamp */ '2026-11-08T18:59:42-08:00',
/* author */ (''),
/* organization */ (''),
/* preprocessor_version */ 'ST-DEVELOPER v20.2',
/* originating_system */ 'Autodesk Translation Framework v15.17.0.0',
/* authorisation */ '');

FILE_SCHEMA (('AUTOMOTIVE_DESIGN { 1 0 10303 214 3 1 1 }'));
ENDSEC;

DATA;
#10=MECHANICAL_DESIGN_GEOMETRIC_PRESENTATION_REPRESENTATION('',(#1599),#63898);
#238=CONICAL_SURFACE('',#16469,5.5,0.785398163397448);
#260=B_SPLINE_SURFACE_WITH_KNOTS('',3,3,((#53360,#53361,#53362,#53363,#53364,
#53365,#53366,#53367,#53368,#53369,#53370,#53371,#53372,#53373,#53374,#53375,
#53376,#53377,#53378,#53379,#53380,#53381,#53382,#53383,#53384,#53385,#53386,
#53387,#53388,#53389,#53390,#53391,#53392,#53393,#53394,#53395,#53396,#53397,
#53398,#53399,#53400,#53401,#53402,#53403,#53404,#53405,#53406,#53407,#53408,
#53409,#53410,#53411,#53412,#53413,#53414,#53415,#53416,#53417,#53418,#53419,
#53420,#53421,#53422,#53423,#53424,#53425,#53426,#53427,#53428,#53429,#53430,
#53431,#53432,#53433,#53434,#53435,#53436,#53437,#53438,#53439,#53440,#53441,
#53442,#53443,#53444,#53445,#53446,#53447,#53448,#53449,#53450,#53451,#53452,
#53453,#53454,#53455,#53456,#53457,#53458,#53459,#53460,#53461,#53462,#53463,
#53464,#53465,#53466,#53467,#53468,#53469,#53470,#53471,#53472,#53473,#53474,
#53475,#53476,#53477,#53478,#53479,#53480,#53481,#53482,#53483,#53484,#53485,
#53486,#53487,#53488,#53489,#53490,#53491,#53492,#53493,#53494,#53495,#53496,
#53497,#53498,#53499,#53500,#53501,#53502,#53503,#53504,#53505,#53506,#53507,
#53508,#53509,#53510,#53511,#53512,#53513,#53514,#53515,#53516,#53517,#53518,
#53519,#53520,#53521,#53522,#53523,#53524,#53525,#53526,#53527,#53528,#53529,
#53530,#53531,#53532,#53533,#53534,#53535,#53536,#53537,#53538,#53539,#53540,
#53541,#53542,#53543,#53544,#53545,#53546,#53547,#53548,#53549,#53550,#53551,
#53552,#53553,#53554,#53555,#53556,#53557,#53558,#53559,#53560,#53561,#53562,
#53563,#53564,#53565,#53566,#53567,#53568,#53569,#53570,#53571,#53572,#53573,
#53574,#53575,#53576,#53577,#53578,#53579,#53580,#53581,#53582,#53583,#53584,
#53585,#53586,#53587,#53588,#53589,#53590,#53591,#53592,#53593,#53594,#53595,
#53596,#53597,#53598,#53599,#53600,#53601,#53602,#53603,#53604,#53605,#53606,
#53607,#53608,#53609,#53610,#53611,#53612,#53613,#53614,#53615,#53616,#53617,
#53618,#53619,#53620,#53621,#53622,#53623,#53624,#53625,#53626,#53627,#53628,
#53629,#53630,#53631,#53632,#53633,#53634,#53635,#53636,#53637,#53638,#53639,
#53640,#53641,#53642,#53643,#53644,#53645,#53646,#53647,#53648,#53649,#53650,
#53651,#53652,#53653,#53654,#53655,#53656,#53657,#53658,#53659,#53660,#53661,
#53662,#53663,#53664,#53665,#53666,#53667,#53668,#53669,#53670,#53671,#53672,
#53673,#53674,#53675,#53676,#53677,#53678,#53679,#53680,#53681,#53682,#53683,
#53684,#53685,#53686,#53687,#53688,#53689,#53690,#53691,#53692,#53693,#53694,
#53695,#53696,#53697,#53698,#53699,#53700,#53701,#53702,#53703,#53704,#53705,
#53706,#53707,#53708,#53709,#53710,#53711,#53712,#53713,#53714,#53715,#53716,
#53717,#53718,#53719,#53720,#53721,#53722,#53723,#53724,#53725,#53726,#53727,
#53728,#53729,#53730,#53731,#53732,#53733,#53734,#53735,#53736,#53737,#53738,
#53739,#53740,#53741,#53742,#53743,#53744,#53745,#53746,#53747,#53748,#53749,
#53750,#53751,#53752,#53753,#53754,#53755,#53756,#53757,#53758,#53759,#53760,
#53761,#53762,#53763,#53764,#53765,#53766,#53767,#53768,#53769,#53770,#53771,
#53772,#53773,#53774,#53775,#53776,#53777,#53778,#53779,#53780,#53781,#53782,
#53783,#53784,#53785,#53786,#53787,#53788,#53789,#53790,#53791,#53792,#53793,
#53794,#53795,#53796,#53797,#53798,#53799,#53800,#53801,#53802,#53803,#53804,
#53805,#53806,#53807,#53808,#53809,#53810,#53811,#53812,#53813,#53814,#53815,
#53816,#53817,#53818,#53819,#53820,#53821,#53822,#53823,#53824,#53825,#53826,
#53827,#53828,#53829,#53830,#53831,#53832,#53833,#53834,#53835,#53836,#53837,
#53838,#53839,#53840,#53841,#53842,#53843,#53844,#53845,#53846,#53847,#53848,
#53849,#53850,#53851,#53852,#53853,#53854,#53855,#53856,#53857,#53858,#53859,
#53860,#53861,#53862,#53863,#53864,#53865,#53866,#53867),(#53868,#53869,
#53870,#53871,#53872,#53873,#53874,#53875,#53876,#53877,#53878,#53879,#53880,
#53881,#53882,#53883,#53884,#53885,#53886,#53887,#53888,#53889,#53890,#53891,
#53892,#53893,#53894,#53895,#53896,#53897,#53898,#53899,#53900,#53901,#53902,
#53903,#53904,#53905,#53906,#53907,#53908,#53909,#53910,#53911,#53912,#53913,
#53914,#53915,#53916,#53917,#53918,#53919,#53920,#53921,#53922,#53923,#53924,
#53925,#53926,#53927,#53928,#53929,#53930,#53931,#53932,#53933,#53934,#53935,
#53936,#53937,#53938,#53939,#53940,#53941,#53942,#53943,#53944,#53945,#53946,
#53947,#53948,#53949,#53950,#53951,#53952,#53953,#53954,#53955,#53956,#53957,
#53958,#53959,#53960,#53961,#53962,#53963,#53964,#53965,#53966,#53967,#53968,
#53969,#53970,#53971,#53972,#53973,#53974,#53975,#53976,#53977,#53978,#53979,
#53980,#53981,#53982,#53983,#53984,#53985,#53986,#53987,#53988,#53989,#53990,
#53991,#53992,#53993,#53994,#53995,#53996,#53997,#53998,#53999,#54000,#54001,
#54002,#54003,#54004,#54005,#54006,#54007,#54008,#54009,#54010,#54011,#54012,
#54013,#54014,#54015,#54016,#54017,#54018,#54019,#54020,#54021,#54022,#54023,
#54024,#54025,#54026,#54027,#54028,#54029,#54030,#54031,#54032,#54033,#54034,
#54035,#54036,#54037,#54038,#54039,#54040,#54041,#54042,#54043,#54044,#54045,
#54046,#54047,#54048,#54049,#54050,#54051,#54052,#54053,#54054,#54055,#54056,
#54057,#54058,#54059,#54060,#54061,#54062,#54063,#54064,#54065,#54066,#54067,
#54068,#54069,#54070,#54071,#54072,#54073,#54074,#54075,#54076,#54077,#54078,
#54079,#54080,#54081,#54082,#54083,#54084,#54085,#54086,#54087,#54088,#54089,
#54090,#54091,#54092,#54093,#54094,#54095,#54096,#54097,#54098,#54099,#54100,
#54101,#54102,#54103,#54104,#54105,#54106,#54107,#54108,#54109,#54110,#54111,
#54112,#54113,#54114,#54115,#54116,#54117,#54118,#54119,#54120,#54121,#54122,
#54123,#54124,#54125,#54126,#54127,#54128,#54129,#54130,#54131,#54132,#54133,
#54134,#54135,#54136,#54137,#54138,#54139,#54140,#54141,#54142,#54143,#54144,
#54145,#54146,#54147,#54148,#54149,#54150,#54151,#54152,#54153,#54154,#54155,
#54156,#54157,#54158,#54159,#54160,#54161,#54162,#54163,#54164,#54165,#54166,
#54167,#54168,#54169,#54170,#54171,#54172,#54173,#54174,#54175,#54176,#54177,
#54178,#54179,#54180,#54181,#54182,#54183,#54184,#54185,#54186,#54187,#54188,
#54189,#54190,#54191,#54192,#54193,#54194,#54195,#54196,#54197,#54198,#54199,
#54200,#54201,#54202,#54203,#54204,#54205,#54206,#54207,#54208,#54209,#54210,
#54211,#54212,#54213,#54214,#54215,#54216,#54217,#54218,#54219,#54220,#54221,
#54222,#54223,#54224,#54225,#54226,#54227,#54228,#54229,#54230,#54231,#54232,
#54233,#54234,#54235,#54236,#54237,#54238,#54239,#54240,#54241,#54242,#54243,
#54244,#54245,#54246,#54247,#54248,#54249,#54250,#54251,#54252,#54253,#54254,
#54255,#54256,#54257,#54258,#54259,#54260,#54261,#54262,#54263,#54264,#54265,
#54266,#54267,#54268,#54269,#54270,#54271,#54272,#54273,#54274,#54275,#54276,
#54277,#54278,#54279,#54280,#54281,#54282,#54283,#54284,#54285,#54286,#54287,
#54288,#54289,#54290,#54291,#54292,#54293,#54294,#54295,#54296,#54297,#54298,
#54299,#54300,#54301,#54302,#54303,#54304,#54305,#54306,#54307,#54308,#54309,
#54310,#54311,#54312,#54313,#54314,#54315,#54316,#54317,#54318,#54319,#54320,
#54321,#54322,#54323,#54324,#54325,#54326,#54327,#54328,#54329,#54330,#54331,
#54332,#54333,#54334,#54335,#54336,#54337,#54338,#54339,#54340,#54341,#54342,
#54343,#54344,#54345,#54346,#54347,#54348,#54349,#54350,#54351,#54352,#54353,
#54354,#54355,#54356,#54357,#54358,#54359,#54360,#54361,#54362,#54363,#54364,
#54365,#54366,#54367,#54368,#54369,#54370,#54371,#54372,#54373,#54374,#54375),
(#54376,#54377,#54378,#54379,#54380,#54381,#54382,#54383,#54384,#54385,
#54386,#54387,#54388,#54389,#54390,#54391,#54392,#54393,#54394,#54395,#54396,
#54397,#54398,#54399,#54400,#54401,#54402,#54403,#54404,#54405,#54406,#54407,
#54408,#54409,#54410,#54411,#54412,#54413,#54414,#54415,#54416,#54417,#54418,
#54419,#54420,#54421,#54422,#54423,#54424,#54425,#54426,#54427,#54428,#54429,
#54430,#54431,#54432,#54433,#54434,#54435,#54436,#54437,#54438,#54439,#54440,
#54441,#54442,#54443,#54444,#54445,#54446,#54447,#54448,#54449,#54450,#54451,
#54452,#54453,#54454,#54455,#54456,#54457,#54458,#54459,#54460,#54461,#54462,
#54463,#54464,#54465,#54466,#54467,#54468,#54469,#54470,#54471,#54472,#54473,
#54474,#54475,#54476,#54477,#54478,#54479,#54480,#54481,#54482,#54483,#54484,
#54485,#54486,#54487,#54488,#54489,#54490,#54491,#54492,#54493,#54494,#54495,
#54496,#54497,#54498,#54499,#54500,#54501,#54502,#54503,#54504,#54505,#54506,
#54507,#54508,#54509,#54510,#54511,#54512,#54513,#54514,#54515,#54516,#54517,
#54518,#54519,#54520,#54521,#54522,#54523,#54524,#54525,#54526,#54527,#54528,
#54529,#54530,#54531,#54532,#54533,#54534,#54535,#54536,#54537,#54538,#54539,
#54540,#54541,#54542,#54543,#54544,#54545,#54546,#54547,#54548,#54549,#54550,
#54551,#54552,#54553,#54554,#54555,#54556,#54557,#54558,#54559,#54560,#54561,
#54562,#54563,#54564,#54565,#54566,#54567,#54568,#54569,#54570,#54571,#54572,
#54573,#54574,#54575,#54576,#54577,#54578,#54579,#54580,#54581,#54582,#54583,
#54584,#54585,#54586,#54587,#54588,#54589,#54590,#54591,#54592,#54593,#54594,
#54595,#54596,#54597,#54598,#54599,#54600,#54601,#54602,#54603,#54604,#54605,
#54606,#54607,#54608,#54609,#54610,#54611,#54612,#54613,#54614,#54615,#54616,
#54617,#54618,#54619,#54620,#54621,#54622,#54623,#54624,#54625,#54626,#54627,
#54628,#54629,#54630,#54631,#54632,#54633,#54634,#54635,#54636,#54637,#54638,
#54639,#54640,#54641,#54642,#54643,#54644,#54645,#54646,#54647,#54648,#54649,
#54650,#54651,#54652,#54653,#54654,#54655,#54656,#54657,#54658,#54659,#54660,
#54661,#54662,#54663,#54664,#54665,#54666,#54667,#54668,#54669,#54670,#54671,
#54672,#54673,#54674,#54675,#54676,#54677,#54678,#54679,#54680,#54681,#54682,
#54683,#54684,#54685,#54686,#54687,#54688,#54689,#54690,#54691,#54692,#54693,
#54694,#54695,#54696,#54697,#54698,#54699,#54700,#54701,#54702,#54703,#54704,
#54705,#54706,#54707,#54708,#54709,#54710,#54711,#54712,#54713,#54714,#54715,
#54716,#54717,#54718,#54719,#54720,#54721,#54722,#54723,#54724,#54725,#54726,
#54727,#54728,#54729,#54730,#54731,#54732,#54733,#54734,#54735,#54736,#54737,
#54738,#54739,#54740,#54741,#54742,#54743,#54744,#54745,#54746,#54747,#54748,
#54749,#54750,#54751,#54752,#54753,#54754,#54755,#54756,#54757,#54758,#54759,
#54760,#54761,#54762,#54763,#54764,#54765,#54766,#54767,#54768,#54769,#54770,
#54771,#54772,#54773,#54774,#54775,#54776,#54777,#54778,#54779,#54780,#54781,
#54782,#54783,#54784,#54785,#54786,#54787,#54788,#54789,#54790,#54791,#54792,
#54793,#54794,#54795,#54796,#54797,#54798,#54799,#54800,#54801,#54802,#54803,
#54804,#54805,#54806,#54807,#54808,#54809,#54810,#54811,#54812,#54813,#54814,
#54815,#54816,#54817,#54818,#54819,#54820,#54821,#54822,#54823,#54824,#54825,
#54826,#54827,#54828,#54829,#54830,#54831,#54832,#54833,#54834,#54835,#54836,
#54837,#54838,#54839,#54840,#54841,#54842,#54843,#54844,#54845,#54846,#54847,
#54848,#54849,#54850,#54851,#54852,#54853,#54854,#54855,#54856,#54857,#54858,
#54859,#54860,#54861,#54862,#54863,#54864,#54865,#54866,#54867,#54868,#54869,
#54870,#54871,#54872,#54873,#54874,#54875,#54876,#54877,#54878,#54879,#54880,
#54881,#54882,#54883),(#54884,#54885,#54886,#54887,#54888,#54889,#54890,
#54891,#54892,#54893,#54894,#54895,#54896,#54897,#54898,#54899,#54900,#54901,
#54902,#54903,#54904,#54905,#54906,#54907,#54908,#54909,#54910,#54911,#54912,
#54913,#54914,#54915,#54916,#54917,#54918,#54919,#54920,#54921,#54922,#54923,
#54924,#54925,#54926,#54927,#54928,#54929,#54930,#54931,#54932,#54933,#54934,
#54935,#54936,#54937,#54938,#54939,#54940,#54941,#54942,#54943,#54944,#54945,
#54946,#54947,#54948,#54949,#54950,#54951,#54952,#54953,#54954,#54955,#54956,
#54957,#54958,#54959,#54960,#54961,#54962,#54963,#54964,#54965,#54966,#54967,
#54968,#54969,#54970,#54971,#54972,#54973,#54974,#54975,#54976,#54977,#54978,
#54979,#54980,#54981,#54982,#54983,#54984,#54985,#54986,#54987,#54988,#54989,
#54990,#54991,#54992,#54993,#54994,#54995,#54996,#54997,#54998,#54999,#55000,
#55001,#55002,#55003,#55004,#55005,#55006,#55007,#55008,#55009,#55010,#55011,
#55012,#55013,#55014,#55015,#55016,#55017,#55018,#55019,#55020,#55021,#55022,
#55023,#55024,#55025,#55026,#55027,#55028,#55029,#55030,#55031,#55032,#55033,
#55034,#55035,#55036,#55037,#55038,#55039,#55040,#55041,#55042,#55043,#55044,
#55045,#55046,#55047,#55048,#55049,#55050,#55051,#55052,#55053,#55054,#55055,
#55056,#55057,#55058,#55059,#55060,#55061,#55062,#55063,#55064,#55065,#55066,
#55067,#55068,#55069,#55070,#55071,#55072,#55073,#55074,#55075,#55076,#55077,
#55078,#55079,#55080,#55081,#55082,#55083,#55084,#55085,#55086,#55087,#55088,
#55089,#55090,#55091,#55092,#55093,#55094,#55095,#55096,#55097,#55098,#55099,
#55100,#55101,#55102,#55103,#55104,#55105,#55106,#55107,#55108,#55109,#55110,
#55111,#55112,#55113,#55114,#55115,#55116,#55117,#55118,#55119,#55120,#55121,
#55122,#55123,#55124,#55125,#55126,#55127,#55128,#55129,#55130,#55131,#55132,
#55133,#55134,#55135,#55136,#55137,#55138,#55139,#55140,#55141,#55142,#55143,
#55144,#55145,#55146,#55147,#55148,#55149,#55150,#55151,#55152,#55153,#55154,
#55155,#55156,#55157,#55158,#55159,#55160,#55161,#55162,#55163,#55164,#55165,
#55166,#55167,#55168,#55169,#55170,#55171,#55172,#55173,#55174,#55175,#55176,
#55177,#55178,#55179,#55180,#55181,#55182,#55183,#55184,#55185,#55186,#55187,
#55188,#55189,#55190,#55191,#55192,#55193,#55194,#55195,#55196,#55197,#55198,
#55199,#55200,#55201,#55202,#55203,#55204,#55205,#55206,#55207,#55208,#55209,
#55210,#55211,#55212,#55213,#55214,#55215,#55216,#55217,#55218,#55219,#55220,
#55221,#55222,#55223,#55224,#55225,#55226,#55227,#55228,#55229,#55230,#55231,
#55232,#55233,#55234,#55235,#55236,#55237,#55238,#55239,#55240,#55241,#55242,
#55243,#55244,#55245,#55246,#55247,#55248,#55249,#55250,#55251,#55252,#55253,
#55254,#55255,#55256,#55257,#55258,#55259,#55260,#55261,#55262,#55263,#55264,
#55265,#55266,#55267,#55268,#55269,#55270,#55271,#55272,#55273,#55274,#55275,
#55276,#55277,#55278,#55279,#55280,#55281,#55282,#55283,#55284,#55285,#55286,
#55287,#55288,#55289,#55290,#55291,#55292,#55293,#55294,#55295,#55296,#55297,
#55298,#55299,#55300,#55301,#55302,#55303,#55304,#55305,#55306,#55307,#55308,
#55309,#55310,#55311,#55312,#55313,#55314,#55315,#55316,#55317,#55318,#55319,
#55320,#55321,#55322,#55323,#55324,#55325,#55326,#55327,#55328,#55329,#55330,
#55331,#55332,#55333,#55334,#55335,#55336,#55337,#55338,#55339,#55340,#55341,
#55342,#55343,#55344,#55345,#55346,#55347,#55348,#55349,#55350,#55351,#55352,
#55353,#55354,#55355,#55356,#55357,#55358,#55359,#55360,#55361,#55362,#55363,
#55364,#55365,#55366,#55367,#55368,#55369,#55370,#55371,#55372,#55373,#55374,
#55375,#55376,#55377,#55378,#55379,#55380,#55381,#55382,#55383,#55384,#55385,
#55386,#55387,#55388,#55389,#55390,#55391)),.UNSPECIFIED.,.F.,.F.,.F.,(4,
4),(4,1,1,1,1,1,1,1,1,1,1,1,1,1,1,1,1,1,1,1,1,1,1,1,1,1,1,1,1,1,1,1,1,1,
1,1,1,1,1,1,1,1,1,1,1,1,1,1,1,1,1,1,1,1,1,1,1,1,1,1,1,1,1,1,1,1,1,1,1,1,
1,1,1,1,1,1,1,1,1,1,1,1,1,1,1,1,1,1,1,1,1,1,1,1,1,1,1,1,1,1,1,1,1,1,1,1,
1,1,1,1,1,1,1,1,1,1,1,1,1,1,1,1,1,1,1,1,1,1,1,1,1,1,1,1,1,1,1,1,1,1,1,1,
1,1,1,1,1,1,1,1,1,1,1,1,1,1,1,1,1,1,1,1,1,1,1,1,1,1,1,1,1,1,1,1,1,1,1,1,
1,1,1,1,1,1,1,1,1,1,1,1,1,1,1,1,1,1,1,1,1,1,1,1,1,1,1,1,1,1,1,1,1,1,1,1,
1,1,1,1,1,1,1,1,1,1,1,1,1,1,1,1,1,1,1,1,1,1,1,1,1,1,1,1,1,1,1,1,1,1,1,1,
1,1,1,1,1,1,1,1,1,1,1,1,1,1,1,1,1,1,1,1,1,1,1,1,1,1,1,1,1,1,1,1,1,1,1,1,
1,1,1,1,1,1,1,1,1,1,1,1,1,1,1,1,1,1,1,1,1,1,1,1,1,1,1,1,1,1,1,1,1,1,1,1,
1,1,1,1,1,1,1,1,1,1,1,1,1,1,1,1,1,1,1,1,1,1,1,1,1,1,1,1,1,1,1,1,1,1,1,1,
1,1,1,1,1,1,1,1,1,1,1,1,1,1,1,1,1,1,1,1,1,1,1,1,1,1,1,1,1,1,1,1,1,1,1,1,
1,1,1,1,1,1,1,1,1,1,1,1,1,1,1,1,1,1,1,1,1,1,1,1,1,1,1,1,1,1,1,1,1,1,1,1,
1,1,1,1,1,1,1,1,1,1,1,1,1,1,1,1,1,1,1,1,1,1,1,1,1,1,1,1,1,1,1,1,1,1,1,1,
1,1,1,1,1,1,1,1,1,1,1,1,1,1,1,1,1,1,1,1,1,1,1,1,1,1,1,1,1,1,1,1,1,1,1,1,
1,1,1,4),(0.,0.115296848757168),(10.2062663725606,10.7060917058189,11.2059170390771,
12.2055677055937,13.2052183721102,14.2048690386268,15.2045197051434,16.2041703716599,
17.2038210381765,18.203471704693,19.2031223712096,20.2027730377261,21.2024237042427,
22.2020743707592,23.2017250372758,24.2013757037923,25.2010263703089,26.2006770368254,
27.200327703342,28.1999783698585,29.1996290363751,30.1992797028916,31.1989303694082,
32.1985810359247,33.1982317024413,34.1978823689578,35.1975330354744,36.1971837019909,
37.1968343685075,38.196485035024,39.1961357015406,40.1957863680571,41.1954370345737,
42.1950877010902,43.1947383676068,44.1943890341233,45.1940397006399,46.1936903671564,
47.193341033673,48.1929917001895,49.1926423667061,50.1922930332226,51.1919436997392,
52.1915943662557,53.1912450327723,54.1908956992888,55.1905463658054,56.1901970323219,
57.1898476988385,58.189498365355,59.1891490318716,60.1887996983882,61.1884503649047,
62.1881010314213,63.1877516979378,64.1874023644544,65.1870530309709,66.1867036974875,
67.186354364004,68.1860050305206,69.1856556970371,70.1853063635537,71.1849570300702,
72.1846076965868,73.1842583631033,74.1839090296199,75.1835596961364,76.183210362653,
77.1828610291695,78.1825116956861,79.1821623622026,80.1818130287192,81.1814636952357,
82.1811143617523,83.1807650282688,84.1804156947854,85.1800663613019,86.1797170278185,
87.179367694335,88.1790183608516,89.1786690273681,90.1783196938847,91.1779703604012,
92.1776210269178,93.1772716934343,94.1769223599509,95.1765730264674,96.176223692984,
97.1758743595006,98.1755250260171,99.1751756925336,100.17482635905,101.174477025567,
102.174127692083,103.1737783586,104.173429025116,105.173079691633,106.17273035815,
107.172381024666,108.172031691183,109.171682357699,110.171333024216,111.170983690732,
112.170634357249,113.170285023765,114.169935690282,115.169586356798,116.169237023315,
117.168887689832,118.168538356348,119.168189022865,120.167839689381,121.167490355898,
122.167141022414,123.166791688931,124.166442355447,125.166093021964,126.165743688481,
127.165394354997,128.165045021514,129.16469568803,130.164346354547,131.163997021063,
132.16364768758,133.163298354096,134.162949020613,135.16259968713,136.162250353646,
137.161901020163,138.161551686679,139.161202353196,140.160853019712,141.160503686229,
142.160154352745,143.159805019262,144.159455685778,145.159106352295,146.158757018812,
147.158407685328,148.158058351845,149.157709018361,150.157359684878,151.157010351394,
152.156661017911,153.156311684427,154.155962350944,155.155613017461,156.155263683977,
157.154914350494,158.15456501701,159.154215683527,160.153866350043,161.15351701656,
162.153167683076,163.152818349593,164.152469016109,165.152119682626,166.151770349143,
167.151421015659,168.151071682176,169.150722348692,170.150373015209,171.150023681725,
172.149674348242,173.149325014758,174.148975681275,175.148626347792,176.148277014308,
177.147927680825,178.147578347341,179.147229013858,180.146879680374,181.146530346891,
182.146181013407,183.145831679924,184.145482346441,185.145133012957,186.144783679474,
187.14443434599,188.144085012507,189.143735679023,190.14338634554,191.143037012056,
192.142687678573,193.142338345089,194.141989011606,195.141639678123,196.141290344639,
197.140941011156,198.140591677672,199.140242344189,200.139893010705,201.139543677222,
202.139194343738,203.138845010255,204.138495676772,205.138146343288,206.137797009805,
207.137447676321,208.137098342838,209.136749009354,210.136399675871,211.136050342387,
212.135701008904,213.135351675421,214.135002341937,215.134653008454,216.13430367497,
217.133954341487,218.133605008003,219.13325567452,220.132906341036,221.132557007553,
222.132207674069,223.131858340586,224.131509007103,225.131159673619,226.130810340136,
227.130461006652,228.130111673169,229.129762339685,230.129413006202,231.129063672718,
232.128714339235,233.128365005752,234.128015672268,235.127666338785,236.127317005301,
237.126967671818,238.126618338334,239.126269004851,240.125919671367,241.125570337884,
242.1252210044,243.124871670917,244.124522337434,245.12417300395,246.123823670467,
247.123474336983,248.1231250035,249.122775670016,250.122426336533,251.122077003049,
252.121727669566,253.121378336083,254.121029002599,255.120679669116,256.120330335632,
257.119981002149,258.119631668665,259.119282335182,260.118933001698,261.118583668215,
262.118234334731,263.117885001248,264.117535667765,265.117186334281,266.116837000798,
267.116487667314,268.116138333831,269.115789000347,270.115439666864,271.11509033338,
272.114740999897,273.114391666414,274.11404233293,275.113692999447,276.113343665963,
277.11299433248,278.112644998996,279.112295665513,280.111946332029,281.111596998546,
282.111247665063,283.110898331579,284.110548998096,285.110199664612,286.109850331129,
287.109500997645,288.109151664162,289.108802330678,290.108452997195,291.108103663712,
292.107754330228,293.107404996745,294.107055663261,295.106706329778,296.106356996294,
297.106007662811,298.105658329327,299.105308995844,300.10495966236,301.104610328877,
302.104260995394,303.10391166191,304.103562328427,305.103212994943,306.10286366146,
307.102514327976,308.102164994493,309.101815661009,310.101466327526,311.101116994043,
312.100767660559,313.100418327076,314.100068993592,315.099719660109,316.099370326625,
317.099020993142,318.098671659658,319.098322326175,320.097972992691,321.097623659208,
322.097274325725,323.096924992241,324.096575658758,325.096226325274,326.095876991791,
327.095527658307,328.095178324824,329.09482899134,330.094479657857,331.094130324374,
332.09378099089,333.093431657407,334.093082323923,335.09273299044,336.092383656956,
337.092034323473,338.091684989989,339.091335656506,340.090986323022,341.090636989539,
342.090287656056,343.089938322572,344.089588989089,345.089239655605,346.088890322122,
347.088540988638,348.088191655155,349.087842321671,350.087492988188,351.087143654705,
352.086794321221,353.086444987738,354.086095654254,355.085746320771,356.085396987287,
357.085047653804,358.08469832032,359.084348986837,360.083999653354,361.08365031987,
362.083300986387,363.082951652903,364.08260231942,365.082252985936,366.081903652453,
367.081554318969,368.081204985486,369.080855652002,370.080506318519,371.080156985036,
372.079807651552,373.079458318069,374.079108984585,375.078759651102,376.078410317618,
377.078060984135,378.077711650651,379.077362317168,380.077012983685,381.076663650201,
382.076314316718,383.075964983234,384.075615649751,385.075266316267,386.074916982784,
387.0745676493,388.074218315817,389.073868982334,390.07351964885,391.073170315367,
392.072820981883,393.0724716484,394.072122314916,395.071772981433,396.071423647949,
397.071074314466,398.070724980982,399.070375647499,400.070026314016,401.069676980532,
402.069327647049,403.068978313565,404.068628980082,405.068279646598,406.067930313115,
407.067580979631,408.067231646148,409.066882312665,410.066532979181,411.066183645698,
412.065834312214,413.065484978731,414.065135645247,415.064786311764,416.06443697828,
417.064087644797,418.063738311314,419.06338897783,420.063039644347,421.062690310863,
422.06234097738,423.061991643896,424.061642310413,425.061292976929,426.060943643446,
427.060594309962,428.060244976479,429.059895642996,430.059546309512,431.059196976029,
432.058847642545,433.058498309062,434.058148975578,435.057799642095,436.057450308611,
437.057100975128,438.056751641645,439.056402308161,440.056052974678,441.055703641194,
442.055354307711,443.055004974227,444.054655640744,445.05430630726,446.053956973777,
447.053607640293,448.05325830681,449.052908973327,450.052559639843,451.05221030636,
452.051860972876,453.051511639393,454.051162305909,455.050812972426,456.050463638942,
457.050114305459,458.049764971976,459.049415638492,460.049066305009,461.048716971525,
462.048367638042,463.048018304558,464.047668971075,465.047319637591,466.046970304108,
467.046620970625,468.046271637141,469.045922303658,470.045572970174,471.045223636691,
472.044874303207,473.044524969724,474.04417563624,475.043826302757,476.043476969273,
477.04312763579,478.042778302307,479.042428968823,480.04207963534,481.041730301856,
482.041380968373,483.041031634889,484.040682301406,485.040332967922,486.039983634439,
487.039634300956,488.039284967472,489.038935633989,490.038586300505,491.038236967022,
492.037887633538,493.037538300055,494.037188966571,495.036839633088,496.036490299605,
497.036140966121,498.035791632638,499.035442299154,500.035092965671,501.034743632187,
502.034394298704,503.03404496522,504.033695631737,505.033346298253,506.03299696477,
507.032647631287,508.032298297803,509.03194896432,510.031599630836,511.031250297353,
512.030900963869,512.530726297128,513.030551630386),.UNSPECIFIED.);
#261=B_SPLINE_SURFACE_WITH_KNOTS('',3,3,((#55434,#55435,#55436,#55437,#55438,
#55439,#55440,#55441,#55442,#55443,#55444,#55445,#55446,#55447,#55448,#55449,
#55450,#55451,#55452,#55453,#55454,#55455,#55456,#55457,#55458,#55459,#55460,
#55461,#55462,#55463,#55464,#55465,#55466,#55467,#55468,#55469,#55470,#55471,
#55472,#55473,#55474,#55475,#55476,#55477,#55478,#55479,#55480,#55481,#55482,
#55483,#55484,#55485,#55486,#55487,#55488,#55489,#55490,#55491,#55492,#55493,
#55494,#55495,#55496,#55497,#55498,#55499,#55500,#55501,#55502,#55503,#55504,
#55505,#55506,#55507,#55508,#55509,#55510,#55511,#55512,#55513,#55514,#55515,
#55516,#55517,#55518,#55519,#55520,#55521,#55522,#55523,#55524,#55525,#55526,
#55527,#55528,#55529,#55530,#55531,#55532,#55533,#55534,#55535,#55536,#55537,
#55538,#55539,#55540,#55541,#55542,#55543,#55544,#55545,#55546,#55547,#55548,
#55549,#55550,#55551,#55552,#55553,#55554,#55555,#55556,#55557,#55558,#55559,
#55560,#55561,#55562,#55563,#55564,#55565,#55566,#55567,#55568,#55569,#55570,
#55571,#55572,#55573,#55574,#55575,#55576,#55577,#55578,#55579,#55580,#55581,
#55582,#55583,#55584,#55585,#55586,#55587,#55588,#55589,#55590,#55591,#55592,
#55593,#55594,#55595,#55596,#55597,#55598,#55599,#55600,#55601,#55602,#55603,
#55604,#55605,#55606,#55607,#55608,#55609,#55610,#55611,#55612,#55613,#55614,
#55615,#55616,#55617,#55618,#55619,#55620,#55621,#55622,#55623,#55624,#55625,
#55626,#55627,#55628,#55629,#55630,#55631,#55632,#55633,#55634,#55635,#55636,
#55637,#55638,#55639,#55640,#55641,#55642,#55643,#55644,#55645,#55646,#55647,
#55648,#55649,#55650,#55651,#55652,#55653,#55654,#55655,#55656,#55657,#55658,
#55659,#55660,#55661,#55662,#55663,#55664,#55665,#55666,#55667,#55668,#55669,
#55670,#55671,#55672,#55673,#55674,#55675,#55676,#55677,#55678,#55679,#55680,
#55681,#55682,#55683,#55684,#55685,#55686,#55687,#55688,#55689,#55690,#55691,
#55692,#55693,#55694,#55695,#55696,#55697,#55698,#55699,#55700,#55701,#55702,
#55703,#55704,#55705,#55706,#55707,#55708,#55709,#55710,#55711,#55712,#55713,
#55714,#55715,#55716,#55717,#55718,#55719,#55720,#55721,#55722,#55723,#55724,
#55725,#55726,#55727,#55728,#55729,#55730,#55731,#55732,#55733,#55734,#55735,
#55736,#55737,#55738,#55739,#55740,#55741,#55742,#55743,#55744,#55745,#55746,
#55747,#55748,#55749,#55750,#55751,#55752,#55753,#55754,#55755,#55756,#55757,
#55758,#55759,#55760,#55761,#55762,#55763,#55764,#55765,#55766,#55767,#55768,
#55769,#55770,#55771,#55772,#55773,#55774,#55775,#55776,#55777,#55778,#55779,
#55780,#55781,#55782,#55783,#55784,#55785,#55786,#55787,#55788,#55789,#55790,
#55791,#55792,#55793,#55794,#55795,#55796,#55797,#55798,#55799,#55800,#55801,
#55802,#55803,#55804,#55805,#55806,#55807,#55808,#55809,#55810,#55811,#55812,
#55813,#55814,#55815,#55816,#55817,#55818,#55819,#55820,#55821,#55822,#55823,
#55824,#55825,#55826,#55827,#55828,#55829,#55830,#55831,#55832,#55833,#55834,
#55835,#55836,#55837,#55838,#55839,#55840,#55841,#55842,#55843,#55844,#55845,
#55846,#55847,#55848,#55849,#55850,#55851,#55852,#55853,#55854,#55855,#55856,
#55857,#55858,#55859,#55860,#55861,#55862,#55863,#55864,#55865,#55866,#55867,
#55868,#55869,#55870,#55871,#55872,#55873,#55874,#55875,#55876,#55877,#55878,
#55879,#55880,#55881,#55882,#55883,#55884,#55885,#55886,#55887,#55888,#55889,
#55890,#55891,#55892,#55893,#55894,#55895,#55896,#55897,#55898,#55899,#55900,
#55901,#55902,#55903,#55904,#55905,#55906,#55907,#55908,#55909,#55910,#55911,
#55912,#55913,#55914,#55915,#55916,#55917,#55918,#55919,#55920,#55921,#55922,
#55923,#55924,#55925,#55926,#55927,#55928,#55929,#55930,#55931,#55932,#55933,
#55934,#55935,#55936,#55937,#55938,#55939,#55940,#55941,#55942,#55943),
(#55944,#55945,#55946,#55947,#55948,#55949,#55950,#55951,#55952,#55953,
#55954,#55955,#55956,#55957,#55958,#55959,#55960,#55961,#55962,#55963,#55964,
#55965,#55966,#55967,#55968,#55969,#55970,#55971,#55972,#55973,#55974,#55975,
#55976,#55977,#55978,#55979,#55980,#55981,#55982,#55983,#55984,#55985,#55986,
#55987,#55988,#55989,#55990,#55991,#55992,#55993,#55994,#55995,#55996,#55997,
#55998,#55999,#56000,#56001,#56002,#56003,#56004,#56005,#56006,#56007,#56008,
#56009,#56010,#56011,#56012,#56013,#56014,#56015,#56016,#56017,#56018,#56019,
#56020,#56021,#56022,#56023,#56024,#56025,#56026,#56027,#56028,#56029,#56030,
#56031,#56032,#56033,#56034,#56035,#56036,#56037,#56038,#56039,#56040,#56041,
#56042,#56043,#56044,#56045,#56046,#56047,#56048,#56049,#56050,#56051,#56052,
#56053,#56054,#56055,#56056,#56057,#56058,#56059,#56060,#56061,#56062,#56063,
#56064,#56065,#56066,#56067,#56068,#56069,#56070,#56071,#56072,#56073,#56074,
#56075,#56076,#56077,#56078,#56079,#56080,#56081,#56082,#56083,#56084,#56085,
#56086,#56087,#56088,#56089,#56090,#56091,#56092,#56093,#56094,#56095,#56096,
#56097,#56098,#56099,#56100,#56101,#56102,#56103,#56104,#56105,#56106,#56107,
#56108,#56109,#56110,#56111,#56112,#56113,#56114,#56115,#56116,#56117,#56118,
#56119,#56120,#56121,#56122,#56123,#56124,#56125,#56126,#56127,#56128,#56129,
#56130,#56131,#56132,#56133,#56134,#56135,#56136,#56137,#56138,#56139,#56140,
#56141,#56142,#56143,#56144,#56145,#56146,#56147,#56148,#56149,#56150,#56151,
#56152,#56153,#56154,#56155,#56156,#56157,#56158,#56159,#56160,#56161,#56162,
#56163,#56164,#56165,#56166,#56167,#56168,#56169,#56170,#56171,#56172,#56173,
#56174,#56175,#56176,#56177,#56178,#56179,#56180,#56181,#56182,#56183,#56184,
#56185,#56186,#56187,#56188,#56189,#56190,#56191,#56192,#56193,#56194,#56195,
#56196,#56197,#56198,#56199,#56200,#56201,#56202,#56203,#56204,#56205,#56206,
#56207,#56208,#56209,#56210,#56211,#56212,#56213,#56214,#56215,#56216,#56217,
#56218,#56219,#56220,#56221,#56222,#56223,#56224,#56225,#56226,#56227,#56228,
#56229,#56230,#56231,#56232,#56233,#56234,#56235,#56236,#56237,#56238,#56239,
#56240,#56241,#56242,#56243,#56244,#56245,#56246,#56247,#56248,#56249,#56250,
#56251,#56252,#56253,#56254,#56255,#56256,#56257,#56258,#56259,#56260,#56261,
#56262,#56263,#56264,#56265,#56266,#56267,#56268,#56269,#56270,#56271,#56272,
#56273,#56274,#56275,#56276,#56277,#56278,#56279,#56280,#56281,#56282,#56283,
#56284,#56285,#56286,#56287,#56288,#56289,#56290,#56291,#56292,#56293,#56294,
#56295,#56296,#56297,#56298,#56299,#56300,#56301,#56302,#56303,#56304,#56305,
#56306,#56307,#56308,#56309,#56310,#56311,#56312,#56313,#56314,#56315,#56316,
#56317,#56318,#56319,#56320,#56321,#56322,#56323,#56324,#56325,#56326,#56327,
#56328,#56329,#56330,#56331,#56332,#56333,#56334,#56335,#56336,#56337,#56338,
#56339,#56340,#56341,#56342,#56343,#56344,#56345,#56346,#56347,#56348,#56349,
#56350,#56351,#56352,#56353,#56354,#56355,#56356,#56357,#56358,#56359,#56360,
#56361,#56362,#56363,#56364,#56365,#56366,#56367,#56368,#56369,#56370,#56371,
#56372,#56373,#56374,#56375,#56376,#56377,#56378,#56379,#56380,#56381,#56382,
#56383,#56384,#56385,#56386,#56387,#56388,#56389,#56390,#56391,#56392,#56393,
#56394,#56395,#56396,#56397,#56398,#56399,#56400,#56401,#56402,#56403,#56404,
#56405,#56406,#56407,#56408,#56409,#56410,#56411,#56412,#56413,#56414,#56415,
#56416,#56417,#56418,#56419,#56420,#56421,#56422,#56423,#56424,#56425,#56426,
#56427,#56428,#56429,#56430,#56431,#56432,#56433,#56434,#56435,#56436,#56437,
#56438,#56439,#56440,#56441,#56442,#56443,#56444,#56445,#56446,#56447,#56448,
#56449,#56450,#56451,#56452,#56453),(#56454,#56455,#56456,#56457,#56458,
#56459,#56460,#56461,#56462,#56463,#56464,#56465,#56466,#56467,#56468,#56469,
#56470,#56471,#56472,#56473,#56474,#56475,#56476,#56477,#56478,#56479,#56480,
#56481,#56482,#56483,#56484,#56485,#56486,#56487,#56488,#56489,#56490,#56491,
#56492,#56493,#56494,#56495,#56496,#56497,#56498,#56499,#56500,#56501,#56502,
#56503,#56504,#56505,#56506,#56507,#56508,#56509,#56510,#56511,#56512,#56513,
#56514,#56515,#56516,#56517,#56518,#56519,#56520,#56521,#56522,#56523,#56524,
#56525,#56526,#56527,#56528,#56529,#56530,#56531,#56532,#56533,#56534,#56535,
#56536,#56537,#56538,#56539,#56540,#56541,#56542,#56543,#56544,#56545,#56546,
#56547,#56548,#56549,#56550,#56551,#56552,#56553,#56554,#56555,#56556,#56557,
#56558,#56559,#56560,#56561,#56562,#56563,#56564,#56565,#56566,#56567,#56568,
#56569,#56570,#56571,#56572,#56573,#56574,#56575,#56576,#56577,#56578,#56579,
#56580,#56581,#56582,#56583,#56584,#56585,#56586,#56587,#56588,#56589,#56590,
#56591,#56592,#56593,#56594,#56595,#56596,#56597,#56598,#56599,#56600,#56601,
#56602,#56603,#56604,#56605,#56606,#56607,#56608,#56609,#56610,#56611,#56612,
#56613,#56614,#56615,#56616,#56617,#56618,#56619,#56620,#56621,#56622,#56623,
#56624,#56625,#56626,#56627,#56628,#56629,#56630,#56631,#56632,#56633,#56634,
#56635,#56636,#56637,#56638,#56639,#56640,#56641,#56642,#56643,#56644,#56645,
#56646,#56647,#56648,#56649,#56650,#56651,#56652,#56653,#56654,#56655,#56656,
#56657,#56658,#56659,#56660,#56661,#56662,#56663,#56664,#56665,#56666,#56667,
#56668,#56669,#56670,#56671,#56672,#56673,#56674,#56675,#56676,#56677,#56678,
#56679,#56680,#56681,#56682,#56683,#56684,#56685,#56686,#56687,#56688,#56689,
#56690,#56691,#56692,#56693,#56694,#56695,#56696,#56697,#56698,#56699,#56700,
#56701,#56702,#56703,#56704,#56705,#56706,#56707,#56708,#56709,#56710,#56711,
#56712,#56713,#56714,#56715,#56716,#56717,#56718,#56719,#56720,#56721,#56722,
#56723,#56724,#56725,#56726,#56727,#56728,#56729,#56730,#56731,#56732,#56733,
#56734,#56735,#56736,#56737,#56738,#56739,#56740,#56741,#56742,#56743,#56744,
#56745,#56746,#56747,#56748,#56749,#56750,#56751,#56752,#56753,#56754,#56755,
#56756,#56757,#56758,#56759,#56760,#56761,#56762,#56763,#56764,#56765,#56766,
#56767,#56768,#56769,#56770,#56771,#56772,#56773,#56774,#56775,#56776,#56777,
#56778,#56779,#56780,#56781,#56782,#56783,#56784,#56785,#56786,#56787,#56788,
#56789,#56790,#56791,#56792,#56793,#56794,#56795,#56796,#56797,#56798,#56799,
#56800,#56801,#56802,#56803,#56804,#56805,#56806,#56807,#56808,#56809,#56810,
#56811,#56812,#56813,#56814,#56815,#56816,#56817,#56818,#56819,#56820,#56821,
#56822,#56823,#56824,#56825,#56826,#56827,#56828,#56829,#56830,#56831,#56832,
#56833,#56834,#56835,#56836,#56837,#56838,#56839,#56840,#56841,#56842,#56843,
#56844,#56845,#56846,#56847,#56848,#56849,#56850,#56851,#56852,#56853,#56854,
#56855,#56856,#56857,#56858,#56859,#56860,#56861,#56862,#56863,#56864,#56865,
#56866,#56867,#56868,#56869,#56870,#56871,#56872,#56873,#56874,#56875,#56876,
#56877,#56878,#56879,#56880,#56881,#56882,#56883,#56884,#56885,#56886,#56887,
#56888,#56889,#56890,#56891,#56892,#56893,#56894,#56895,#56896,#56897,#56898,
#56899,#56900,#56901,#56902,#56903,#56904,#56905,#56906,#56907,#56908,#56909,
#56910,#56911,#56912,#56913,#56914,#56915,#56916,#56917,#56918,#56919,#56920,
#56921,#56922,#56923,#56924,#56925,#56926,#56927,#56928,#56929,#56930,#56931,
#56932,#56933,#56934,#56935,#56936,#56937,#56938,#56939,#56940,#56941,#56942,
#56943,#56944,#56945,#56946,#56947,#56948,#56949,#56950,#56951,#56952,#56953,
#56954,#56955,#56956,#56957,#56958,#56959,#56960,#56961,#56962,#56963),
(#56964,#56965,#56966,#56967,#56968,#56969,#56970,#56971,#56972,#56973,
#56974,#56975,#56976,#56977,#56978,#56979,#56980,#56981,#56982,#56983,#56984,
#56985,#56986,#56987,#56988,#56989,#56990,#56991,#56992,#56993,#56994,#56995,
#56996,#56997,#56998,#56999,#57000,#57001,#57002,#57003,#57004,#57005,#57006,
#57007,#57008,#57009,#57010,#57011,#57012,#57013,#57014,#57015,#57016,#57017,
#57018,#57019,#57020,#57021,#57022,#57023,#57024,#57025,#57026,#57027,#57028,
#57029,#57030,#57031,#57032,#57033,#57034,#57035,#57036,#57037,#57038,#57039,
#57040,#57041,#57042,#57043,#57044,#57045,#57046,#57047,#57048,#57049,#57050,
#57051,#57052,#57053,#57054,#57055,#57056,#57057,#57058,#57059,#57060,#57061,
#57062,#57063,#57064,#57065,#57066,#57067,#57068,#57069,#57070,#57071,#57072,
#57073,#57074,#57075,#57076,#57077,#57078,#57079,#57080,#57081,#57082,#57083,
#57084,#57085,#57086,#57087,#57088,#57089,#57090,#57091,#57092,#57093,#57094,
#57095,#57096,#57097,#57098,#57099,#57100,#57101,#57102,#57103,#57104,#57105,
#57106,#57107,#57108,#57109,#57110,#57111,#57112,#57113,#57114,#57115,#57116,
#57117,#57118,#57119,#57120,#57121,#57122,#57123,#57124,#57125,#57126,#57127,
#57128,#57129,#57130,#57131,#57132,#57133,#57134,#57135,#57136,#57137,#57138,
#57139,#57140,#57141,#57142,#57143,#57144,#57145,#57146,#57147,#57148,#57149,
#57150,#57151,#57152,#57153,#57154,#57155,#57156,#57157,#57158,#57159,#57160,
#57161,#57162,#57163,#57164,#57165,#57166,#57167,#57168,#57169,#57170,#57171,
#57172,#57173,#57174,#57175,#57176,#57177,#57178,#57179,#57180,#57181,#57182,
#57183,#57184,#57185,#57186,#57187,#57188,#57189,#57190,#57191,#57192,#57193,
#57194,#57195,#57196,#57197,#57198,#57199,#57200,#57201,#57202,#57203,#57204,
#57205,#57206,#57207,#57208,#57209,#57210,#57211,#57212,#57213,#57214,#57215,
#57216,#57217,#57218,#57219,#57220,#57221,#57222,#57223,#57224,#57225,#57226,
#57227,#57228,#57229,#57230,#57231,#57232,#57233,#57234,#57235,#57236,#57237,
#57238,#57239,#57240,#57241,#57242,#57243,#57244,#57245,#57246,#57247,#57248,
#57249,#57250,#57251,#57252,#57253,#57254,#57255,#57256,#57257,#57258,#57259,
#57260,#57261,#57262,#57263,#57264,#57265,#57266,#57267,#57268,#57269,#57270,
#57271,#57272,#57273,#57274,#57275,#57276,#57277,#57278,#57279,#57280,#57281,
#57282,#57283,#57284,#57285,#57286,#57287,#57288,#57289,#57290,#57291,#57292,
#57293,#57294,#57295,#57296,#57297,#57298,#57299,#57300,#57301,#57302,#57303,
#57304,#57305,#57306,#57307,#57308,#57309,#57310,#57311,#57312,#57313,#57314,
#57315,#57316,#57317,#57318,#57319,#57320,#57321,#57322,#57323,#57324,#57325,
#57326,#57327,#57328,#57329,#57330,#57331,#57332,#57333,#57334,#57335,#57336,
#57337,#57338,#57339,#57340,#57341,#57342,#57343,#57344,#57345,#57346,#57347,
#57348,#57349,#57350,#57351,#57352,#57353,#57354,#57355,#57356,#57357,#57358,
#57359,#57360,#57361,#57362,#57363,#57364,#57365,#57366,#57367,#57368,#57369,
#57370,#57371,#57372,#57373,#57374,#57375,#57376,#57377,#57378,#57379,#57380,
#57381,#57382,#57383,#57384,#57385,#57386,#57387,#57388,#57389,#57390,#57391,
#57392,#57393,#57394,#57395,#57396,#57397,#57398,#57399,#57400,#57401,#57402,
#57403,#57404,#57405,#57406,#57407,#57408,#57409,#57410,#57411,#57412,#57413,
#57414,#57415,#57416,#57417,#57418,#57419,#57420,#57421,#57422,#57423,#57424,
#57425,#57426,#57427,#57428,#57429,#57430,#57431,#57432,#57433,#57434,#57435,
#57436,#57437,#57438,#57439,#57440,#57441,#57442,#57443,#57444,#57445,#57446,
#57447,#57448,#57449,#57450,#57451,#57452,#57453,#57454,#57455,#57456,#57457,
#57458,#57459,#57460,#57461,#57462,#57463,#57464,#57465,#57466,#57467,#57468,
#57469,#57470,#57471,#57472,#57473)),.UNSPECIFIED.,.F.,.F.,.F.,(4,4),(4,
1,1,1,1,1,1,1,1,1,1,1,1,1,1,1,1,1,1,1,1,1,1,1,1,1,1,1,1,1,1,1,1,1,1,1,1,
1,1,1,1,1,1,1,1,1,1,1,1,1,1,1,1,1,1,1,1,1,1,1,1,1,1,1,1,1,1,1,1,1,1,1,1,
1,1,1,1,1,1,1,1,1,1,1,1,1,1,1,1,1,1,1,1,1,1,1,1,1,1,1,1,1,1,1,1,1,1,1,1,
1,1,1,1,1,1,1,1,1,1,1,1,1,1,1,1,1,1,1,1,1,1,1,1,1,1,1,1,1,1,1,1,1,1,1,1,
1,1,1,1,1,1,1,1,1,1,1,1,1,1,1,1,1,1,1,1,1,1,1,1,1,1,1,1,1,1,1,1,1,1,1,1,
1,1,1,1,1,1,1,1,1,1,1,1,1,1,1,1,1,1,1,1,1,1,1,1,1,1,1,1,1,1,1,1,1,1,1,1,
1,1,1,1,1,1,1,1,1,1,1,1,1,1,1,1,1,1,1,1,1,1,1,1,1,1,1,1,1,1,1,1,1,1,1,1,
1,1,1,1,1,1,1,1,1,1,1,1,1,1,1,1,1,1,1,1,1,1,1,1,1,1,1,1,1,1,1,1,1,1,1,1,
1,1,1,1,1,1,1,1,1,1,1,1,1,1,1,1,1,1,1,1,1,1,1,1,1,1,1,1,1,1,1,1,1,1,1,1,
1,1,1,1,1,1,1,1,1,1,1,1,1,1,1,1,1,1,1,1,1,1,1,1,1,1,1,1,1,1,1,1,1,1,1,1,
1,1,1,1,1,1,1,1,1,1,1,1,1,1,1,1,1,1,1,1,1,1,1,1,1,1,1,1,1,1,1,1,1,1,1,1,
1,1,1,1,1,1,1,1,1,1,1,1,1,1,1,1,1,1,1,1,1,1,1,1,1,1,1,1,1,1,1,1,1,1,1,1,
1,1,1,1,1,1,1,1,1,1,1,1,1,1,1,1,1,1,1,1,1,1,1,1,1,1,1,1,1,1,1,1,1,1,1,1,
1,1,1,1,1,1,1,1,1,1,1,1,1,1,1,1,1,1,1,1,1,1,1,1,1,1,1,1,1,1,1,1,1,1,1,1,
1,1,4),(0.,0.115296848757168),(11.6154215191118,12.1151488743229,12.6148762295339,
13.614330939956,14.6137856503781,15.6132403608002,16.6126950712223,17.6121497816443,
18.6116044920664,19.6110592024885,20.6105139129106,21.6099686233327,22.6094233337548,
23.6088780441768,24.6083327545989,25.607787465021,26.6072421754431,27.6066968858652,
28.6061515962873,29.6056063067094,30.6050610171314,31.6045157275535,32.6039704379756,
33.6034251483977,34.6028798588198,35.6023345692419,36.601789279664,37.601243990086,
38.6006987005081,39.6001534109302,40.5996081213523,41.5990628317744,42.5985175421965,
43.5979722526185,44.5974269630406,45.5968816734627,46.5963363838848,47.5957910943069,
48.595245804729,49.5947005151511,50.5941552255731,51.5936099359952,52.5930646464173,
53.5925193568394,54.5919740672615,55.5914287776836,56.5908834881057,57.5903381985277,
58.5897929089498,59.5892476193719,60.588702329794,61.5881570402161,62.5876117506382,
63.5870664610603,64.5865211714823,65.5859758819044,66.5854305923265,67.5848853027486,
68.5843400131707,69.5837947235928,70.5832494340148,71.5827041444369,72.582158854859,
73.5816135652811,74.5810682757032,75.5805229861253,76.5799776965474,77.5794324069694,
78.5788871173915,79.5783418278136,80.5777965382357,81.5772512486578,82.5767059590799,
83.5761606695019,84.575615379924,85.5750700903461,86.5745248007682,87.5739795111903,
88.5734342216124,89.5728889320345,90.5723436424566,91.5717983528786,92.5712530633007,
93.5707077737228,94.5701624841449,95.569617194567,96.5690719049891,97.5685266154111,
98.5679813258332,99.5674360362553,100.566890746677,101.566345457099,102.565800167522,
103.565254877944,104.564709588366,105.564164298788,106.56361900921,107.563073719632,
108.562528430054,109.561983140476,110.561437850898,111.56089256132,112.560347271742,
113.559801982165,114.559256692587,115.558711403009,116.558166113431,117.557620823853,
118.557075534275,119.556530244697,120.555984955119,121.555439665541,122.554894375963,
123.554349086385,124.553803796807,125.55325850723,126.552713217652,127.552167928074,
128.551622638496,129.551077348918,130.55053205934,131.549986769762,132.549441480184,
133.548896190606,134.548350901028,135.54780561145,136.547260321872,137.546715032295,
138.546169742717,139.545624453139,140.545079163561,141.544533873983,142.543988584405,
143.543443294827,144.542898005249,145.542352715671,146.541807426093,147.541262136515,
148.540716846937,149.54017155736,150.539626267782,151.539080978204,152.538535688626,
153.537990399048,154.53744510947,155.536899819892,156.536354530314,157.535809240736,
158.535263951158,159.53471866158,160.534173372003,161.533628082425,162.533082792847,
163.532537503269,164.531992213691,165.531446924113,166.530901634535,167.530356344957,
168.529811055379,169.529265765801,170.528720476223,171.528175186645,172.527629897068,
173.52708460749,174.526539317912,175.525994028334,176.525448738756,177.524903449178,
178.5243581596,179.523812870022,180.523267580444,181.522722290866,182.522177001288,
183.52163171171,184.521086422133,185.520541132555,186.519995842977,187.519450553399,
188.518905263821,189.518359974243,190.517814684665,191.517269395087,192.516724105509,
193.516178815931,194.515633526353,195.515088236775,196.514542947198,197.51399765762,
198.513452368042,199.512907078464,200.512361788886,201.511816499308,202.51127120973,
203.510725920152,204.510180630574,205.509635340996,206.509090051418,207.508544761841,
208.507999472263,209.507454182685,210.506908893107,211.506363603529,212.505818313951,
213.505273024373,214.504727734795,215.504182445217,216.503637155639,217.503091866061,
218.502546576483,219.502001286906,220.501455997328,221.50091070775,222.500365418172,
223.499820128594,224.499274839016,225.498729549438,226.49818425986,227.497638970282,
228.497093680704,229.496548391126,230.496003101548,231.495457811971,232.494912522393,
233.494367232815,234.493821943237,235.493276653659,236.492731364081,237.492186074503,
238.491640784925,239.491095495347,240.490550205769,241.490004916191,242.489459626613,
243.488914337036,244.488369047458,245.48782375788,246.487278468302,247.486733178724,
248.486187889146,249.485642599568,250.48509730999,251.484552020412,252.484006730834,
253.483461441256,254.482916151679,255.482370862101,256.481825572523,257.481280282945,
258.480734993367,259.480189703789,260.479644414211,261.479099124633,262.478553835055,
263.478008545477,264.477463255899,265.476917966321,266.476372676744,267.475827387166,
268.475282097588,269.47473680801,270.474191518432,271.473646228854,272.473100939276,
273.472555649698,274.47201036012,275.471465070542,276.470919780964,277.470374491386,
278.469829201809,279.469283912231,280.468738622653,281.468193333075,282.467648043497,
283.467102753919,284.466557464341,285.466012174763,286.465466885185,287.464921595607,
288.464376306029,289.463831016451,290.463285726874,291.462740437296,292.462195147718,
293.46164985814,294.461104568562,295.460559278984,296.460013989406,297.459468699828,
298.45892341025,299.458378120672,300.457832831094,301.457287541517,302.456742251939,
303.456196962361,304.455651672783,305.455106383205,306.454561093627,307.454015804049,
308.453470514471,309.452925224893,310.452379935315,311.451834645737,312.451289356159,
313.450744066582,314.450198777004,315.449653487426,316.449108197848,317.44856290827,
318.448017618692,319.447472329114,320.446927039536,321.446381749958,322.44583646038,
323.445291170802,324.444745881224,325.444200591647,326.443655302069,327.443110012491,
328.442564722913,329.442019433335,330.441474143757,331.440928854179,332.440383564601,
333.439838275023,334.439292985445,335.438747695867,336.438202406289,337.437657116712,
338.437111827134,339.436566537556,340.436021247978,341.4354759584,342.434930668822,
343.434385379244,344.433840089666,345.433294800088,346.43274951051,347.432204220932,
348.431658931354,349.431113641777,350.430568352199,351.430023062621,352.429477773043,
353.428932483465,354.428387193887,355.427841904309,356.427296614731,357.426751325153,
358.426206035575,359.425660745997,360.42511545642,361.424570166842,362.424024877264,
363.423479587686,364.422934298108,365.42238900853,366.421843718952,367.421298429374,
368.420753139796,369.420207850218,370.41966256064,371.419117271062,372.418571981485,
373.418026691907,374.417481402329,375.416936112751,376.416390823173,377.415845533595,
378.415300244017,379.414754954439,380.414209664861,381.413664375283,382.413119085705,
383.412573796127,384.41202850655,385.411483216972,386.410937927394,387.410392637816,
388.409847348238,389.40930205866,390.408756769082,391.408211479504,392.407666189926,
393.407120900348,394.40657561077,395.406030321192,396.405485031615,397.404939742037,
398.404394452459,399.403849162881,400.403303873303,401.402758583725,402.402213294147,
403.401668004569,404.401122714991,405.400577425413,406.400032135835,407.399486846258,
408.39894155668,409.398396267102,410.397850977524,411.397305687946,412.396760398368,
413.39621510879,414.395669819212,415.395124529634,416.394579240056,417.394033950478,
418.3934886609,419.392943371323,420.392398081745,421.391852792167,422.391307502589,
423.390762213011,424.390216923433,425.389671633855,426.389126344277,427.388581054699,
428.388035765121,429.387490475543,430.386945185965,431.386399896388,432.38585460681,
433.385309317232,434.384764027654,435.384218738076,436.383673448498,437.38312815892,
438.382582869342,439.382037579764,440.381492290186,441.380947000608,442.380401711031,
443.379856421453,444.379311131875,445.378765842297,446.378220552719,447.377675263141,
448.377129973563,449.376584683985,450.376039394407,451.375494104829,452.374948815251,
453.374403525673,454.373858236095,455.373312946518,456.37276765694,457.372222367362,
458.371677077784,459.371131788206,460.370586498628,461.37004120905,462.369495919472,
463.368950629894,464.368405340316,465.367860050738,466.367314761161,467.366769471583,
468.366224182005,469.365678892427,470.365133602849,471.364588313271,472.364043023693,
473.363497734115,474.362952444537,475.362407154959,476.361861865381,477.361316575803,
478.360771286226,479.360225996648,480.35968070707,481.359135417492,482.358590127914,
483.358044838336,484.357499548758,485.35695425918,486.356408969602,487.355863680024,
488.355318390446,489.354773100868,490.354227811291,491.353682521713,492.353137232135,
493.352591942557,494.352046652979,495.351501363401,496.350956073823,497.350410784245,
498.349865494667,499.349320205089,500.348774915511,501.348229625934,502.347684336356,
503.347139046778,504.3465937572,505.346048467622,506.345503178044,507.344957888466,
508.344412598888,509.34386730931,510.343322019732,511.342776730154,512.342231440576,
513.341686150999,514.341140861421,515.340595571843,515.840322927054,516.340050282265),
 .UNSPECIFIED.);
#1040=B_SPLINE_CURVE_WITH_KNOTS('',3,(#46845,#46846,#46847,#46848,#46849,
#46850,#46851,#46852,#46853,#46854,#46855,#46856,#46857,#46858,#46859,#46860,
#46861,#46862,#46863),.UNSPECIFIED.,.F.,.F.,(4,3,3,3,3,3,4),(-10.3757270560179,
-9.99454710422085,-8.99509239379876,-7.99563768337668,-6.9961829729546,
-5.99672826253251,-5.36129569184721),.UNSPECIFIED.);
#1041=B_SPLINE_CURVE_WITH_KNOTS('',3,(#46866,#46867,#46868,#46869,#46870,
#46871,#46872,#46873,#46874,#46875,#46876,#46877,#46878,#46879,#46880,#46881),
 .UNSPECIFIED.,.F.,.F.,(4,3,3,3,3,4),(3.29149150306132,3.89964483836103,
4.89929550487756,5.8989461713941,6.89859683791064,7.40204040071886),
 .UNSPECIFIED.);
#1042=B_SPLINE_CURVE_WITH_KNOTS('',3,(#46886,#46887,#46888,#46889,#46890,
#46891,#46892,#46893,#46894,#46895,#46896,#46897,#46898,#46899,#46900,#46901,
#46902,#46903,#46904,#46905,#46906,#46907),.UNSPECIFIED.,.F.,.F.,(4,3,3,
3,3,3,3,4),(-16.6589123631975,-15.9912753667534,-14.9918206563313,-13.9923659459092,
-12.9929112354871,-11.993456525065,-10.9940018146429,-10.3757270560179),
 .UNSPECIFIED.);
#1043=B_SPLINE_CURVE_WITH_KNOTS('',3,(#46908,#46909,#46910,#46911,#46912,
#46913,#46914,#46915,#46916,#46917,#46918,#46919,#46920,#46921,#46922,#46923,
#46924,#46925,#46926,#46927,#46928,#46929),.UNSPECIFIED.,.F.,.F.,(4,3,3,
3,3,3,3,4),(7.40204040071886,7.89824750442719,8.89789817094375,9.89754883746032,
10.8971995039769,11.8968501704934,12.89650083701,13.6852257078984),
 .UNSPECIFIED.);
#1044=B_SPLINE_CURVE_WITH_KNOTS('',3,(#46934,#46935,#46936,#46937,#46938,
#46939,#46940,#46941,#46942,#46943,#46944,#46945,#46946,#46947,#46948,#46949,
#46950,#46951,#46952,#46953,#46954,#46955),.UNSPECIFIED.,.F.,.F.,(4,3,3,
3,3,3,3,4),(-22.9420976703771,-21.9880036292859,-20.9885489188638,-19.9890942084417,
-18.9896394980196,-17.9901847875975,-16.9907300771754,-16.6589123631975),
 .UNSPECIFIED.);
#1045=B_SPLINE_CURVE_WITH_KNOTS('',3,(#46956,#46957,#46958,#46959,#46960,
#46961,#46962,#46963,#46964,#46965,#46966,#46967,#46968,#46969,#46970,#46971,
#46972,#46973,#46974,#46975,#46976,#46977,#46978,#46979,#46980),
 .UNSPECIFIED.,.F.,.F.,(4,3,3,3,3,3,3,3,4),(13.6852257078984,13.8961515035266,
14.8958021700431,15.8954528365597,16.8951035030762,17.8947541695928,18.8944048361093,
19.8940555026259,19.968411015078),.UNSPECIFIED.);
#1046=B_SPLINE_CURVE_WITH_KNOTS('',3,(#46985,#46986,#46987,#46988,#46989,
#46990,#46991,#46992,#46993,#46994,#46995,#46996,#46997,#46998,#46999,#47000,
#47001,#47002,#47003,#47004,#47005,#47006,#47007,#47008,#47009),
 .UNSPECIFIED.,.F.,.F.,(4,3,3,3,3,3,3,3,4),(-29.2252829775566,-28.9841866022405,
-27.9847318918184,-26.9852771813963,-25.9858224709742,-24.9863677605521,
-23.98691305013,-22.987458339708,-22.9420976703771),.UNSPECIFIED.);
#1047=B_SPLINE_CURVE_WITH_KNOTS('',3,(#47010,#47011,#47012,#47013,#47014,
#47015,#47016,#47017,#47018,#47019,#47020,#47021,#47022,#47023,#47024,#47025,
#47026,#47027,#47028,#47029,#47030,#47031),.UNSPECIFIED.,.F.,.F.,(4,3,3,
3,3,3,3,4),(19.968411015078,20.8937061691424,21.8933568356589,22.8930075021755,
23.892658168692,24.8923088352086,25.8919595017251,26.2515963222576),
 .UNSPECIFIED.);
#1048=B_SPLINE_CURVE_WITH_KNOTS('',3,(#47036,#47037,#47038,#47039,#47040,
#47041,#47042,#47043,#47044,#47045,#47046,#47047,#47048,#47049,#47050,#47051,
#47052,#47053,#47054,#47055,#47056,#47057),.UNSPECIFIED.,.F.,.F.,(4,3,3,
3,3,3,3,4),(-35.5084682847362,-34.980914864773,-33.9814601543509,-32.9820054439288,
-31.9825507335067,-30.9830960230846,-29.9836413126625,-29.2252829775566),
 .UNSPECIFIED.);
#1049=B_SPLINE_CURVE_WITH_KNOTS('',3,(#47058,#47059,#47060,#47061,#47062,
#47063,#47064,#47065,#47066,#47067,#47068,#47069,#47070,#47071,#47072,#47073,
#47074,#47075,#47076,#47077,#47078,#47079),.UNSPECIFIED.,.F.,.F.,(4,3,3,
3,3,3,3,4),(26.2515963222576,26.8916101682417,27.8912608347582,28.8909115012748,
29.8905621677914,30.8902128343079,31.8898635008245,32.5347816294372),
 .UNSPECIFIED.);
#1050=B_SPLINE_CURVE_WITH_KNOTS('',3,(#47084,#47085,#47086,#47087,#47088,
#47089,#47090,#47091,#47092,#47093,#47094,#47095,#47096,#47097,#47098,#47099,
#47100,#47101,#47102,#47103,#47104,#47105),.UNSPECIFIED.,.F.,.F.,(4,3,3,
3,3,3,3,4),(-41.7916535919158,-40.9776431273055,-39.9781884168834,-38.9787337064613,
-37.9792789960392,-36.9798242856171,-35.9803695751951,-35.5084682847362),
 .UNSPECIFIED.);
#1051=B_SPLINE_CURVE_WITH_KNOTS('',3,(#47106,#47107,#47108,#47109,#47110,
#47111,#47112,#47113,#47114,#47115,#47116,#47117,#47118,#47119,#47120,#47121,
#47122,#47123,#47124,#47125,#47126,#47127),.UNSPECIFIED.,.F.,.F.,(4,3,3,
3,3,3,3,4),(32.5347816294372,32.889514167341,33.8891648338576,34.8888155003741,
35.8884661668906,36.8881168334072,37.8877674999237,38.8179669366168),
 .UNSPECIFIED.);
#1052=B_SPLINE_CURVE_WITH_KNOTS('',3,(#47132,#47133,#47134,#47135,#47136,
#47137,#47138,#47139,#47140,#47141,#47142,#47143,#47144,#47145,#47146,#47147,
#47148,#47149,#47150,#47151,#47152,#47153,#47154,#47155,#47156),
 .UNSPECIFIED.,.F.,.F.,(4,3,3,3,3,3,3,3,4),(-48.0748388990954,-47.9738261002601,
-46.974371389838,-45.9749166794159,-44.9754619689938,-43.9760072585717,
-42.9765525481497,-41.9770978377276,-41.7916535919158),.UNSPECIFIED.);
#1053=B_SPLINE_CURVE_WITH_KNOTS('',3,(#47157,#47158,#47159,#47160,#47161,
#47162,#47163,#47164,#47165,#47166,#47167,#47168,#47169,#47170,#47171,#47172,
#47173,#47174,#47175,#47176,#47177,#47178,#47179,#47180,#47181),
 .UNSPECIFIED.,.F.,.F.,(4,3,3,3,3,3,3,3,4),(38.8179669366168,38.8874181664403,
39.8870688329568,40.8867194994734,41.8863701659899,42.8860208325065,43.8856714990231,
44.8853221655396,45.1011522437964),.UNSPECIFIED.);
#1054=B_SPLINE_CURVE_WITH_KNOTS('',3,(#47186,#47187,#47188,#47189,#47190,
#47191,#47192,#47193,#47194,#47195,#47196,#47197,#47198,#47199,#47200,#47201,
#47202,#47203,#47204,#47205,#47206,#47207),.UNSPECIFIED.,.F.,.F.,(4,3,3,
3,3,3,3,4),(-54.358024206275,-53.9705543627926,-52.9710996523705,-51.9716449419484,
-50.9721902315264,-49.9727355211043,-48.9732808106822,-48.0748388990954),
 .UNSPECIFIED.);
#1055=B_SPLINE_CURVE_WITH_KNOTS('',3,(#47208,#47209,#47210,#47211,#47212,
#47213,#47214,#47215,#47216,#47217,#47218,#47219,#47220,#47221,#47222,#47223,
#47224,#47225,#47226,#47227,#47228,#47229),.UNSPECIFIED.,.F.,.F.,(4,3,3,
3,3,3,3,4),(45.1011522437964,45.8849728320562,46.8846234985727,47.8842741650893,
48.8839248316058,49.8835754981223,50.8832261646389,51.384337550976),
 .UNSPECIFIED.);
#1056=B_SPLINE_CURVE_WITH_KNOTS('',3,(#47234,#47235,#47236,#47237,#47238,
#47239,#47240,#47241,#47242,#47243,#47244,#47245,#47246,#47247,#47248,#47249,
#47250,#47251,#47252,#47253,#47254,#47255),.UNSPECIFIED.,.F.,.F.,(4,3,3,
3,3,3,3,4),(-60.6412095134546,-59.9672826253251,-58.967827914903,-57.9683732044809,
-56.9689184940589,-55.9694637836368,-54.9700090732147,-54.358024206275),
 .UNSPECIFIED.);
#1057=B_SPLINE_CURVE_WITH_KNOTS('',3,(#47256,#47257,#47258,#47259,#47260,
#47261,#47262,#47263,#47264,#47265,#47266,#47267,#47268,#47269,#47270,#47271,
#47272,#47273,#47274,#47275,#47276,#47277),.UNSPECIFIED.,.F.,.F.,(4,3,3,
3,3,3,3,4),(51.384337550976,51.8828768311554,52.882527497672,53.8821781641886,
54.8818288307051,55.8814794972217,56.8811301637383,57.6675228581556),
 .UNSPECIFIED.);
#1058=B_SPLINE_CURVE_WITH_KNOTS('',3,(#47282,#47283,#47284,#47285,#47286,
#47287,#47288,#47289,#47290,#47291,#47292,#47293,#47294,#47295,#47296,#47297,
#47298,#47299,#47300,#47301,#47302,#47303),.UNSPECIFIED.,.F.,.F.,(4,3,3,
3,3,3,3,4),(-66.9243948206342,-65.9640108878576,-64.9645561774355,-63.9651014670135,
-62.9656467565914,-61.9661920461693,-60.9667373357472,-60.6412095134546),
 .UNSPECIFIED.);
#1059=B_SPLINE_CURVE_WITH_KNOTS('',3,(#47304,#47305,#47306,#47307,#47308,
#47309,#47310,#47311,#47312,#47313,#47314,#47315,#47316,#47317,#47318,#47319,
#47320,#47321,#47322,#47323,#47324,#47325,#47326,#47327,#47328),
 .UNSPECIFIED.,.F.,.F.,(4,3,3,3,3,3,3,3,4),(57.6675228581556,57.8807808302548,
58.8804314967713,59.8800821632879,60.8797328298044,61.8793834963209,62.8790341628375,
63.878684829354,63.9507081653352),.UNSPECIFIED.);
#1060=B_SPLINE_CURVE_WITH_KNOTS('',3,(#47333,#47334,#47335,#47336,#47337,
#47338,#47339,#47340,#47341,#47342,#47343,#47344,#47345,#47346,#47347,#47348,
#47349,#47350,#47351,#47352,#47353,#47354,#47355,#47356,#47357),
 .UNSPECIFIED.,.F.,.F.,(4,3,3,3,3,3,3,3,4),(-73.2075801278138,-72.9601938608122,
-71.9607391503901,-70.9612844399681,-69.9618297295459,-68.9623750191239,
-67.9629203087018,-66.9634655982797,-66.9243948206342),.UNSPECIFIED.);
#1061=B_SPLINE_CURVE_WITH_KNOTS('',3,(#47358,#47359,#47360,#47361,#47362,
#47363,#47364,#47365,#47366,#47367,#47368,#47369,#47370,#47371,#47372,#47373,
#47374,#47375,#47376,#47377,#47378,#47379),.UNSPECIFIED.,.F.,.F.,(4,3,3,
3,3,3,3,4),(63.9507081653352,64.8783354958706,65.8779861623872,66.8776368289037,
67.8772874954203,68.8769381619369,69.8765888284534,70.2338934725148),
 .UNSPECIFIED.);
#1062=B_SPLINE_CURVE_WITH_KNOTS('',3,(#47384,#47385,#47386,#47387,#47388,
#47389,#47390,#47391,#47392,#47393,#47394,#47395,#47396,#47397,#47398,#47399,
#47400,#47401,#47402,#47403,#47404,#47405),.UNSPECIFIED.,.F.,.F.,(4,3,3,
3,3,3,3,4),(-79.4907654349934,-78.9569221233447,-77.9574674129226,-76.9580127025006,
-75.9585579920785,-74.9591032816564,-73.9596485712343,-73.2075801278138),
 .UNSPECIFIED.);
#1063=B_SPLINE_CURVE_WITH_KNOTS('',3,(#47406,#47407,#47408,#47409,#47410,
#47411,#47412,#47413,#47414,#47415,#47416,#47417,#47418,#47419,#47420,#47421,
#47422,#47423,#47424,#47425,#47426,#47427),.UNSPECIFIED.,.F.,.F.,(4,3,3,
3,3,3,3,4),(70.2338934725148,70.87623949497,71.8758901614865,72.8755408280031,
73.8751914945196,74.8748421610361,75.8744928275527,76.5170787796944),
 .UNSPECIFIED.);
#1064=B_SPLINE_CURVE_WITH_KNOTS('',3,(#47432,#47433,#47434,#47435,#47436,
#47437,#47438,#47439,#47440,#47441,#47442,#47443,#47444,#47445,#47446,#47447,
#47448,#47449,#47450,#47451,#47452,#47453),.UNSPECIFIED.,.F.,.F.,(4,3,3,
3,3,3,3,4),(-85.773950742173,-84.9536503858773,-83.9541956754552,-82.9547409650331,
-81.955286254611,-80.9558315441889,-79.9563768337668,-79.4907654349934),
 .UNSPECIFIED.);
#1065=B_SPLINE_CURVE_WITH_KNOTS('',3,(#47454,#47455,#47456,#47457,#47458,
#47459,#47460,#47461,#47462,#47463,#47464,#47465,#47466,#47467,#47468,#47469,
#47470,#47471,#47472,#47473,#47474,#47475),.UNSPECIFIED.,.F.,.F.,(4,3,3,
3,3,3,3,4),(76.5170787796944,76.8741434940692,77.8737941605858,78.8734448271023,
79.8730954936189,80.8727461601354,81.872396826652,82.800264086874),
 .UNSPECIFIED.);
#1066=B_SPLINE_CURVE_WITH_KNOTS('',3,(#47480,#47481,#47482,#47483,#47484,
#47485,#47486,#47487,#47488,#47489,#47490,#47491,#47492,#47493,#47494,#47495,
#47496,#47497,#47498,#47499,#47500,#47501,#47502,#47503,#47504),
 .UNSPECIFIED.,.F.,.F.,(4,3,3,3,3,3,3,3,4),(-92.0571360493526,-91.9498333588318,
-90.9503786484097,-89.9509239379877,-88.9514692275656,-87.9520145171435,
-86.9525598067214,-85.9531050962993,-85.773950742173),.UNSPECIFIED.);
#1067=B_SPLINE_CURVE_WITH_KNOTS('',3,(#47505,#47506,#47507,#47508,#47509,
#47510,#47511,#47512,#47513,#47514,#47515,#47516,#47517,#47518,#47519,#47520,
#47521,#47522,#47523,#47524,#47525,#47526,#47527,#47528,#47529),
 .UNSPECIFIED.,.F.,.F.,(4,3,3,3,3,3,3,3,4),(82.800264086874,82.8720474931686,
83.8716981596851,84.8713488262017,85.8709994927182,86.8706501592348,87.8703008257513,
88.8699514922679,89.0834493940535),.UNSPECIFIED.);
#1068=B_SPLINE_CURVE_WITH_KNOTS('',3,(#47534,#47535,#47536,#47537,#47538,
#47539,#47540,#47541,#47542,#47543,#47544,#47545,#47546,#47547,#47548,#47549,
#47550,#47551,#47552,#47553,#47554,#47555),.UNSPECIFIED.,.F.,.F.,(4,3,3,
3,3,3,3,4),(-98.3403213565322,-97.9465616213644,-96.9471069109423,-95.9476522005202,
-94.9481974900981,-93.948742779676,-92.9492880692539,-92.0571360493526),
 .UNSPECIFIED.);
#1069=B_SPLINE_CURVE_WITH_KNOTS('',3,(#47556,#47557,#47558,#47559,#47560,
#47561,#47562,#47563,#47564,#47565,#47566,#47567,#47568,#47569,#47570,#47571,
#47572,#47573,#47574,#47575,#47576,#47577),.UNSPECIFIED.,.F.,.F.,(4,3,3,
3,3,3,3,4),(89.0834493940535,89.8696021587844,90.869252825301,91.8689034918175,
92.8685541583341,93.8682048248506,94.8678554913672,95.3666347012331),
 .UNSPECIFIED.);
#1070=B_SPLINE_CURVE_WITH_KNOTS('',3,(#47582,#47583,#47584,#47585,#47586,
#47587,#47588,#47589,#47590,#47591,#47592,#47593,#47594,#47595,#47596,#47597,
#47598,#47599,#47600,#47601,#47602,#47603),.UNSPECIFIED.,.F.,.F.,(4,3,3,
3,3,3,3,4),(-104.623506663712,-103.943289883897,-102.943835173475,-101.944380463053,
-100.944925752631,-99.9454710422085,-98.9460163317864,-98.3403213565322),
 .UNSPECIFIED.);
#1071=B_SPLINE_CURVE_WITH_KNOTS('',3,(#47604,#47605,#47606,#47607,#47608,
#47609,#47610,#47611,#47612,#47613,#47614,#47615,#47616,#47617,#47618,#47619,
#47620,#47621,#47622,#47623,#47624,#47625),.UNSPECIFIED.,.F.,.F.,(4,3,3,
3,3,3,3,4),(95.3666347012331,95.8675061578838,96.8671568244003,97.8668074909168,
98.8664581574334,99.8661088239499,100.865759490466,101.649820008413),
 .UNSPECIFIED.);
#1072=B_SPLINE_CURVE_WITH_KNOTS('',3,(#47630,#47631,#47632,#47633,#47634,
#47635,#47636,#47637,#47638,#47639,#47640,#47641,#47642,#47643,#47644,#47645,
#47646,#47647,#47648,#47649,#47650,#47651),.UNSPECIFIED.,.F.,.F.,(4,3,3,
3,3,3,3,4),(-110.906691970891,-109.940018146429,-108.940563436007,-107.941108725585,
-106.941654015163,-105.942199304741,-104.942744594319,-104.623506663712),
 .UNSPECIFIED.);
#1073=B_SPLINE_CURVE_WITH_KNOTS('',3,(#47652,#47653,#47654,#47655,#47656,
#47657,#47658,#47659,#47660,#47661,#47662,#47663,#47664,#47665,#47666,#47667,
#47668,#47669,#47670,#47671,#47672,#47673,#47674,#47675,#47676),
 .UNSPECIFIED.,.F.,.F.,(4,3,3,3,3,3,3,3,4),(101.649820008413,101.865410156983,
102.8650608235,103.864711490016,104.864362156533,105.864012823049,106.863663489566,
107.863314156082,107.933005315592),.UNSPECIFIED.);
#1074=B_SPLINE_CURVE_WITH_KNOTS('',3,(#47681,#47682,#47683,#47684,#47685,
#47686,#47687,#47688,#47689,#47690,#47691,#47692,#47693,#47694,#47695,#47696,
#47697,#47698,#47699,#47700,#47701,#47702,#47703,#47704,#47705),
 .UNSPECIFIED.,.F.,.F.,(4,3,3,3,3,3,3,3,4),(-117.189877278071,-116.936201119384,
-115.936746408962,-114.93729169854,-113.937836988118,-112.938382277696,
-111.938927567274,-110.939472856851,-110.906691970891),.UNSPECIFIED.);
#1075=B_SPLINE_CURVE_WITH_KNOTS('',3,(#47706,#47707,#47708,#47709,#47710,
#47711,#47712,#47713,#47714,#47715,#47716,#47717,#47718,#47719,#47720,#47721,
#47722,#47723,#47724,#47725,#47726,#47727),.UNSPECIFIED.,.F.,.F.,(4,3,3,
3,3,3,3,4),(107.933005315592,108.862964822599,109.862615489115,110.862266155632,
111.861916822149,112.861567488665,113.861218155182,114.216190622772),
 .UNSPECIFIED.);
#1076=B_SPLINE_CURVE_WITH_KNOTS('',3,(#47732,#47733,#47734,#47735,#47736,
#47737,#47738,#47739,#47740,#47741,#47742,#47743,#47744,#47745,#47746,#47747,
#47748,#47749,#47750,#47751,#47752,#47753),.UNSPECIFIED.,.F.,.F.,(4,3,3,
3,3,3,3,4),(-123.473062585251,-122.932929381916,-121.933474671494,-120.934019961072,
-119.93456525065,-118.935110540228,-117.935655829806,-117.189877278071),
 .UNSPECIFIED.);
#1077=B_SPLINE_CURVE_WITH_KNOTS('',3,(#47754,#47755,#47756,#47757,#47758,
#47759,#47760,#47761,#47762,#47763,#47764,#47765,#47766,#47767,#47768,#47769,
#47770,#47771,#47772,#47773,#47774,#47775),.UNSPECIFIED.,.F.,.F.,(4,3,3,
3,3,3,3,4),(114.216190622772,114.860868821698,115.860519488215,116.860170154731,
117.859820821248,118.859471487764,119.859122154281,120.499375929952),
 .UNSPECIFIED.);
#1078=B_SPLINE_CURVE_WITH_KNOTS('',3,(#47780,#47781,#47782,#47783,#47784,
#47785,#47786,#47787,#47788,#47789,#47790,#47791,#47792,#47793,#47794,#47795,
#47796,#47797,#47798,#47799,#47800,#47801),.UNSPECIFIED.,.F.,.F.,(4,3,3,
3,3,3,3,4),(-129.75624789243,-128.929657644449,-127.930202934027,-126.930748223605,
-125.931293513183,-124.931838802761,-123.932384092339,-123.473062585251),
 .UNSPECIFIED.);
#1079=B_SPLINE_CURVE_WITH_KNOTS('',3,(#47802,#47803,#47804,#47805,#47806,
#47807,#47808,#47809,#47810,#47811,#47812,#47813,#47814,#47815,#47816,#47817,
#47818,#47819,#47820,#47821,#47822,#47823),.UNSPECIFIED.,.F.,.F.,(4,3,3,
3,3,3,3,4),(120.499375929952,120.858772820798,121.858423487314,122.858074153831,
123.857724820347,124.857375486864,125.85702615338,126.782561237131),
 .UNSPECIFIED.);
#1080=B_SPLINE_CURVE_WITH_KNOTS('',3,(#47828,#47829,#47830,#47831,#47832,
#47833,#47834,#47835,#47836,#47837,#47838,#47839,#47840,#47841,#47842,#47843,
#47844,#47845,#47846,#47847,#47848,#47849,#47850,#47851,#47852),
 .UNSPECIFIED.,.F.,.F.,(4,3,3,3,3,3,3,3,4),(-136.03943319961,-135.925840617404,
-134.926385906981,-133.926931196559,-132.927476486137,-131.928021775715,
-130.928567065293,-129.929112354871,-129.75624789243),.UNSPECIFIED.);
#1081=B_SPLINE_CURVE_WITH_KNOTS('',3,(#47853,#47854,#47855,#47856,#47857,
#47858,#47859,#47860,#47861,#47862,#47863,#47864,#47865,#47866,#47867,#47868,
#47869,#47870,#47871,#47872,#47873,#47874,#47875,#47876,#47877),
 .UNSPECIFIED.,.F.,.F.,(4,3,3,3,3,3,3,3,4),(126.782561237131,126.856676819897,
127.856327486413,128.85597815293,129.855628819447,130.855279485963,131.85493015248,
132.854580818996,133.065746544311),.UNSPECIFIED.);
#1082=B_SPLINE_CURVE_WITH_KNOTS('',3,(#47882,#47883,#47884,#47885,#47886,
#47887,#47888,#47889,#47890,#47891,#47892,#47893,#47894,#47895,#47896,#47897,
#47898,#47899,#47900,#47901,#47902,#47903),.UNSPECIFIED.,.F.,.F.,(4,3,3,
3,3,3,3,4),(-142.322618506789,-141.922568879936,-140.923114169514,-139.923659459092,
-138.92420474867,-137.924750038248,-136.925295327826,-136.03943319961),
 .UNSPECIFIED.);
#1083=B_SPLINE_CURVE_WITH_KNOTS('',3,(#47904,#47905,#47906,#47907,#47908,
#47909,#47910,#47911,#47912,#47913,#47914,#47915,#47916,#47917,#47918,#47919,
#47920,#47921,#47922,#47923,#47924,#47925),.UNSPECIFIED.,.F.,.F.,(4,3,3,
3,3,3,3,4),(133.065746544311,133.854231485513,134.853882152029,135.853532818546,
136.853183485062,137.852834151579,138.852484818095,139.34893185149),
 .UNSPECIFIED.);
#1084=B_SPLINE_CURVE_WITH_KNOTS('',3,(#47930,#47931,#47932,#47933,#47934,
#47935,#47936,#47937,#47938,#47939,#47940,#47941,#47942,#47943,#47944,#47945,
#47946,#47947,#47948,#47949,#47950,#47951),.UNSPECIFIED.,.F.,.F.,(4,3,3,
3,3,3,3,4),(-148.605803813969,-147.919297142469,-146.919842432047,-145.920387721624,
-144.920933011202,-143.92147830078,-142.922023590358,-142.322618506789),
 .UNSPECIFIED.);
#1085=B_SPLINE_CURVE_WITH_KNOTS('',3,(#47952,#47953,#47954,#47955,#47956,
#47957,#47958,#47959,#47960,#47961,#47962,#47963,#47964,#47965,#47966,#47967,
#47968,#47969,#47970,#47971,#47972,#47973),.UNSPECIFIED.,.F.,.F.,(4,3,3,
3,3,3,3,4),(139.34893185149,139.852135484612,140.851786151129,141.851436817645,
142.851087484162,143.850738150678,144.850388817195,145.63211715867),
 .UNSPECIFIED.);
#1086=B_SPLINE_CURVE_WITH_KNOTS('',3,(#47978,#47979,#47980,#47981,#47982,
#47983,#47984,#47985,#47986,#47987,#47988,#47989,#47990,#47991,#47992,#47993,
#47994,#47995,#47996,#47997,#47998,#47999),.UNSPECIFIED.,.F.,.F.,(4,3,3,
3,3,3,3,4),(-154.888989121148,-153.916025405001,-152.916570694579,-151.917115984157,
-150.917661273735,-149.918206563313,-148.918751852891,-148.605803813969),
 .UNSPECIFIED.);
#1087=B_SPLINE_CURVE_WITH_KNOTS('',3,(#48000,#48001,#48002,#48003,#48004,
#48005,#48006,#48007,#48008,#48009,#48010,#48011,#48012,#48013,#48014,#48015,
#48016,#48017,#48018,#48019,#48020,#48021,#48022,#48023,#48024),
 .UNSPECIFIED.,.F.,.F.,(4,3,3,3,3,3,3,3,4),(145.63211715867,145.850039483711,
146.849690150228,147.849340816744,148.848991483261,149.848642149777,150.848292816294,
151.847943482811,151.915302465849),.UNSPECIFIED.);
#1088=B_SPLINE_CURVE_WITH_KNOTS('',3,(#48029,#48030,#48031,#48032,#48033,
#48034,#48035,#48036,#48037,#48038,#48039,#48040,#48041,#48042,#48043,#48044,
#48045,#48046,#48047,#48048,#48049,#48050,#48051,#48052,#48053),
 .UNSPECIFIED.,.F.,.F.,(4,3,3,3,3,3,3,3,4),(-161.172174428328,-160.912208377956,
-159.912753667534,-158.913298957112,-157.913844246689,-156.914389536267,
-155.914934825845,-154.915480115423,-154.888989121148),.UNSPECIFIED.);
#1089=B_SPLINE_CURVE_WITH_KNOTS('',3,(#48054,#48055,#48056,#48057,#48058,
#48059,#48060,#48061,#48062,#48063,#48064,#48065,#48066,#48067,#48068,#48069,
#48070,#48071,#48072,#48073,#48074,#48075),.UNSPECIFIED.,.F.,.F.,(4,3,3,
3,3,3,3,4),(151.915302465849,152.847594149327,153.847244815844,154.84689548236,
155.846546148877,156.846196815393,157.84584748191,158.198487773029),
 .UNSPECIFIED.);
#1090=B_SPLINE_CURVE_WITH_KNOTS('',3,(#48080,#48081,#48082,#48083,#48084,
#48085,#48086,#48087,#48088,#48089,#48090,#48091,#48092,#48093,#48094,#48095,
#48096,#48097,#48098,#48099,#48100,#48101),.UNSPECIFIED.,.F.,.F.,(4,3,3,
3,3,3,3,4),(-167.455359735508,-166.908936640488,-165.909481930066,-164.910027219644,
-163.910572509222,-162.9111177988,-161.911663088378,-161.172174428328),
 .UNSPECIFIED.);
#1091=B_SPLINE_CURVE_WITH_KNOTS('',3,(#48102,#48103,#48104,#48105,#48106,
#48107,#48108,#48109,#48110,#48111,#48112,#48113,#48114,#48115,#48116,#48117,
#48118,#48119,#48120,#48121,#48122,#48123),.UNSPECIFIED.,.F.,.F.,(4,3,3,
3,3,3,3,4),(158.198487773029,158.845498148427,159.845148814943,160.84479948146,
161.844450147976,162.844100814493,163.843751481009,164.481673080209),
 .UNSPECIFIED.);
#1092=B_SPLINE_CURVE_WITH_KNOTS('',3,(#48128,#48129,#48130,#48131,#48132,
#48133,#48134,#48135,#48136,#48137,#48138,#48139,#48140,#48141,#48142,#48143,
#48144,#48145,#48146,#48147,#48148,#48149),.UNSPECIFIED.,.F.,.F.,(4,3,3,
3,3,3,3,4),(-173.738545042687,-172.905664903021,-171.906210192599,-170.906755482177,
-169.907300771755,-168.907846061332,-167.90839135091,-167.455359735508),
 .UNSPECIFIED.);
#1093=B_SPLINE_CURVE_WITH_KNOTS('',3,(#48150,#48151,#48152,#48153,#48154,
#48155,#48156,#48157,#48158,#48159,#48160,#48161,#48162,#48163,#48164,#48165,
#48166,#48167,#48168,#48169,#48170,#48171),.UNSPECIFIED.,.F.,.F.,(4,3,3,
3,3,3,3,4),(164.481673080209,164.843402147526,165.843052814042,166.842703480559,
167.842354147075,168.842004813592,169.841655480109,170.764858387388),
 .UNSPECIFIED.);
#1094=B_SPLINE_CURVE_WITH_KNOTS('',3,(#48176,#48177,#48178,#48179,#48180,
#48181,#48182,#48183,#48184,#48185,#48186,#48187,#48188,#48189,#48190,#48191,
#48192,#48193,#48194,#48195,#48196,#48197,#48198,#48199,#48200),
 .UNSPECIFIED.,.F.,.F.,(4,3,3,3,3,3,3,3,4),(-180.021730349867,-179.901847875975,
-178.902393165553,-177.902938455131,-176.903483744709,-175.904029034287,
-174.904574323865,-173.905119613443,-173.738545042687),.UNSPECIFIED.);
#1095=B_SPLINE_CURVE_WITH_KNOTS('',3,(#48201,#48202,#48203,#48204,#48205,
#48206,#48207,#48208,#48209,#48210,#48211,#48212,#48213,#48214,#48215,#48216,
#48217,#48218,#48219,#48220,#48221,#48222,#48223,#48224,#48225),
 .UNSPECIFIED.,.F.,.F.,(4,3,3,3,3,3,3,3,4),(170.764858387388,170.841306146625,
171.840956813142,172.840607479658,173.840258146175,174.839908812691,175.839559479208,
176.839210145724,177.048043694568),.UNSPECIFIED.);
#1096=B_SPLINE_CURVE_WITH_KNOTS('',3,(#48230,#48231,#48232,#48233,#48234,
#48235,#48236,#48237,#48238,#48239,#48240,#48241,#48242,#48243,#48244,#48245,
#48246,#48247,#48248,#48249,#48250,#48251),.UNSPECIFIED.,.F.,.F.,(4,3,3,
3,3,3,3,4),(-186.304915657046,-185.898576138508,-184.899121428086,-183.899666717664,
-182.900212007242,-181.90075729682,-180.901302586397,-180.021730349867),
 .UNSPECIFIED.);
#1097=B_SPLINE_CURVE_WITH_KNOTS('',3,(#48252,#48253,#48254,#48255,#48256,
#48257,#48258,#48259,#48260,#48261,#48262,#48263,#48264,#48265,#48266,#48267,
#48268,#48269,#48270,#48271,#48272,#48273),.UNSPECIFIED.,.F.,.F.,(4,3,3,
3,3,3,3,4),(177.048043694568,177.838860812241,178.838511478758,179.838162145274,
180.837812811791,181.837463478307,182.837114144824,183.331229001747),
 .UNSPECIFIED.);
#1098=B_SPLINE_CURVE_WITH_KNOTS('',3,(#48278,#48279,#48280,#48281,#48282,
#48283,#48284,#48285,#48286,#48287,#48288,#48289,#48290,#48291,#48292,#48293,
#48294,#48295,#48296,#48297,#48298,#48299),.UNSPECIFIED.,.F.,.F.,(4,3,3,
3,3,3,3,4),(-192.588100964226,-191.89530440104,-190.895849690618,-189.896394980196,
-188.896940269774,-187.897485559352,-186.89803084893,-186.304915657046),
 .UNSPECIFIED.);
#1099=B_SPLINE_CURVE_WITH_KNOTS('',3,(#48300,#48301,#48302,#48303,#48304,
#48305,#48306,#48307,#48308,#48309,#48310,#48311,#48312,#48313,#48314,#48315,
#48316,#48317,#48318,#48319,#48320,#48321),.UNSPECIFIED.,.F.,.F.,(4,3,3,
3,3,3,3,4),(183.331229001747,183.83676481134,184.836415477857,185.836066144373,
186.83571681089,187.835367477406,188.835018143923,189.614414308927),
 .UNSPECIFIED.);
#1100=B_SPLINE_CURVE_WITH_KNOTS('',3,(#48326,#48327,#48328,#48329,#48330,
#48331,#48332,#48333,#48334,#48335,#48336,#48337,#48338,#48339,#48340,#48341,
#48342,#48343,#48344,#48345,#48346,#48347),.UNSPECIFIED.,.F.,.F.,(4,3,3,
3,3,3,3,4),(-198.871286271405,-197.892032663573,-196.892577953151,-195.893123242729,
-194.893668532307,-193.894213821885,-192.894759111462,-192.588100964226),
 .UNSPECIFIED.);
#1101=B_SPLINE_CURVE_WITH_KNOTS('',3,(#48348,#48349,#48350,#48351,#48352,
#48353,#48354,#48355,#48356,#48357,#48358,#48359,#48360,#48361,#48362,#48363,
#48364,#48365,#48366,#48367,#48368,#48369,#48370,#48371,#48372),
 .UNSPECIFIED.,.F.,.F.,(4,3,3,3,3,3,3,3,4),(189.614414308927,189.834668810439,
190.834319476956,191.833970143473,192.833620809989,193.833271476506,194.832922143022,
195.832572809539,195.897599616106),.UNSPECIFIED.);
#1102=B_SPLINE_CURVE_WITH_KNOTS('',3,(#48377,#48378,#48379,#48380,#48381,
#48382,#48383,#48384,#48385,#48386,#48387,#48388,#48389,#48390,#48391,#48392,
#48393,#48394,#48395,#48396,#48397,#48398,#48399,#48400,#48401),
 .UNSPECIFIED.,.F.,.F.,(4,3,3,3,3,3,3,3,4),(-205.154471578585,-204.888215636527,
-203.888760926105,-202.889306215683,-201.889851505261,-200.890396794839,
-199.890942084417,-198.891487373995,-198.871286271405),.UNSPECIFIED.);
#1103=B_SPLINE_CURVE_WITH_KNOTS('',3,(#48402,#48403,#48404,#48405,#48406,
#48407,#48408,#48409,#48410,#48411,#48412,#48413,#48414,#48415,#48416,#48417,
#48418,#48419,#48420,#48421,#48422,#48423),.UNSPECIFIED.,.F.,.F.,(4,3,3,
3,3,3,3,4),(195.897599616106,196.832223476055,197.831874142572,198.831524809089,
199.831175475605,200.830826142122,201.830476808638,202.180784923286),
 .UNSPECIFIED.);
#1104=B_SPLINE_CURVE_WITH_KNOTS('',3,(#48428,#48429,#48430,#48431,#48432,
#48433,#48434,#48435,#48436,#48437,#48438,#48439,#48440,#48441,#48442,#48443,
#48444,#48445,#48446,#48447,#48448,#48449),.UNSPECIFIED.,.F.,.F.,(4,3,3,
3,3,3,3,4),(-211.437656885764,-210.88494389906,-209.885489188638,-208.886034478216,
-207.886579767794,-206.887125057372,-205.88767034695,-205.154471578585),
 .UNSPECIFIED.);
#1105=B_SPLINE_CURVE_WITH_KNOTS('',3,(#48450,#48451,#48452,#48453,#48454,
#48455,#48456,#48457,#48458,#48459,#48460,#48461,#48462,#48463,#48464,#48465,
#48466,#48467,#48468,#48469,#48470,#48471),.UNSPECIFIED.,.F.,.F.,(4,3,3,
3,3,3,3,4),(202.180784923286,202.830127475155,203.829778141671,204.829428808188,
205.829079474704,206.828730141221,207.828380807737,208.463970230465),
 .UNSPECIFIED.);
#1106=B_SPLINE_CURVE_WITH_KNOTS('',3,(#48476,#48477,#48478,#48479,#48480,
#48481,#48482,#48483,#48484,#48485,#48486,#48487,#48488,#48489,#48490,#48491,
#48492,#48493,#48494,#48495,#48496,#48497),.UNSPECIFIED.,.F.,.F.,(4,3,3,
3,3,3,3,4),(-217.720842192944,-216.881672161592,-215.88221745117,-214.882762740748,
-213.883308030326,-212.883853319904,-211.884398609482,-211.437656885764),
 .UNSPECIFIED.);
#1107=B_SPLINE_CURVE_WITH_KNOTS('',3,(#48498,#48499,#48500,#48501,#48502,
#48503,#48504,#48505,#48506,#48507,#48508,#48509,#48510,#48511,#48512,#48513,
#48514,#48515,#48516,#48517,#48518,#48519),.UNSPECIFIED.,.F.,.F.,(4,3,3,
3,3,3,3,4),(208.463970230465,208.828031474254,209.827682140771,210.827332807287,
211.826983473804,212.82663414032,213.826284806837,214.747155537645),
 .UNSPECIFIED.);
#1108=B_SPLINE_CURVE_WITH_KNOTS('',3,(#48524,#48525,#48526,#48527,#48528,
#48529,#48530,#48531,#48532,#48533,#48534,#48535,#48536,#48537,#48538,#48539,
#48540,#48541,#48542,#48543,#48544,#48545,#48546,#48547,#48548),
 .UNSPECIFIED.,.F.,.F.,(4,3,3,3,3,3,3,3,4),(-224.004027500124,-223.877855134547,
-222.878400424125,-221.878945713703,-220.879491003281,-219.880036292859,
-218.880581582437,-217.881126872015,-217.720842192944),.UNSPECIFIED.);
#1109=B_SPLINE_CURVE_WITH_KNOTS('',3,(#48549,#48550,#48551,#48552,#48553,
#48554,#48555,#48556,#48557,#48558,#48559,#48560,#48561,#48562,#48563,#48564,
#48565,#48566,#48567,#48568,#48569,#48570,#48571,#48572,#48573),
 .UNSPECIFIED.,.F.,.F.,(4,3,3,3,3,3,3,3,4),(214.747155537645,214.825935473353,
215.82558613987,216.825236806386,217.824887472903,218.82453813942,219.824188805936,
220.823839472453,221.030340844825),.UNSPECIFIED.);
#1110=B_SPLINE_CURVE_WITH_KNOTS('',3,(#48578,#48579,#48580,#48581,#48582,
#48583,#48584,#48585,#48586,#48587,#48588,#48589,#48590,#48591,#48592,#48593,
#48594,#48595,#48596,#48597,#48598,#48599),.UNSPECIFIED.,.F.,.F.,(4,3,3,
3,3,3,3,4),(-230.287212807303,-229.87458339708,-228.875128686658,-227.875673976235,
-226.876219265813,-225.876764555391,-224.877309844969,-224.004027500124),
 .UNSPECIFIED.);
#1111=B_SPLINE_CURVE_WITH_KNOTS('',3,(#48600,#48601,#48602,#48603,#48604,
#48605,#48606,#48607,#48608,#48609,#48610,#48611,#48612,#48613,#48614,#48615,
#48616,#48617,#48618,#48619,#48620,#48621),.UNSPECIFIED.,.F.,.F.,(4,3,3,
3,3,3,3,4),(221.030340844825,221.823490138969,222.823140805486,223.822791472002,
224.822442138519,225.822092805035,226.821743471552,227.313526152004),
 .UNSPECIFIED.);
#1112=B_SPLINE_CURVE_WITH_KNOTS('',3,(#48626,#48627,#48628,#48629,#48630,
#48631,#48632,#48633,#48634,#48635,#48636,#48637,#48638,#48639,#48640,#48641,
#48642,#48643,#48644,#48645,#48646,#48647),.UNSPECIFIED.,.F.,.F.,(4,3,3,
3,3,3,3,4),(-236.570398114483,-235.871311659612,-234.87185694919,-233.872402238768,
-232.872947528346,-231.873492817924,-230.874038107502,-230.287212807303),
 .UNSPECIFIED.);
#1113=B_SPLINE_CURVE_WITH_KNOTS('',3,(#48648,#48649,#48650,#48651,#48652,
#48653,#48654,#48655,#48656,#48657,#48658,#48659,#48660,#48661,#48662,#48663,
#48664,#48665,#48666,#48667,#48668,#48669),.UNSPECIFIED.,.F.,.F.,(4,3,3,
3,3,3,3,4),(227.313526152004,227.821394138069,228.821044804585,229.820695471102,
230.820346137618,231.819996804135,232.819647470651,233.596711459184),
 .UNSPECIFIED.);
#1114=B_SPLINE_CURVE_WITH_KNOTS('',3,(#48674,#48675,#48676,#48677,#48678,
#48679,#48680,#48681,#48682,#48683,#48684,#48685,#48686,#48687,#48688,#48689,
#48690,#48691,#48692,#48693,#48694,#48695),.UNSPECIFIED.,.F.,.F.,(4,3,3,
3,3,3,3,4),(-242.853583421662,-241.868039922145,-240.868585211723,-239.8691305013,
-238.869675790878,-237.870221080456,-236.870766370034,-236.570398114483),
 .UNSPECIFIED.);
#1115=B_SPLINE_CURVE_WITH_KNOTS('',3,(#48696,#48697,#48698,#48699,#48700,
#48701,#48702,#48703,#48704,#48705,#48706,#48707,#48708,#48709,#48710,#48711,
#48712,#48713,#48714,#48715,#48716,#48717,#48718,#48719,#48720),
 .UNSPECIFIED.,.F.,.F.,(4,3,3,3,3,3,3,3,4),(233.596711459184,233.819298137168,
234.818948803684,235.818599470201,236.818250136717,237.817900803234,238.817551469751,
239.817202136267,239.879896766363),.UNSPECIFIED.);
#1116=B_SPLINE_CURVE_WITH_KNOTS('',3,(#48725,#48726,#48727,#48728,#48729,
#48730,#48731,#48732,#48733,#48734,#48735,#48736,#48737,#48738,#48739,#48740,
#48741,#48742,#48743,#48744,#48745,#48746,#48747,#48748,#48749),
 .UNSPECIFIED.,.F.,.F.,(4,3,3,3,3,3,3,3,4),(-249.136768728842,-248.864222895099,
-247.864768184677,-246.865313474255,-245.865858763833,-244.866404053411,
-243.866949342989,-242.867494632567,-242.853583421662),.UNSPECIFIED.);
#1117=B_SPLINE_CURVE_WITH_KNOTS('',3,(#48750,#48751,#48752,#48753,#48754,
#48755,#48756,#48757,#48758,#48759,#48760,#48761,#48762,#48763,#48764,#48765,
#48766,#48767,#48768,#48769,#48770,#48771),.UNSPECIFIED.,.F.,.F.,(4,3,3,
3,3,3,3,4),(239.879896766363,240.816852802784,241.8165034693,242.816154135817,
243.815804802333,244.81545546885,245.815106135366,246.163082073543),
 .UNSPECIFIED.);
#1118=B_SPLINE_CURVE_WITH_KNOTS('',3,(#48776,#48777,#48778,#48779,#48780,
#48781,#48782,#48783,#48784,#48785,#48786,#48787,#48788,#48789,#48790,#48791,
#48792,#48793,#48794,#48795,#48796,#48797),.UNSPECIFIED.,.F.,.F.,(4,3,3,
3,3,3,3,4),(-255.419954036021,-254.860951157632,-253.86149644721,-252.862041736788,
-251.862587026365,-250.863132315943,-249.863677605521,-249.136768728842),
 .UNSPECIFIED.);
#1119=B_SPLINE_CURVE_WITH_KNOTS('',3,(#48798,#48799,#48800,#48801,#48802,
#48803,#48804,#48805,#48806,#48807,#48808,#48809,#48810,#48811,#48812,#48813,
#48814,#48815,#48816,#48817,#48818,#48819),.UNSPECIFIED.,.F.,.F.,(4,3,3,
3,3,3,3,4),(246.163082073543,246.814756801883,247.8144074684,248.814058134916,
249.813708801433,250.813359467949,251.813010134466,252.446267380722),
 .UNSPECIFIED.);
#1120=B_SPLINE_CURVE_WITH_KNOTS('',3,(#48824,#48825,#48826,#48827,#48828,
#48829,#48830,#48831,#48832,#48833,#48834,#48835,#48836,#48837,#48838,#48839,
#48840,#48841,#48842,#48843,#48844,#48845),.UNSPECIFIED.,.F.,.F.,(4,3,3,
3,3,3,3,4),(-261.703139343201,-260.857679420164,-259.858224709742,-258.85876999932,
-257.859315288898,-256.859860578476,-255.860405868054,-255.419954036021),
 .UNSPECIFIED.);
#1121=B_SPLINE_CURVE_WITH_KNOTS('',3,(#48846,#48847,#48848,#48849,#48850,
#48851,#48852,#48853,#48854,#48855,#48856,#48857,#48858,#48859,#48860,#48861,
#48862,#48863,#48864,#48865,#48866,#48867),.UNSPECIFIED.,.F.,.F.,(4,3,3,
3,3,3,3,4),(252.446267380722,252.812660800982,253.812311467499,254.811962134015,
255.811612800532,256.811263467048,257.810914133565,258.729452687902),
 .UNSPECIFIED.);
#1122=B_SPLINE_CURVE_WITH_KNOTS('',3,(#48872,#48873,#48874,#48875,#48876,
#48877,#48878,#48879,#48880,#48881,#48882,#48883,#48884,#48885,#48886,#48887,
#48888,#48889,#48890,#48891,#48892,#48893,#48894,#48895,#48896),
 .UNSPECIFIED.,.F.,.F.,(4,3,3,3,3,3,3,3,4),(-267.986324650381,-267.853862393119,
-266.854407682697,-265.854952972275,-264.855498261853,-263.85604355143,
-262.856588841008,-261.857134130586,-261.703139343201),.UNSPECIFIED.);
#1123=B_SPLINE_CURVE_WITH_KNOTS('',3,(#48897,#48898,#48899,#48900,#48901,
#48902,#48903,#48904,#48905,#48906,#48907,#48908,#48909,#48910,#48911,#48912,
#48913,#48914,#48915,#48916,#48917,#48918,#48919,#48920,#48921),
 .UNSPECIFIED.,.F.,.F.,(4,3,3,3,3,3,3,3,4),(258.729452687902,258.810564800082,
259.810215466598,260.809866133115,261.809516799631,262.809167466148,263.808818132664,
264.808468799181,265.012637995082),.UNSPECIFIED.);
#1124=B_SPLINE_CURVE_WITH_KNOTS('',3,(#48926,#48927,#48928,#48929,#48930,
#48931,#48932,#48933,#48934,#48935,#48936,#48937,#48938,#48939,#48940,#48941,
#48942,#48943,#48944,#48945,#48946,#48947),.UNSPECIFIED.,.F.,.F.,(4,3,3,
3,3,3,3,4),(-274.26950995756,-273.850590655651,-272.851135945229,-271.851681234807,
-270.852226524385,-269.852771813963,-268.853317103541,-267.986324650381),
 .UNSPECIFIED.);
#1125=B_SPLINE_CURVE_WITH_KNOTS('',3,(#48948,#48949,#48950,#48951,#48952,
#48953,#48954,#48955,#48956,#48957,#48958,#48959,#48960,#48961,#48962,#48963,
#48964,#48965,#48966,#48967,#48968,#48969),.UNSPECIFIED.,.F.,.F.,(4,3,3,
3,3,3,3,4),(265.012637995082,265.808119465698,266.807770132214,267.807420798731,
268.807071465247,269.806722131764,270.80637279828,271.295823302261),
 .UNSPECIFIED.);
#1126=B_SPLINE_CURVE_WITH_KNOTS('',3,(#48974,#48975,#48976,#48977,#48978,
#48979,#48980,#48981,#48982,#48983,#48984,#48985,#48986,#48987,#48988,#48989,
#48990,#48991,#48992,#48993,#48994,#48995),.UNSPECIFIED.,.F.,.F.,(4,3,3,
3,3,3,3,4),(-280.55269526474,-279.847318918184,-278.847864207762,-277.84840949734,
-276.848954786918,-275.849500076495,-274.850045366073,-274.26950995756),
 .UNSPECIFIED.);
#1127=B_SPLINE_CURVE_WITH_KNOTS('',3,(#48996,#48997,#48998,#48999,#49000,
#49001,#49002,#49003,#49004,#49005,#49006,#49007,#49008,#49009,#49010,#49011,
#49012,#49013,#49014,#49015,#49016,#49017),.UNSPECIFIED.,.F.,.F.,(4,3,3,
3,3,3,3,4),(271.295823302261,271.806023464797,272.805674131313,273.80532479783,
274.804975464346,275.804626130863,276.80427679738,277.579008609441),
 .UNSPECIFIED.);
#1128=B_SPLINE_CURVE_WITH_KNOTS('',3,(#49022,#49023,#49024,#49025,#49026,
#49027,#49028,#49029,#49030,#49031,#49032,#49033,#49034,#49035,#49036,#49037,
#49038,#49039,#49040,#49041,#49042,#49043),.UNSPECIFIED.,.F.,.F.,(4,3,3,
3,3,3,3,4),(-286.835880571919,-285.844047180716,-284.844592470294,-283.845137759872,
-282.84568304945,-281.846228339028,-280.846773628606,-280.55269526474),
 .UNSPECIFIED.);
#1129=B_SPLINE_CURVE_WITH_KNOTS('',3,(#49044,#49045,#49046,#49047,#49048,
#49049,#49050,#49051,#49052,#49053,#49054,#49055,#49056,#49057,#49058,#49059,
#49060,#49061,#49062,#49063,#49064,#49065,#49066,#49067,#49068),
 .UNSPECIFIED.,.F.,.F.,(4,3,3,3,3,3,3,3,4),(277.579008609441,277.803927463896,
278.803578130413,279.803228796929,280.802879463446,281.802530129962,282.802180796479,
283.801831462995,283.86219391662),.UNSPECIFIED.);
#1130=B_SPLINE_CURVE_WITH_KNOTS('',3,(#49073,#49074,#49075,#49076,#49077,
#49078,#49079,#49080,#49081,#49082,#49083,#49084,#49085,#49086,#49087,#49088,
#49089,#49090,#49091,#49092,#49093,#49094,#49095,#49096,#49097),
 .UNSPECIFIED.,.F.,.F.,(4,3,3,3,3,3,3,3,4),(-293.119065879099,-292.840230153671,
-291.840775443249,-290.841320732827,-289.841866022405,-288.842411311983,
-287.842956601561,-286.843501891138,-286.835880571919),.UNSPECIFIED.);
#1131=B_SPLINE_CURVE_WITH_KNOTS('',3,(#49098,#49099,#49100,#49101,#49102,
#49103,#49104,#49105,#49106,#49107,#49108,#49109,#49110,#49111,#49112,#49113,
#49114,#49115,#49116,#49117,#49118,#49119),.UNSPECIFIED.,.F.,.F.,(4,3,3,
3,3,3,3,4),(283.86219391662,284.801482129512,285.801132796029,286.800783462545,
287.800434129062,288.800084795578,289.799735462095,290.1453792238),
 .UNSPECIFIED.);
#1132=B_SPLINE_CURVE_WITH_KNOTS('',3,(#49124,#49125,#49126,#49127,#49128,
#49129,#49130,#49131,#49132,#49133,#49134,#49135,#49136,#49137,#49138,#49139,
#49140,#49141,#49142,#49143,#49144,#49145),.UNSPECIFIED.,.F.,.F.,(4,3,3,
3,3,3,3,4),(-299.402251186278,-298.836958416203,-297.837503705781,-296.838048995359,
-295.838594284937,-294.839139574515,-293.839684864093,-293.119065879099),
 .UNSPECIFIED.);
#1133=B_SPLINE_CURVE_WITH_KNOTS('',3,(#49146,#49147,#49148,#49149,#49150,
#49151,#49152,#49153,#49154,#49155,#49156,#49157,#49158,#49159,#49160,#49161,
#49162,#49163,#49164,#49165,#49166,#49167),.UNSPECIFIED.,.F.,.F.,(4,3,3,
3,3,3,3,4),(290.1453792238,290.799386128611,291.799036795128,292.798687461644,
293.798338128161,294.797988794677,295.797639461194,296.428564530979),
 .UNSPECIFIED.);
#1134=B_SPLINE_CURVE_WITH_KNOTS('',3,(#49172,#49173,#49174,#49175,#49176,
#49177,#49178,#49179,#49180,#49181,#49182,#49183,#49184,#49185,#49186,#49187,
#49188,#49189,#49190,#49191,#49192,#49193),.UNSPECIFIED.,.F.,.F.,(4,3,3,
3,3,3,3,4),(-305.685436493458,-304.833686678736,-303.834231968314,-302.834777257892,
-301.83532254747,-300.835867837048,-299.836413126626,-299.402251186278),
 .UNSPECIFIED.);
#1135=B_SPLINE_CURVE_WITH_KNOTS('',3,(#49194,#49195,#49196,#49197,#49198,
#49199,#49200,#49201,#49202,#49203,#49204,#49205,#49206,#49207,#49208,#49209,
#49210,#49211,#49212,#49213,#49214,#49215),.UNSPECIFIED.,.F.,.F.,(4,3,3,
3,3,3,3,4),(296.428564530979,296.797290127711,297.796940794227,298.796591460744,
299.79624212726,300.795892793777,301.795543460293,302.711749838159),
 .UNSPECIFIED.);
#1136=B_SPLINE_CURVE_WITH_KNOTS('',3,(#49220,#49221,#49222,#49223,#49224,
#49225,#49226,#49227,#49228,#49229,#49230,#49231,#49232,#49233,#49234,#49235,
#49236,#49237,#49238,#49239,#49240,#49241,#49242,#49243,#49244),
 .UNSPECIFIED.,.F.,.F.,(4,3,3,3,3,3,3,3,4),(-311.968621800638,-311.829869651691,
-310.830414941268,-309.830960230846,-308.831505520424,-307.832050810002,
-306.83259609958,-305.833141389158,-305.685436493458),.UNSPECIFIED.);
#1137=B_SPLINE_CURVE_WITH_KNOTS('',3,(#49245,#49246,#49247,#49248,#49249,
#49250,#49251,#49252,#49253,#49254,#49255,#49256,#49257,#49258,#49259,#49260,
#49261,#49262,#49263,#49264,#49265,#49266,#49267,#49268,#49269),
 .UNSPECIFIED.,.F.,.F.,(4,3,3,3,3,3,3,3,4),(302.711749838159,302.79519412681,
303.794844793326,304.794495459843,305.79414612636,306.793796792876,307.793447459393,
308.793098125909,308.994935145339),.UNSPECIFIED.);
#1138=B_SPLINE_CURVE_WITH_KNOTS('',3,(#49274,#49275,#49276,#49277,#49278,
#49279,#49280,#49281,#49282,#49283,#49284,#49285,#49286,#49287,#49288,#49289,
#49290,#49291,#49292,#49293,#49294,#49295),.UNSPECIFIED.,.F.,.F.,(4,3,3,
3,3,3,3,4),(-318.251807107817,-317.826597914223,-316.827143203801,-315.827688493379,
-314.828233782957,-313.828779072535,-312.829324362113,-311.968621800638),
 .UNSPECIFIED.);
#1139=B_SPLINE_CURVE_WITH_KNOTS('',3,(#49296,#49297,#49298,#49299,#49300,
#49301,#49302,#49303,#49304,#49305,#49306,#49307,#49308,#49309,#49310,#49311,
#49312,#49313,#49314,#49315,#49316,#49317),.UNSPECIFIED.,.F.,.F.,(4,3,3,
3,3,3,3,4),(308.994935145339,309.792748792426,310.792399458942,311.792050125459,
312.791700791975,313.791351458492,314.791002125009,315.278120452518),
 .UNSPECIFIED.);
#1140=B_SPLINE_CURVE_WITH_KNOTS('',3,(#49322,#49323,#49324,#49325,#49326,
#49327,#49328,#49329,#49330,#49331,#49332,#49333,#49334,#49335,#49336,#49337,
#49338,#49339,#49340,#49341,#49342,#49343),.UNSPECIFIED.,.F.,.F.,(4,3,3,
3,3,3,3,4),(-324.534992414997,-323.823326176756,-322.823871466334,-321.824416755911,
-320.824962045489,-319.825507335067,-318.826052624645,-318.251807107817),
 .UNSPECIFIED.);
#1141=B_SPLINE_CURVE_WITH_KNOTS('',3,(#49344,#49345,#49346,#49347,#49348,
#49349,#49350,#49351,#49352,#49353,#49354,#49355,#49356,#49357,#49358,#49359,
#49360,#49361,#49362,#49363,#49364,#49365),.UNSPECIFIED.,.F.,.F.,(4,3,3,
3,3,3,3,4),(315.278120452518,315.790652791525,316.790303458042,317.789954124558,
318.789604791075,319.789255457591,320.788906124108,321.561305759698),
 .UNSPECIFIED.);
#1142=B_SPLINE_CURVE_WITH_KNOTS('',3,(#49370,#49371,#49372,#49373,#49374,
#49375,#49376,#49377,#49378,#49379,#49380,#49381,#49382,#49383,#49384,#49385,
#49386,#49387,#49388,#49389,#49390,#49391),.UNSPECIFIED.,.F.,.F.,(4,3,3,
3,3,3,3,4),(-330.818177722176,-329.820054439288,-328.820599728866,-327.821145018444,
-326.821690308022,-325.8222355976,-324.822780887178,-324.534992414997),
 .UNSPECIFIED.);
#1143=B_SPLINE_CURVE_WITH_KNOTS('',3,(#49392,#49393,#49394,#49395,#49396,
#49397,#49398,#49399,#49400,#49401,#49402,#49403,#49404,#49405,#49406,#49407,
#49408,#49409,#49410,#49411,#49412,#49413,#49414,#49415,#49416),
 .UNSPECIFIED.,.F.,.F.,(4,3,3,3,3,3,3,3,4),(321.561305759698,321.788556790624,
322.788207457141,323.787858123657,324.787508790174,325.787159456691,326.786810123207,
327.786460789724,327.844491066877),.UNSPECIFIED.);
#1144=B_SPLINE_CURVE_WITH_KNOTS('',3,(#49421,#49422,#49423,#49424,#49425,
#49426,#49427,#49428,#49429,#49430,#49431,#49432,#49433,#49434,#49435,#49436,
#49437,#49438,#49439,#49440,#49441,#49442),.UNSPECIFIED.,.F.,.F.,(4,3,3,
3,3,3,3,4),(-337.101363029356,-336.816237412243,-335.816782701821,-334.817327991398,
-333.817873280976,-332.818418570554,-331.818963860132,-330.818177722176),
 .UNSPECIFIED.);
#1145=B_SPLINE_CURVE_WITH_KNOTS('',3,(#49443,#49444,#49445,#49446,#49447,
#49448,#49449,#49450,#49451,#49452,#49453,#49454,#49455,#49456,#49457,#49458,
#49459,#49460,#49461,#49462,#49463,#49464),.UNSPECIFIED.,.F.,.F.,(4,3,3,
3,3,3,3,4),(327.844491066877,328.78611145624,329.785762122757,330.785412789273,
331.78506345579,332.784714122306,333.784364788823,334.127676374057),
 .UNSPECIFIED.);
#1146=B_SPLINE_CURVE_WITH_KNOTS('',3,(#49469,#49470,#49471,#49472,#49473,
#49474,#49475,#49476,#49477,#49478,#49479,#49480,#49481,#49482,#49483,#49484,
#49485,#49486,#49487,#49488,#49489,#49490),.UNSPECIFIED.,.F.,.F.,(4,3,3,
3,3,3,3,4),(-343.384548336535,-342.812965674775,-341.813510964353,-340.814056253931,
-339.814601543509,-338.815146833087,-337.815692122665,-337.101363029356),
 .UNSPECIFIED.);
#1147=B_SPLINE_CURVE_WITH_KNOTS('',3,(#49491,#49492,#49493,#49494,#49495,
#49496,#49497,#49498,#49499,#49500,#49501,#49502,#49503,#49504,#49505,#49506,
#49507,#49508,#49509,#49510,#49511,#49512),.UNSPECIFIED.,.F.,.F.,(4,3,3,
3,3,3,3,4),(334.127676374057,334.784015455339,335.783666121856,336.783316788373,
337.782967454889,338.782618121406,339.782268787922,340.410861681236),
 .UNSPECIFIED.);
#1148=B_SPLINE_CURVE_WITH_KNOTS('',3,(#49517,#49518,#49519,#49520,#49521,
#49522,#49523,#49524,#49525,#49526,#49527,#49528,#49529,#49530,#49531,#49532,
#49533,#49534,#49535,#49536,#49537,#49538),.UNSPECIFIED.,.F.,.F.,(4,3,3,
3,3,3,3,4),(-349.667733643715,-348.809693937308,-347.810239226886,-346.810784516464,
-345.811329806041,-344.811875095619,-343.812420385197,-343.384548336535),
 .UNSPECIFIED.);
#1149=B_SPLINE_CURVE_WITH_KNOTS('',3,(#49539,#49540,#49541,#49542,#49543,
#49544,#49545,#49546,#49547,#49548,#49549,#49550,#49551,#49552,#49553,#49554,
#49555,#49556,#49557,#49558,#49559,#49560),.UNSPECIFIED.,.F.,.F.,(4,3,3,
3,3,3,3,4),(340.410861681236,340.781919454439,341.781570120955,342.781220787472,
343.780871453988,344.780522120505,345.780172787022,346.694046988416),
 .UNSPECIFIED.);
#1150=B_SPLINE_CURVE_WITH_KNOTS('',3,(#49565,#49566,#49567,#49568,#49569,
#49570,#49571,#49572,#49573,#49574,#49575,#49576,#49577,#49578,#49579,#49580,
#49581,#49582,#49583,#49584,#49585,#49586,#49587,#49588,#49589),
 .UNSPECIFIED.,.F.,.F.,(4,3,3,3,3,3,3,3,4),(-355.950918950894,-355.805876910262,
-354.80642219984,-353.806967489418,-352.807512778996,-351.808058068574,
-350.808603358152,-349.80914864773,-349.667733643715),.UNSPECIFIED.);
#1151=B_SPLINE_CURVE_WITH_KNOTS('',3,(#49590,#49591,#49592,#49593,#49594,
#49595,#49596,#49597,#49598,#49599,#49600,#49601,#49602,#49603,#49604,#49605,
#49606,#49607,#49608,#49609,#49610,#49611,#49612,#49613,#49614),
 .UNSPECIFIED.,.F.,.F.,(4,3,3,3,3,3,3,3,4),(346.694046988416,346.779823453538,
347.779474120055,348.779124786571,349.778775453088,350.778426119604,351.778076786121,
352.777727452637,352.977232295595),.UNSPECIFIED.);
#1152=B_SPLINE_CURVE_WITH_KNOTS('',3,(#49619,#49620,#49621,#49622,#49623,
#49624,#49625,#49626,#49627,#49628,#49629,#49630,#49631,#49632,#49633,#49634,
#49635,#49636,#49637,#49638,#49639,#49640),.UNSPECIFIED.,.F.,.F.,(4,3,3,
3,3,3,3,4),(-362.234104258074,-361.802605172795,-360.803150462373,-359.803695751951,
-358.804241041529,-357.804786331106,-356.805331620684,-355.950918950894),
 .UNSPECIFIED.);
#1153=B_SPLINE_CURVE_WITH_KNOTS('',3,(#49641,#49642,#49643,#49644,#49645,
#49646,#49647,#49648,#49649,#49650,#49651,#49652,#49653,#49654,#49655,#49656,
#49657,#49658,#49659,#49660,#49661,#49662),.UNSPECIFIED.,.F.,.F.,(4,3,3,
3,3,3,3,4),(352.977232295595,353.777378119154,354.777028785671,355.776679452187,
356.776330118704,357.77598078522,358.775631451737,359.260417602775),
 .UNSPECIFIED.);
#1154=B_SPLINE_CURVE_WITH_KNOTS('',3,(#49667,#49668,#49669,#49670,#49671,
#49672,#49673,#49674,#49675,#49676,#49677,#49678,#49679,#49680,#49681,#49682,
#49683,#49684,#49685,#49686,#49687,#49688),.UNSPECIFIED.,.F.,.F.,(4,3,3,
3,3,3,3,4),(-368.517289565254,-367.799333435327,-366.799878724905,-365.800424014483,
-364.800969304061,-363.801514593639,-362.802059883217,-362.234104258074),
 .UNSPECIFIED.);
#1155=B_SPLINE_CURVE_WITH_KNOTS('',3,(#49689,#49690,#49691,#49692,#49693,
#49694,#49695,#49696,#49697,#49698,#49699,#49700,#49701,#49702,#49703,#49704,
#49705,#49706,#49707,#49708,#49709,#49710),.UNSPECIFIED.,.F.,.F.,(4,3,3,
3,3,3,3,4),(359.260417602775,359.775282118253,360.77493278477,361.774583451286,
362.774234117803,363.77388478432,364.773535450836,365.543602909955),
 .UNSPECIFIED.);
#1156=B_SPLINE_CURVE_WITH_KNOTS('',3,(#49715,#49716,#49717,#49718,#49719,
#49720,#49721,#49722,#49723,#49724,#49725,#49726,#49727,#49728,#49729,#49730,
#49731,#49732,#49733,#49734,#49735,#49736,#49737,#49738,#49739),
 .UNSPECIFIED.,.F.,.F.,(4,3,3,3,3,3,3,3,4),(-374.800474872433,-374.795516408282,
-373.79606169786,-372.796606987438,-371.797152277016,-370.797697566594,
-369.798242856171,-368.798788145749,-368.517289565254),.UNSPECIFIED.);
#1157=B_SPLINE_CURVE_WITH_KNOTS('',3,(#49740,#49741,#49742,#49743,#49744,
#49745,#49746,#49747,#49748,#49749,#49750,#49751,#49752,#49753,#49754,#49755,
#49756,#49757,#49758,#49759,#49760,#49761,#49762,#49763,#49764),
 .UNSPECIFIED.,.F.,.F.,(4,3,3,3,3,3,3,3,4),(365.543602909955,365.773186117353,
366.772836783869,367.772487450386,368.772138116902,369.771788783419,370.771439449935,
371.771090116452,371.826788217134),.UNSPECIFIED.);
#1158=B_SPLINE_CURVE_WITH_KNOTS('',3,(#49769,#49770,#49771,#49772,#49773,
#49774,#49775,#49776,#49777,#49778,#49779,#49780,#49781,#49782,#49783,#49784,
#49785,#49786,#49787,#49788,#49789,#49790),.UNSPECIFIED.,.F.,.F.,(4,3,3,
3,3,3,3,4),(-381.083660179613,-380.792244670814,-379.792789960392,-378.79333524997,
-377.793880539548,-376.794425829126,-375.794971118704,-374.800474872433),
 .UNSPECIFIED.);
#1159=B_SPLINE_CURVE_WITH_KNOTS('',3,(#49791,#49792,#49793,#49794,#49795,
#49796,#49797,#49798,#49799,#49800,#49801,#49802,#49803,#49804,#49805,#49806,
#49807,#49808,#49809,#49810,#49811,#49812),.UNSPECIFIED.,.F.,.F.,(4,3,3,
3,3,3,3,4),(371.826788217134,372.770740782968,373.770391449485,374.770042116002,
375.769692782518,376.769343449035,377.768994115551,378.109973524314),
 .UNSPECIFIED.);
#1160=B_SPLINE_CURVE_WITH_KNOTS('',3,(#49817,#49818,#49819,#49820,#49821,
#49822,#49823,#49824,#49825,#49826,#49827,#49828,#49829,#49830,#49831,#49832,
#49833,#49834,#49835,#49836,#49837,#49838),.UNSPECIFIED.,.F.,.F.,(4,3,3,
3,3,3,3,4),(-387.366845486792,-386.788972933347,-385.789518222925,-384.790063512503,
-383.790608802081,-382.791154091659,-381.791699381237,-381.083660179613),
 .UNSPECIFIED.);
#1161=B_SPLINE_CURVE_WITH_KNOTS('',3,(#49839,#49840,#49841,#49842,#49843,
#49844,#49845,#49846,#49847,#49848,#49849,#49850,#49851,#49852,#49853,#49854,
#49855,#49856,#49857,#49858,#49859,#49860),.UNSPECIFIED.,.F.,.F.,(4,3,3,
3,3,3,3,4),(378.109973524314,378.768644782068,379.768295448584,380.767946115101,
381.767596781617,382.767247448134,383.76689811465,384.393158831493),
 .UNSPECIFIED.);
#1162=B_SPLINE_CURVE_WITH_KNOTS('',3,(#49865,#49866,#49867,#49868,#49869,
#49870,#49871,#49872,#49873,#49874,#49875,#49876,#49877,#49878,#49879,#49880,
#49881,#49882,#49883,#49884,#49885,#49886),.UNSPECIFIED.,.F.,.F.,(4,3,3,
3,3,3,3,4),(-393.650030793972,-392.785701195879,-391.786246485457,-390.786791775035,
-389.787337064613,-388.787882354191,-387.788427643769,-387.366845486792),
 .UNSPECIFIED.);
#1163=B_SPLINE_CURVE_WITH_KNOTS('',3,(#49887,#49888,#49889,#49890,#49891,
#49892,#49893,#49894,#49895,#49896,#49897,#49898,#49899,#49900,#49901,#49902,
#49903,#49904,#49905,#49906,#49907,#49908),.UNSPECIFIED.,.F.,.F.,(4,3,3,
3,3,3,3,4),(384.393158831493,384.766548781167,385.766199447684,386.7658501142,
387.765500780717,388.765151447233,389.76480211375,390.676344138673),
 .UNSPECIFIED.);
#1164=B_SPLINE_CURVE_WITH_KNOTS('',3,(#49913,#49914,#49915,#49916,#49917,
#49918,#49919,#49920,#49921,#49922,#49923,#49924,#49925,#49926,#49927,#49928,
#49929,#49930,#49931,#49932,#49933,#49934,#49935,#49936,#49937),
 .UNSPECIFIED.,.F.,.F.,(4,3,3,3,3,3,3,3,4),(-399.933216101151,-399.781884168834,
-398.782429458412,-397.78297474799,-396.783520037568,-395.784065327146,
-394.784610616724,-393.785155906302,-393.650030793972),.UNSPECIFIED.);
#1165=B_SPLINE_CURVE_WITH_KNOTS('',3,(#49938,#49939,#49940,#49941,#49942,
#49943,#49944,#49945,#49946,#49947,#49948,#49949,#49950,#49951,#49952,#49953,
#49954,#49955,#49956,#49957,#49958,#49959,#49960,#49961,#49962),
 .UNSPECIFIED.,.F.,.F.,(4,3,3,3,3,3,3,3,4),(390.676344138673,390.764452780266,
391.764103446783,392.763754113299,393.763404779816,394.763055446333,395.762706112849,
396.762356779366,396.959529445852),.UNSPECIFIED.);
#1166=B_SPLINE_CURVE_WITH_KNOTS('',3,(#49967,#49968,#49969,#49970,#49971,
#49972,#49973,#49974,#49975,#49976,#49977,#49978,#49979,#49980,#49981,#49982,
#49983,#49984,#49985,#49986,#49987,#49988),.UNSPECIFIED.,.F.,.F.,(4,3,3,
3,3,3,3,4),(-406.216401408331,-405.778612431367,-404.779157720944,-403.779703010522,
-402.7802483001,-401.780793589678,-400.781338879256,-399.933216101151),
 .UNSPECIFIED.);
#1167=B_SPLINE_CURVE_WITH_KNOTS('',3,(#49989,#49990,#49991,#49992,#49993,
#49994,#49995,#49996,#49997,#49998,#49999,#50000,#50001,#50002,#50003,#50004,
#50005,#50006,#50007,#50008,#50009,#50010),.UNSPECIFIED.,.F.,.F.,(4,3,3,
3,3,3,3,4),(396.959529445852,397.762007445882,398.761658112399,399.761308778915,
400.760959445432,401.760610111948,402.760260778465,403.242714753032),
 .UNSPECIFIED.);
#1168=B_SPLINE_CURVE_WITH_KNOTS('',3,(#50015,#50016,#50017,#50018,#50019,
#50020,#50021,#50022,#50023,#50024,#50025,#50026,#50027,#50028,#50029,#50030,
#50031,#50032,#50033,#50034,#50035,#50036),.UNSPECIFIED.,.F.,.F.,(4,3,3,
3,3,3,3,4),(-412.499586715511,-411.775340693899,-410.775885983477,-409.776431273055,
-408.776976562633,-407.777521852211,-406.778067141789,-406.216401408331),
 .UNSPECIFIED.);
#1169=B_SPLINE_CURVE_WITH_KNOTS('',3,(#50037,#50038,#50039,#50040,#50041,
#50042,#50043,#50044,#50045,#50046,#50047,#50048,#50049,#50050,#50051,#50052,
#50053,#50054,#50055,#50056,#50057,#50058),.UNSPECIFIED.,.F.,.F.,(4,3,3,
3,3,3,3,4),(403.242714753032,403.759911444982,404.759562111498,405.759212778015,
406.758863444531,407.758514111048,408.758164777564,409.525900060212),
 .UNSPECIFIED.);
#1170=B_SPLINE_CURVE_WITH_KNOTS('',3,(#50063,#50064,#50065,#50066,#50067,
#50068,#50069,#50070,#50071,#50072,#50073,#50074,#50075,#50076,#50077,#50078,
#50079,#50080,#50081,#50082,#50083,#50084,#50085,#50086,#50087),
 .UNSPECIFIED.,.F.,.F.,(4,3,3,3,3,3,3,3,4),(-418.78277202269,-418.771523666854,
-417.772068956432,-416.772614246009,-415.773159535587,-414.773704825165,
-413.774250114743,-412.774795404321,-412.499586715511),.UNSPECIFIED.);
#1171=B_SPLINE_CURVE_WITH_KNOTS('',3,(#50088,#50089,#50090,#50091,#50092,
#50093,#50094,#50095,#50096,#50097,#50098,#50099,#50100,#50101,#50102,#50103,
#50104,#50105,#50106,#50107,#50108,#50109,#50110,#50111,#50112),
 .UNSPECIFIED.,.F.,.F.,(4,3,3,3,3,3,3,3,4),(409.525900060212,409.757815444081,
410.757466110597,411.757116777114,412.756767443631,413.756418110147,414.756068776664,
415.75571944318,415.809085367391),.UNSPECIFIED.);
#1172=B_SPLINE_CURVE_WITH_KNOTS('',3,(#50117,#50118,#50119,#50120,#50121,
#50122,#50123,#50124,#50125,#50126,#50127,#50128,#50129,#50130,#50131,#50132,
#50133,#50134,#50135,#50136,#50137,#50138),.UNSPECIFIED.,.F.,.F.,(4,3,3,
3,3,3,3,4),(-425.06595732987,-424.768251929386,-423.768797218964,-422.769342508542,
-421.76988779812,-420.770433087698,-419.770978377276,-418.78277202269),
 .UNSPECIFIED.);
#1173=B_SPLINE_CURVE_WITH_KNOTS('',3,(#50139,#50140,#50141,#50142,#50143,
#50144,#50145,#50146,#50147,#50148,#50149,#50150,#50151,#50152,#50153,#50154,
#50155,#50156,#50157,#50158,#50159,#50160),.UNSPECIFIED.,.F.,.F.,(4,3,3,
3,3,3,3,4),(415.809085367391,416.755370109697,417.755020776213,418.75467144273,
419.754322109246,420.753972775763,421.753623442279,422.092270674571),
 .UNSPECIFIED.);
#1174=B_SPLINE_CURVE_WITH_KNOTS('',3,(#50165,#50166,#50167,#50168,#50169,
#50170,#50171,#50172,#50173,#50174,#50175,#50176,#50177,#50178,#50179,#50180,
#50181,#50182,#50183,#50184,#50185,#50186),.UNSPECIFIED.,.F.,.F.,(4,3,3,
3,3,3,3,4),(-431.349142637049,-430.764980191919,-429.765525481497,-428.766070771075,
-427.766616060652,-426.76716135023,-425.767706639808,-425.06595732987),
 .UNSPECIFIED.);
#1175=B_SPLINE_CURVE_WITH_KNOTS('',3,(#50187,#50188,#50189,#50190,#50191,
#50192,#50193,#50194,#50195,#50196,#50197,#50198,#50199,#50200,#50201,#50202,
#50203,#50204,#50205,#50206,#50207,#50208),.UNSPECIFIED.,.F.,.F.,(4,3,3,
3,3,3,3,4),(422.092270674571,422.753274108796,423.752924775313,424.752575441829,
425.752226108346,426.751876774862,427.751527441379,428.37545598175),
 .UNSPECIFIED.);
#1176=B_SPLINE_CURVE_WITH_KNOTS('',3,(#50213,#50214,#50215,#50216,#50217,
#50218,#50219,#50220,#50221,#50222,#50223,#50224,#50225,#50226,#50227,#50228,
#50229,#50230,#50231,#50232,#50233,#50234),.UNSPECIFIED.,.F.,.F.,(4,3,3,
3,3,3,3,4),(-437.632327944229,-436.761708454451,-435.762253744029,-434.762799033607,
-433.763344323185,-432.763889612763,-431.764434902341,-431.349142637049),
 .UNSPECIFIED.);
#1177=B_SPLINE_CURVE_WITH_KNOTS('',3,(#50235,#50236,#50237,#50238,#50239,
#50240,#50241,#50242,#50243,#50244,#50245,#50246,#50247,#50248,#50249,#50250,
#50251,#50252,#50253,#50254,#50255,#50256),.UNSPECIFIED.,.F.,.F.,(4,3,3,
3,3,3,3,4),(428.37545598175,428.751178107895,429.750828774412,430.750479440928,
431.750130107445,432.749780773961,433.749431440478,434.65864128893),
 .UNSPECIFIED.);
#1178=B_SPLINE_CURVE_WITH_KNOTS('',3,(#50261,#50262,#50263,#50264,#50265,
#50266,#50267,#50268,#50269,#50270,#50271,#50272,#50273,#50274,#50275,#50276,
#50277,#50278,#50279,#50280,#50281,#50282,#50283,#50284,#50285),
 .UNSPECIFIED.,.F.,.F.,(4,3,3,3,3,3,3,3,4),(-443.915513251408,-443.757891427406,
-442.758436716984,-441.758982006562,-440.75952729614,-439.760072585717,
-438.760617875295,-437.761163164873,-437.632327944229),.UNSPECIFIED.);
#1179=B_SPLINE_CURVE_WITH_KNOTS('',3,(#50286,#50287,#50288,#50289,#50290,
#50291,#50292,#50293,#50294,#50295,#50296,#50297,#50298,#50299,#50300,#50301,
#50302,#50303,#50304,#50305,#50306,#50307,#50308,#50309,#50310),
 .UNSPECIFIED.,.F.,.F.,(4,3,3,3,3,3,3,3,4),(434.65864128893,434.749082106995,
435.748732773511,436.748383440028,437.748034106544,438.747684773061,439.747335439577,
440.746986106094,440.941826596109),.UNSPECIFIED.);
#1180=B_SPLINE_CURVE_WITH_KNOTS('',3,(#50315,#50316,#50317,#50318,#50319,
#50320,#50321,#50322,#50323,#50324,#50325,#50326,#50327,#50328,#50329,#50330,
#50331,#50332,#50333,#50334,#50335,#50336),.UNSPECIFIED.,.F.,.F.,(4,3,3,
3,3,3,3,4),(-450.198698558588,-449.754619689938,-448.755164979516,-447.755710269094,
-446.756255558672,-445.75680084825,-444.757346137828,-443.915513251408),
 .UNSPECIFIED.);
#1181=B_SPLINE_CURVE_WITH_KNOTS('',3,(#50337,#50338,#50339,#50340,#50341,
#50342,#50343,#50344,#50345,#50346,#50347,#50348,#50349,#50350,#50351,#50352,
#50353,#50354,#50355,#50356,#50357,#50358),.UNSPECIFIED.,.F.,.F.,(4,3,3,
3,3,3,3,4),(440.941826596109,441.74663677261,442.746287439127,443.745938105644,
444.74558877216,445.745239438677,446.744890105193,447.225011903289),
 .UNSPECIFIED.);
#1182=B_SPLINE_CURVE_WITH_KNOTS('',3,(#50363,#50364,#50365,#50366,#50367,
#50368,#50369,#50370,#50371,#50372,#50373,#50374,#50375,#50376,#50377,#50378,
#50379,#50380,#50381,#50382,#50383,#50384),.UNSPECIFIED.,.F.,.F.,(4,3,3,
3,3,3,3,4),(-456.481883865768,-455.751347952471,-454.751893242049,-453.752438531627,
-452.752983821205,-451.753529110783,-450.75407440036,-450.198698558588),
 .UNSPECIFIED.);
#1183=B_SPLINE_CURVE_WITH_KNOTS('',3,(#50385,#50386,#50387,#50388,#50389,
#50390,#50391,#50392,#50393,#50394,#50395,#50396,#50397,#50398,#50399,#50400,
#50401,#50402,#50403,#50404,#50405,#50406),.UNSPECIFIED.,.F.,.F.,(4,3,3,
3,3,3,3,4),(447.225011903289,447.74454077171,448.744191438226,449.743842104743,
450.74349277126,451.743143437776,452.742794104293,453.508197210468),
 .UNSPECIFIED.);
#1184=B_SPLINE_CURVE_WITH_KNOTS('',3,(#50411,#50412,#50413,#50414,#50415,
#50416,#50417,#50418,#50419,#50420,#50421,#50422,#50423,#50424,#50425,#50426,
#50427,#50428,#50429,#50430,#50431,#50432,#50433,#50434,#50435),
 .UNSPECIFIED.,.F.,.F.,(4,3,3,3,3,3,3,3,4),(-462.765069172947,-462.747530925425,
-461.748076215003,-460.748621504581,-459.749166794159,-458.749712083737,
-457.750257373315,-456.750802662893,-456.481883865768),.UNSPECIFIED.);
#1185=B_SPLINE_CURVE_WITH_KNOTS('',3,(#50436,#50437,#50438,#50439,#50440,
#50441,#50442,#50443,#50444,#50445,#50446,#50447,#50448,#50449,#50450,#50451,
#50452,#50453,#50454,#50455,#50456,#50457,#50458,#50459,#50460),
 .UNSPECIFIED.,.F.,.F.,(4,3,3,3,3,3,3,3,4),(453.508197210468,453.742444770809,
454.742095437326,455.741746103842,456.741396770359,457.741047436875,458.740698103392,
459.740348769908,459.791382517648),.UNSPECIFIED.);
#1186=B_SPLINE_CURVE_WITH_KNOTS('',3,(#50465,#50466,#50467,#50468,#50469,
#50470,#50471,#50472,#50473,#50474,#50475,#50476,#50477,#50478,#50479,#50480,
#50481,#50482,#50483,#50484,#50485,#50486),.UNSPECIFIED.,.F.,.F.,(4,3,3,
3,3,3,3,4),(-469.048254480127,-468.744259187958,-467.744804477536,-466.745349767114,
-465.745895056692,-464.74644034627,-463.746985635847,-462.765069172947),
 .UNSPECIFIED.);
#1187=B_SPLINE_CURVE_WITH_KNOTS('',3,(#50487,#50488,#50489,#50490,#50491,
#50492,#50493,#50494,#50495,#50496,#50497,#50498,#50499,#50500,#50501,#50502,
#50503,#50504,#50505,#50506,#50507,#50508),.UNSPECIFIED.,.F.,.F.,(4,3,3,
3,3,3,3,4),(459.791382517648,460.739999436425,461.739650102942,462.739300769458,
463.738951435975,464.738602102491,465.738252769008,466.074567824828),
 .UNSPECIFIED.);
#1188=B_SPLINE_CURVE_WITH_KNOTS('',3,(#50513,#50514,#50515,#50516,#50517,
#50518,#50519,#50520,#50521,#50522,#50523,#50524,#50525,#50526,#50527,#50528,
#50529,#50530,#50531,#50532,#50533,#50534),.UNSPECIFIED.,.F.,.F.,(4,3,3,
3,3,3,3,4),(-475.331439787306,-474.74098745049,-473.741532740068,-472.742078029646,
-471.742623319224,-470.743168608802,-469.74371389838,-469.048254480127),
 .UNSPECIFIED.);
#1189=B_SPLINE_CURVE_WITH_KNOTS('',3,(#50535,#50536,#50537,#50538,#50539,
#50540,#50541,#50542,#50543,#50544,#50545,#50546,#50547,#50548,#50549,#50550,
#50551,#50552,#50553,#50554,#50555,#50556),.UNSPECIFIED.,.F.,.F.,(4,3,3,
3,3,3,3,4),(466.074567824828,466.737903435524,467.737554102041,468.737204768557,
469.736855435074,470.736506101591,471.736156768107,472.357753132007),
 .UNSPECIFIED.);
#1190=B_SPLINE_CURVE_WITH_KNOTS('',3,(#50561,#50562,#50563,#50564,#50565,
#50566,#50567,#50568,#50569,#50570,#50571,#50572,#50573,#50574,#50575,#50576,
#50577,#50578,#50579,#50580,#50581,#50582),.UNSPECIFIED.,.F.,.F.,(4,3,3,
3,3,3,3,4),(-481.614625094486,-480.737715713023,-479.738261002601,-478.738806292179,
-477.739351581757,-476.739896871335,-475.740442160912,-475.331439787306),
 .UNSPECIFIED.);
#1191=B_SPLINE_CURVE_WITH_KNOTS('',3,(#50583,#50584,#50585,#50586,#50587,
#50588,#50589,#50590,#50591,#50592,#50593,#50594,#50595,#50596,#50597,#50598,
#50599,#50600,#50601,#50602,#50603,#50604),.UNSPECIFIED.,.F.,.F.,(4,3,3,
3,3,3,3,4),(472.357753132007,472.735807434623,473.73545810114,474.735108767657,
475.734759434173,476.73441010069,477.734060767206,478.640938439187),
 .UNSPECIFIED.);
#1192=B_SPLINE_CURVE_WITH_KNOTS('',3,(#50609,#50610,#50611,#50612,#50613,
#50614,#50615,#50616,#50617,#50618,#50619,#50620,#50621,#50622,#50623,#50624,
#50625,#50626,#50627,#50628,#50629,#50630,#50631,#50632,#50633),
 .UNSPECIFIED.,.F.,.F.,(4,3,3,3,3,3,3,3,4),(-487.897810401665,-487.733898685978,
-486.734443975555,-485.734989265133,-484.735534554711,-483.736079844289,
-482.736625133867,-481.737170423445,-481.614625094486),.UNSPECIFIED.);
#1193=B_SPLINE_CURVE_WITH_KNOTS('',3,(#50634,#50635,#50636,#50637,#50638,
#50639,#50640,#50641,#50642,#50643,#50644,#50645,#50646,#50647,#50648,#50649,
#50650,#50651,#50652,#50653,#50654,#50655,#50656,#50657,#50658),
 .UNSPECIFIED.,.F.,.F.,(4,3,3,3,3,3,3,3,4),(478.640938439187,478.733711433723,
479.733362100239,480.733012766756,481.732663433272,482.732314099789,483.731964766306,
484.731615432822,484.924123746366),.UNSPECIFIED.);
#1194=B_SPLINE_CURVE_WITH_KNOTS('',3,(#50663,#50664,#50665,#50666,#50667,
#50668,#50669,#50670,#50671,#50672,#50673,#50674,#50675,#50676,#50677,#50678,
#50679,#50680,#50681,#50682,#50683,#50684),.UNSPECIFIED.,.F.,.F.,(4,3,3,
3,3,3,3,4),(-494.180995708845,-493.73062694851,-492.731172238088,-491.731717527666,
-490.732262817244,-489.732808106822,-488.7333533964,-487.897810401665),
 .UNSPECIFIED.);
#1195=B_SPLINE_CURVE_WITH_KNOTS('',3,(#50685,#50686,#50687,#50688,#50689,
#50690,#50691,#50692,#50693,#50694,#50695,#50696,#50697,#50698,#50699,#50700,
#50701,#50702,#50703,#50704,#50705,#50706),.UNSPECIFIED.,.F.,.F.,(4,3,3,
3,3,3,3,4),(484.924123746366,485.731266099339,486.730916765855,487.730567432372,
488.730218098888,489.729868765405,490.729519431921,491.207309053546),
 .UNSPECIFIED.);
#1196=B_SPLINE_CURVE_WITH_KNOTS('',3,(#50715,#50716,#50717,#50718,#50719,
#50720,#50721,#50722,#50723,#50724,#50725,#50726,#50727,#50728,#50729,#50730,
#50731,#50732,#50733),.UNSPECIFIED.,.F.,.F.,(4,3,3,3,3,3,4),(-504.724628763153,
-504.224901407942,-503.725174052731,-502.725719342309,-501.726264631887,
-500.726809921465,-500.464181016024),.UNSPECIFIED.);
#1197=B_SPLINE_CURVE_WITH_KNOTS('',3,(#50737,#50738,#50739,#50740,#50741,
#50742,#50743,#50744,#50745,#50746,#50747,#50748,#50749,#50750,#50751,#50752,
#50753,#50754,#50755),.UNSPECIFIED.,.F.,.F.,(4,3,3,3,3,3,4),(497.490494360725,
497.727074097537,498.726724764054,499.726375430571,500.726026097087,501.725676763604,
502.654824574367),.UNSPECIFIED.);
#1198=B_SPLINE_CURVE_WITH_KNOTS('',3,(#50762,#50763,#50764,#50765,#50766,
#50767,#50768,#50769,#50770,#50771),.UNSPECIFIED.,.F.,.F.,(4,3,3,4),(512.079602535136,
512.342231440576,513.341686150999,514.270246093479),.UNSPECIFIED.);
#1199=B_SPLINE_CURVE_WITH_KNOTS('',3,(#50774,#50775,#50776,#50777,#50778,
#50779,#50780),.UNSPECIFIED.,.F.,.F.,(4,3,4),(512.079602535136,512.530726297128,
513.030551630386),.UNSPECIFIED.);
#1200=B_SPLINE_CURVE_WITH_KNOTS('',3,(#50785,#50786,#50787,#50788,#50789,
#50790,#50791,#50792,#50793,#50794),.UNSPECIFIED.,.F.,.F.,(4,1,1,1,1,1,
1,4),(505.796417227957,506.345503178044,507.344957888466,508.344412598888,
509.34386730931,510.343322019732,511.342776730154,512.079602535136),
 .UNSPECIFIED.);
#1201=B_SPLINE_CURVE_WITH_KNOTS('',3,(#50795,#50796,#50797,#50798,#50799,
#50800,#50801,#50802,#50803,#50804,#50805),.UNSPECIFIED.,.F.,.F.,(4,1,1,
1,1,1,1,1,4),(505.796417227957,506.03299696477,507.032647631287,508.032298297803,
509.03194896432,510.031599630836,511.031250297353,512.030900963869,512.079602535136),
 .UNSPECIFIED.);
#1202=B_SPLINE_CURVE_WITH_KNOTS('',3,(#50810,#50811,#50812,#50813,#50814,
#50815,#50816,#50817,#50818,#50819),.UNSPECIFIED.,.F.,.F.,(4,1,1,1,1,1,
1,4),(499.513231920777,500.348774915511,501.348229625934,502.347684336356,
503.347139046778,504.3465937572,505.346048467622,505.796417227957),
 .UNSPECIFIED.);
#1203=B_SPLINE_CURVE_WITH_KNOTS('',3,(#50820,#50821,#50822,#50823,#50824,
#50825,#50826,#50827,#50828,#50829),.UNSPECIFIED.,.F.,.F.,(4,1,1,1,1,1,
1,4),(499.513231920777,500.035092965671,501.034743632187,502.034394298704,
503.03404496522,504.033695631737,505.033346298253,505.796417227957),
 .UNSPECIFIED.);
#1204=B_SPLINE_CURVE_WITH_KNOTS('',3,(#50834,#50835,#50836,#50837,#50838,
#50839,#50840,#50841,#50842,#50843,#50844),.UNSPECIFIED.,.F.,.F.,(4,1,1,
1,1,1,1,1,4),(493.230046613597,493.352591942557,494.352046652979,495.351501363401,
496.350956073823,497.350410784245,498.349865494667,499.349320205089,499.513231920777),
 .UNSPECIFIED.);
#1205=B_SPLINE_CURVE_WITH_KNOTS('',3,(#50845,#50846,#50847,#50848,#50849,
#50850,#50851,#50852,#50853,#50854),.UNSPECIFIED.,.F.,.F.,(4,1,1,1,1,1,
1,4),(493.230046613598,494.037188966571,495.036839633088,496.036490299605,
497.036140966121,498.035791632638,499.035442299154,499.513231920777),
 .UNSPECIFIED.);
#1206=B_SPLINE_CURVE_WITH_KNOTS('',3,(#50859,#50860,#50861,#50862,#50863,
#50864,#50865,#50866,#50867,#50868),.UNSPECIFIED.,.F.,.F.,(4,1,1,1,1,1,
1,4),(486.946861306418,487.355863680024,488.355318390446,489.354773100868,
490.354227811291,491.353682521713,492.353137232135,493.230046613597),
 .UNSPECIFIED.);
#1207=B_SPLINE_CURVE_WITH_KNOTS('',3,(#50869,#50870,#50871,#50872,#50873,
#50874,#50875,#50876,#50877,#50878,#50879),.UNSPECIFIED.,.F.,.F.,(4,1,1,
1,1,1,1,1,4),(486.946861306418,487.039634300956,488.039284967472,489.038935633989,
490.038586300505,491.038236967022,492.037887633538,493.037538300055,493.230046613598),
 .UNSPECIFIED.);
#1208=B_SPLINE_CURVE_WITH_KNOTS('',3,(#50884,#50885,#50886,#50887,#50888,
#50889,#50890,#50891,#50892,#50893),.UNSPECIFIED.,.F.,.F.,(4,1,1,1,1,1,
1,4),(480.663675999238,481.359135417492,482.358590127914,483.358044838336,
484.357499548758,485.35695425918,486.356408969602,486.946861306418),
 .UNSPECIFIED.);
#1209=B_SPLINE_CURVE_WITH_KNOTS('',3,(#50894,#50895,#50896,#50897,#50898,
#50899,#50900,#50901,#50902,#50903),.UNSPECIFIED.,.F.,.F.,(4,1,1,1,1,1,
1,4),(480.663675999238,481.041730301856,482.041380968373,483.041031634889,
484.040682301406,485.040332967922,486.039983634439,486.946861306418),
 .UNSPECIFIED.);
#1210=B_SPLINE_CURVE_WITH_KNOTS('',3,(#50908,#50909,#50910,#50911,#50912,
#50913,#50914,#50915,#50916,#50917),.UNSPECIFIED.,.F.,.F.,(4,1,1,1,1,1,
1,4),(474.380490692059,475.362407154959,476.361861865381,477.361316575803,
478.360771286226,479.360225996648,480.35968070707,480.663675999238),
 .UNSPECIFIED.);
#1211=B_SPLINE_CURVE_WITH_KNOTS('',3,(#50918,#50919,#50920,#50921,#50922,
#50923,#50924,#50925,#50926,#50927),.UNSPECIFIED.,.F.,.F.,(4,1,1,1,1,1,
1,4),(474.380490692059,475.043826302757,476.043476969273,477.04312763579,
478.042778302307,479.042428968823,480.04207963534,480.663675999238),
 .UNSPECIFIED.);
#1212=B_SPLINE_CURVE_WITH_KNOTS('',3,(#50932,#50933,#50934,#50935,#50936,
#50937,#50938,#50939,#50940,#50941,#50942),.UNSPECIFIED.,.F.,.F.,(4,1,1,
1,1,1,1,1,4),(468.097305384879,468.366224182005,469.365678892427,470.365133602849,
471.364588313271,472.364043023693,473.363497734115,474.362952444537,474.380490692059),
 .UNSPECIFIED.);
#1213=B_SPLINE_CURVE_WITH_KNOTS('',3,(#50943,#50944,#50945,#50946,#50947,
#50948,#50949,#50950,#50951,#50952),.UNSPECIFIED.,.F.,.F.,(4,1,1,1,1,1,
1,4),(468.097305384879,469.045922303658,470.045572970174,471.045223636691,
472.044874303207,473.044524969724,474.04417563624,474.380490692059),
 .UNSPECIFIED.);
#1214=B_SPLINE_CURVE_WITH_KNOTS('',3,(#50957,#50958,#50959,#50960,#50961,
#50962,#50963,#50964,#50965,#50966),.UNSPECIFIED.,.F.,.F.,(4,1,1,1,1,1,
1,4),(461.814120077699,462.369495919472,463.368950629894,464.368405340316,
465.367860050738,466.367314761161,467.366769471583,468.097305384879),
 .UNSPECIFIED.);
#1215=B_SPLINE_CURVE_WITH_KNOTS('',3,(#50967,#50968,#50969,#50970,#50971,
#50972,#50973,#50974,#50975,#50976,#50977),.UNSPECIFIED.,.F.,.F.,(4,1,1,
1,1,1,1,1,4),(461.8141200777,462.048367638042,463.048018304558,464.047668971075,
465.047319637591,466.046970304108,467.046620970625,468.046271637141,468.097305384879),
 .UNSPECIFIED.);
#1216=B_SPLINE_CURVE_WITH_KNOTS('',3,(#50982,#50983,#50984,#50985,#50986,
#50987,#50988,#50989,#50990,#50991),.UNSPECIFIED.,.F.,.F.,(4,1,1,1,1,1,
1,4),(455.53093477052,456.37276765694,457.372222367362,458.371677077784,
459.371131788206,460.370586498628,461.37004120905,461.814120077699),
 .UNSPECIFIED.);
#1217=B_SPLINE_CURVE_WITH_KNOTS('',3,(#50992,#50993,#50994,#50995,#50996,
#50997,#50998,#50999,#51000,#51001),.UNSPECIFIED.,.F.,.F.,(4,1,1,1,1,1,
1,4),(455.53093477052,456.050463638942,457.050114305459,458.049764971976,
459.049415638492,460.049066305009,461.048716971525,461.8141200777),
 .UNSPECIFIED.);
#1218=B_SPLINE_CURVE_WITH_KNOTS('',3,(#51006,#51007,#51008,#51009,#51010,
#51011,#51012,#51013,#51014,#51015,#51016),.UNSPECIFIED.,.F.,.F.,(4,1,1,
1,1,1,1,1,4),(449.24774946334,449.376584683985,450.376039394407,451.375494104829,
452.374948815251,453.374403525673,454.373858236095,455.373312946518,455.53093477052),
 .UNSPECIFIED.);
#1219=B_SPLINE_CURVE_WITH_KNOTS('',3,(#51017,#51018,#51019,#51020,#51021,
#51022,#51023,#51024,#51025,#51026),.UNSPECIFIED.,.F.,.F.,(4,1,1,1,1,1,
1,4),(449.247749463341,450.052559639843,451.05221030636,452.051860972876,
453.051511639393,454.051162305909,455.050812972426,455.53093477052),
 .UNSPECIFIED.);
#1220=B_SPLINE_CURVE_WITH_KNOTS('',3,(#51031,#51032,#51033,#51034,#51035,
#51036,#51037,#51038,#51039,#51040),.UNSPECIFIED.,.F.,.F.,(4,1,1,1,1,1,
1,4),(442.964564156161,443.379856421453,444.379311131875,445.378765842297,
446.378220552719,447.377675263141,448.377129973563,449.24774946334),
 .UNSPECIFIED.);
#1221=B_SPLINE_CURVE_WITH_KNOTS('',3,(#51041,#51042,#51043,#51044,#51045,
#51046,#51047,#51048,#51049,#51050,#51051),.UNSPECIFIED.,.F.,.F.,(4,1,1,
1,1,1,1,1,4),(442.964564156161,443.055004974227,444.054655640744,445.05430630726,
446.053956973777,447.053607640293,448.05325830681,449.052908973327,449.247749463341),
 .UNSPECIFIED.);
#1222=B_SPLINE_CURVE_WITH_KNOTS('',3,(#51056,#51057,#51058,#51059,#51060,
#51061,#51062,#51063,#51064,#51065),.UNSPECIFIED.,.F.,.F.,(4,1,1,1,1,1,
1,4),(436.681378848981,437.38312815892,438.382582869342,439.382037579764,
440.381492290186,441.380947000608,442.380401711031,442.964564156161),
 .UNSPECIFIED.);
#1223=B_SPLINE_CURVE_WITH_KNOTS('',3,(#51066,#51067,#51068,#51069,#51070,
#51071,#51072,#51073,#51074,#51075),.UNSPECIFIED.,.F.,.F.,(4,1,1,1,1,1,
1,4),(436.681378848981,437.057100975128,438.056751641645,439.056402308161,
440.056052974678,441.055703641194,442.055354307711,442.964564156161),
 .UNSPECIFIED.);
#1224=B_SPLINE_CURVE_WITH_KNOTS('',3,(#51080,#51081,#51082,#51083,#51084,
#51085,#51086,#51087,#51088,#51089),.UNSPECIFIED.,.F.,.F.,(4,1,1,1,1,1,
1,4),(430.398193541802,431.386399896388,432.38585460681,433.385309317232,
434.384764027654,435.384218738076,436.383673448498,436.681378848981),
 .UNSPECIFIED.);
#1225=B_SPLINE_CURVE_WITH_KNOTS('',3,(#51090,#51091,#51092,#51093,#51094,
#51095,#51096,#51097,#51098,#51099),.UNSPECIFIED.,.F.,.F.,(4,1,1,1,1,1,
1,4),(430.398193541802,431.059196976029,432.058847642545,433.058498309062,
434.058148975578,435.057799642095,436.057450308611,436.681378848981),
 .UNSPECIFIED.);
#1226=B_SPLINE_CURVE_WITH_KNOTS('',3,(#51104,#51105,#51106,#51107,#51108,
#51109,#51110,#51111,#51112,#51113,#51114),.UNSPECIFIED.,.F.,.F.,(4,1,1,
1,1,1,1,1,4),(424.115008234622,424.390216923433,425.389671633855,426.389126344277,
427.388581054699,428.388035765121,429.387490475543,430.386945185965,430.398193541802),
 .UNSPECIFIED.);
#1227=B_SPLINE_CURVE_WITH_KNOTS('',3,(#51115,#51116,#51117,#51118,#51119,
#51120,#51121,#51122,#51123,#51124),.UNSPECIFIED.,.F.,.F.,(4,1,1,1,1,1,
1,4),(424.115008234622,425.061292976929,426.060943643446,427.060594309962,
428.060244976479,429.059895642996,430.059546309512,430.398193541802),
 .UNSPECIFIED.);
#1228=B_SPLINE_CURVE_WITH_KNOTS('',3,(#51129,#51130,#51131,#51132,#51133,
#51134,#51135,#51136,#51137,#51138),.UNSPECIFIED.,.F.,.F.,(4,1,1,1,1,1,
1,4),(417.831822927443,418.3934886609,419.392943371323,420.392398081745,
421.391852792167,422.391307502589,423.390762213011,424.115008234622),
 .UNSPECIFIED.);
#1229=B_SPLINE_CURVE_WITH_KNOTS('',3,(#51139,#51140,#51141,#51142,#51143,
#51144,#51145,#51146,#51147,#51148,#51149),.UNSPECIFIED.,.F.,.F.,(4,1,1,
1,1,1,1,1,4),(417.831822927443,418.063738311314,419.06338897783,420.063039644347,
421.062690310863,422.06234097738,423.061991643896,424.061642310413,424.115008234622),
 .UNSPECIFIED.);
#1230=B_SPLINE_CURVE_WITH_KNOTS('',3,(#51154,#51155,#51156,#51157,#51158,
#51159,#51160,#51161,#51162,#51163),.UNSPECIFIED.,.F.,.F.,(4,1,1,1,1,1,
1,4),(411.548637620263,412.396760398368,413.39621510879,414.395669819212,
415.395124529634,416.394579240056,417.394033950478,417.831822927443),
 .UNSPECIFIED.);
#1231=B_SPLINE_CURVE_WITH_KNOTS('',3,(#51164,#51165,#51166,#51167,#51168,
#51169,#51170,#51171,#51172,#51173),.UNSPECIFIED.,.F.,.F.,(4,1,1,1,1,1,
1,4),(411.548637620263,412.065834312214,413.065484978731,414.065135645247,
415.064786311764,416.06443697828,417.064087644797,417.831822927443),
 .UNSPECIFIED.);
#1232=B_SPLINE_CURVE_WITH_KNOTS('',3,(#51178,#51179,#51180,#51181,#51182,
#51183,#51184,#51185,#51186,#51187,#51188),.UNSPECIFIED.,.F.,.F.,(4,1,1,
1,1,1,1,1,4),(405.265452313083,405.400577425413,406.400032135835,407.399486846258,
408.39894155668,409.398396267102,410.397850977524,411.397305687946,411.548637620263),
 .UNSPECIFIED.);
#1233=B_SPLINE_CURVE_WITH_KNOTS('',3,(#51189,#51190,#51191,#51192,#51193,
#51194,#51195,#51196,#51197,#51198),.UNSPECIFIED.,.F.,.F.,(4,1,1,1,1,1,
1,4),(405.265452313084,406.067930313115,407.067580979631,408.067231646148,
409.066882312665,410.066532979181,411.066183645698,411.548637620263),
 .UNSPECIFIED.);
#1234=B_SPLINE_CURVE_WITH_KNOTS('',3,(#51203,#51204,#51205,#51206,#51207,
#51208,#51209,#51210,#51211,#51212),.UNSPECIFIED.,.F.,.F.,(4,1,1,1,1,1,
1,4),(398.982267005904,399.403849162881,400.403303873303,401.402758583725,
402.402213294147,403.401668004569,404.401122714991,405.265452313083),
 .UNSPECIFIED.);
#1235=B_SPLINE_CURVE_WITH_KNOTS('',3,(#51213,#51214,#51215,#51216,#51217,
#51218,#51219,#51220,#51221,#51222,#51223),.UNSPECIFIED.,.F.,.F.,(4,1,1,
1,1,1,1,1,4),(398.982267005904,399.070375647499,400.070026314016,401.069676980532,
402.069327647049,403.068978313565,404.068628980082,405.068279646598,405.265452313084),
 .UNSPECIFIED.);
#1236=B_SPLINE_CURVE_WITH_KNOTS('',3,(#51228,#51229,#51230,#51231,#51232,
#51233,#51234,#51235,#51236,#51237),.UNSPECIFIED.,.F.,.F.,(4,1,1,1,1,1,
1,4),(392.699081698724,393.407120900348,394.40657561077,395.406030321192,
396.405485031615,397.404939742037,398.404394452459,398.982267005904),
 .UNSPECIFIED.);
#1237=B_SPLINE_CURVE_WITH_KNOTS('',3,(#51238,#51239,#51240,#51241,#51242,
#51243,#51244,#51245,#51246,#51247),.UNSPECIFIED.,.F.,.F.,(4,1,1,1,1,1,
1,4),(392.699081698725,393.0724716484,394.072122314916,395.071772981433,
396.071423647949,397.071074314466,398.070724980982,398.982267005904),
 .UNSPECIFIED.);
#1238=B_SPLINE_CURVE_WITH_KNOTS('',3,(#51252,#51253,#51254,#51255,#51256,
#51257,#51258,#51259,#51260,#51261),.UNSPECIFIED.,.F.,.F.,(4,1,1,1,1,1,
1,4),(386.415896391545,387.410392637816,388.409847348238,389.40930205866,
390.408756769082,391.408211479504,392.407666189926,392.699081698724),
 .UNSPECIFIED.);
#1239=B_SPLINE_CURVE_WITH_KNOTS('',3,(#51262,#51263,#51264,#51265,#51266,
#51267,#51268,#51269,#51270,#51271),.UNSPECIFIED.,.F.,.F.,(4,1,1,1,1,1,
1,4),(386.415896391545,387.0745676493,388.074218315817,389.073868982334,
390.07351964885,391.073170315367,392.072820981883,392.699081698725),
 .UNSPECIFIED.);
#1240=B_SPLINE_CURVE_WITH_KNOTS('',3,(#51276,#51277,#51278,#51279,#51280,
#51281,#51282,#51283,#51284,#51285,#51286),.UNSPECIFIED.,.F.,.F.,(4,1,1,
1,1,1,1,1,4),(380.132711084365,380.414209664861,381.413664375283,382.413119085705,
383.412573796127,384.41202850655,385.411483216972,386.410937927394,386.415896391545),
 .UNSPECIFIED.);
#1241=B_SPLINE_CURVE_WITH_KNOTS('',3,(#51287,#51288,#51289,#51290,#51291,
#51292,#51293,#51294,#51295,#51296),.UNSPECIFIED.,.F.,.F.,(4,1,1,1,1,1,
1,4),(380.132711084365,381.076663650201,382.076314316718,383.075964983234,
384.075615649751,385.075266316267,386.074916982784,386.415896391545),
 .UNSPECIFIED.);
#1242=B_SPLINE_CURVE_WITH_KNOTS('',3,(#51301,#51302,#51303,#51304,#51305,
#51306,#51307,#51308,#51309,#51310),.UNSPECIFIED.,.F.,.F.,(4,1,1,1,1,1,
1,4),(373.849525777186,374.417481402329,375.416936112751,376.416390823173,
377.415845533595,378.415300244017,379.414754954439,380.132711084365),
 .UNSPECIFIED.);
#1243=B_SPLINE_CURVE_WITH_KNOTS('',3,(#51311,#51312,#51313,#51314,#51315,
#51316,#51317,#51318,#51319,#51320,#51321),.UNSPECIFIED.,.F.,.F.,(4,1,1,
1,1,1,1,1,4),(373.849525777186,374.079108984585,375.078759651102,376.078410317618,
377.078060984135,378.077711650651,379.077362317168,380.077012983685,380.132711084365),
 .UNSPECIFIED.);
#1244=B_SPLINE_CURVE_WITH_KNOTS('',3,(#51326,#51327,#51328,#51329,#51330,
#51331,#51332,#51333,#51334,#51335),.UNSPECIFIED.,.F.,.F.,(4,1,1,1,1,1,
1,4),(367.566340470006,368.420753139796,369.420207850218,370.41966256064,
371.419117271062,372.418571981485,373.418026691907,373.849525777186),
 .UNSPECIFIED.);
#1245=B_SPLINE_CURVE_WITH_KNOTS('',3,(#51336,#51337,#51338,#51339,#51340,
#51341,#51342,#51343,#51344,#51345),.UNSPECIFIED.,.F.,.F.,(4,1,1,1,1,1,
1,4),(367.566340470006,368.081204985486,369.080855652002,370.080506318519,
371.080156985036,372.079807651552,373.079458318069,373.849525777186),
 .UNSPECIFIED.);
#1246=B_SPLINE_CURVE_WITH_KNOTS('',3,(#51350,#51351,#51352,#51353,#51354,
#51355,#51356,#51357,#51358,#51359,#51360),.UNSPECIFIED.,.F.,.F.,(4,1,1,
1,1,1,1,1,4),(361.283155162826,361.424570166842,362.424024877264,363.423479587686,
364.422934298108,365.42238900853,366.421843718952,367.421298429374,367.566340470006),
 .UNSPECIFIED.);
#1247=B_SPLINE_CURVE_WITH_KNOTS('',3,(#51361,#51362,#51363,#51364,#51365,
#51366,#51367,#51368,#51369,#51370),.UNSPECIFIED.,.F.,.F.,(4,1,1,1,1,1,
1,4),(361.283155162827,362.083300986387,363.082951652903,364.08260231942,
365.082252985936,366.081903652453,367.081554318969,367.566340470006),
 .UNSPECIFIED.);
#1248=B_SPLINE_CURVE_WITH_KNOTS('',3,(#51375,#51376,#51377,#51378,#51379,
#51380,#51381,#51382,#51383,#51384,#51385,#51386,#51387,#51388,#51389,#51390,
#51391,#51392,#51393,#51394,#51395,#51396),.UNSPECIFIED.,.F.,.F.,(4,3,3,
3,3,3,3,4),(354.999969855647,355.427841904309,356.427296614731,357.426751325153,
358.426206035575,359.425660745998,360.42511545642,361.283155162826),
 .UNSPECIFIED.);
#1249=B_SPLINE_CURVE_WITH_KNOTS('',3,(#51397,#51398,#51399,#51400,#51401,
#51402,#51403,#51404,#51405,#51406,#51407),.UNSPECIFIED.,.F.,.F.,(4,1,1,
1,1,1,1,1,4),(354.999969855647,355.085746320771,356.085396987287,357.085047653804,
358.08469832032,359.084348986837,360.083999653354,361.08365031987,361.283155162827),
 .UNSPECIFIED.);
#1250=B_SPLINE_CURVE_WITH_KNOTS('',3,(#51412,#51413,#51414,#51415,#51416,
#51417,#51418,#51419,#51420,#51421,#51422,#51423,#51424,#51425,#51426,#51427,
#51428,#51429,#51430,#51431,#51432,#51433),.UNSPECIFIED.,.F.,.F.,(4,3,3,
3,3,3,3,4),(348.716784548467,349.431113641777,350.430568352199,351.430023062621,
352.429477773043,353.428932483465,354.428387193887,354.999969855647),
 .UNSPECIFIED.);
#1251=B_SPLINE_CURVE_WITH_KNOTS('',3,(#51434,#51435,#51436,#51437,#51438,
#51439,#51440,#51441,#51442,#51443),.UNSPECIFIED.,.F.,.F.,(4,1,1,1,1,1,
1,4),(348.716784548468,349.087842321671,350.087492988188,351.087143654705,
352.086794321221,353.086444987738,354.086095654254,354.999969855647),
 .UNSPECIFIED.);
#1252=B_SPLINE_CURVE_WITH_KNOTS('',3,(#51448,#51449,#51450,#51451,#51452,
#51453,#51454,#51455,#51456,#51457,#51458),.UNSPECIFIED.,.F.,.F.,(4,1,1,
1,1,1,1,1,4),(342.433599241288,342.434930668822,343.434385379244,344.433840089666,
345.433294800088,346.43274951051,347.432204220932,348.431658931354,348.716784548467),
 .UNSPECIFIED.);
#1253=B_SPLINE_CURVE_WITH_KNOTS('',3,(#51459,#51460,#51461,#51462,#51463,
#51464,#51465,#51466,#51467,#51468),.UNSPECIFIED.,.F.,.F.,(4,1,1,1,1,1,
1,4),(342.433599241288,343.089938322572,344.089588989089,345.089239655605,
346.088890322122,347.088540988638,348.088191655155,348.716784548468),
 .UNSPECIFIED.);
#1254=B_SPLINE_CURVE_WITH_KNOTS('',3,(#51473,#51474,#51475,#51476,#51477,
#51478,#51479,#51480,#51481,#51482),.UNSPECIFIED.,.F.,.F.,(4,1,1,1,1,1,
1,4),(336.150413934108,336.438202406289,337.437657116712,338.437111827134,
339.436566537556,340.436021247978,341.4354759584,342.433599241288),
 .UNSPECIFIED.);
#1255=B_SPLINE_CURVE_WITH_KNOTS('',3,(#51483,#51484,#51485,#51486,#51487,
#51488,#51489,#51490,#51491,#51492),.UNSPECIFIED.,.F.,.F.,(4,1,1,1,1,1,
1,4),(336.150413934108,337.092034323473,338.091684989989,339.091335656506,
340.090986323022,341.090636989539,342.090287656056,342.433599241288),
 .UNSPECIFIED.);
#1256=B_SPLINE_CURVE_WITH_KNOTS('',3,(#51497,#51498,#51499,#51500,#51501,
#51502,#51503,#51504,#51505,#51506),.UNSPECIFIED.,.F.,.F.,(4,1,1,1,1,1,
1,4),(329.867228626929,330.441474143757,331.440928854179,332.440383564601,
333.439838275023,334.439292985445,335.438747695867,336.150413934108),
 .UNSPECIFIED.);
#1257=B_SPLINE_CURVE_WITH_KNOTS('',3,(#51507,#51508,#51509,#51510,#51511,
#51512,#51513,#51514,#51515,#51516,#51517),.UNSPECIFIED.,.F.,.F.,(4,1,1,
1,1,1,1,1,4),(329.867228626929,330.094479657857,331.094130324374,332.09378099089,
333.093431657407,334.093082323923,335.09273299044,336.092383656956,336.150413934108),
 .UNSPECIFIED.);
#1258=B_SPLINE_CURVE_WITH_KNOTS('',3,(#51522,#51523,#51524,#51525,#51526,
#51527,#51528,#51529,#51530,#51531),.UNSPECIFIED.,.F.,.F.,(4,1,1,1,1,1,
1,4),(323.584043319749,324.444745881224,325.444200591647,326.443655302069,
327.443110012491,328.442564722913,329.442019433335,329.867228626929),
 .UNSPECIFIED.);
#1259=B_SPLINE_CURVE_WITH_KNOTS('',3,(#51532,#51533,#51534,#51535,#51536,
#51537,#51538,#51539,#51540,#51541),.UNSPECIFIED.,.F.,.F.,(4,1,1,1,1,1,
1,4),(323.584043319749,324.096575658758,325.096226325274,326.095876991791,
327.095527658307,328.095178324824,329.09482899134,329.867228626929),
 .UNSPECIFIED.);
#1260=B_SPLINE_CURVE_WITH_KNOTS('',3,(#51546,#51547,#51548,#51549,#51550,
#51551,#51552,#51553,#51554,#51555,#51556),.UNSPECIFIED.,.F.,.F.,(4,1,1,
1,1,1,1,1,4),(317.300858012569,317.44856290827,318.448017618692,319.447472329114,
320.446927039536,321.446381749958,322.44583646038,323.445291170802,323.584043319749),
 .UNSPECIFIED.);
#1261=B_SPLINE_CURVE_WITH_KNOTS('',3,(#51557,#51558,#51559,#51560,#51561,
#51562,#51563,#51564,#51565,#51566),.UNSPECIFIED.,.F.,.F.,(4,1,1,1,1,1,
1,4),(317.30085801257,318.098671659658,319.098322326175,320.097972992691,
321.097623659208,322.097274325725,323.096924992241,323.584043319749),
 .UNSPECIFIED.);
#1262=B_SPLINE_CURVE_WITH_KNOTS('',3,(#51571,#51572,#51573,#51574,#51575,
#51576,#51577,#51578,#51579,#51580),.UNSPECIFIED.,.F.,.F.,(4,1,1,1,1,1,
1,4),(311.01767270539,311.451834645737,312.451289356159,313.450744066582,
314.450198777004,315.449653487426,316.449108197848,317.300858012569),
 .UNSPECIFIED.);
#1263=B_SPLINE_CURVE_WITH_KNOTS('',3,(#51581,#51582,#51583,#51584,#51585,
#51586,#51587,#51588,#51589,#51590,#51591),.UNSPECIFIED.,.F.,.F.,(4,1,1,
1,1,1,1,1,4),(311.01767270539,311.101116994043,312.100767660559,313.100418327076,
314.100068993592,315.099719660109,316.099370326625,317.099020993142,317.30085801257),
 .UNSPECIFIED.);
#1264=B_SPLINE_CURVE_WITH_KNOTS('',3,(#51596,#51597,#51598,#51599,#51600,
#51601,#51602,#51603,#51604,#51605),.UNSPECIFIED.,.F.,.F.,(4,1,1,1,1,1,
1,4),(304.73448739821,305.455106383205,306.454561093627,307.454015804049,
308.453470514471,309.452925224893,310.452379935315,311.01767270539),
 .UNSPECIFIED.);
#1265=B_SPLINE_CURVE_WITH_KNOTS('',3,(#51606,#51607,#51608,#51609,#51610,
#51611,#51612,#51613,#51614,#51615),.UNSPECIFIED.,.F.,.F.,(4,1,1,1,1,1,
1,4),(304.734487398211,305.103212994943,306.10286366146,307.102514327976,
308.102164994493,309.101815661009,310.101466327526,311.01767270539),
 .UNSPECIFIED.);
#1266=B_SPLINE_CURVE_WITH_KNOTS('',3,(#51620,#51621,#51622,#51623,#51624,
#51625,#51626,#51627,#51628,#51629,#51630),.UNSPECIFIED.,.F.,.F.,(4,1,1,
1,1,1,1,1,4),(298.451302091031,298.45892341025,299.458378120672,300.457832831094,
301.457287541517,302.456742251939,303.456196962361,304.455651672783,304.73448739821),
 .UNSPECIFIED.);
#1267=B_SPLINE_CURVE_WITH_KNOTS('',3,(#51631,#51632,#51633,#51634,#51635,
#51636,#51637,#51638,#51639,#51640),.UNSPECIFIED.,.F.,.F.,(4,1,1,1,1,1,
1,4),(298.451302091031,299.105308995844,300.10495966236,301.104610328877,
302.104260995394,303.10391166191,304.103562328427,304.734487398211),
 .UNSPECIFIED.);
#1268=B_SPLINE_CURVE_WITH_KNOTS('',3,(#51645,#51646,#51647,#51648,#51649,
#51650,#51651,#51652,#51653,#51654),.UNSPECIFIED.,.F.,.F.,(4,1,1,1,1,1,
1,4),(292.168116783851,292.462195147718,293.46164985814,294.461104568562,
295.460559278984,296.460013989406,297.459468699828,298.451302091031),
 .UNSPECIFIED.);
#1269=B_SPLINE_CURVE_WITH_KNOTS('',3,(#51655,#51656,#51657,#51658,#51659,
#51660,#51661,#51662,#51663,#51664),.UNSPECIFIED.,.F.,.F.,(4,1,1,1,1,1,
1,4),(292.168116783851,293.107404996745,294.107055663261,295.106706329778,
296.106356996294,297.106007662811,298.105658329327,298.451302091031),
 .UNSPECIFIED.);
#1270=B_SPLINE_CURVE_WITH_KNOTS('',3,(#51669,#51670,#51671,#51672,#51673,
#51674,#51675,#51676,#51677,#51678),.UNSPECIFIED.,.F.,.F.,(4,1,1,1,1,1,
1,4),(285.884931476672,286.465466885185,287.464921595607,288.464376306029,
289.463831016451,290.463285726874,291.462740437296,292.168116783851),
 .UNSPECIFIED.);
#1271=B_SPLINE_CURVE_WITH_KNOTS('',3,(#51679,#51680,#51681,#51682,#51683,
#51684,#51685,#51686,#51687,#51688,#51689),.UNSPECIFIED.,.F.,.F.,(4,1,1,
1,1,1,1,1,4),(285.884931476672,286.109850331129,287.109500997645,288.109151664162,
289.108802330678,290.108452997195,291.108103663712,292.107754330228,292.168116783851),
 .UNSPECIFIED.);
#1272=B_SPLINE_CURVE_WITH_KNOTS('',3,(#51694,#51695,#51696,#51697,#51698,
#51699,#51700,#51701,#51702,#51703),.UNSPECIFIED.,.F.,.F.,(4,1,1,1,1,1,
1,4),(279.601746169492,280.468738622653,281.468193333075,282.467648043497,
283.467102753919,284.466557464341,285.466012174763,285.884931476672),
 .UNSPECIFIED.);
#1273=B_SPLINE_CURVE_WITH_KNOTS('',3,(#51704,#51705,#51706,#51707,#51708,
#51709,#51710,#51711,#51712,#51713),.UNSPECIFIED.,.F.,.F.,(4,1,1,1,1,1,
1,4),(279.601746169492,280.111946332029,281.111596998546,282.111247665063,
283.110898331579,284.110548998096,285.110199664612,285.884931476672),
 .UNSPECIFIED.);
#1274=B_SPLINE_CURVE_WITH_KNOTS('',3,(#51718,#51719,#51720,#51721,#51722,
#51723,#51724,#51725,#51726,#51727,#51728),.UNSPECIFIED.,.F.,.F.,(4,1,1,
1,1,1,1,1,4),(273.318560862312,273.472555649698,274.47201036012,275.471465070542,
276.470919780964,277.470374491386,278.469829201809,279.469283912231,279.601746169492),
 .UNSPECIFIED.);
#1275=B_SPLINE_CURVE_WITH_KNOTS('',3,(#51729,#51730,#51731,#51732,#51733,
#51734,#51735,#51736,#51737,#51738),.UNSPECIFIED.,.F.,.F.,(4,1,1,1,1,1,
1,4),(273.318560862313,274.11404233293,275.113692999447,276.113343665963,
277.11299433248,278.112644998996,279.112295665513,279.601746169492),
 .UNSPECIFIED.);
#1276=B_SPLINE_CURVE_WITH_KNOTS('',3,(#51743,#51744,#51745,#51746,#51747,
#51748,#51749,#51750,#51751,#51752),.UNSPECIFIED.,.F.,.F.,(4,1,1,1,1,1,
1,4),(267.035375555133,267.475827387166,268.475282097588,269.47473680801,
270.474191518432,271.473646228854,272.473100939276,273.318560862312),
 .UNSPECIFIED.);
#1277=B_SPLINE_CURVE_WITH_KNOTS('',3,(#51753,#51754,#51755,#51756,#51757,
#51758,#51759,#51760,#51761,#51762,#51763),.UNSPECIFIED.,.F.,.F.,(4,1,1,
1,1,1,1,1,4),(267.035375555133,267.116487667314,268.116138333831,269.115789000347,
270.115439666864,271.11509033338,272.114740999897,273.114391666414,273.318560862313),
 .UNSPECIFIED.);
#1278=B_SPLINE_CURVE_WITH_KNOTS('',3,(#51768,#51769,#51770,#51771,#51772,
#51773,#51774,#51775,#51776,#51777),.UNSPECIFIED.,.F.,.F.,(4,1,1,1,1,1,
1,4),(260.752190247953,261.479099124633,262.478553835055,263.478008545477,
264.477463255899,265.476917966321,266.476372676744,267.035375555133),
 .UNSPECIFIED.);
#1279=B_SPLINE_CURVE_WITH_KNOTS('',3,(#51778,#51779,#51780,#51781,#51782,
#51783,#51784,#51785,#51786,#51787),.UNSPECIFIED.,.F.,.F.,(4,1,1,1,1,1,
1,4),(260.752190247954,261.118583668215,262.118234334731,263.117885001248,
264.117535667765,265.117186334281,266.116837000798,267.035375555133),
 .UNSPECIFIED.);
#1280=B_SPLINE_CURVE_WITH_KNOTS('',3,(#51792,#51793,#51794,#51795,#51796,
#51797,#51798,#51799,#51800,#51801,#51802),.UNSPECIFIED.,.F.,.F.,(4,1,1,
1,1,1,1,1,4),(254.469004940774,254.482916151679,255.482370862101,256.481825572523,
257.481280282945,258.480734993367,259.480189703789,260.479644414211,260.752190247953),
 .UNSPECIFIED.);
#1281=B_SPLINE_CURVE_WITH_KNOTS('',3,(#51803,#51804,#51805,#51806,#51807,
#51808,#51809,#51810,#51811,#51812),.UNSPECIFIED.,.F.,.F.,(4,1,1,1,1,1,
1,4),(254.469004940774,255.120679669116,256.120330335632,257.119981002149,
258.119631668665,259.119282335182,260.118933001698,260.752190247954),
 .UNSPECIFIED.);
#1282=B_SPLINE_CURVE_WITH_KNOTS('',3,(#51817,#51818,#51819,#51820,#51821,
#51822,#51823,#51824,#51825,#51826),.UNSPECIFIED.,.F.,.F.,(4,1,1,1,1,1,
1,4),(248.185819633594,248.486187889146,249.485642599568,250.48509730999,
251.484552020412,252.484006730834,253.483461441256,254.469004940774),
 .UNSPECIFIED.);
#1283=B_SPLINE_CURVE_WITH_KNOTS('',3,(#51827,#51828,#51829,#51830,#51831,
#51832,#51833,#51834,#51835,#51836),.UNSPECIFIED.,.F.,.F.,(4,1,1,1,1,1,
1,4),(248.185819633595,249.122775670016,250.122426336533,251.122077003049,
252.121727669566,253.121378336083,254.121029002599,254.469004940774),
 .UNSPECIFIED.);
#1284=B_SPLINE_CURVE_WITH_KNOTS('',3,(#51841,#51842,#51843,#51844,#51845,
#51846,#51847,#51848,#51849,#51850),.UNSPECIFIED.,.F.,.F.,(4,1,1,1,1,1,
1,4),(241.902634326415,242.489459626613,243.488914337036,244.488369047458,
245.48782375788,246.487278468302,247.486733178724,248.185819633594),
 .UNSPECIFIED.);
#1285=B_SPLINE_CURVE_WITH_KNOTS('',3,(#51851,#51852,#51853,#51854,#51855,
#51856,#51857,#51858,#51859,#51860,#51861),.UNSPECIFIED.,.F.,.F.,(4,1,1,
1,1,1,1,1,4),(241.902634326415,242.1252210044,243.124871670917,244.124522337434,
245.12417300395,246.123823670467,247.123474336983,248.1231250035,248.185819633595),
 .UNSPECIFIED.);
#1286=B_SPLINE_CURVE_WITH_KNOTS('',3,(#51866,#51867,#51868,#51869,#51870,
#51871,#51872,#51873,#51874,#51875),.UNSPECIFIED.,.F.,.F.,(4,1,1,1,1,1,
1,4),(235.619449019235,236.492731364081,237.492186074503,238.491640784925,
239.491095495347,240.490550205769,241.490004916191,241.902634326415),
 .UNSPECIFIED.);
#1287=B_SPLINE_CURVE_WITH_KNOTS('',3,(#51876,#51877,#51878,#51879,#51880,
#51881,#51882,#51883,#51884,#51885),.UNSPECIFIED.,.F.,.F.,(4,1,1,1,1,1,
1,4),(235.619449019235,236.127317005301,237.126967671818,238.126618338334,
239.126269004851,240.125919671367,241.125570337884,241.902634326415),
 .UNSPECIFIED.);
#1288=B_SPLINE_CURVE_WITH_KNOTS('',3,(#51890,#51891,#51892,#51893,#51894,
#51895,#51896,#51897,#51898,#51899,#51900),.UNSPECIFIED.,.F.,.F.,(4,1,1,
1,1,1,1,1,4),(229.336263712056,229.496548391126,230.496003101548,231.495457811971,
232.494912522393,233.494367232815,234.493821943237,235.493276653659,235.619449019235),
 .UNSPECIFIED.);
#1289=B_SPLINE_CURVE_WITH_KNOTS('',3,(#51901,#51902,#51903,#51904,#51905,
#51906,#51907,#51908,#51909,#51910),.UNSPECIFIED.,.F.,.F.,(4,1,1,1,1,1,
1,4),(229.336263712056,230.129413006202,231.129063672718,232.128714339235,
233.128365005752,234.128015672268,235.127666338785,235.619449019235),
 .UNSPECIFIED.);
#1290=B_SPLINE_CURVE_WITH_KNOTS('',3,(#51915,#51916,#51917,#51918,#51919,
#51920,#51921,#51922,#51923,#51924),.UNSPECIFIED.,.F.,.F.,(4,1,1,1,1,1,
1,4),(223.053078404876,223.499820128594,224.499274839016,225.498729549438,
226.49818425986,227.497638970282,228.497093680704,229.336263712056),
 .UNSPECIFIED.);
#1291=B_SPLINE_CURVE_WITH_KNOTS('',3,(#51925,#51926,#51927,#51928,#51929,
#51930,#51931,#51932,#51933,#51934,#51935),.UNSPECIFIED.,.F.,.F.,(4,1,1,
1,1,1,1,1,4),(223.053078404876,223.131858340586,224.131509007103,225.131159673619,
226.130810340136,227.130461006652,228.130111673169,229.129762339685,229.336263712056),
 .UNSPECIFIED.);
#1292=B_SPLINE_CURVE_WITH_KNOTS('',3,(#51940,#51941,#51942,#51943,#51944,
#51945,#51946,#51947,#51948,#51949),.UNSPECIFIED.,.F.,.F.,(4,1,1,1,1,1,
1,4),(216.769893097696,217.503091866061,218.502546576483,219.502001286906,
220.501455997328,221.50091070775,222.500365418172,223.053078404876),
 .UNSPECIFIED.);
#1293=B_SPLINE_CURVE_WITH_KNOTS('',3,(#51950,#51951,#51952,#51953,#51954,
#51955,#51956,#51957,#51958,#51959),.UNSPECIFIED.,.F.,.F.,(4,1,1,1,1,1,
1,4),(216.769893097697,217.133954341487,218.133605008003,219.13325567452,
220.132906341036,221.132557007553,222.132207674069,223.053078404876),
 .UNSPECIFIED.);
#1294=B_SPLINE_CURVE_WITH_KNOTS('',3,(#51964,#51965,#51966,#51967,#51968,
#51969,#51970,#51971,#51972,#51973,#51974),.UNSPECIFIED.,.F.,.F.,(4,1,1,
1,1,1,1,1,4),(210.486707790517,210.506908893107,211.506363603529,212.505818313951,
213.505273024373,214.504727734795,215.504182445217,216.503637155639,216.769893097696),
 .UNSPECIFIED.);
#1295=B_SPLINE_CURVE_WITH_KNOTS('',3,(#51975,#51976,#51977,#51978,#51979,
#51980,#51981,#51982,#51983,#51984),.UNSPECIFIED.,.F.,.F.,(4,1,1,1,1,1,
1,4),(210.486707790517,211.136050342387,212.135701008904,213.135351675421,
214.135002341937,215.134653008454,216.13430367497,216.769893097697),
 .UNSPECIFIED.);
#1296=B_SPLINE_CURVE_WITH_KNOTS('',3,(#51989,#51990,#51991,#51992,#51993,
#51994,#51995,#51996,#51997,#51998),.UNSPECIFIED.,.F.,.F.,(4,1,1,1,1,1,
1,4),(204.203522483337,204.510180630574,205.509635340996,206.509090051418,
207.508544761841,208.507999472263,209.507454182685,210.486707790517),
 .UNSPECIFIED.);
#1297=B_SPLINE_CURVE_WITH_KNOTS('',3,(#51999,#52000,#52001,#52002,#52003,
#52004,#52005,#52006,#52007,#52008),.UNSPECIFIED.,.F.,.F.,(4,1,1,1,1,1,
1,4),(204.203522483338,205.138146343288,206.137797009805,207.137447676321,
208.137098342838,209.136749009354,210.136399675871,210.486707790517),
 .UNSPECIFIED.);
#1298=B_SPLINE_CURVE_WITH_KNOTS('',3,(#52013,#52014,#52015,#52016,#52017,
#52018,#52019,#52020,#52021,#52022),.UNSPECIFIED.,.F.,.F.,(4,1,1,1,1,1,
1,4),(197.920337176158,198.513452368042,199.512907078464,200.512361788886,
201.511816499308,202.51127120973,203.510725920152,204.203522483337),
 .UNSPECIFIED.);
#1299=B_SPLINE_CURVE_WITH_KNOTS('',3,(#52023,#52024,#52025,#52026,#52027,
#52028,#52029,#52030,#52031,#52032,#52033),.UNSPECIFIED.,.F.,.F.,(4,1,1,
1,1,1,1,1,4),(197.920337176158,198.140591677672,199.140242344189,200.139893010705,
201.139543677222,202.139194343738,203.138845010255,204.138495676772,204.203522483338),
 .UNSPECIFIED.);
#1300=B_SPLINE_CURVE_WITH_KNOTS('',3,(#52038,#52039,#52040,#52041,#52042,
#52043,#52044,#52045,#52046,#52047),.UNSPECIFIED.,.F.,.F.,(4,1,1,1,1,1,
1,4),(191.637151868978,192.516724105509,193.516178815931,194.515633526353,
195.515088236775,196.514542947198,197.51399765762,197.920337176158),
 .UNSPECIFIED.);
#1301=B_SPLINE_CURVE_WITH_KNOTS('',3,(#52048,#52049,#52050,#52051,#52052,
#52053,#52054,#52055,#52056,#52057),.UNSPECIFIED.,.F.,.F.,(4,1,1,1,1,1,
1,4),(191.637151868978,192.142687678573,193.142338345089,194.141989011606,
195.141639678123,196.141290344639,197.140941011156,197.920337176158),
 .UNSPECIFIED.);
#1302=B_SPLINE_CURVE_WITH_KNOTS('',3,(#52062,#52063,#52064,#52065,#52066,
#52067,#52068,#52069,#52070,#52071,#52072),.UNSPECIFIED.,.F.,.F.,(4,1,1,
1,1,1,1,1,4),(185.353966561799,185.520541132555,186.519995842977,187.519450553399,
188.518905263821,189.518359974243,190.517814684665,191.517269395087,191.637151868978),
 .UNSPECIFIED.);
#1303=B_SPLINE_CURVE_WITH_KNOTS('',3,(#52073,#52074,#52075,#52076,#52077,
#52078,#52079,#52080,#52081,#52082),.UNSPECIFIED.,.F.,.F.,(4,1,1,1,1,1,
1,4),(185.353966561799,186.144783679474,187.14443434599,188.144085012507,
189.143735679023,190.14338634554,191.143037012056,191.637151868978),
 .UNSPECIFIED.);
#1304=B_SPLINE_CURVE_WITH_KNOTS('',3,(#52087,#52088,#52089,#52090,#52091,
#52092,#52093,#52094,#52095,#52096),.UNSPECIFIED.,.F.,.F.,(4,1,1,1,1,1,
1,4),(179.070781254619,179.523812870022,180.523267580444,181.522722290866,
182.522177001288,183.52163171171,184.521086422133,185.353966561799),
 .UNSPECIFIED.);
#1305=B_SPLINE_CURVE_WITH_KNOTS('',3,(#52097,#52098,#52099,#52100,#52101,
#52102,#52103,#52104,#52105,#52106,#52107),.UNSPECIFIED.,.F.,.F.,(4,1,1,
1,1,1,1,1,4),(179.070781254619,179.147229013858,180.146879680374,181.146530346891,
182.146181013407,183.145831679924,184.145482346441,185.145133012957,185.353966561799),
 .UNSPECIFIED.);
#1306=B_SPLINE_CURVE_WITH_KNOTS('',3,(#52112,#52113,#52114,#52115,#52116,
#52117,#52118,#52119,#52120,#52121),.UNSPECIFIED.,.F.,.F.,(4,1,1,1,1,1,
1,4),(172.787595947439,173.52708460749,174.526539317912,175.525994028334,
176.525448738756,177.524903449178,178.5243581596,179.070781254619),
 .UNSPECIFIED.);
#1307=B_SPLINE_CURVE_WITH_KNOTS('',3,(#52122,#52123,#52124,#52125,#52126,
#52127,#52128,#52129,#52130,#52131),.UNSPECIFIED.,.F.,.F.,(4,1,1,1,1,1,
1,4),(172.78759594744,173.149325014758,174.148975681275,175.148626347792,
176.148277014308,177.147927680825,178.147578347341,179.070781254619),
 .UNSPECIFIED.);
#1308=B_SPLINE_CURVE_WITH_KNOTS('',3,(#52136,#52137,#52138,#52139,#52140,
#52141,#52142,#52143,#52144,#52145,#52146),.UNSPECIFIED.,.F.,.F.,(4,1,1,
1,1,1,1,1,4),(166.50441064026,166.530901634535,167.530356344957,168.529811055379,
169.529265765801,170.528720476223,171.528175186645,172.527629897068,172.787595947439),
 .UNSPECIFIED.);
#1309=B_SPLINE_CURVE_WITH_KNOTS('',3,(#52147,#52148,#52149,#52150,#52151,
#52152,#52153,#52154,#52155,#52156),.UNSPECIFIED.,.F.,.F.,(4,1,1,1,1,1,
1,4),(166.50441064026,167.151421015659,168.151071682176,169.150722348692,
170.150373015209,171.150023681725,172.149674348242,172.78759594744),
 .UNSPECIFIED.);
#1310=B_SPLINE_CURVE_WITH_KNOTS('',3,(#52161,#52162,#52163,#52164,#52165,
#52166,#52167,#52168,#52169,#52170),.UNSPECIFIED.,.F.,.F.,(4,1,1,1,1,1,
1,4),(160.22122533308,160.534173372003,161.533628082425,162.533082792847,
163.532537503269,164.531992213691,165.531446924113,166.50441064026),
 .UNSPECIFIED.);
#1311=B_SPLINE_CURVE_WITH_KNOTS('',3,(#52171,#52172,#52173,#52174,#52175,
#52176,#52177,#52178,#52179,#52180),.UNSPECIFIED.,.F.,.F.,(4,1,1,1,1,1,
1,4),(160.221225333081,161.15351701656,162.153167683076,163.152818349593,
164.152469016109,165.152119682626,166.151770349143,166.50441064026),
 .UNSPECIFIED.);
#1312=B_SPLINE_CURVE_WITH_KNOTS('',3,(#52185,#52186,#52187,#52188,#52189,
#52190,#52191,#52192,#52193,#52194),.UNSPECIFIED.,.F.,.F.,(4,1,1,1,1,1,
1,4),(153.938040025901,154.53744510947,155.536899819892,156.536354530314,
157.535809240736,158.535263951158,159.53471866158,160.22122533308),
 .UNSPECIFIED.);
#1313=B_SPLINE_CURVE_WITH_KNOTS('',3,(#52195,#52196,#52197,#52198,#52199,
#52200,#52201,#52202,#52203,#52204,#52205),.UNSPECIFIED.,.F.,.F.,(4,1,1,
1,1,1,1,1,4),(153.938040025901,154.155962350944,155.155613017461,156.155263683977,
157.154914350494,158.15456501701,159.154215683527,160.153866350043,160.221225333081),
 .UNSPECIFIED.);
#1314=B_SPLINE_CURVE_WITH_KNOTS('',3,(#52210,#52211,#52212,#52213,#52214,
#52215,#52216,#52217,#52218,#52219),.UNSPECIFIED.,.F.,.F.,(4,1,1,1,1,1,
1,4),(147.654854718721,148.540716846937,149.54017155736,150.539626267782,
151.539080978204,152.538535688626,153.537990399048,153.938040025901),
 .UNSPECIFIED.);
#1315=B_SPLINE_CURVE_WITH_KNOTS('',3,(#52220,#52221,#52222,#52223,#52224,
#52225,#52226,#52227,#52228,#52229),.UNSPECIFIED.,.F.,.F.,(4,1,1,1,1,1,
1,4),(147.654854718721,148.158058351845,149.157709018361,150.157359684878,
151.157010351394,152.156661017911,153.156311684427,153.938040025901),
 .UNSPECIFIED.);
#1316=B_SPLINE_CURVE_WITH_KNOTS('',3,(#52234,#52235,#52236,#52237,#52238,
#52239,#52240,#52241,#52242,#52243,#52244),.UNSPECIFIED.,.F.,.F.,(4,1,1,
1,1,1,1,1,4),(141.371669411542,141.544533873983,142.543988584405,143.543443294827,
144.542898005249,145.542352715671,146.541807426093,147.541262136515,147.654854718721),
 .UNSPECIFIED.);
#1317=B_SPLINE_CURVE_WITH_KNOTS('',3,(#52245,#52246,#52247,#52248,#52249,
#52250,#52251,#52252,#52253,#52254),.UNSPECIFIED.,.F.,.F.,(4,1,1,1,1,1,
1,4),(141.371669411542,142.160154352745,143.159805019262,144.159455685778,
145.159106352295,146.158757018812,147.158407685328,147.654854718721),
 .UNSPECIFIED.);
#1318=B_SPLINE_CURVE_WITH_KNOTS('',3,(#52259,#52260,#52261,#52262,#52263,
#52264,#52265,#52266,#52267,#52268),.UNSPECIFIED.,.F.,.F.,(4,1,1,1,1,1,
1,4),(135.088484104362,135.54780561145,136.547260321872,137.546715032295,
138.546169742717,139.545624453139,140.545079163561,141.371669411542),
 .UNSPECIFIED.);
#1319=B_SPLINE_CURVE_WITH_KNOTS('',3,(#52269,#52270,#52271,#52272,#52273,
#52274,#52275,#52276,#52277,#52278,#52279),.UNSPECIFIED.,.F.,.F.,(4,1,1,
1,1,1,1,1,4),(135.088484104362,135.16259968713,136.162250353646,137.161901020163,
138.161551686679,139.161202353196,140.160853019712,141.160503686229,141.371669411542),
 .UNSPECIFIED.);
#1320=B_SPLINE_CURVE_WITH_KNOTS('',3,(#52284,#52285,#52286,#52287,#52288,
#52289,#52290,#52291,#52292,#52293),.UNSPECIFIED.,.F.,.F.,(4,1,1,1,1,1,
1,4),(128.805298797183,129.551077348918,130.55053205934,131.549986769762,
132.549441480184,133.548896190606,134.548350901028,135.088484104362),
 .UNSPECIFIED.);
#1321=B_SPLINE_CURVE_WITH_KNOTS('',3,(#52294,#52295,#52296,#52297,#52298,
#52299,#52300,#52301,#52302,#52303),.UNSPECIFIED.,.F.,.F.,(4,1,1,1,1,1,
1,4),(128.805298797183,129.16469568803,130.164346354547,131.163997021063,
132.16364768758,133.163298354096,134.162949020613,135.088484104362),
 .UNSPECIFIED.);
#1322=B_SPLINE_CURVE_WITH_KNOTS('',3,(#52308,#52309,#52310,#52311,#52312,
#52313,#52314,#52315,#52316,#52317,#52318),.UNSPECIFIED.,.F.,.F.,(4,1,1,
1,1,1,1,1,4),(122.522113490003,122.554894375963,123.554349086385,124.553803796807,
125.55325850723,126.552713217652,127.552167928074,128.551622638496,128.805298797183),
 .UNSPECIFIED.);
#1323=B_SPLINE_CURVE_WITH_KNOTS('',3,(#52319,#52320,#52321,#52322,#52323,
#52324,#52325,#52326,#52327,#52328),.UNSPECIFIED.,.F.,.F.,(4,1,1,1,1,1,
1,4),(122.522113490003,123.166791688931,124.166442355447,125.166093021964,
126.165743688481,127.165394354997,128.165045021514,128.805298797183),
 .UNSPECIFIED.);
#1324=B_SPLINE_CURVE_WITH_KNOTS('',3,(#52333,#52334,#52335,#52336,#52337,
#52338,#52339,#52340,#52341,#52342),.UNSPECIFIED.,.F.,.F.,(4,1,1,1,1,1,
1,4),(116.238928182823,116.558166113431,117.557620823853,118.557075534275,
119.556530244697,120.555984955119,121.555439665541,122.522113490003),
 .UNSPECIFIED.);
#1325=B_SPLINE_CURVE_WITH_KNOTS('',3,(#52343,#52344,#52345,#52346,#52347,
#52348,#52349,#52350,#52351,#52352),.UNSPECIFIED.,.F.,.F.,(4,1,1,1,1,1,
1,4),(116.238928182824,117.168887689832,118.168538356348,119.168189022865,
120.167839689381,121.167490355898,122.167141022414,122.522113490003),
 .UNSPECIFIED.);
#1326=B_SPLINE_CURVE_WITH_KNOTS('',3,(#52357,#52358,#52359,#52360,#52361,
#52362,#52363,#52364,#52365,#52366),.UNSPECIFIED.,.F.,.F.,(4,1,1,1,1,1,
1,4),(109.955742875644,110.561437850898,111.56089256132,112.560347271742,
113.559801982165,114.559256692587,115.558711403009,116.238928182823),
 .UNSPECIFIED.);
#1327=B_SPLINE_CURVE_WITH_KNOTS('',3,(#52367,#52368,#52369,#52370,#52371,
#52372,#52373,#52374,#52375,#52376,#52377),.UNSPECIFIED.,.F.,.F.,(4,1,1,
1,1,1,1,1,4),(109.955742875644,110.171333024216,111.170983690732,112.170634357249,
113.170285023765,114.169935690282,115.169586356798,116.169237023315,116.238928182824),
 .UNSPECIFIED.);
#1328=B_SPLINE_CURVE_WITH_KNOTS('',3,(#52382,#52383,#52384,#52385,#52386,
#52387,#52388,#52389,#52390,#52391),.UNSPECIFIED.,.F.,.F.,(4,1,1,1,1,1,
1,4),(103.672557568464,104.564709588366,105.564164298788,106.56361900921,
107.563073719632,108.562528430054,109.561983140476,109.955742875644),
 .UNSPECIFIED.);
#1329=B_SPLINE_CURVE_WITH_KNOTS('',3,(#52392,#52393,#52394,#52395,#52396,
#52397,#52398,#52399,#52400,#52401),.UNSPECIFIED.,.F.,.F.,(4,1,1,1,1,1,
1,4),(103.672557568464,104.173429025116,105.173079691633,106.17273035815,
107.172381024666,108.172031691183,109.171682357699,109.955742875644),
 .UNSPECIFIED.);
#1330=B_SPLINE_CURVE_WITH_KNOTS('',3,(#52406,#52407,#52408,#52409,#52410,
#52411,#52412,#52413,#52414,#52415,#52416),.UNSPECIFIED.,.F.,.F.,(4,1,1,
1,1,1,1,1,4),(97.3893722612846,97.5685266154111,98.5679813258332,99.5674360362553,
100.566890746677,101.566345457099,102.565800167522,103.565254877944,103.672557568464),
 .UNSPECIFIED.);
#1331=B_SPLINE_CURVE_WITH_KNOTS('',3,(#52417,#52418,#52419,#52420,#52421,
#52422,#52423,#52424,#52425,#52426),.UNSPECIFIED.,.F.,.F.,(4,1,1,1,1,1,
1,4),(97.3893722612848,98.1755250260171,99.1751756925336,100.17482635905,
101.174477025567,102.174127692083,103.1737783586,103.672557568464),
 .UNSPECIFIED.);
#1332=B_SPLINE_CURVE_WITH_KNOTS('',3,(#52431,#52432,#52433,#52434,#52435,
#52436,#52437,#52438,#52439,#52440),.UNSPECIFIED.,.F.,.F.,(4,1,1,1,1,1,
1,4),(91.106186954105,91.5717983528786,92.5712530633007,93.5707077737228,
94.5701624841449,95.569617194567,96.5690719049891,97.3893722612846),
 .UNSPECIFIED.);
#1333=B_SPLINE_CURVE_WITH_KNOTS('',3,(#52441,#52442,#52443,#52444,#52445,
#52446,#52447,#52448,#52449,#52450,#52451),.UNSPECIFIED.,.F.,.F.,(4,1,1,
1,1,1,1,1,4),(91.1061869541052,91.1779703604012,92.1776210269178,93.1772716934343,
94.1769223599509,95.1765730264674,96.176223692984,97.1758743595006,97.3893722612848),
 .UNSPECIFIED.);
#1334=B_SPLINE_CURVE_WITH_KNOTS('',3,(#52456,#52457,#52458,#52459,#52460,
#52461,#52462,#52463,#52464,#52465),.UNSPECIFIED.,.F.,.F.,(4,1,1,1,1,1,
1,4),(84.8230016469254,85.5750700903461,86.5745248007682,87.5739795111903,
88.5734342216124,89.5728889320345,90.5723436424566,91.106186954105),
 .UNSPECIFIED.);
#1335=B_SPLINE_CURVE_WITH_KNOTS('',3,(#52466,#52467,#52468,#52469,#52470,
#52471,#52472,#52473,#52474,#52475),.UNSPECIFIED.,.F.,.F.,(4,1,1,1,1,1,
1,4),(84.8230016469256,85.1800663613019,86.1797170278185,87.179367694335,
88.1790183608516,89.1786690273681,90.1783196938847,91.1061869541052),
 .UNSPECIFIED.);
#1336=B_SPLINE_CURVE_WITH_KNOTS('',3,(#52480,#52481,#52482,#52483,#52484,
#52485,#52486,#52487,#52488,#52489,#52490),.UNSPECIFIED.,.F.,.F.,(4,1,1,
1,1,1,1,1,4),(78.5398163397458,78.5788871173915,79.5783418278136,80.5777965382357,
81.5772512486578,82.5767059590799,83.5761606695019,84.575615379924,84.8230016469254),
 .UNSPECIFIED.);
#1337=B_SPLINE_CURVE_WITH_KNOTS('',3,(#52491,#52492,#52493,#52494,#52495,
#52496,#52497,#52498,#52499,#52500),.UNSPECIFIED.,.F.,.F.,(4,1,1,1,1,1,
1,4),(78.539816339746,79.1821623622026,80.1818130287192,81.1814636952357,
82.1811143617523,83.1807650282688,84.1804156947854,84.8230016469256),
 .UNSPECIFIED.);
#1338=B_SPLINE_CURVE_WITH_KNOTS('',3,(#52505,#52506,#52507,#52508,#52509,
#52510,#52511,#52512,#52513,#52514),.UNSPECIFIED.,.F.,.F.,(4,1,1,1,1,1,
1,4),(72.2566310325662,72.582158854859,73.5816135652811,74.5810682757032,
75.5805229861253,76.5799776965474,77.5794324069694,78.5398163397458),
 .UNSPECIFIED.);
#1339=B_SPLINE_CURVE_WITH_KNOTS('',3,(#52515,#52516,#52517,#52518,#52519,
#52520,#52521,#52522,#52523,#52524),.UNSPECIFIED.,.F.,.F.,(4,1,1,1,1,1,
1,4),(72.2566310325664,73.1842583631033,74.1839090296199,75.1835596961364,
76.183210362653,77.1828610291695,78.1825116956861,78.539816339746),
 .UNSPECIFIED.);
#1340=B_SPLINE_CURVE_WITH_KNOTS('',3,(#52529,#52530,#52531,#52532,#52533,
#52534,#52535,#52536,#52537,#52538),.UNSPECIFIED.,.F.,.F.,(4,1,1,1,1,1,
1,4),(65.9734457253866,66.5854305923265,67.5848853027486,68.5843400131707,
69.5837947235928,70.5832494340148,71.5827041444369,72.2566310325662),
 .UNSPECIFIED.);
#1341=B_SPLINE_CURVE_WITH_KNOTS('',3,(#52539,#52540,#52541,#52542,#52543,
#52544,#52545,#52546,#52547,#52548,#52549),.UNSPECIFIED.,.F.,.F.,(4,1,1,
1,1,1,1,1,4),(65.9734457253868,66.1867036974875,67.186354364004,68.1860050305206,
69.1856556970371,70.1853063635537,71.1849570300702,72.1846076965868,72.2566310325664),
 .UNSPECIFIED.);
#1342=B_SPLINE_CURVE_WITH_KNOTS('',3,(#52554,#52555,#52556,#52557,#52558,
#52559,#52560,#52561,#52562,#52563),.UNSPECIFIED.,.F.,.F.,(4,1,1,1,1,1,
1,4),(59.690260418207,60.588702329794,61.5881570402161,62.5876117506382,
63.5870664610603,64.5865211714823,65.5859758819044,65.9734457253866),
 .UNSPECIFIED.);
#1343=B_SPLINE_CURVE_WITH_KNOTS('',3,(#52564,#52565,#52566,#52567,#52568,
#52569,#52570,#52571,#52572,#52573),.UNSPECIFIED.,.F.,.F.,(4,1,1,1,1,1,
1,4),(59.6902604182073,60.1887996983882,61.1884503649047,62.1881010314213,
63.1877516979378,64.1874023644544,65.1870530309709,65.9734457253868),
 .UNSPECIFIED.);
#1344=B_SPLINE_CURVE_WITH_KNOTS('',3,(#52578,#52579,#52580,#52581,#52582,
#52583,#52584,#52585,#52586,#52587,#52588),.UNSPECIFIED.,.F.,.F.,(4,1,1,
1,1,1,1,1,4),(53.4070751110274,53.5925193568394,54.5919740672615,55.5914287776836,
56.5908834881057,57.5903381985277,58.5897929089498,59.5892476193719,59.690260418207),
 .UNSPECIFIED.);
#1345=B_SPLINE_CURVE_WITH_KNOTS('',3,(#52589,#52590,#52591,#52592,#52593,
#52594,#52595,#52596,#52597,#52598),.UNSPECIFIED.,.F.,.F.,(4,1,1,1,1,1,
1,4),(53.4070751110277,54.1908956992888,55.1905463658054,56.1901970323219,
57.1898476988385,58.189498365355,59.1891490318716,59.6902604182073),
 .UNSPECIFIED.);
#1346=B_SPLINE_CURVE_WITH_KNOTS('',3,(#52603,#52604,#52605,#52606,#52607,
#52608,#52609,#52610,#52611,#52612),.UNSPECIFIED.,.F.,.F.,(4,1,1,1,1,1,
1,4),(47.1238898038478,47.5957910943069,48.595245804729,49.5947005151511,
50.5941552255731,51.5936099359952,52.5930646464173,53.4070751110274),
 .UNSPECIFIED.);
#1347=B_SPLINE_CURVE_WITH_KNOTS('',3,(#52613,#52614,#52615,#52616,#52617,
#52618,#52619,#52620,#52621,#52622,#52623),.UNSPECIFIED.,.F.,.F.,(4,1,1,
1,1,1,1,1,4),(47.1238898038481,47.193341033673,48.1929917001895,49.1926423667061,
50.1922930332226,51.1919436997392,52.1915943662557,53.1912450327723,53.4070751110277),
 .UNSPECIFIED.);
#1348=B_SPLINE_CURVE_WITH_KNOTS('',3,(#52628,#52629,#52630,#52631,#52632,
#52633,#52634,#52635,#52636,#52637),.UNSPECIFIED.,.F.,.F.,(4,1,1,1,1,1,
1,4),(40.8407044966683,41.5990628317744,42.5985175421965,43.5979722526185,
44.5974269630406,45.5968816734627,46.5963363838848,47.1238898038478),
 .UNSPECIFIED.);
#1349=B_SPLINE_CURVE_WITH_KNOTS('',3,(#52638,#52639,#52640,#52641,#52642,
#52643,#52644,#52645,#52646,#52647),.UNSPECIFIED.,.F.,.F.,(4,1,1,1,1,1,
1,4),(40.8407044966685,41.1954370345737,42.1950877010902,43.1947383676068,
44.1943890341233,45.1940397006399,46.1936903671564,47.1238898038481),
 .UNSPECIFIED.);
#1350=B_SPLINE_CURVE_WITH_KNOTS('',3,(#52652,#52653,#52654,#52655,#52656,
#52657,#52658,#52659,#52660,#52661,#52662),.UNSPECIFIED.,.F.,.F.,(4,1,1,
1,1,1,1,1,4),(34.5575191894887,34.6028798588198,35.6023345692419,36.601789279664,
37.601243990086,38.6006987005081,39.6001534109302,40.5996081213523,40.8407044966683),
 .UNSPECIFIED.);
#1351=B_SPLINE_CURVE_WITH_KNOTS('',3,(#52663,#52664,#52665,#52666,#52667,
#52668,#52669,#52670,#52671,#52672),.UNSPECIFIED.,.F.,.F.,(4,1,1,1,1,1,
1,4),(34.5575191894889,35.1975330354744,36.1971837019909,37.1968343685075,
38.196485035024,39.1961357015406,40.1957863680571,40.8407044966685),
 .UNSPECIFIED.);
#1352=B_SPLINE_CURVE_WITH_KNOTS('',3,(#52677,#52678,#52679,#52680,#52681,
#52682,#52683,#52684,#52685,#52686),.UNSPECIFIED.,.F.,.F.,(4,1,1,1,1,1,
1,4),(28.2743338823091,28.6061515962873,29.6056063067094,30.6050610171314,
31.6045157275535,32.6039704379756,33.6034251483977,34.5575191894887),
 .UNSPECIFIED.);
#1353=B_SPLINE_CURVE_WITH_KNOTS('',3,(#52687,#52688,#52689,#52690,#52691,
#52692,#52693,#52694,#52695,#52696),.UNSPECIFIED.,.F.,.F.,(4,1,1,1,1,1,
1,4),(28.2743338823093,29.1996290363751,30.1992797028916,31.1989303694082,
32.1985810359247,33.1982317024413,34.1978823689578,34.5575191894889),
 .UNSPECIFIED.);
#1354=B_SPLINE_CURVE_WITH_KNOTS('',3,(#52701,#52702,#52703,#52704,#52705,
#52706,#52707,#52708,#52709,#52710),.UNSPECIFIED.,.F.,.F.,(4,1,1,1,1,1,
1,4),(21.9911485751295,22.6094233337548,23.6088780441768,24.6083327545989,
25.607787465021,26.6072421754431,27.6066968858652,28.2743338823091),
 .UNSPECIFIED.);
#1355=B_SPLINE_CURVE_WITH_KNOTS('',3,(#52711,#52712,#52713,#52714,#52715,
#52716,#52717,#52718,#52719,#52720,#52721),.UNSPECIFIED.,.F.,.F.,(4,1,1,
1,1,1,1,1,4),(21.9911485751297,22.2020743707592,23.2017250372758,24.2013757037923,
25.2010263703089,26.2006770368254,27.200327703342,28.1999783698585,28.2743338823093),
 .UNSPECIFIED.);
#1356=B_SPLINE_CURVE_WITH_KNOTS('',3,(#52726,#52727,#52728,#52729,#52730,
#52731,#52732,#52733,#52734,#52735),.UNSPECIFIED.,.F.,.F.,(4,1,1,1,1,1,
1,4),(15.7079632679499,16.6126950712223,17.6121497816443,18.6116044920664,
19.6110592024885,20.6105139129106,21.6099686233327,21.9911485751295),
 .UNSPECIFIED.);
#1357=B_SPLINE_CURVE_WITH_KNOTS('',3,(#52736,#52737,#52738,#52739,#52740,
#52741,#52742,#52743,#52744,#52745),.UNSPECIFIED.,.F.,.F.,(4,1,1,1,1,1,
1,4),(15.7079632679501,16.2041703716599,17.2038210381765,18.203471704693,
19.2031223712096,20.2027730377261,21.2024237042427,21.9911485751297),
 .UNSPECIFIED.);
#1358=B_SPLINE_CURVE_WITH_KNOTS('',3,(#52748,#52749,#52750,#52751,#52752,
#52753,#52754,#52755,#52756,#52757,#52758,#52759,#52760,#52761,#52762,#52763,
#52764,#52765,#52766,#52767,#52768,#52769,#52770,#52771,#52772,#52773,#52774,
#52775,#52776,#52777,#52778,#52779,#52780,#52781,#52782,#52783,#52784,#52785,
#52786,#52787,#52788,#52789,#52790,#52791,#52792,#52793,#52794,#52795,#52796,
#52797,#52798,#52799,#52800,#52801,#52802,#52803,#52804,#52805,#52806,#52807,
#52808,#52809,#52810,#52811,#52812,#52813,#52814,#52815,#52816,#52817,#52818,
#52819,#52820),.UNSPECIFIED.,.F.,.F.,(4,3,3,3,3,3,3,3,3,3,3,3,3,3,3,3,3,
3,3,3,3,3,3,3,4),(-0.833806508238614,-0.784110841134283,-0.735306998950323,
-0.687259726601284,-0.645877709227694,-0.62807402512667,-0.620323068728151,
-0.604495691854104,-0.557043524288525,-0.509117916148162,-0.461617173214432,
-0.427640023675466,-0.414574598236473,-0.406906758156835,-0.401016345434302,
-0.354784550175495,-0.325708575058567,-0.279459204769296,-0.233637516184487,
-0.212276112655899,-0.199827110241752,-0.194271984707397,-0.14972919330764,
-0.105716619472331,-0.0627462879557836),.UNSPECIFIED.);
#1359=B_SPLINE_CURVE_WITH_KNOTS('',3,(#52822,#52823,#52824,#52825,#52826,
#52827,#52828,#52829,#52830,#52831,#52832,#52833,#52834,#52835,#52836,#52837,
#52838,#52839,#52840,#52841,#52842,#52843,#52844,#52845,#52846,#52847,#52848,
#52849,#52850,#52851,#52852,#52853,#52854,#52855,#52856,#52857,#52858,#52859,
#52860,#52861,#52862,#52863,#52864,#52865,#52866,#52867,#52868,#52869,#52870,
#52871,#52872,#52873,#52874,#52875,#52876,#52877,#52878,#52879,#52880,#52881,
#52882,#52883,#52884,#52885,#52886,#52887,#52888,#52889,#52890,#52891,#52892,
#52893,#52894,#52895,#52896,#52897,#52898,#52899,#52900,#52901,#52902,#52903,
#52904,#52905,#52906,#52907,#52908,#52909,#52910,#52911,#52912,#52913,#52914,
#52915,#52916,#52917,#52918,#52919,#52920,#52921,#52922,#52923,#52924,#52925,
#52926,#52927,#52928,#52929,#52930,#52931,#52932,#52933,#52934,#52935,#52936,
#52937,#52938,#52939,#52940,#52941,#52942,#52943,#52944,#52945,#52946,#52947,
#52948,#52949,#52950,#52951,#52952,#52953,#52954,#52955,#52956,#52957,#52958,
#52959,#52960,#52961,#52962,#52963,#52964,#52965,#52966,#52967,#52968,#52969,
#52970,#52971,#52972,#52973,#52974,#52975,#52976,#52977,#52978,#52979,#52980,
#52981,#52982,#52983,#52984,#52985,#52986,#52987,#52988,#52989,#52990,#52991,
#52992,#52993,#52994,#52995,#52996,#52997,#52998,#52999,#53000,#53001,#53002,
#53003,#53004,#53005,#53006,#53007,#53008,#53009,#53010,#53011,#53012,#53013,
#53014,#53015,#53016,#53017,#53018,#53019,#53020,#53021,#53022,#53023,#53024,
#53025,#53026,#53027,#53028,#53029,#53030,#53031,#53032,#53033,#53034,#53035,
#53036,#53037,#53038,#53039,#53040,#53041,#53042,#53043,#53044,#53045,#53046,
#53047,#53048,#53049,#53050,#53051,#53052,#53053,#53054,#53055,#53056,#53057,
#53058,#53059,#53060,#53061,#53062,#53063,#53064,#53065,#53066,#53067,#53068,
#53069,#53070,#53071,#53072,#53073,#53074,#53075,#53076,#53077,#53078,#53079,
#53080,#53081,#53082,#53083,#53084,#53085,#53086,#53087,#53088,#53089,#53090,
#53091,#53092,#53093,#53094,#53095,#53096,#53097,#53098,#53099,#53100,#53101),
 .UNSPECIFIED.,.F.,.F.,(4,3,3,3,3,3,3,3,3,3,3,3,3,3,3,3,3,3,3,3,3,3,3,3,
3,3,3,3,3,3,3,3,3,3,3,3,3,3,3,3,3,3,3,3,3,3,3,3,3,3,3,3,3,3,3,3,3,3,3,3,
3,3,3,3,3,3,3,3,3,3,3,3,3,3,3,3,3,3,3,3,3,3,3,3,3,3,3,3,3,3,3,3,3,4),(-2.8505485327553,
-2.80573427450524,-2.77511892064891,-2.76323501298752,-2.7578271088511,
-2.71268252538819,-2.68327285907993,-2.63807445758683,-2.61160951174613,
-2.59853995865707,-2.5879328823648,-2.5817358151457,-2.5361463925531,-2.49054398414152,
-2.44565509913639,-2.42635489086124,-2.39343442202386,-2.38640148315151,
-2.38063442805171,-2.33614443609276,-2.29063594485493,-2.24440704909113,
-2.20130959163764,-2.18782840844821,-2.1815609373624,-2.17543544873235,
-2.1287835245443,-2.08184078143437,-2.03551021638789,-2.00153950965672,
-1.98594287672261,-1.97665838033466,-1.97074492343949,-1.92364723254399,
-1.89962738946321,-1.8536836277288,-1.80688299109426,-1.77866383131902,
-1.769614968468,-1.76173733059279,-1.71535978925738,-1.66772881631917,-1.61991043415747,
-1.58684368422409,-1.55789442552168,-1.55016980216945,-1.5014714602997,
-1.4534466233461,-1.40441152901827,-1.35822610122742,-1.35537643469044,
-1.34088108273801,-1.33444858249317,-1.28819265226034,-1.24082690028513,
-1.19260099076567,-1.14276637745728,-1.12831574751615,-1.12231458018188,
-1.07369356250354,-1.02459245907517,-0.975558021868307,-0.930149537475869,
-0.913121355828704,-0.904001509154352,-0.898152153874911,-0.84868958328962,
-0.799775975381224,-0.793924084298553,-0.745422579095372,-0.712280661750332,
-0.69384093619032,-0.68376800953834,-0.677703857148311,-0.629392367529373,
-0.577612309285043,-0.527597792884359,-0.488542056470656,-0.471325584677335,
-0.461423807374008,-0.452963847209369,-0.402681212061588,-0.352415085644384,
-0.302711700252363,-0.258931800913549,-0.237041851244141,-0.230232856748154,
-0.224025422271845,-0.215151901574734,-0.167089464755252,-0.117446387488254,
-0.0671034891247927,-0.0162957457720915,0.),.UNSPECIFIED.);
#1360=B_SPLINE_CURVE_WITH_KNOTS('',3,(#53105,#53106,#53107,#53108,#53109,
#53110,#53111),.UNSPECIFIED.,.F.,.F.,(4,3,4),(1.04608885943707,1.08948735834114,
1.13094109509796),.UNSPECIFIED.);
#1361=B_SPLINE_CURVE_WITH_KNOTS('',3,(#53114,#53115,#53116,#53117,#53118,
#53119,#53120),.UNSPECIFIED.,.F.,.F.,(4,3,4),(0.,0.0443247549663995,0.084677685176745),
 .UNSPECIFIED.);
#1362=B_SPLINE_CURVE_WITH_KNOTS('',3,(#53136,#53137,#53138,#53139,#53140,
#53141,#53142,#53143,#53144,#53145,#53146,#53147,#53148,#53149,#53150,#53151,
#53152,#53153,#53154,#53155,#53156,#53157,#53158,#53159,#53160,#53161,#53162,
#53163,#53164,#53165,#53166,#53167,#53168,#53169,#53170,#53171,#53172,#53173,
#53174,#53175,#53176,#53177,#53178,#53179,#53180,#53181,#53182,#53183,#53184,
#53185,#53186,#53187,#53188,#53189,#53190,#53191,#53192,#53193,#53194,#53195,
#53196,#53197,#53198,#53199,#53200,#53201,#53202,#53203,#53204,#53205,#53206,
#53207,#53208,#53209,#53210,#53211,#53212,#53213,#53214,#53215,#53216,#53217,
#53218,#53219,#53220,#53221,#53222,#53223,#53224,#53225,#53226,#53227,#53228,
#53229,#53230,#53231,#53232,#53233,#53234,#53235,#53236,#53237,#53238,#53239,
#53240,#53241,#53242,#53243,#53244,#53245,#53246,#53247,#53248,#53249,#53250),
 .UNSPECIFIED.,.F.,.F.,(4,3,3,3,3,3,3,3,3,3,3,3,3,3,3,3,3,3,3,3,3,3,3,3,
3,3,3,3,3,3,3,3,3,3,3,3,3,3,4),(-1.13094109509824,-1.09563331911551,-1.05277492694931,
-1.02270576365399,-1.00715902947279,-0.999434161139063,-0.992415787646934,
-0.948423021491772,-0.901328683083329,-0.880724910029636,-0.865673266591215,
-0.85985042234436,-0.814096270843057,-0.767722321418939,-0.721190349721597,
-0.683809840847257,-0.669300679648143,-0.659993560535856,-0.654189217743676,
-0.606509202994476,-0.571668314224235,-0.525516476930707,-0.478640819134196,
-0.455267754576504,-0.447581100598068,-0.442041462532518,-0.39477738260878,
-0.346766372069733,-0.298184121586594,-0.291656302672655,-0.255199264838573,
-0.239249310786162,-0.229177328973695,-0.222810242437123,-0.173603985401498,
-0.123778246004826,-0.0739959577271227,-0.0248532857217371,0.),
 .UNSPECIFIED.);
#1363=B_SPLINE_CURVE_WITH_KNOTS('',3,(#53251,#53252,#53253,#53254,#53255,
#53256,#53257,#53258,#53259,#53260,#53261,#53262,#53263,#53264,#53265,#53266,
#53267,#53268,#53269,#53270,#53271,#53272,#53273,#53274,#53275,#53276,#53277,
#53278,#53279,#53280,#53281,#53282,#53283,#53284,#53285,#53286,#53287,#53288,
#53289,#53290,#53291,#53292,#53293,#53294,#53295,#53296,#53297,#53298,#53299,
#53300,#53301,#53302,#53303,#53304,#53305,#53306,#53307,#53308,#53309,#53310,
#53311,#53312,#53313,#53314,#53315,#53316,#53317,#53318,#53319,#53320,#53321,
#53322,#53323,#53324,#53325,#53326,#53327,#53328,#53329,#53330,#53331,#53332,
#53333,#53334,#53335,#53336,#53337,#53338,#53339,#53340,#53341,#53342,#53343,
#53344,#53345,#53346,#53347,#53348,#53349,#53350,#53351,#53352,#53353,#53354,
#53355,#53356,#53357,#53358,#53359),.UNSPECIFIED.,.F.,.F.,(4,3,3,3,3,3,
3,3,3,3,3,3,3,3,3,3,3,3,3,3,3,3,3,3,3,3,3,3,3,3,3,3,3,3,3,3,4),(-1.12653966532762,
-1.08490854816515,-1.03522530378325,-1.00297074027101,-0.98193935568292,
-0.97317885460119,-0.965315969455476,-0.916182132148453,-0.86655340157831,
-0.822266762307489,-0.815588448831975,-0.767271193265127,-0.719185403827295,
-0.671761178654938,-0.633608955888029,-0.616498884302865,-0.606206529965436,
-0.599913578153287,-0.553803068539291,-0.519152287587304,-0.472463419784273,
-0.425808948481975,-0.404285750458287,-0.397320170626258,-0.391056720436118,
-0.345587767561757,-0.299605565927115,-0.253623364292473,-0.221920443755914,
-0.205347277549075,-0.194960257430732,-0.189028113959442,-0.144730321897778,
-0.100642231601604,-0.0569916939973363,-0.014221171191207,0.),
 .UNSPECIFIED.);
#1364=B_SPLINE_CURVE_WITH_KNOTS('',3,(#55392,#55393,#55394,#55395,#55396,
#55397,#55398,#55399,#55400,#55401),.UNSPECIFIED.,.F.,.F.,(4,1,1,1,1,1,
1,4),(10.375727056019,10.7060917058189,11.2059170390771,12.2055677055937,
13.2052183721102,14.2048690386268,15.2045197051434,15.7079632679501),
 .UNSPECIFIED.);
#1365=B_SPLINE_CURVE_WITH_KNOTS('',3,(#55402,#55403,#55404,#55405,#55406,
#55407,#55408,#55409,#55410,#55411,#55412,#55413,#55414,#55415,#55416,#55417,
#55418,#55419,#55420,#55421,#55422,#55423),.UNSPECIFIED.,.F.,.F.,(4,3,3,
3,3,3,3,4),(491.207309053546,491.729170098438,492.728820764955,493.728471431471,
494.728122097988,495.727772764504,496.727423431021,497.490494360725),
 .UNSPECIFIED.);
#1366=B_SPLINE_CURVE_WITH_KNOTS('',3,(#55425,#55426,#55427,#55428,#55429,
#55430,#55431,#55432,#55433),.UNSPECIFIED.,.F.,.F.,(4,1,1,1,1,1,4),(11.6154215191118,
12.1151488743229,12.6148762295339,13.614330939956,14.6137856503781,15.6132403608002,
15.7079632679499),.UNSPECIFIED.);
#1367=B_SPLINE_CURVE_WITH_KNOTS('',3,(#57474,#57475,#57476,#57477,#57478,
#57479,#57480,#57481,#57482,#57483,#57484,#57485,#57486,#57487,#57488,#57489,
#57490,#57491,#57492,#57493,#57494,#57495),.UNSPECIFIED.,.F.,.F.,(4,3,3,
3,3,3,3,4),(-500.464181016024,-499.727355211043,-498.72790050062,-497.728445790198,
-496.728991079776,-495.729536369354,-494.730081658932,-494.180995708845),
 .UNSPECIFIED.);
#1563=SHAPE_REPRESENTATION_RELATIONSHIP('SRR','None',#64002,#1581);
#1581=ADVANCED_BREP_SHAPE_REPRESENTATION('',(#1617),#63887);
#1599=STYLED_ITEM('',(#64098),#1617);
#1617=MANIFOLD_SOLID_BREP('Body1',#15485);
#1673=FACE_BOUND('',#4196,.T.);
#1674=FACE_BOUND('',#4198,.T.);
#1675=FACE_BOUND('',#4212,.T.);
#1676=FACE_BOUND('',#4213,.T.);
#1677=FACE_BOUND('',#4214,.T.);
#1678=FACE_BOUND('',#4215,.T.);
#1679=FACE_BOUND('',#4216,.T.);
#1680=FACE_BOUND('',#4217,.T.);
#1681=FACE_BOUND('',#4218,.T.);
#1682=FACE_BOUND('',#4221,.T.);
#1683=FACE_BOUND('',#4222,.T.);
#1684=FACE_BOUND('',#4223,.T.);
#1685=FACE_BOUND('',#4224,.T.);
#1686=FACE_BOUND('',#4225,.T.);
#1687=FACE_BOUND('',#4226,.T.);
#1688=FACE_BOUND('',#4228,.T.);
#2112=CYLINDRICAL_SURFACE('',#16305,5.91675);
#2113=CYLINDRICAL_SURFACE('',#16307,5.91675);
#2114=CYLINDRICAL_SURFACE('',#16308,5.91675);
#2115=CYLINDRICAL_SURFACE('',#16309,5.91675);
#2116=CYLINDRICAL_SURFACE('',#16310,5.91675);
#2117=CYLINDRICAL_SURFACE('',#16311,5.91675);
#2118=CYLINDRICAL_SURFACE('',#16312,5.91675);
#2119=CYLINDRICAL_SURFACE('',#16313,5.91675);
#2120=CYLINDRICAL_SURFACE('',#16314,5.91675);
#2121=CYLINDRICAL_SURFACE('',#16315,5.91675);
#2122=CYLINDRICAL_SURFACE('',#16316,5.91675);
#2123=CYLINDRICAL_SURFACE('',#16317,5.91675);
#2124=CYLINDRICAL_SURFACE('',#16318,5.91675);
#2125=CYLINDRICAL_SURFACE('',#16319,5.91675);
#2126=CYLINDRICAL_SURFACE('',#16320,5.91675);
#2127=CYLINDRICAL_SURFACE('',#16321,5.91675);
#2128=CYLINDRICAL_SURFACE('',#16322,5.91675);
#2129=CYLINDRICAL_SURFACE('',#16323,5.91675);
#2130=CYLINDRICAL_SURFACE('',#16324,5.91675);
#2131=CYLINDRICAL_SURFACE('',#16325,5.91675);
#2132=CYLINDRICAL_SURFACE('',#16326,5.91675);
#2133=CYLINDRICAL_SURFACE('',#16327,5.91675);
#2134=CYLINDRICAL_SURFACE('',#16328,5.91675);
#2135=CYLINDRICAL_SURFACE('',#16329,5.91675);
#2136=CYLINDRICAL_SURFACE('',#16330,5.91675);
#2137=CYLINDRICAL_SURFACE('',#16331,5.91675);
#2138=CYLINDRICAL_SURFACE('',#16332,5.91675);
#2139=CYLINDRICAL_SURFACE('',#16333,5.91675);
#2140=CYLINDRICAL_SURFACE('',#16334,5.91675);
#2141=CYLINDRICAL_SURFACE('',#16335,5.91675);
#2142=CYLINDRICAL_SURFACE('',#16336,5.91675);
#2143=CYLINDRICAL_SURFACE('',#16337,5.91675);
#2144=CYLINDRICAL_SURFACE('',#16338,5.91675);
#2145=CYLINDRICAL_SURFACE('',#16339,5.91675);
#2146=CYLINDRICAL_SURFACE('',#16340,5.91675);
#2147=CYLINDRICAL_SURFACE('',#16341,5.91675);
#2148=CYLINDRICAL_SURFACE('',#16342,5.91675);
#2149=CYLINDRICAL_SURFACE('',#16343,5.91675);
#2150=CYLINDRICAL_SURFACE('',#16344,5.91675);
#2151=CYLINDRICAL_SURFACE('',#16345,5.91675);
#2152=CYLINDRICAL_SURFACE('',#16346,5.91675);
#2153=CYLINDRICAL_SURFACE('',#16347,5.91675);
#2154=CYLINDRICAL_SURFACE('',#16348,5.91675);
#2155=CYLINDRICAL_SURFACE('',#16349,5.91675);
#2156=CYLINDRICAL_SURFACE('',#16350,5.91675);
#2157=CYLINDRICAL_SURFACE('',#16351,5.91675);
#2158=CYLINDRICAL_SURFACE('',#16352,5.91675);
#2159=CYLINDRICAL_SURFACE('',#16353,5.91675);
#2160=CYLINDRICAL_SURFACE('',#16354,5.91675);
#2161=CYLINDRICAL_SURFACE('',#16355,5.91675);
#2162=CYLINDRICAL_SURFACE('',#16356,5.91675);
#2163=CYLINDRICAL_SURFACE('',#16357,5.91675);
#2164=CYLINDRICAL_SURFACE('',#16358,5.91675);
#2165=CYLINDRICAL_SURFACE('',#16359,5.91675);
#2166=CYLINDRICAL_SURFACE('',#16360,5.91675);
#2167=CYLINDRICAL_SURFACE('',#16361,5.91675);
#2168=CYLINDRICAL_SURFACE('',#16362,5.91675);
#2169=CYLINDRICAL_SURFACE('',#16363,5.91675);
#2170=CYLINDRICAL_SURFACE('',#16364,5.91675);
#2171=CYLINDRICAL_SURFACE('',#16365,5.91675);
#2172=CYLINDRICAL_SURFACE('',#16366,5.91675);
#2173=CYLINDRICAL_SURFACE('',#16367,5.91675);
#2174=CYLINDRICAL_SURFACE('',#16368,5.91675);
#2175=CYLINDRICAL_SURFACE('',#16369,5.91675);
#2176=CYLINDRICAL_SURFACE('',#16370,5.91675);
#2177=CYLINDRICAL_SURFACE('',#16371,5.91675);
#2178=CYLINDRICAL_SURFACE('',#16372,5.91675);
#2179=CYLINDRICAL_SURFACE('',#16373,5.91675);
#2180=CYLINDRICAL_SURFACE('',#16374,5.91675);
#2181=CYLINDRICAL_SURFACE('',#16375,5.91675);
#2182=CYLINDRICAL_SURFACE('',#16376,5.91675);
#2183=CYLINDRICAL_SURFACE('',#16377,5.91675);
#2184=CYLINDRICAL_SURFACE('',#16378,5.91675);
#2185=CYLINDRICAL_SURFACE('',#16379,5.91675);
#2186=CYLINDRICAL_SURFACE('',#16380,5.91675);
#2187=CYLINDRICAL_SURFACE('',#16381,5.91675);
#2188=CYLINDRICAL_SURFACE('',#16382,5.91675);
#2189=CYLINDRICAL_SURFACE('',#16383,5.91675);
#2190=CYLINDRICAL_SURFACE('',#16384,5.91675);
#2191=CYLINDRICAL_SURFACE('',#16388,4.91825);
#2192=CYLINDRICAL_SURFACE('',#16390,4.91825);
#2193=CYLINDRICAL_SURFACE('',#16391,4.91825);
#2194=CYLINDRICAL_SURFACE('',#16392,4.91825);
#2195=CYLINDRICAL_SURFACE('',#16393,4.91825);
#2196=CYLINDRICAL_SURFACE('',#16394,4.91825);
#2197=CYLINDRICAL_SURFACE('',#16395,4.91825);
#2198=CYLINDRICAL_SURFACE('',#16396,4.91825);
#2199=CYLINDRICAL_SURFACE('',#16397,4.91825);
#2200=CYLINDRICAL_SURFACE('',#16398,4.91825);
#2201=CYLINDRICAL_SURFACE('',#16399,4.91825);
#2202=CYLINDRICAL_SURFACE('',#16400,4.91825);
#2203=CYLINDRICAL_SURFACE('',#16401,4.91825);
#2204=CYLINDRICAL_SURFACE('',#16402,4.91825);
#2205=CYLINDRICAL_SURFACE('',#16403,4.91825);
#2206=CYLINDRICAL_SURFACE('',#16404,4.91825);
#2207=CYLINDRICAL_SURFACE('',#16405,4.91825);
#2208=CYLINDRICAL_SURFACE('',#16406,4.91825);
#2209=CYLINDRICAL_SURFACE('',#16407,4.91825);
#2210=CYLINDRICAL_SURFACE('',#16408,4.91825);
#2211=CYLINDRICAL_SURFACE('',#16409,4.91825);
#2212=CYLINDRICAL_SURFACE('',#16410,4.91825);
#2213=CYLINDRICAL_SURFACE('',#16411,4.91825);
#2214=CYLINDRICAL_SURFACE('',#16412,4.91825);
#2215=CYLINDRICAL_SURFACE('',#16413,4.91825);
#2216=CYLINDRICAL_SURFACE('',#16414,4.91825);
#2217=CYLINDRICAL_SURFACE('',#16415,4.91825);
#2218=CYLINDRICAL_SURFACE('',#16416,4.91825);
#2219=CYLINDRICAL_SURFACE('',#16417,4.91825);
#2220=CYLINDRICAL_SURFACE('',#16418,4.91825);
#2221=CYLINDRICAL_SURFACE('',#16419,4.91825);
#2222=CYLINDRICAL_SURFACE('',#16420,4.91825);
#2223=CYLINDRICAL_SURFACE('',#16421,4.91825);
#2224=CYLINDRICAL_SURFACE('',#16422,4.91825);
#2225=CYLINDRICAL_SURFACE('',#16423,4.91825);
#2226=CYLINDRICAL_SURFACE('',#16424,4.91825);
#2227=CYLINDRICAL_SURFACE('',#16425,4.91825);
#2228=CYLINDRICAL_SURFACE('',#16426,4.91825);
#2229=CYLINDRICAL_SURFACE('',#16427,4.91825);
#2230=CYLINDRICAL_SURFACE('',#16428,4.91825);
#2231=CYLINDRICAL_SURFACE('',#16429,4.91825);
#2232=CYLINDRICAL_SURFACE('',#16430,4.91825);
#2233=CYLINDRICAL_SURFACE('',#16431,4.91825);
#2234=CYLINDRICAL_SURFACE('',#16432,4.91825);
#2235=CYLINDRICAL_SURFACE('',#16433,4.91825);
#2236=CYLINDRICAL_SURFACE('',#16434,4.91825);
#2237=CYLINDRICAL_SURFACE('',#16435,4.91825);
#2238=CYLINDRICAL_SURFACE('',#16436,4.91825);
#2239=CYLINDRICAL_SURFACE('',#16437,4.91825);
#2240=CYLINDRICAL_SURFACE('',#16438,4.91825);
#2241=CYLINDRICAL_SURFACE('',#16439,4.91825);
#2242=CYLINDRICAL_SURFACE('',#16440,4.91825);
#2243=CYLINDRICAL_SURFACE('',#16441,4.91825);
#2244=CYLINDRICAL_SURFACE('',#16442,4.91825);
#2245=CYLINDRICAL_SURFACE('',#16443,4.91825);
#2246=CYLINDRICAL_SURFACE('',#16444,4.91825);
#2247=CYLINDRICAL_SURFACE('',#16445,4.91825);
#2248=CYLINDRICAL_SURFACE('',#16446,4.91825);
#2249=CYLINDRICAL_SURFACE('',#16447,4.91825);
#2250=CYLINDRICAL_SURFACE('',#16448,4.91825);
#2251=CYLINDRICAL_SURFACE('',#16449,4.91825);
#2252=CYLINDRICAL_SURFACE('',#16450,4.91825);
#2253=CYLINDRICAL_SURFACE('',#16451,4.91825);
#2254=CYLINDRICAL_SURFACE('',#16452,4.91825);
#2255=CYLINDRICAL_SURFACE('',#16453,4.91825);
#2256=CYLINDRICAL_SURFACE('',#16454,4.91825);
#2257=CYLINDRICAL_SURFACE('',#16455,4.91825);
#2258=CYLINDRICAL_SURFACE('',#16456,4.91825);
#2259=CYLINDRICAL_SURFACE('',#16457,4.91825);
#2260=CYLINDRICAL_SURFACE('',#16458,4.91825);
#2261=CYLINDRICAL_SURFACE('',#16459,4.91825);
#2262=CYLINDRICAL_SURFACE('',#16460,4.91825);
#2263=CYLINDRICAL_SURFACE('',#16461,4.91825);
#2264=CYLINDRICAL_SURFACE('',#16462,4.91825);
#2265=CYLINDRICAL_SURFACE('',#16463,4.91825);
#2266=CYLINDRICAL_SURFACE('',#16464,4.91825);
#2267=CYLINDRICAL_SURFACE('',#16465,4.91825);
#2268=CYLINDRICAL_SURFACE('',#16466,4.91825);
#2269=CYLINDRICAL_SURFACE('',#16467,4.91825);
#2270=CYLINDRICAL_SURFACE('',#16468,4.91825);
#2271=CYLINDRICAL_SURFACE('',#16473,5.);
#2272=CYLINDRICAL_SURFACE('',#16479,5.91675);
#2273=CYLINDRICAL_SURFACE('',#16482,4.91825);
#2274=CYLINDRICAL_SURFACE('',#16483,5.91675);
#2275=CYLINDRICAL_SURFACE('',#16484,3.);
#2276=CYLINDRICAL_SURFACE('',#16487,3.);
#2277=CYLINDRICAL_SURFACE('',#16490,3.);
#2278=CYLINDRICAL_SURFACE('',#16493,3.);
#2279=CYLINDRICAL_SURFACE('',#16496,3.);
#2280=CYLINDRICAL_SURFACE('',#16499,3.);
#2281=CYLINDRICAL_SURFACE('',#16505,25.);
#2282=CYLINDRICAL_SURFACE('',#16510,12.);
#2511=CIRCLE('',#16306,5.91675);
#2512=CIRCLE('',#16385,5.91675);
#2513=CIRCLE('',#16386,5.91675);
#2514=CIRCLE('',#16387,5.91675);
#2515=CIRCLE('',#16389,4.91825);
#2516=CIRCLE('',#16470,5.);
#2517=CIRCLE('',#16472,4.91825);
#2518=CIRCLE('',#16474,5.);
#2519=CIRCLE('',#16475,5.);
#2520=CIRCLE('',#16478,5.91675);
#2521=CIRCLE('',#16480,5.91675);
#2522=CIRCLE('',#16485,3.);
#2523=CIRCLE('',#16486,3.);
#2524=CIRCLE('',#16488,3.);
#2525=CIRCLE('',#16489,3.);
#2526=CIRCLE('',#16491,3.);
#2527=CIRCLE('',#16492,3.);
#2528=CIRCLE('',#16494,3.);
#2529=CIRCLE('',#16495,3.);
#2530=CIRCLE('',#16497,3.);
#2531=CIRCLE('',#16498,3.);
#2532=CIRCLE('',#16500,3.);
#2533=CIRCLE('',#16501,3.);
#2534=CIRCLE('',#16503,25.);
#2535=CIRCLE('',#16504,12.);
#2536=CIRCLE('',#16506,25.);
#2537=CIRCLE('',#16509,12.);
#3150=FACE_OUTER_BOUND('',#4033,.T.);
#3151=FACE_OUTER_BOUND('',#4034,.T.);
#3152=FACE_OUTER_BOUND('',#4035,.T.);
#3153=FACE_OUTER_BOUND('',#4036,.T.);
#3154=FACE_OUTER_BOUND('',#4037,.T.);
#3155=FACE_OUTER_BOUND('',#4038,.T.);
#3156=FACE_OUTER_BOUND('',#4039,.T.);
#3157=FACE_OUTER_BOUND('',#4040,.T.);
#3158=FACE_OUTER_BOUND('',#4041,.T.);
#3159=FACE_OUTER_BOUND('',#4042,.T.);
#3160=FACE_OUTER_BOUND('',#4043,.T.);
#3161=FACE_OUTER_BOUND('',#4044,.T.);
#3162=FACE_OUTER_BOUND('',#4045,.T.);
#3163=FACE_OUTER_BOUND('',#4046,.T.);
#3164=FACE_OUTER_BOUND('',#4047,.T.);
#3165=FACE_OUTER_BOUND('',#4048,.T.);
#3166=FACE_OUTER_BOUND('',#4049,.T.);
#3167=FACE_OUTER_BOUND('',#4050,.T.);
#3168=FACE_OUTER_BOUND('',#4051,.T.);
#3169=FACE_OUTER_BOUND('',#4052,.T.);
#3170=FACE_OUTER_BOUND('',#4053,.T.);
#3171=FACE_OUTER_BOUND('',#4054,.T.);
#3172=FACE_OUTER_BOUND('',#4055,.T.);
#3173=FACE_OUTER_BOUND('',#4056,.T.);
#3174=FACE_OUTER_BOUND('',#4057,.T.);
#3175=FACE_OUTER_BOUND('',#4058,.T.);
#3176=FACE_OUTER_BOUND('',#4059,.T.);
#3177=FACE_OUTER_BOUND('',#4060,.T.);
#3178=FACE_OUTER_BOUND('',#4061,.T.);
#3179=FACE_OUTER_BOUND('',#4062,.T.);
#3180=FACE_OUTER_BOUND('',#4063,.T.);
#3181=FACE_OUTER_BOUND('',#4064,.T.);
#3182=FACE_OUTER_BOUND('',#4065,.T.);
#3183=FACE_OUTER_BOUND('',#4066,.T.);
#3184=FACE_OUTER_BOUND('',#4067,.T.);
#3185=FACE_OUTER_BOUND('',#4068,.T.);
#3186=FACE_OUTER_BOUND('',#4069,.T.);
#3187=FACE_OUTER_BOUND('',#4070,.T.);
#3188=FACE_OUTER_BOUND('',#4071,.T.);
#3189=FACE_OUTER_BOUND('',#4072,.T.);
#3190=FACE_OUTER_BOUND('',#4073,.T.);
#3191=FACE_OUTER_BOUND('',#4074,.T.);
#3192=FACE_OUTER_BOUND('',#4075,.T.);
#3193=FACE_OUTER_BOUND('',#4076,.T.);
#3194=FACE_OUTER_BOUND('',#4077,.T.);
#3195=FACE_OUTER_BOUND('',#4078,.T.);
#3196=FACE_OUTER_BOUND('',#4079,.T.);
#3197=FACE_OUTER_BOUND('',#4080,.T.);
#3198=FACE_OUTER_BOUND('',#4081,.T.);
#3199=FACE_OUTER_BOUND('',#4082,.T.);
#3200=FACE_OUTER_BOUND('',#4083,.T.);
#3201=FACE_OUTER_BOUND('',#4084,.T.);
#3202=FACE_OUTER_BOUND('',#4085,.T.);
#3203=FACE_OUTER_BOUND('',#4086,.T.);
#3204=FACE_OUTER_BOUND('',#4087,.T.);
#3205=FACE_OUTER_BOUND('',#4088,.T.);
#3206=FACE_OUTER_BOUND('',#4089,.T.);
#3207=FACE_OUTER_BOUND('',#4090,.T.);
#3208=FACE_OUTER_BOUND('',#4091,.T.);
#3209=FACE_OUTER_BOUND('',#4092,.T.);
#3210=FACE_OUTER_BOUND('',#4093,.T.);
#3211=FACE_OUTER_BOUND('',#4094,.T.);
#3212=FACE_OUTER_BOUND('',#4095,.T.);
#3213=FACE_OUTER_BOUND('',#4096,.T.);
#3214=FACE_OUTER_BOUND('',#4097,.T.);
#3215=FACE_OUTER_BOUND('',#4098,.T.);
#3216=FACE_OUTER_BOUND('',#4099,.T.);
#3217=FACE_OUTER_BOUND('',#4100,.T.);
#3218=FACE_OUTER_BOUND('',#4101,.T.);
#3219=FACE_OUTER_BOUND('',#4102,.T.);
#3220=FACE_OUTER_BOUND('',#4103,.T.);
#3221=FACE_OUTER_BOUND('',#4104,.T.);
#3222=FACE_OUTER_BOUND('',#4105,.T.);
#3223=FACE_OUTER_BOUND('',#4106,.T.);
#3224=FACE_OUTER_BOUND('',#4107,.T.);
#3225=FACE_OUTER_BOUND('',#4108,.T.);
#3226=FACE_OUTER_BOUND('',#4109,.T.);
#3227=FACE_OUTER_BOUND('',#4110,.T.);
#3228=FACE_OUTER_BOUND('',#4111,.T.);
#3229=FACE_OUTER_BOUND('',#4112,.T.);
#3230=FACE_OUTER_BOUND('',#4113,.T.);
#3231=FACE_OUTER_BOUND('',#4114,.T.);
#3232=FACE_OUTER_BOUND('',#4115,.T.);
#3233=FACE_OUTER_BOUND('',#4116,.T.);
#3234=FACE_OUTER_BOUND('',#4117,.T.);
#3235=FACE_OUTER_BOUND('',#4118,.T.);
#3236=FACE_OUTER_BOUND('',#4119,.T.);
#3237=FACE_OUTER_BOUND('',#4120,.T.);
#3238=FACE_OUTER_BOUND('',#4121,.T.);
#3239=FACE_OUTER_BOUND('',#4122,.T.);
#3240=FACE_OUTER_BOUND('',#4123,.T.);
#3241=FACE_OUTER_BOUND('',#4124,.T.);
#3242=FACE_OUTER_BOUND('',#4125,.T.);
#3243=FACE_OUTER_BOUND('',#4126,.T.);
#3244=FACE_OUTER_BOUND('',#4127,.T.);
#3245=FACE_OUTER_BOUND('',#4128,.T.);
#3246=FACE_OUTER_BOUND('',#4129,.T.);
#3247=FACE_OUTER_BOUND('',#4130,.T.);
#3248=FACE_OUTER_BOUND('',#4131,.T.);
#3249=FACE_OUTER_BOUND('',#4132,.T.);
#3250=FACE_OUTER_BOUND('',#4133,.T.);
#3251=FACE_OUTER_BOUND('',#4134,.T.);
#3252=FACE_OUTER_BOUND('',#4135,.T.);
#3253=FACE_OUTER_BOUND('',#4136,.T.);
#3254=FACE_OUTER_BOUND('',#4137,.T.);
#3255=FACE_OUTER_BOUND('',#4138,.T.);
#3256=FACE_OUTER_BOUND('',#4139,.T.);
#3257=FACE_OUTER_BOUND('',#4140,.T.);
#3258=FACE_OUTER_BOUND('',#4141,.T.);
#3259=FACE_OUTER_BOUND('',#4142,.T.);
#3260=FACE_OUTER_BOUND('',#4143,.T.);
#3261=FACE_OUTER_BOUND('',#4144,.T.);
#3262=FACE_OUTER_BOUND('',#4145,.T.);
#3263=FACE_OUTER_BOUND('',#4146,.T.);
#3264=FACE_OUTER_BOUND('',#4147,.T.);
#3265=FACE_OUTER_BOUND('',#4148,.T.);
#3266=FACE_OUTER_BOUND('',#4149,.T.);
#3267=FACE_OUTER_BOUND('',#4150,.T.);
#3268=FACE_OUTER_BOUND('',#4151,.T.);
#3269=FACE_OUTER_BOUND('',#4152,.T.);
#3270=FACE_OUTER_BOUND('',#4153,.T.);
#3271=FACE_OUTER_BOUND('',#4154,.T.);
#3272=FACE_OUTER_BOUND('',#4155,.T.);
#3273=FACE_OUTER_BOUND('',#4156,.T.);
#3274=FACE_OUTER_BOUND('',#4157,.T.);
#3275=FACE_OUTER_BOUND('',#4158,.T.);
#3276=FACE_OUTER_BOUND('',#4159,.T.);
#3277=FACE_OUTER_BOUND('',#4160,.T.);
#3278=FACE_OUTER_BOUND('',#4161,.T.);
#3279=FACE_OUTER_BOUND('',#4162,.T.);
#3280=FACE_OUTER_BOUND('',#4163,.T.);
#3281=FACE_OUTER_BOUND('',#4164,.T.);
#3282=FACE_OUTER_BOUND('',#4165,.T.);
#3283=FACE_OUTER_BOUND('',#4166,.T.);
#3284=FACE_OUTER_BOUND('',#4167,.T.);
#3285=FACE_OUTER_BOUND('',#4168,.T.);
#3286=FACE_OUTER_BOUND('',#4169,.T.);
#3287=FACE_OUTER_BOUND('',#4170,.T.);
#3288=FACE_OUTER_BOUND('',#4171,.T.);
#3289=FACE_OUTER_BOUND('',#4172,.T.);
#3290=FACE_OUTER_BOUND('',#4173,.T.);
#3291=FACE_OUTER_BOUND('',#4174,.T.);
#3292=FACE_OUTER_BOUND('',#4175,.T.);
#3293=FACE_OUTER_BOUND('',#4176,.T.);
#3294=FACE_OUTER_BOUND('',#4177,.T.);
#3295=FACE_OUTER_BOUND('',#4178,.T.);
#3296=FACE_OUTER_BOUND('',#4179,.T.);
#3297=FACE_OUTER_BOUND('',#4180,.T.);
#3298=FACE_OUTER_BOUND('',#4181,.T.);
#3299=FACE_OUTER_BOUND('',#4182,.T.);
#3300=FACE_OUTER_BOUND('',#4183,.T.);
#3301=FACE_OUTER_BOUND('',#4184,.T.);
#3302=FACE_OUTER_BOUND('',#4185,.T.);
#3303=FACE_OUTER_BOUND('',#4186,.T.);
#3304=FACE_OUTER_BOUND('',#4187,.T.);
#3305=FACE_OUTER_BOUND('',#4188,.T.);
#3306=FACE_OUTER_BOUND('',#4189,.T.);
#3307=FACE_OUTER_BOUND('',#4190,.T.);
#3308=FACE_OUTER_BOUND('',#4191,.T.);
#3309=FACE_OUTER_BOUND('',#4192,.T.);
#3310=FACE_OUTER_BOUND('',#4193,.T.);
#3311=FACE_OUTER_BOUND('',#4194,.T.);
#3312=FACE_OUTER_BOUND('',#4195,.T.);
#3313=FACE_OUTER_BOUND('',#4197,.T.);
#3314=FACE_OUTER_BOUND('',#4199,.T.);
#3315=FACE_OUTER_BOUND('',#4200,.T.);
#3316=FACE_OUTER_BOUND('',#4201,.T.);
#3317=FACE_OUTER_BOUND('',#4202,.T.);
#3318=FACE_OUTER_BOUND('',#4203,.T.);
#3319=FACE_OUTER_BOUND('',#4204,.T.);
#3320=FACE_OUTER_BOUND('',#4205,.T.);
#3321=FACE_OUTER_BOUND('',#4206,.T.);
#3322=FACE_OUTER_BOUND('',#4207,.T.);
#3323=FACE_OUTER_BOUND('',#4208,.T.);
#3324=FACE_OUTER_BOUND('',#4209,.T.);
#3325=FACE_OUTER_BOUND('',#4210,.T.);
#3326=FACE_OUTER_BOUND('',#4211,.T.);
#3327=FACE_OUTER_BOUND('',#4219,.T.);
#3328=FACE_OUTER_BOUND('',#4220,.T.);
#3329=FACE_OUTER_BOUND('',#4227,.T.);
#3330=FACE_OUTER_BOUND('',#4229,.T.);
#4033=EDGE_LOOP('',(#12568,#12569,#12570,#12571));
#4034=EDGE_LOOP('',(#12572,#12573,#12574,#12575));
#4035=EDGE_LOOP('',(#12576,#12577,#12578,#12579));
#4036=EDGE_LOOP('',(#12580,#12581,#12582,#12583));
#4037=EDGE_LOOP('',(#12584,#12585,#12586,#12587));
#4038=EDGE_LOOP('',(#12588,#12589,#12590,#12591));
#4039=EDGE_LOOP('',(#12592,#12593,#12594,#12595));
#4040=EDGE_LOOP('',(#12596,#12597,#12598,#12599));
#4041=EDGE_LOOP('',(#12600,#12601,#12602,#12603));
#4042=EDGE_LOOP('',(#12604,#12605,#12606,#12607));
#4043=EDGE_LOOP('',(#12608,#12609,#12610,#12611));
#4044=EDGE_LOOP('',(#12612,#12613,#12614,#12615));
#4045=EDGE_LOOP('',(#12616,#12617,#12618,#12619));
#4046=EDGE_LOOP('',(#12620,#12621,#12622,#12623));
#4047=EDGE_LOOP('',(#12624,#12625,#12626,#12627));
#4048=EDGE_LOOP('',(#12628,#12629,#12630,#12631));
#4049=EDGE_LOOP('',(#12632,#12633,#12634,#12635));
#4050=EDGE_LOOP('',(#12636,#12637,#12638,#12639));
#4051=EDGE_LOOP('',(#12640,#12641,#12642,#12643));
#4052=EDGE_LOOP('',(#12644,#12645,#12646,#12647));
#4053=EDGE_LOOP('',(#12648,#12649,#12650,#12651));
#4054=EDGE_LOOP('',(#12652,#12653,#12654,#12655));
#4055=EDGE_LOOP('',(#12656,#12657,#12658,#12659));
#4056=EDGE_LOOP('',(#12660,#12661,#12662,#12663));
#4057=EDGE_LOOP('',(#12664,#12665,#12666,#12667));
#4058=EDGE_LOOP('',(#12668,#12669,#12670,#12671));
#4059=EDGE_LOOP('',(#12672,#12673,#12674,#12675));
#4060=EDGE_LOOP('',(#12676,#12677,#12678,#12679));
#4061=EDGE_LOOP('',(#12680,#12681,#12682,#12683));
#4062=EDGE_LOOP('',(#12684,#12685,#12686,#12687));
#4063=EDGE_LOOP('',(#12688,#12689,#12690,#12691));
#4064=EDGE_LOOP('',(#12692,#12693,#12694,#12695));
#4065=EDGE_LOOP('',(#12696,#12697,#12698,#12699));
#4066=EDGE_LOOP('',(#12700,#12701,#12702,#12703));
#4067=EDGE_LOOP('',(#12704,#12705,#12706,#12707));
#4068=EDGE_LOOP('',(#12708,#12709,#12710,#12711));
#4069=EDGE_LOOP('',(#12712,#12713,#12714,#12715));
#4070=EDGE_LOOP('',(#12716,#12717,#12718,#12719));
#4071=EDGE_LOOP('',(#12720,#12721,#12722,#12723));
#4072=EDGE_LOOP('',(#12724,#12725,#12726,#12727));
#4073=EDGE_LOOP('',(#12728,#12729,#12730,#12731));
#4074=EDGE_LOOP('',(#12732,#12733,#12734,#12735));
#4075=EDGE_LOOP('',(#12736,#12737,#12738,#12739));
#4076=EDGE_LOOP('',(#12740,#12741,#12742,#12743));
#4077=EDGE_LOOP('',(#12744,#12745,#12746,#12747));
#4078=EDGE_LOOP('',(#12748,#12749,#12750,#12751));
#4079=EDGE_LOOP('',(#12752,#12753,#12754,#12755));
#4080=EDGE_LOOP('',(#12756,#12757,#12758,#12759));
#4081=EDGE_LOOP('',(#12760,#12761,#12762,#12763));
#4082=EDGE_LOOP('',(#12764,#12765,#12766,#12767));
#4083=EDGE_LOOP('',(#12768,#12769,#12770,#12771));
#4084=EDGE_LOOP('',(#12772,#12773,#12774,#12775));
#4085=EDGE_LOOP('',(#12776,#12777,#12778,#12779));
#4086=EDGE_LOOP('',(#12780,#12781,#12782,#12783));
#4087=EDGE_LOOP('',(#12784,#12785,#12786,#12787));
#4088=EDGE_LOOP('',(#12788,#12789,#12790,#12791));
#4089=EDGE_LOOP('',(#12792,#12793,#12794,#12795));
#4090=EDGE_LOOP('',(#12796,#12797,#12798,#12799));
#4091=EDGE_LOOP('',(#12800,#12801,#12802,#12803));
#4092=EDGE_LOOP('',(#12804,#12805,#12806,#12807));
#4093=EDGE_LOOP('',(#12808,#12809,#12810,#12811));
#4094=EDGE_LOOP('',(#12812,#12813,#12814,#12815));
#4095=EDGE_LOOP('',(#12816,#12817,#12818,#12819));
#4096=EDGE_LOOP('',(#12820,#12821,#12822,#12823));
#4097=EDGE_LOOP('',(#12824,#12825,#12826,#12827));
#4098=EDGE_LOOP('',(#12828,#12829,#12830,#12831));
#4099=EDGE_LOOP('',(#12832,#12833,#12834,#12835));
#4100=EDGE_LOOP('',(#12836,#12837,#12838,#12839));
#4101=EDGE_LOOP('',(#12840,#12841,#12842,#12843));
#4102=EDGE_LOOP('',(#12844,#12845,#12846,#12847));
#4103=EDGE_LOOP('',(#12848,#12849,#12850,#12851));
#4104=EDGE_LOOP('',(#12852,#12853,#12854,#12855));
#4105=EDGE_LOOP('',(#12856,#12857,#12858,#12859));
#4106=EDGE_LOOP('',(#12860,#12861,#12862,#12863));
#4107=EDGE_LOOP('',(#12864,#12865,#12866,#12867));
#4108=EDGE_LOOP('',(#12868,#12869,#12870,#12871));
#4109=EDGE_LOOP('',(#12872,#12873,#12874,#12875));
#4110=EDGE_LOOP('',(#12876,#12877,#12878,#12879));
#4111=EDGE_LOOP('',(#12880,#12881,#12882,#12883,#12884,#12885,#12886,#12887));
#4112=EDGE_LOOP('',(#12888,#12889,#12890,#12891));
#4113=EDGE_LOOP('',(#12892,#12893,#12894,#12895));
#4114=EDGE_LOOP('',(#12896,#12897,#12898,#12899));
#4115=EDGE_LOOP('',(#12900,#12901,#12902,#12903));
#4116=EDGE_LOOP('',(#12904,#12905,#12906,#12907));
#4117=EDGE_LOOP('',(#12908,#12909,#12910,#12911));
#4118=EDGE_LOOP('',(#12912,#12913,#12914,#12915));
#4119=EDGE_LOOP('',(#12916,#12917,#12918,#12919));
#4120=EDGE_LOOP('',(#12920,#12921,#12922,#12923));
#4121=EDGE_LOOP('',(#12924,#12925,#12926,#12927));
#4122=EDGE_LOOP('',(#12928,#12929,#12930,#12931));
#4123=EDGE_LOOP('',(#12932,#12933,#12934,#12935));
#4124=EDGE_LOOP('',(#12936,#12937,#12938,#12939));
#4125=EDGE_LOOP('',(#12940,#12941,#12942,#12943));
#4126=EDGE_LOOP('',(#12944,#12945,#12946,#12947));
#4127=EDGE_LOOP('',(#12948,#12949,#12950,#12951));
#4128=EDGE_LOOP('',(#12952,#12953,#12954,#12955));
#4129=EDGE_LOOP('',(#12956,#12957,#12958,#12959));
#4130=EDGE_LOOP('',(#12960,#12961,#12962,#12963));
#4131=EDGE_LOOP('',(#12964,#12965,#12966,#12967));
#4132=EDGE_LOOP('',(#12968,#12969,#12970,#12971));
#4133=EDGE_LOOP('',(#12972,#12973,#12974,#12975));
#4134=EDGE_LOOP('',(#12976,#12977,#12978,#12979));
#4135=EDGE_LOOP('',(#12980,#12981,#12982,#12983));
#4136=EDGE_LOOP('',(#12984,#12985,#12986,#12987));
#4137=EDGE_LOOP('',(#12988,#12989,#12990,#12991));
#4138=EDGE_LOOP('',(#12992,#12993,#12994,#12995));
#4139=EDGE_LOOP('',(#12996,#12997,#12998,#12999));
#4140=EDGE_LOOP('',(#13000,#13001,#13002,#13003));
#4141=EDGE_LOOP('',(#13004,#13005,#13006,#13007));
#4142=EDGE_LOOP('',(#13008,#13009,#13010,#13011));
#4143=EDGE_LOOP('',(#13012,#13013,#13014,#13015));
#4144=EDGE_LOOP('',(#13016,#13017,#13018,#13019));
#4145=EDGE_LOOP('',(#13020,#13021,#13022,#13023));
#4146=EDGE_LOOP('',(#13024,#13025,#13026,#13027));
#4147=EDGE_LOOP('',(#13028,#13029,#13030,#13031));
#4148=EDGE_LOOP('',(#13032,#13033,#13034,#13035));
#4149=EDGE_LOOP('',(#13036,#13037,#13038,#13039));
#4150=EDGE_LOOP('',(#13040,#13041,#13042,#13043));
#4151=EDGE_LOOP('',(#13044,#13045,#13046,#13047));
#4152=EDGE_LOOP('',(#13048,#13049,#13050,#13051));
#4153=EDGE_LOOP('',(#13052,#13053,#13054,#13055));
#4154=EDGE_LOOP('',(#13056,#13057,#13058,#13059));
#4155=EDGE_LOOP('',(#13060,#13061,#13062,#13063));
#4156=EDGE_LOOP('',(#13064,#13065,#13066,#13067));
#4157=EDGE_LOOP('',(#13068,#13069,#13070,#13071));
#4158=EDGE_LOOP('',(#13072,#13073,#13074,#13075));
#4159=EDGE_LOOP('',(#13076,#13077,#13078,#13079));
#4160=EDGE_LOOP('',(#13080,#13081,#13082,#13083));
#4161=EDGE_LOOP('',(#13084,#13085,#13086,#13087));
#4162=EDGE_LOOP('',(#13088,#13089,#13090,#13091));
#4163=EDGE_LOOP('',(#13092,#13093,#13094,#13095));
#4164=EDGE_LOOP('',(#13096,#13097,#13098,#13099));
#4165=EDGE_LOOP('',(#13100,#13101,#13102,#13103));
#4166=EDGE_LOOP('',(#13104,#13105,#13106,#13107));
#4167=EDGE_LOOP('',(#13108,#13109,#13110,#13111));
#4168=EDGE_LOOP('',(#13112,#13113,#13114,#13115));
#4169=EDGE_LOOP('',(#13116,#13117,#13118,#13119));
#4170=EDGE_LOOP('',(#13120,#13121,#13122,#13123));
#4171=EDGE_LOOP('',(#13124,#13125,#13126,#13127));
#4172=EDGE_LOOP('',(#13128,#13129,#13130,#13131));
#4173=EDGE_LOOP('',(#13132,#13133,#13134,#13135));
#4174=EDGE_LOOP('',(#13136,#13137,#13138,#13139));
#4175=EDGE_LOOP('',(#13140,#13141,#13142,#13143));
#4176=EDGE_LOOP('',(#13144,#13145,#13146,#13147));
#4177=EDGE_LOOP('',(#13148,#13149,#13150,#13151));
#4178=EDGE_LOOP('',(#13152,#13153,#13154,#13155));
#4179=EDGE_LOOP('',(#13156,#13157,#13158,#13159));
#4180=EDGE_LOOP('',(#13160,#13161,#13162,#13163));
#4181=EDGE_LOOP('',(#13164,#13165,#13166,#13167));
#4182=EDGE_LOOP('',(#13168,#13169,#13170,#13171));
#4183=EDGE_LOOP('',(#13172,#13173,#13174,#13175));
#4184=EDGE_LOOP('',(#13176,#13177,#13178,#13179));
#4185=EDGE_LOOP('',(#13180,#13181,#13182,#13183));
#4186=EDGE_LOOP('',(#13184,#13185,#13186,#13187));
#4187=EDGE_LOOP('',(#13188,#13189,#13190,#13191));
#4188=EDGE_LOOP('',(#13192,#13193,#13194,#13195));
#4189=EDGE_LOOP('',(#13196,#13197,#13198,#13199));
#4190=EDGE_LOOP('',(#13200,#13201,#13202,#13203));
#4191=EDGE_LOOP('',(#13204,#13205,#13206,#13207));
#4192=EDGE_LOOP('',(#13208,#13209,#13210,#13211));
#4193=EDGE_LOOP('',(#13212,#13213,#13214,#13215));
#4194=EDGE_LOOP('',(#13216,#13217,#13218,#13219));
#4195=EDGE_LOOP('',(#13220));
#4196=EDGE_LOOP('',(#13221));
#4197=EDGE_LOOP('',(#13222));
#4198=EDGE_LOOP('',(#13223));
#4199=EDGE_LOOP('',(#13224,#13225,#13226,#13227));
#4200=EDGE_LOOP('',(#13228,#13229,#13230,#13231,#13232));
#4201=EDGE_LOOP('',(#13233,#13234,#13235,#13236,#13237,#13238,#13239,#13240,
#13241,#13242,#13243,#13244,#13245,#13246,#13247,#13248,#13249,#13250,#13251,
#13252,#13253,#13254,#13255,#13256,#13257,#13258,#13259,#13260,#13261,#13262,
#13263,#13264,#13265,#13266,#13267,#13268,#13269,#13270,#13271,#13272,#13273,
#13274,#13275,#13276,#13277,#13278,#13279,#13280,#13281,#13282,#13283,#13284,
#13285,#13286,#13287,#13288,#13289,#13290,#13291,#13292,#13293,#13294,#13295,
#13296,#13297,#13298,#13299,#13300,#13301,#13302,#13303,#13304,#13305,#13306,
#13307,#13308,#13309,#13310,#13311,#13312,#13313,#13314,#13315,#13316,#13317,
#13318,#13319,#13320,#13321,#13322,#13323,#13324,#13325,#13326,#13327,#13328,
#13329,#13330,#13331,#13332,#13333,#13334,#13335,#13336,#13337,#13338,#13339,
#13340,#13341,#13342,#13343,#13344,#13345,#13346,#13347,#13348,#13349,#13350,
#13351,#13352,#13353,#13354,#13355,#13356,#13357,#13358,#13359,#13360,#13361,
#13362,#13363,#13364,#13365,#13366,#13367,#13368,#13369,#13370,#13371,#13372,
#13373,#13374,#13375,#13376,#13377,#13378,#13379,#13380,#13381,#13382,#13383,
#13384,#13385,#13386,#13387,#13388,#13389,#13390,#13391,#13392,#13393,#13394,
#13395,#13396));
#4202=EDGE_LOOP('',(#13397,#13398,#13399,#13400));
#4203=EDGE_LOOP('',(#13401,#13402,#13403,#13404,#13405,#13406,#13407,#13408,
#13409,#13410,#13411,#13412,#13413,#13414,#13415,#13416,#13417,#13418,#13419,
#13420,#13421,#13422,#13423,#13424,#13425,#13426,#13427,#13428,#13429,#13430,
#13431,#13432,#13433,#13434,#13435,#13436,#13437,#13438,#13439,#13440,#13441,
#13442,#13443,#13444,#13445,#13446,#13447,#13448,#13449,#13450,#13451,#13452,
#13453,#13454,#13455,#13456,#13457,#13458,#13459,#13460,#13461,#13462,#13463,
#13464,#13465,#13466,#13467,#13468,#13469,#13470,#13471,#13472,#13473,#13474,
#13475,#13476,#13477,#13478,#13479,#13480,#13481,#13482,#13483,#13484,#13485,
#13486,#13487,#13488,#13489,#13490,#13491,#13492,#13493,#13494,#13495,#13496,
#13497,#13498,#13499,#13500,#13501,#13502,#13503,#13504,#13505,#13506,#13507,
#13508,#13509,#13510,#13511,#13512,#13513,#13514,#13515,#13516,#13517,#13518,
#13519,#13520,#13521,#13522,#13523,#13524,#13525,#13526,#13527,#13528,#13529,
#13530,#13531,#13532,#13533,#13534,#13535,#13536,#13537,#13538,#13539,#13540,
#13541,#13542,#13543,#13544,#13545,#13546,#13547,#13548,#13549,#13550,#13551,
#13552,#13553,#13554,#13555,#13556,#13557,#13558,#13559,#13560,#13561,#13562,
#13563,#13564));
#4204=EDGE_LOOP('',(#13565,#13566,#13567,#13568));
#4205=EDGE_LOOP('',(#13569,#13570,#13571,#13572));
#4206=EDGE_LOOP('',(#13573,#13574,#13575,#13576));
#4207=EDGE_LOOP('',(#13577,#13578,#13579,#13580));
#4208=EDGE_LOOP('',(#13581,#13582,#13583,#13584));
#4209=EDGE_LOOP('',(#13585,#13586,#13587,#13588));
#4210=EDGE_LOOP('',(#13589,#13590,#13591,#13592));
#4211=EDGE_LOOP('',(#13593));
#4212=EDGE_LOOP('',(#13594));
#4213=EDGE_LOOP('',(#13595));
#4214=EDGE_LOOP('',(#13596));
#4215=EDGE_LOOP('',(#13597));
#4216=EDGE_LOOP('',(#13598));
#4217=EDGE_LOOP('',(#13599));
#4218=EDGE_LOOP('',(#13600));
#4219=EDGE_LOOP('',(#13601,#13602,#13603,#13604));
#4220=EDGE_LOOP('',(#13605));
#4221=EDGE_LOOP('',(#13606));
#4222=EDGE_LOOP('',(#13607));
#4223=EDGE_LOOP('',(#13608));
#4224=EDGE_LOOP('',(#13609));
#4225=EDGE_LOOP('',(#13610));
#4226=EDGE_LOOP('',(#13611));
#4227=EDGE_LOOP('',(#13612));
#4228=EDGE_LOOP('',(#13613));
#4229=EDGE_LOOP('',(#13614,#13615,#13616,#13617));
#4880=LINE('',#46843,#5643);
#4881=LINE('',#46885,#5644);
#4882=LINE('',#46933,#5645);
#4883=LINE('',#46984,#5646);
#4884=LINE('',#47035,#5647);
#4885=LINE('',#47083,#5648);
#4886=LINE('',#47131,#5649);
#4887=LINE('',#47185,#5650);
#4888=LINE('',#47233,#5651);
#4889=LINE('',#47281,#5652);
#4890=LINE('',#47332,#5653);
#4891=LINE('',#47383,#5654);
#4892=LINE('',#47431,#5655);
#4893=LINE('',#47479,#5656);
#4894=LINE('',#47533,#5657);
#4895=LINE('',#47581,#5658);
#4896=LINE('',#47629,#5659);
#4897=LINE('',#47680,#5660);
#4898=LINE('',#47731,#5661);
#4899=LINE('',#47779,#5662);
#4900=LINE('',#47827,#5663);
#4901=LINE('',#47881,#5664);
#4902=LINE('',#47929,#5665);
#4903=LINE('',#47977,#5666);
#4904=LINE('',#48028,#5667);
#4905=LINE('',#48079,#5668);
#4906=LINE('',#48127,#5669);
#4907=LINE('',#48175,#5670);
#4908=LINE('',#48229,#5671);
#4909=LINE('',#48277,#5672);
#4910=LINE('',#48325,#5673);
#4911=LINE('',#48376,#5674);
#4912=LINE('',#48427,#5675);
#4913=LINE('',#48475,#5676);
#4914=LINE('',#48523,#5677);
#4915=LINE('',#48577,#5678);
#4916=LINE('',#48625,#5679);
#4917=LINE('',#48673,#5680);
#4918=LINE('',#48724,#5681);
#4919=LINE('',#48775,#5682);
#4920=LINE('',#48823,#5683);
#4921=LINE('',#48871,#5684);
#4922=LINE('',#48925,#5685);
#4923=LINE('',#48973,#5686);
#4924=LINE('',#49021,#5687);
#4925=LINE('',#49072,#5688);
#4926=LINE('',#49123,#5689);
#4927=LINE('',#49171,#5690);
#4928=LINE('',#49219,#5691);
#4929=LINE('',#49273,#5692);
#4930=LINE('',#49321,#5693);
#4931=LINE('',#49369,#5694);
#4932=LINE('',#49420,#5695);
#4933=LINE('',#49468,#5696);
#4934=LINE('',#49516,#5697);
#4935=LINE('',#49564,#5698);
#4936=LINE('',#49618,#5699);
#4937=LINE('',#49666,#5700);
#4938=LINE('',#49714,#5701);
#4939=LINE('',#49768,#5702);
#4940=LINE('',#49816,#5703);
#4941=LINE('',#49864,#5704);
#4942=LINE('',#49912,#5705);
#4943=LINE('',#49966,#5706);
#4944=LINE('',#50014,#5707);
#4945=LINE('',#50062,#5708);
#4946=LINE('',#50116,#5709);
#4947=LINE('',#50164,#5710);
#4948=LINE('',#50212,#5711);
#4949=LINE('',#50260,#5712);
#4950=LINE('',#50314,#5713);
#4951=LINE('',#50362,#5714);
#4952=LINE('',#50410,#5715);
#4953=LINE('',#50464,#5716);
#4954=LINE('',#50512,#5717);
#4955=LINE('',#50560,#5718);
#4956=LINE('',#50608,#5719);
#4957=LINE('',#50662,#5720);
#4958=LINE('',#50711,#5721);
#4959=LINE('',#50735,#5722);
#4960=LINE('',#50760,#5723);
#4961=LINE('',#50784,#5724);
#4962=LINE('',#50809,#5725);
#4963=LINE('',#50833,#5726);
#4964=LINE('',#50858,#5727);
#4965=LINE('',#50883,#5728);
#4966=LINE('',#50907,#5729);
#4967=LINE('',#50931,#5730);
#4968=LINE('',#50956,#5731);
#4969=LINE('',#50981,#5732);
#4970=LINE('',#51005,#5733);
#4971=LINE('',#51030,#5734);
#4972=LINE('',#51055,#5735);
#4973=LINE('',#51079,#5736);
#4974=LINE('',#51103,#5737);
#4975=LINE('',#51128,#5738);
#4976=LINE('',#51153,#5739);
#4977=LINE('',#51177,#5740);
#4978=LINE('',#51202,#5741);
#4979=LINE('',#51227,#5742);
#4980=LINE('',#51251,#5743);
#4981=LINE('',#51275,#5744);
#4982=LINE('',#51300,#5745);
#4983=LINE('',#51325,#5746);
#4984=LINE('',#51349,#5747);
#4985=LINE('',#51374,#5748);
#4986=LINE('',#51411,#5749);
#4987=LINE('',#51447,#5750);
#4988=LINE('',#51472,#5751);
#4989=LINE('',#51496,#5752);
#4990=LINE('',#51521,#5753);
#4991=LINE('',#51545,#5754);
#4992=LINE('',#51570,#5755);
#4993=LINE('',#51595,#5756);
#4994=LINE('',#51619,#5757);
#4995=LINE('',#51644,#5758);
#4996=LINE('',#51668,#5759);
#4997=LINE('',#51693,#5760);
#4998=LINE('',#51717,#5761);
#4999=LINE('',#51742,#5762);
#5000=LINE('',#51767,#5763);
#5001=LINE('',#51791,#5764);
#5002=LINE('',#51816,#5765);
#5003=LINE('',#51840,#5766);
#5004=LINE('',#51865,#5767);
#5005=LINE('',#51889,#5768);
#5006=LINE('',#51914,#5769);
#5007=LINE('',#51939,#5770);
#5008=LINE('',#51963,#5771);
#5009=LINE('',#51988,#5772);
#5010=LINE('',#52012,#5773);
#5011=LINE('',#52037,#5774);
#5012=LINE('',#52061,#5775);
#5013=LINE('',#52086,#5776);
#5014=LINE('',#52111,#5777);
#5015=LINE('',#52135,#5778);
#5016=LINE('',#52160,#5779);
#5017=LINE('',#52184,#5780);
#5018=LINE('',#52209,#5781);
#5019=LINE('',#52233,#5782);
#5020=LINE('',#52258,#5783);
#5021=LINE('',#52283,#5784);
#5022=LINE('',#52307,#5785);
#5023=LINE('',#52332,#5786);
#5024=LINE('',#52356,#5787);
#5025=LINE('',#52381,#5788);
#5026=LINE('',#52405,#5789);
#5027=LINE('',#52430,#5790);
#5028=LINE('',#52455,#5791);
#5029=LINE('',#52479,#5792);
#5030=LINE('',#52504,#5793);
#5031=LINE('',#52528,#5794);
#5032=LINE('',#52553,#5795);
#5033=LINE('',#52577,#5796);
#5034=LINE('',#52602,#5797);
#5035=LINE('',#52627,#5798);
#5036=LINE('',#52651,#5799);
#5037=LINE('',#52676,#5800);
#5038=LINE('',#52700,#5801);
#5039=LINE('',#52725,#5802);
#5040=LINE('',#53125,#5803);
#5041=LINE('',#53134,#5804);
#5042=LINE('',#57501,#5805);
#5043=LINE('',#57507,#5806);
#5044=LINE('',#57513,#5807);
#5045=LINE('',#57519,#5808);
#5046=LINE('',#57525,#5809);
#5047=LINE('',#57531,#5810);
#5048=LINE('',#57541,#5811);
#5049=LINE('',#57547,#5812);
#5643=VECTOR('',#18538,6.);
#5644=VECTOR('',#18543,6.);
#5645=VECTOR('',#18546,6.);
#5646=VECTOR('',#18549,6.);
#5647=VECTOR('',#18552,6.);
#5648=VECTOR('',#18555,6.);
#5649=VECTOR('',#18558,6.);
#5650=VECTOR('',#18561,6.);
#5651=VECTOR('',#18564,6.);
#5652=VECTOR('',#18567,6.);
#5653=VECTOR('',#18570,6.);
#5654=VECTOR('',#18573,6.);
#5655=VECTOR('',#18576,6.);
#5656=VECTOR('',#18579,6.);
#5657=VECTOR('',#18582,6.);
#5658=VECTOR('',#18585,6.);
#5659=VECTOR('',#18588,6.);
#5660=VECTOR('',#18591,6.);
#5661=VECTOR('',#18594,6.);
#5662=VECTOR('',#18597,6.);
#5663=VECTOR('',#18600,6.);
#5664=VECTOR('',#18603,6.);
#5665=VECTOR('',#18606,6.);
#5666=VECTOR('',#18609,6.);
#5667=VECTOR('',#18612,6.);
#5668=VECTOR('',#18615,6.);
#5669=VECTOR('',#18618,6.);
#5670=VECTOR('',#18621,6.);
#5671=VECTOR('',#18624,6.);
#5672=VECTOR('',#18627,6.);
#5673=VECTOR('',#18630,6.);
#5674=VECTOR('',#18633,6.);
#5675=VECTOR('',#18636,6.);
#5676=VECTOR('',#18639,6.);
#5677=VECTOR('',#18642,6.);
#5678=VECTOR('',#18645,6.);
#5679=VECTOR('',#18648,6.);
#5680=VECTOR('',#18651,6.);
#5681=VECTOR('',#18654,6.);
#5682=VECTOR('',#18657,6.);
#5683=VECTOR('',#18660,6.);
#5684=VECTOR('',#18663,6.);
#5685=VECTOR('',#18666,6.);
#5686=VECTOR('',#18669,6.);
#5687=VECTOR('',#18672,6.);
#5688=VECTOR('',#18675,6.);
#5689=VECTOR('',#18678,6.);
#5690=VECTOR('',#18681,6.);
#5691=VECTOR('',#18684,6.);
#5692=VECTOR('',#18687,6.);
#5693=VECTOR('',#18690,6.);
#5694=VECTOR('',#18693,6.);
#5695=VECTOR('',#18696,6.);
#5696=VECTOR('',#18699,6.);
#5697=VECTOR('',#18702,6.);
#5698=VECTOR('',#18705,6.);
#5699=VECTOR('',#18708,6.);
#5700=VECTOR('',#18711,6.);
#5701=VECTOR('',#18714,6.);
#5702=VECTOR('',#18717,6.);
#5703=VECTOR('',#18720,6.);
#5704=VECTOR('',#18723,6.);
#5705=VECTOR('',#18726,6.);
#5706=VECTOR('',#18729,6.);
#5707=VECTOR('',#18732,6.);
#5708=VECTOR('',#18735,6.);
#5709=VECTOR('',#18738,6.);
#5710=VECTOR('',#18741,6.);
#5711=VECTOR('',#18744,6.);
#5712=VECTOR('',#18747,6.);
#5713=VECTOR('',#18750,6.);
#5714=VECTOR('',#18753,6.);
#5715=VECTOR('',#18756,6.);
#5716=VECTOR('',#18759,6.);
#5717=VECTOR('',#18762,6.);
#5718=VECTOR('',#18765,6.);
#5719=VECTOR('',#18768,6.);
#5720=VECTOR('',#18771,6.);
#5721=VECTOR('',#18776,6.);
#5722=VECTOR('',#18779,6.);
#5723=VECTOR('',#18784,4.91825);
#5724=VECTOR('',#18789,4.91825);
#5725=VECTOR('',#18792,4.91825);
#5726=VECTOR('',#18795,4.91825);
#5727=VECTOR('',#18798,4.91825);
#5728=VECTOR('',#18801,4.91825);
#5729=VECTOR('',#18804,4.91825);
#5730=VECTOR('',#18807,4.91825);
#5731=VECTOR('',#18810,4.91825);
#5732=VECTOR('',#18813,4.91825);
#5733=VECTOR('',#18816,4.91825);
#5734=VECTOR('',#18819,4.91825);
#5735=VECTOR('',#18822,4.91825);
#5736=VECTOR('',#18825,4.91825);
#5737=VECTOR('',#18828,4.91825);
#5738=VECTOR('',#18831,4.91825);
#5739=VECTOR('',#18834,4.91825);
#5740=VECTOR('',#18837,4.91825);
#5741=VECTOR('',#18840,4.91825);
#5742=VECTOR('',#18843,4.91825);
#5743=VECTOR('',#18846,4.91825);
#5744=VECTOR('',#18849,4.91825);
#5745=VECTOR('',#18852,4.91825);
#5746=VECTOR('',#18855,4.91825);
#5747=VECTOR('',#18858,4.91825);
#5748=VECTOR('',#18861,4.91825);
#5749=VECTOR('',#18864,4.91825);
#5750=VECTOR('',#18867,4.91825);
#5751=VECTOR('',#18870,4.91825);
#5752=VECTOR('',#18873,4.91825);
#5753=VECTOR('',#18876,4.91825);
#5754=VECTOR('',#18879,4.91825);
#5755=VECTOR('',#18882,4.91825);
#5756=VECTOR('',#18885,4.91825);
#5757=VECTOR('',#18888,4.91825);
#5758=VECTOR('',#18891,4.91825);
#5759=VECTOR('',#18894,4.91825);
#5760=VECTOR('',#18897,4.91825);
#5761=VECTOR('',#18900,4.91825);
#5762=VECTOR('',#18903,4.91825);
#5763=VECTOR('',#18906,4.91825);
#5764=VECTOR('',#18909,4.91825);
#5765=VECTOR('',#18912,4.91825);
#5766=VECTOR('',#18915,4.91825);
#5767=VECTOR('',#18918,4.91825);
#5768=VECTOR('',#18921,4.91825);
#5769=VECTOR('',#18924,4.91825);
#5770=VECTOR('',#18927,4.91825);
#5771=VECTOR('',#18930,4.91825);
#5772=VECTOR('',#18933,4.91825);
#5773=VECTOR('',#18936,4.91825);
#5774=VECTOR('',#18939,4.91825);
#5775=VECTOR('',#18942,4.91825);
#5776=VECTOR('',#18945,4.91825);
#5777=VECTOR('',#18948,4.91825);
#5778=VECTOR('',#18951,4.91825);
#5779=VECTOR('',#18954,4.91825);
#5780=VECTOR('',#18957,4.91825);
#5781=VECTOR('',#18960,4.91825);
#5782=VECTOR('',#18963,4.91825);
#5783=VECTOR('',#18966,4.91825);
#5784=VECTOR('',#18969,4.91825);
#5785=VECTOR('',#18972,4.91825);
#5786=VECTOR('',#18975,4.91825);
#5787=VECTOR('',#18978,4.91825);
#5788=VECTOR('',#18981,4.91825);
#5789=VECTOR('',#18984,4.91825);
#5790=VECTOR('',#18987,4.91825);
#5791=VECTOR('',#18990,4.91825);
#5792=VECTOR('',#18993,4.91825);
#5793=VECTOR('',#18996,4.91825);
#5794=VECTOR('',#18999,4.91825);
#5795=VECTOR('',#19002,4.91825);
#5796=VECTOR('',#19005,4.91825);
#5797=VECTOR('',#19008,4.91825);
#5798=VECTOR('',#19011,4.91825);
#5799=VECTOR('',#19014,4.91825);
#5800=VECTOR('',#19017,4.91825);
#5801=VECTOR('',#19020,4.91825);
#5802=VECTOR('',#19023,4.91825);
#5803=VECTOR('',#19036,5.);
#5804=VECTOR('',#19049,6.);
#5805=VECTOR('',#19060,3.);
#5806=VECTOR('',#19067,3.);
#5807=VECTOR('',#19074,3.);
#5808=VECTOR('',#19081,3.);
#5809=VECTOR('',#19088,3.);
#5810=VECTOR('',#19095,3.);
#5811=VECTOR('',#19108,25.);
#5812=VECTOR('',#19117,12.);
#6856=VERTEX_POINT('',#46841);
#6857=VERTEX_POINT('',#46842);
#6858=VERTEX_POINT('',#46844);
#6859=VERTEX_POINT('',#46864);
#6860=VERTEX_POINT('',#46883);
#6861=VERTEX_POINT('',#46884);
#6862=VERTEX_POINT('',#46931);
#6863=VERTEX_POINT('',#46932);
#6864=VERTEX_POINT('',#46982);
#6865=VERTEX_POINT('',#46983);
#6866=VERTEX_POINT('',#47033);
#6867=VERTEX_POINT('',#47034);
#6868=VERTEX_POINT('',#47081);
#6869=VERTEX_POINT('',#47082);
#6870=VERTEX_POINT('',#47129);
#6871=VERTEX_POINT('',#47130);
#6872=VERTEX_POINT('',#47183);
#6873=VERTEX_POINT('',#47184);
#6874=VERTEX_POINT('',#47231);
#6875=VERTEX_POINT('',#47232);
#6876=VERTEX_POINT('',#47279);
#6877=VERTEX_POINT('',#47280);
#6878=VERTEX_POINT('',#47330);
#6879=VERTEX_POINT('',#47331);
#6880=VERTEX_POINT('',#47381);
#6881=VERTEX_POINT('',#47382);
#6882=VERTEX_POINT('',#47429);
#6883=VERTEX_POINT('',#47430);
#6884=VERTEX_POINT('',#47477);
#6885=VERTEX_POINT('',#47478);
#6886=VERTEX_POINT('',#47531);
#6887=VERTEX_POINT('',#47532);
#6888=VERTEX_POINT('',#47579);
#6889=VERTEX_POINT('',#47580);
#6890=VERTEX_POINT('',#47627);
#6891=VERTEX_POINT('',#47628);
#6892=VERTEX_POINT('',#47678);
#6893=VERTEX_POINT('',#47679);
#6894=VERTEX_POINT('',#47729);
#6895=VERTEX_POINT('',#47730);
#6896=VERTEX_POINT('',#47777);
#6897=VERTEX_POINT('',#47778);
#6898=VERTEX_POINT('',#47825);
#6899=VERTEX_POINT('',#47826);
#6900=VERTEX_POINT('',#47879);
#6901=VERTEX_POINT('',#47880);
#6902=VERTEX_POINT('',#47927);
#6903=VERTEX_POINT('',#47928);
#6904=VERTEX_POINT('',#47975);
#6905=VERTEX_POINT('',#47976);
#6906=VERTEX_POINT('',#48026);
#6907=VERTEX_POINT('',#48027);
#6908=VERTEX_POINT('',#48077);
#6909=VERTEX_POINT('',#48078);
#6910=VERTEX_POINT('',#48125);
#6911=VERTEX_POINT('',#48126);
#6912=VERTEX_POINT('',#48173);
#6913=VERTEX_POINT('',#48174);
#6914=VERTEX_POINT('',#48227);
#6915=VERTEX_POINT('',#48228);
#6916=VERTEX_POINT('',#48275);
#6917=VERTEX_POINT('',#48276);
#6918=VERTEX_POINT('',#48323);
#6919=VERTEX_POINT('',#48324);
#6920=VERTEX_POINT('',#48374);
#6921=VERTEX_POINT('',#48375);
#6922=VERTEX_POINT('',#48425);
#6923=VERTEX_POINT('',#48426);
#6924=VERTEX_POINT('',#48473);
#6925=VERTEX_POINT('',#48474);
#6926=VERTEX_POINT('',#48521);
#6927=VERTEX_POINT('',#48522);
#6928=VERTEX_POINT('',#48575);
#6929=VERTEX_POINT('',#48576);
#6930=VERTEX_POINT('',#48623);
#6931=VERTEX_POINT('',#48624);
#6932=VERTEX_POINT('',#48671);
#6933=VERTEX_POINT('',#48672);
#6934=VERTEX_POINT('',#48722);
#6935=VERTEX_POINT('',#48723);
#6936=VERTEX_POINT('',#48773);
#6937=VERTEX_POINT('',#48774);
#6938=VERTEX_POINT('',#48821);
#6939=VERTEX_POINT('',#48822);
#6940=VERTEX_POINT('',#48869);
#6941=VERTEX_POINT('',#48870);
#6942=VERTEX_POINT('',#48923);
#6943=VERTEX_POINT('',#48924);
#6944=VERTEX_POINT('',#48971);
#6945=VERTEX_POINT('',#48972);
#6946=VERTEX_POINT('',#49019);
#6947=VERTEX_POINT('',#49020);
#6948=VERTEX_POINT('',#49070);
#6949=VERTEX_POINT('',#49071);
#6950=VERTEX_POINT('',#49121);
#6951=VERTEX_POINT('',#49122);
#6952=VERTEX_POINT('',#49169);
#6953=VERTEX_POINT('',#49170);
#6954=VERTEX_POINT('',#49217);
#6955=VERTEX_POINT('',#49218);
#6956=VERTEX_POINT('',#49271);
#6957=VERTEX_POINT('',#49272);
#6958=VERTEX_POINT('',#49319);
#6959=VERTEX_POINT('',#49320);
#6960=VERTEX_POINT('',#49367);
#6961=VERTEX_POINT('',#49368);
#6962=VERTEX_POINT('',#49418);
#6963=VERTEX_POINT('',#49419);
#6964=VERTEX_POINT('',#49466);
#6965=VERTEX_POINT('',#49467);
#6966=VERTEX_POINT('',#49514);
#6967=VERTEX_POINT('',#49515);
#6968=VERTEX_POINT('',#49562);
#6969=VERTEX_POINT('',#49563);
#6970=VERTEX_POINT('',#49616);
#6971=VERTEX_POINT('',#49617);
#6972=VERTEX_POINT('',#49664);
#6973=VERTEX_POINT('',#49665);
#6974=VERTEX_POINT('',#49712);
#6975=VERTEX_POINT('',#49713);
#6976=VERTEX_POINT('',#49766);
#6977=VERTEX_POINT('',#49767);
#6978=VERTEX_POINT('',#49814);
#6979=VERTEX_POINT('',#49815);
#6980=VERTEX_POINT('',#49862);
#6981=VERTEX_POINT('',#49863);
#6982=VERTEX_POINT('',#49910);
#6983=VERTEX_POINT('',#49911);
#6984=VERTEX_POINT('',#49964);
#6985=VERTEX_POINT('',#49965);
#6986=VERTEX_POINT('',#50012);
#6987=VERTEX_POINT('',#50013);
#6988=VERTEX_POINT('',#50060);
#6989=VERTEX_POINT('',#50061);
#6990=VERTEX_POINT('',#50114);
#6991=VERTEX_POINT('',#50115);
#6992=VERTEX_POINT('',#50162);
#6993=VERTEX_POINT('',#50163);
#6994=VERTEX_POINT('',#50210);
#6995=VERTEX_POINT('',#50211);
#6996=VERTEX_POINT('',#50258);
#6997=VERTEX_POINT('',#50259);
#6998=VERTEX_POINT('',#50312);
#6999=VERTEX_POINT('',#50313);
#7000=VERTEX_POINT('',#50360);
#7001=VERTEX_POINT('',#50361);
#7002=VERTEX_POINT('',#50408);
#7003=VERTEX_POINT('',#50409);
#7004=VERTEX_POINT('',#50462);
#7005=VERTEX_POINT('',#50463);
#7006=VERTEX_POINT('',#50510);
#7007=VERTEX_POINT('',#50511);
#7008=VERTEX_POINT('',#50558);
#7009=VERTEX_POINT('',#50559);
#7010=VERTEX_POINT('',#50606);
#7011=VERTEX_POINT('',#50607);
#7012=VERTEX_POINT('',#50660);
#7013=VERTEX_POINT('',#50661);
#7014=VERTEX_POINT('',#50708);
#7015=VERTEX_POINT('',#50710);
#7016=VERTEX_POINT('',#50712);
#7017=VERTEX_POINT('',#50714);
#7018=VERTEX_POINT('',#50734);
#7019=VERTEX_POINT('',#50736);
#7020=VERTEX_POINT('',#50758);
#7021=VERTEX_POINT('',#50759);
#7022=VERTEX_POINT('',#50761);
#7023=VERTEX_POINT('',#50772);
#7024=VERTEX_POINT('',#50782);
#7025=VERTEX_POINT('',#50783);
#7026=VERTEX_POINT('',#50807);
#7027=VERTEX_POINT('',#50808);
#7028=VERTEX_POINT('',#50831);
#7029=VERTEX_POINT('',#50832);
#7030=VERTEX_POINT('',#50856);
#7031=VERTEX_POINT('',#50857);
#7032=VERTEX_POINT('',#50881);
#7033=VERTEX_POINT('',#50882);
#7034=VERTEX_POINT('',#50905);
#7035=VERTEX_POINT('',#50906);
#7036=VERTEX_POINT('',#50929);
#7037=VERTEX_POINT('',#50930);
#7038=VERTEX_POINT('',#50954);
#7039=VERTEX_POINT('',#50955);
#7040=VERTEX_POINT('',#50979);
#7041=VERTEX_POINT('',#50980);
#7042=VERTEX_POINT('',#51003);
#7043=VERTEX_POINT('',#51004);
#7044=VERTEX_POINT('',#51028);
#7045=VERTEX_POINT('',#51029);
#7046=VERTEX_POINT('',#51053);
#7047=VERTEX_POINT('',#51054);
#7048=VERTEX_POINT('',#51077);
#7049=VERTEX_POINT('',#51078);
#7050=VERTEX_POINT('',#51101);
#7051=VERTEX_POINT('',#51102);
#7052=VERTEX_POINT('',#51126);
#7053=VERTEX_POINT('',#51127);
#7054=VERTEX_POINT('',#51151);
#7055=VERTEX_POINT('',#51152);
#7056=VERTEX_POINT('',#51175);
#7057=VERTEX_POINT('',#51176);
#7058=VERTEX_POINT('',#51200);
#7059=VERTEX_POINT('',#51201);
#7060=VERTEX_POINT('',#51225);
#7061=VERTEX_POINT('',#51226);
#7062=VERTEX_POINT('',#51249);
#7063=VERTEX_POINT('',#51250);
#7064=VERTEX_POINT('',#51273);
#7065=VERTEX_POINT('',#51274);
#7066=VERTEX_POINT('',#51298);
#7067=VERTEX_POINT('',#51299);
#7068=VERTEX_POINT('',#51323);
#7069=VERTEX_POINT('',#51324);
#7070=VERTEX_POINT('',#51347);
#7071=VERTEX_POINT('',#51348);
#7072=VERTEX_POINT('',#51372);
#7073=VERTEX_POINT('',#51373);
#7074=VERTEX_POINT('',#51409);
#7075=VERTEX_POINT('',#51410);
#7076=VERTEX_POINT('',#51445);
#7077=VERTEX_POINT('',#51446);
#7078=VERTEX_POINT('',#51470);
#7079=VERTEX_POINT('',#51471);
#7080=VERTEX_POINT('',#51494);
#7081=VERTEX_POINT('',#51495);
#7082=VERTEX_POINT('',#51519);
#7083=VERTEX_POINT('',#51520);
#7084=VERTEX_POINT('',#51543);
#7085=VERTEX_POINT('',#51544);
#7086=VERTEX_POINT('',#51568);
#7087=VERTEX_POINT('',#51569);
#7088=VERTEX_POINT('',#51593);
#7089=VERTEX_POINT('',#51594);
#7090=VERTEX_POINT('',#51617);
#7091=VERTEX_POINT('',#51618);
#7092=VERTEX_POINT('',#51642);
#7093=VERTEX_POINT('',#51643);
#7094=VERTEX_POINT('',#51666);
#7095=VERTEX_POINT('',#51667);
#7096=VERTEX_POINT('',#51691);
#7097=VERTEX_POINT('',#51692);
#7098=VERTEX_POINT('',#51715);
#7099=VERTEX_POINT('',#51716);
#7100=VERTEX_POINT('',#51740);
#7101=VERTEX_POINT('',#51741);
#7102=VERTEX_POINT('',#51765);
#7103=VERTEX_POINT('',#51766);
#7104=VERTEX_POINT('',#51789);
#7105=VERTEX_POINT('',#51790);
#7106=VERTEX_POINT('',#51814);
#7107=VERTEX_POINT('',#51815);
#7108=VERTEX_POINT('',#51838);
#7109=VERTEX_POINT('',#51839);
#7110=VERTEX_POINT('',#51863);
#7111=VERTEX_POINT('',#51864);
#7112=VERTEX_POINT('',#51887);
#7113=VERTEX_POINT('',#51888);
#7114=VERTEX_POINT('',#51912);
#7115=VERTEX_POINT('',#51913);
#7116=VERTEX_POINT('',#51937);
#7117=VERTEX_POINT('',#51938);
#7118=VERTEX_POINT('',#51961);
#7119=VERTEX_POINT('',#51962);
#7120=VERTEX_POINT('',#51986);
#7121=VERTEX_POINT('',#51987);
#7122=VERTEX_POINT('',#52010);
#7123=VERTEX_POINT('',#52011);
#7124=VERTEX_POINT('',#52035);
#7125=VERTEX_POINT('',#52036);
#7126=VERTEX_POINT('',#52059);
#7127=VERTEX_POINT('',#52060);
#7128=VERTEX_POINT('',#52084);
#7129=VERTEX_POINT('',#52085);
#7130=VERTEX_POINT('',#52109);
#7131=VERTEX_POINT('',#52110);
#7132=VERTEX_POINT('',#52133);
#7133=VERTEX_POINT('',#52134);
#7134=VERTEX_POINT('',#52158);
#7135=VERTEX_POINT('',#52159);
#7136=VERTEX_POINT('',#52182);
#7137=VERTEX_POINT('',#52183);
#7138=VERTEX_POINT('',#52207);
#7139=VERTEX_POINT('',#52208);
#7140=VERTEX_POINT('',#52231);
#7141=VERTEX_POINT('',#52232);
#7142=VERTEX_POINT('',#52256);
#7143=VERTEX_POINT('',#52257);
#7144=VERTEX_POINT('',#52281);
#7145=VERTEX_POINT('',#52282);
#7146=VERTEX_POINT('',#52305);
#7147=VERTEX_POINT('',#52306);
#7148=VERTEX_POINT('',#52330);
#7149=VERTEX_POINT('',#52331);
#7150=VERTEX_POINT('',#52354);
#7151=VERTEX_POINT('',#52355);
#7152=VERTEX_POINT('',#52379);
#7153=VERTEX_POINT('',#52380);
#7154=VERTEX_POINT('',#52403);
#7155=VERTEX_POINT('',#52404);
#7156=VERTEX_POINT('',#52428);
#7157=VERTEX_POINT('',#52429);
#7158=VERTEX_POINT('',#52453);
#7159=VERTEX_POINT('',#52454);
#7160=VERTEX_POINT('',#52477);
#7161=VERTEX_POINT('',#52478);
#7162=VERTEX_POINT('',#52502);
#7163=VERTEX_POINT('',#52503);
#7164=VERTEX_POINT('',#52526);
#7165=VERTEX_POINT('',#52527);
#7166=VERTEX_POINT('',#52551);
#7167=VERTEX_POINT('',#52552);
#7168=VERTEX_POINT('',#52575);
#7169=VERTEX_POINT('',#52576);
#7170=VERTEX_POINT('',#52600);
#7171=VERTEX_POINT('',#52601);
#7172=VERTEX_POINT('',#52625);
#7173=VERTEX_POINT('',#52626);
#7174=VERTEX_POINT('',#52649);
#7175=VERTEX_POINT('',#52650);
#7176=VERTEX_POINT('',#52674);
#7177=VERTEX_POINT('',#52675);
#7178=VERTEX_POINT('',#52698);
#7179=VERTEX_POINT('',#52699);
#7180=VERTEX_POINT('',#52723);
#7181=VERTEX_POINT('',#52724);
#7182=VERTEX_POINT('',#52747);
#7183=VERTEX_POINT('',#52821);
#7184=VERTEX_POINT('',#53104);
#7185=VERTEX_POINT('',#53112);
#7186=VERTEX_POINT('',#53122);
#7187=VERTEX_POINT('',#53124);
#7188=VERTEX_POINT('',#53129);
#7189=VERTEX_POINT('',#53132);
#7190=VERTEX_POINT('',#57498);
#7191=VERTEX_POINT('',#57500);
#7192=VERTEX_POINT('',#57504);
#7193=VERTEX_POINT('',#57506);
#7194=VERTEX_POINT('',#57510);
#7195=VERTEX_POINT('',#57512);
#7196=VERTEX_POINT('',#57516);
#7197=VERTEX_POINT('',#57518);
#7198=VERTEX_POINT('',#57522);
#7199=VERTEX_POINT('',#57524);
#7200=VERTEX_POINT('',#57528);
#7201=VERTEX_POINT('',#57530);
#7202=VERTEX_POINT('',#57534);
#7203=VERTEX_POINT('',#57536);
#7204=VERTEX_POINT('',#57539);
#7205=VERTEX_POINT('',#57544);
#8873=EDGE_CURVE('',#6856,#6857,#4880,.T.);
#8874=EDGE_CURVE('',#6856,#6858,#1040,.T.);
#8875=EDGE_CURVE('',#6858,#6859,#2511,.T.);
#8876=EDGE_CURVE('',#6859,#6857,#1041,.T.);
#8877=EDGE_CURVE('',#6860,#6861,#4881,.T.);
#8878=EDGE_CURVE('',#6860,#6856,#1042,.T.);
#8879=EDGE_CURVE('',#6857,#6861,#1043,.T.);
#8880=EDGE_CURVE('',#6862,#6863,#4882,.T.);
#8881=EDGE_CURVE('',#6862,#6860,#1044,.T.);
#8882=EDGE_CURVE('',#6861,#6863,#1045,.T.);
#8883=EDGE_CURVE('',#6864,#6865,#4883,.T.);
#8884=EDGE_CURVE('',#6864,#6862,#1046,.T.);
#8885=EDGE_CURVE('',#6863,#6865,#1047,.T.);
#8886=EDGE_CURVE('',#6866,#6867,#4884,.T.);
#8887=EDGE_CURVE('',#6866,#6864,#1048,.T.);
#8888=EDGE_CURVE('',#6865,#6867,#1049,.T.);
#8889=EDGE_CURVE('',#6868,#6869,#4885,.T.);
#8890=EDGE_CURVE('',#6868,#6866,#1050,.T.);
#8891=EDGE_CURVE('',#6867,#6869,#1051,.T.);
#8892=EDGE_CURVE('',#6870,#6871,#4886,.T.);
#8893=EDGE_CURVE('',#6870,#6868,#1052,.T.);
#8894=EDGE_CURVE('',#6869,#6871,#1053,.T.);
#8895=EDGE_CURVE('',#6872,#6873,#4887,.T.);
#8896=EDGE_CURVE('',#6872,#6870,#1054,.T.);
#8897=EDGE_CURVE('',#6871,#6873,#1055,.T.);
#8898=EDGE_CURVE('',#6874,#6875,#4888,.T.);
#8899=EDGE_CURVE('',#6874,#6872,#1056,.T.);
#8900=EDGE_CURVE('',#6873,#6875,#1057,.T.);
#8901=EDGE_CURVE('',#6876,#6877,#4889,.T.);
#8902=EDGE_CURVE('',#6876,#6874,#1058,.T.);
#8903=EDGE_CURVE('',#6875,#6877,#1059,.T.);
#8904=EDGE_CURVE('',#6878,#6879,#4890,.T.);
#8905=EDGE_CURVE('',#6878,#6876,#1060,.T.);
#8906=EDGE_CURVE('',#6877,#6879,#1061,.T.);
#8907=EDGE_CURVE('',#6880,#6881,#4891,.T.);
#8908=EDGE_CURVE('',#6880,#6878,#1062,.T.);
#8909=EDGE_CURVE('',#6879,#6881,#1063,.T.);
#8910=EDGE_CURVE('',#6882,#6883,#4892,.T.);
#8911=EDGE_CURVE('',#6882,#6880,#1064,.T.);
#8912=EDGE_CURVE('',#6881,#6883,#1065,.T.);
#8913=EDGE_CURVE('',#6884,#6885,#4893,.T.);
#8914=EDGE_CURVE('',#6884,#6882,#1066,.T.);
#8915=EDGE_CURVE('',#6883,#6885,#1067,.T.);
#8916=EDGE_CURVE('',#6886,#6887,#4894,.T.);
#8917=EDGE_CURVE('',#6886,#6884,#1068,.T.);
#8918=EDGE_CURVE('',#6885,#6887,#1069,.T.);
#8919=EDGE_CURVE('',#6888,#6889,#4895,.T.);
#8920=EDGE_CURVE('',#6888,#6886,#1070,.T.);
#8921=EDGE_CURVE('',#6887,#6889,#1071,.T.);
#8922=EDGE_CURVE('',#6890,#6891,#4896,.T.);
#8923=EDGE_CURVE('',#6890,#6888,#1072,.T.);
#8924=EDGE_CURVE('',#6889,#6891,#1073,.T.);
#8925=EDGE_CURVE('',#6892,#6893,#4897,.T.);
#8926=EDGE_CURVE('',#6892,#6890,#1074,.T.);
#8927=EDGE_CURVE('',#6891,#6893,#1075,.T.);
#8928=EDGE_CURVE('',#6894,#6895,#4898,.T.);
#8929=EDGE_CURVE('',#6894,#6892,#1076,.T.);
#8930=EDGE_CURVE('',#6893,#6895,#1077,.T.);
#8931=EDGE_CURVE('',#6896,#6897,#4899,.T.);
#8932=EDGE_CURVE('',#6896,#6894,#1078,.T.);
#8933=EDGE_CURVE('',#6895,#6897,#1079,.T.);
#8934=EDGE_CURVE('',#6898,#6899,#4900,.T.);
#8935=EDGE_CURVE('',#6898,#6896,#1080,.T.);
#8936=EDGE_CURVE('',#6897,#6899,#1081,.T.);
#8937=EDGE_CURVE('',#6900,#6901,#4901,.T.);
#8938=EDGE_CURVE('',#6900,#6898,#1082,.T.);
#8939=EDGE_CURVE('',#6899,#6901,#1083,.T.);
#8940=EDGE_CURVE('',#6902,#6903,#4902,.T.);
#8941=EDGE_CURVE('',#6902,#6900,#1084,.T.);
#8942=EDGE_CURVE('',#6901,#6903,#1085,.T.);
#8943=EDGE_CURVE('',#6904,#6905,#4903,.T.);
#8944=EDGE_CURVE('',#6904,#6902,#1086,.T.);
#8945=EDGE_CURVE('',#6903,#6905,#1087,.T.);
#8946=EDGE_CURVE('',#6906,#6907,#4904,.T.);
#8947=EDGE_CURVE('',#6906,#6904,#1088,.T.);
#8948=EDGE_CURVE('',#6905,#6907,#1089,.T.);
#8949=EDGE_CURVE('',#6908,#6909,#4905,.T.);
#8950=EDGE_CURVE('',#6908,#6906,#1090,.T.);
#8951=EDGE_CURVE('',#6907,#6909,#1091,.T.);
#8952=EDGE_CURVE('',#6910,#6911,#4906,.T.);
#8953=EDGE_CURVE('',#6910,#6908,#1092,.T.);
#8954=EDGE_CURVE('',#6909,#6911,#1093,.T.);
#8955=EDGE_CURVE('',#6912,#6913,#4907,.T.);
#8956=EDGE_CURVE('',#6912,#6910,#1094,.T.);
#8957=EDGE_CURVE('',#6911,#6913,#1095,.T.);
#8958=EDGE_CURVE('',#6914,#6915,#4908,.T.);
#8959=EDGE_CURVE('',#6914,#6912,#1096,.T.);
#8960=EDGE_CURVE('',#6913,#6915,#1097,.T.);
#8961=EDGE_CURVE('',#6916,#6917,#4909,.T.);
#8962=EDGE_CURVE('',#6916,#6914,#1098,.T.);
#8963=EDGE_CURVE('',#6915,#6917,#1099,.T.);
#8964=EDGE_CURVE('',#6918,#6919,#4910,.T.);
#8965=EDGE_CURVE('',#6918,#6916,#1100,.T.);
#8966=EDGE_CURVE('',#6917,#6919,#1101,.T.);
#8967=EDGE_CURVE('',#6920,#6921,#4911,.T.);
#8968=EDGE_CURVE('',#6920,#6918,#1102,.T.);
#8969=EDGE_CURVE('',#6919,#6921,#1103,.T.);
#8970=EDGE_CURVE('',#6922,#6923,#4912,.T.);
#8971=EDGE_CURVE('',#6922,#6920,#1104,.T.);
#8972=EDGE_CURVE('',#6921,#6923,#1105,.T.);
#8973=EDGE_CURVE('',#6924,#6925,#4913,.T.);
#8974=EDGE_CURVE('',#6924,#6922,#1106,.T.);
#8975=EDGE_CURVE('',#6923,#6925,#1107,.T.);
#8976=EDGE_CURVE('',#6926,#6927,#4914,.T.);
#8977=EDGE_CURVE('',#6926,#6924,#1108,.T.);
#8978=EDGE_CURVE('',#6925,#6927,#1109,.T.);
#8979=EDGE_CURVE('',#6928,#6929,#4915,.T.);
#8980=EDGE_CURVE('',#6928,#6926,#1110,.T.);
#8981=EDGE_CURVE('',#6927,#6929,#1111,.T.);
#8982=EDGE_CURVE('',#6930,#6931,#4916,.T.);
#8983=EDGE_CURVE('',#6930,#6928,#1112,.T.);
#8984=EDGE_CURVE('',#6929,#6931,#1113,.T.);
#8985=EDGE_CURVE('',#6932,#6933,#4917,.T.);
#8986=EDGE_CURVE('',#6932,#6930,#1114,.T.);
#8987=EDGE_CURVE('',#6931,#6933,#1115,.T.);
#8988=EDGE_CURVE('',#6934,#6935,#4918,.T.);
#8989=EDGE_CURVE('',#6934,#6932,#1116,.T.);
#8990=EDGE_CURVE('',#6933,#6935,#1117,.T.);
#8991=EDGE_CURVE('',#6936,#6937,#4919,.T.);
#8992=EDGE_CURVE('',#6936,#6934,#1118,.T.);
#8993=EDGE_CURVE('',#6935,#6937,#1119,.T.);
#8994=EDGE_CURVE('',#6938,#6939,#4920,.T.);
#8995=EDGE_CURVE('',#6938,#6936,#1120,.T.);
#8996=EDGE_CURVE('',#6937,#6939,#1121,.T.);
#8997=EDGE_CURVE('',#6940,#6941,#4921,.T.);
#8998=EDGE_CURVE('',#6940,#6938,#1122,.T.);
#8999=EDGE_CURVE('',#6939,#6941,#1123,.T.);
#9000=EDGE_CURVE('',#6942,#6943,#4922,.T.);
#9001=EDGE_CURVE('',#6942,#6940,#1124,.T.);
#9002=EDGE_CURVE('',#6941,#6943,#1125,.T.);
#9003=EDGE_CURVE('',#6944,#6945,#4923,.T.);
#9004=EDGE_CURVE('',#6944,#6942,#1126,.T.);
#9005=EDGE_CURVE('',#6943,#6945,#1127,.T.);
#9006=EDGE_CURVE('',#6946,#6947,#4924,.T.);
#9007=EDGE_CURVE('',#6946,#6944,#1128,.T.);
#9008=EDGE_CURVE('',#6945,#6947,#1129,.T.);
#9009=EDGE_CURVE('',#6948,#6949,#4925,.T.);
#9010=EDGE_CURVE('',#6948,#6946,#1130,.T.);
#9011=EDGE_CURVE('',#6947,#6949,#1131,.T.);
#9012=EDGE_CURVE('',#6950,#6951,#4926,.T.);
#9013=EDGE_CURVE('',#6950,#6948,#1132,.T.);
#9014=EDGE_CURVE('',#6949,#6951,#1133,.T.);
#9015=EDGE_CURVE('',#6952,#6953,#4927,.T.);
#9016=EDGE_CURVE('',#6952,#6950,#1134,.T.);
#9017=EDGE_CURVE('',#6951,#6953,#1135,.T.);
#9018=EDGE_CURVE('',#6954,#6955,#4928,.T.);
#9019=EDGE_CURVE('',#6954,#6952,#1136,.T.);
#9020=EDGE_CURVE('',#6953,#6955,#1137,.T.);
#9021=EDGE_CURVE('',#6956,#6957,#4929,.T.);
#9022=EDGE_CURVE('',#6956,#6954,#1138,.T.);
#9023=EDGE_CURVE('',#6955,#6957,#1139,.T.);
#9024=EDGE_CURVE('',#6958,#6959,#4930,.T.);
#9025=EDGE_CURVE('',#6958,#6956,#1140,.T.);
#9026=EDGE_CURVE('',#6957,#6959,#1141,.T.);
#9027=EDGE_CURVE('',#6960,#6961,#4931,.T.);
#9028=EDGE_CURVE('',#6960,#6958,#1142,.T.);
#9029=EDGE_CURVE('',#6959,#6961,#1143,.T.);
#9030=EDGE_CURVE('',#6962,#6963,#4932,.T.);
#9031=EDGE_CURVE('',#6962,#6960,#1144,.T.);
#9032=EDGE_CURVE('',#6961,#6963,#1145,.T.);
#9033=EDGE_CURVE('',#6964,#6965,#4933,.T.);
#9034=EDGE_CURVE('',#6964,#6962,#1146,.T.);
#9035=EDGE_CURVE('',#6963,#6965,#1147,.T.);
#9036=EDGE_CURVE('',#6966,#6967,#4934,.T.);
#9037=EDGE_CURVE('',#6966,#6964,#1148,.T.);
#9038=EDGE_CURVE('',#6965,#6967,#1149,.T.);
#9039=EDGE_CURVE('',#6968,#6969,#4935,.T.);
#9040=EDGE_CURVE('',#6968,#6966,#1150,.T.);
#9041=EDGE_CURVE('',#6967,#6969,#1151,.T.);
#9042=EDGE_CURVE('',#6970,#6971,#4936,.T.);
#9043=EDGE_CURVE('',#6970,#6968,#1152,.T.);
#9044=EDGE_CURVE('',#6969,#6971,#1153,.T.);
#9045=EDGE_CURVE('',#6972,#6973,#4937,.T.);
#9046=EDGE_CURVE('',#6972,#6970,#1154,.T.);
#9047=EDGE_CURVE('',#6971,#6973,#1155,.T.);
#9048=EDGE_CURVE('',#6974,#6975,#4938,.T.);
#9049=EDGE_CURVE('',#6974,#6972,#1156,.T.);
#9050=EDGE_CURVE('',#6973,#6975,#1157,.T.);
#9051=EDGE_CURVE('',#6976,#6977,#4939,.T.);
#9052=EDGE_CURVE('',#6976,#6974,#1158,.T.);
#9053=EDGE_CURVE('',#6975,#6977,#1159,.T.);
#9054=EDGE_CURVE('',#6978,#6979,#4940,.T.);
#9055=EDGE_CURVE('',#6978,#6976,#1160,.T.);
#9056=EDGE_CURVE('',#6977,#6979,#1161,.T.);
#9057=EDGE_CURVE('',#6980,#6981,#4941,.T.);
#9058=EDGE_CURVE('',#6980,#6978,#1162,.T.);
#9059=EDGE_CURVE('',#6979,#6981,#1163,.T.);
#9060=EDGE_CURVE('',#6982,#6983,#4942,.T.);
#9061=EDGE_CURVE('',#6982,#6980,#1164,.T.);
#9062=EDGE_CURVE('',#6981,#6983,#1165,.T.);
#9063=EDGE_CURVE('',#6984,#6985,#4943,.T.);
#9064=EDGE_CURVE('',#6984,#6982,#1166,.T.);
#9065=EDGE_CURVE('',#6983,#6985,#1167,.T.);
#9066=EDGE_CURVE('',#6986,#6987,#4944,.T.);
#9067=EDGE_CURVE('',#6986,#6984,#1168,.T.);
#9068=EDGE_CURVE('',#6985,#6987,#1169,.T.);
#9069=EDGE_CURVE('',#6988,#6989,#4945,.T.);
#9070=EDGE_CURVE('',#6988,#6986,#1170,.T.);
#9071=EDGE_CURVE('',#6987,#6989,#1171,.T.);
#9072=EDGE_CURVE('',#6990,#6991,#4946,.T.);
#9073=EDGE_CURVE('',#6990,#6988,#1172,.T.);
#9074=EDGE_CURVE('',#6989,#6991,#1173,.T.);
#9075=EDGE_CURVE('',#6992,#6993,#4947,.T.);
#9076=EDGE_CURVE('',#6992,#6990,#1174,.T.);
#9077=EDGE_CURVE('',#6991,#6993,#1175,.T.);
#9078=EDGE_CURVE('',#6994,#6995,#4948,.T.);
#9079=EDGE_CURVE('',#6994,#6992,#1176,.T.);
#9080=EDGE_CURVE('',#6993,#6995,#1177,.T.);
#9081=EDGE_CURVE('',#6996,#6997,#4949,.T.);
#9082=EDGE_CURVE('',#6996,#6994,#1178,.T.);
#9083=EDGE_CURVE('',#6995,#6997,#1179,.T.);
#9084=EDGE_CURVE('',#6998,#6999,#4950,.T.);
#9085=EDGE_CURVE('',#6998,#6996,#1180,.T.);
#9086=EDGE_CURVE('',#6997,#6999,#1181,.T.);
#9087=EDGE_CURVE('',#7000,#7001,#4951,.T.);
#9088=EDGE_CURVE('',#7000,#6998,#1182,.T.);
#9089=EDGE_CURVE('',#6999,#7001,#1183,.T.);
#9090=EDGE_CURVE('',#7002,#7003,#4952,.T.);
#9091=EDGE_CURVE('',#7002,#7000,#1184,.T.);
#9092=EDGE_CURVE('',#7001,#7003,#1185,.T.);
#9093=EDGE_CURVE('',#7004,#7005,#4953,.T.);
#9094=EDGE_CURVE('',#7004,#7002,#1186,.T.);
#9095=EDGE_CURVE('',#7003,#7005,#1187,.T.);
#9096=EDGE_CURVE('',#7006,#7007,#4954,.T.);
#9097=EDGE_CURVE('',#7006,#7004,#1188,.T.);
#9098=EDGE_CURVE('',#7005,#7007,#1189,.T.);
#9099=EDGE_CURVE('',#7008,#7009,#4955,.T.);
#9100=EDGE_CURVE('',#7008,#7006,#1190,.T.);
#9101=EDGE_CURVE('',#7007,#7009,#1191,.T.);
#9102=EDGE_CURVE('',#7010,#7011,#4956,.T.);
#9103=EDGE_CURVE('',#7010,#7008,#1192,.T.);
#9104=EDGE_CURVE('',#7009,#7011,#1193,.T.);
#9105=EDGE_CURVE('',#7012,#7013,#4957,.T.);
#9106=EDGE_CURVE('',#7012,#7010,#1194,.T.);
#9107=EDGE_CURVE('',#7011,#7013,#1195,.T.);
#9108=EDGE_CURVE('',#7014,#7014,#2512,.T.);
#9109=EDGE_CURVE('',#7014,#7015,#4958,.T.);
#9110=EDGE_CURVE('',#7015,#7016,#2513,.T.);
#9111=EDGE_CURVE('',#7016,#7017,#1196,.T.);
#9112=EDGE_CURVE('',#7017,#7018,#4959,.T.);
#9113=EDGE_CURVE('',#7018,#7019,#1197,.T.);
#9114=EDGE_CURVE('',#7019,#7015,#2514,.T.);
#9115=EDGE_CURVE('',#7020,#7021,#4960,.T.);
#9116=EDGE_CURVE('',#7020,#7022,#1198,.T.);
#9117=EDGE_CURVE('',#7023,#7022,#2515,.T.);
#9118=EDGE_CURVE('',#7021,#7023,#1199,.T.);
#9119=EDGE_CURVE('',#7024,#7025,#4961,.T.);
#9120=EDGE_CURVE('',#7024,#7020,#1200,.T.);
#9121=EDGE_CURVE('',#7025,#7021,#1201,.T.);
#9122=EDGE_CURVE('',#7026,#7027,#4962,.T.);
#9123=EDGE_CURVE('',#7026,#7024,#1202,.T.);
#9124=EDGE_CURVE('',#7027,#7025,#1203,.T.);
#9125=EDGE_CURVE('',#7028,#7029,#4963,.T.);
#9126=EDGE_CURVE('',#7028,#7026,#1204,.T.);
#9127=EDGE_CURVE('',#7029,#7027,#1205,.T.);
#9128=EDGE_CURVE('',#7030,#7031,#4964,.T.);
#9129=EDGE_CURVE('',#7030,#7028,#1206,.T.);
#9130=EDGE_CURVE('',#7031,#7029,#1207,.T.);
#9131=EDGE_CURVE('',#7032,#7033,#4965,.T.);
#9132=EDGE_CURVE('',#7032,#7030,#1208,.T.);
#9133=EDGE_CURVE('',#7033,#7031,#1209,.T.);
#9134=EDGE_CURVE('',#7034,#7035,#4966,.T.);
#9135=EDGE_CURVE('',#7034,#7032,#1210,.T.);
#9136=EDGE_CURVE('',#7035,#7033,#1211,.T.);
#9137=EDGE_CURVE('',#7036,#7037,#4967,.T.);
#9138=EDGE_CURVE('',#7036,#7034,#1212,.T.);
#9139=EDGE_CURVE('',#7037,#7035,#1213,.T.);
#9140=EDGE_CURVE('',#7038,#7039,#4968,.T.);
#9141=EDGE_CURVE('',#7038,#7036,#1214,.T.);
#9142=EDGE_CURVE('',#7039,#7037,#1215,.T.);
#9143=EDGE_CURVE('',#7040,#7041,#4969,.T.);
#9144=EDGE_CURVE('',#7040,#7038,#1216,.T.);
#9145=EDGE_CURVE('',#7041,#7039,#1217,.T.);
#9146=EDGE_CURVE('',#7042,#7043,#4970,.T.);
#9147=EDGE_CURVE('',#7042,#7040,#1218,.T.);
#9148=EDGE_CURVE('',#7043,#7041,#1219,.T.);
#9149=EDGE_CURVE('',#7044,#7045,#4971,.T.);
#9150=EDGE_CURVE('',#7044,#7042,#1220,.T.);
#9151=EDGE_CURVE('',#7045,#7043,#1221,.T.);
#9152=EDGE_CURVE('',#7046,#7047,#4972,.T.);
#9153=EDGE_CURVE('',#7046,#7044,#1222,.T.);
#9154=EDGE_CURVE('',#7047,#7045,#1223,.T.);
#9155=EDGE_CURVE('',#7048,#7049,#4973,.T.);
#9156=EDGE_CURVE('',#7048,#7046,#1224,.T.);
#9157=EDGE_CURVE('',#7049,#7047,#1225,.T.);
#9158=EDGE_CURVE('',#7050,#7051,#4974,.T.);
#9159=EDGE_CURVE('',#7050,#7048,#1226,.T.);
#9160=EDGE_CURVE('',#7051,#7049,#1227,.T.);
#9161=EDGE_CURVE('',#7052,#7053,#4975,.T.);
#9162=EDGE_CURVE('',#7052,#7050,#1228,.T.);
#9163=EDGE_CURVE('',#7053,#7051,#1229,.T.);
#9164=EDGE_CURVE('',#7054,#7055,#4976,.T.);
#9165=EDGE_CURVE('',#7054,#7052,#1230,.T.);
#9166=EDGE_CURVE('',#7055,#7053,#1231,.T.);
#9167=EDGE_CURVE('',#7056,#7057,#4977,.T.);
#9168=EDGE_CURVE('',#7056,#7054,#1232,.T.);
#9169=EDGE_CURVE('',#7057,#7055,#1233,.T.);
#9170=EDGE_CURVE('',#7058,#7059,#4978,.T.);
#9171=EDGE_CURVE('',#7058,#7056,#1234,.T.);
#9172=EDGE_CURVE('',#7059,#7057,#1235,.T.);
#9173=EDGE_CURVE('',#7060,#7061,#4979,.T.);
#9174=EDGE_CURVE('',#7060,#7058,#1236,.T.);
#9175=EDGE_CURVE('',#7061,#7059,#1237,.T.);
#9176=EDGE_CURVE('',#7062,#7063,#4980,.T.);
#9177=EDGE_CURVE('',#7062,#7060,#1238,.T.);
#9178=EDGE_CURVE('',#7063,#7061,#1239,.T.);
#9179=EDGE_CURVE('',#7064,#7065,#4981,.T.);
#9180=EDGE_CURVE('',#7064,#7062,#1240,.T.);
#9181=EDGE_CURVE('',#7065,#7063,#1241,.T.);
#9182=EDGE_CURVE('',#7066,#7067,#4982,.T.);
#9183=EDGE_CURVE('',#7066,#7064,#1242,.T.);
#9184=EDGE_CURVE('',#7067,#7065,#1243,.T.);
#9185=EDGE_CURVE('',#7068,#7069,#4983,.T.);
#9186=EDGE_CURVE('',#7068,#7066,#1244,.T.);
#9187=EDGE_CURVE('',#7069,#7067,#1245,.T.);
#9188=EDGE_CURVE('',#7070,#7071,#4984,.T.);
#9189=EDGE_CURVE('',#7070,#7068,#1246,.T.);
#9190=EDGE_CURVE('',#7071,#7069,#1247,.T.);
#9191=EDGE_CURVE('',#7072,#7073,#4985,.T.);
#9192=EDGE_CURVE('',#7072,#7070,#1248,.T.);
#9193=EDGE_CURVE('',#7073,#7071,#1249,.T.);
#9194=EDGE_CURVE('',#7074,#7075,#4986,.T.);
#9195=EDGE_CURVE('',#7074,#7072,#1250,.T.);
#9196=EDGE_CURVE('',#7075,#7073,#1251,.T.);
#9197=EDGE_CURVE('',#7076,#7077,#4987,.T.);
#9198=EDGE_CURVE('',#7076,#7074,#1252,.T.);
#9199=EDGE_CURVE('',#7077,#7075,#1253,.T.);
#9200=EDGE_CURVE('',#7078,#7079,#4988,.T.);
#9201=EDGE_CURVE('',#7078,#7076,#1254,.T.);
#9202=EDGE_CURVE('',#7079,#7077,#1255,.T.);
#9203=EDGE_CURVE('',#7080,#7081,#4989,.T.);
#9204=EDGE_CURVE('',#7080,#7078,#1256,.T.);
#9205=EDGE_CURVE('',#7081,#7079,#1257,.T.);
#9206=EDGE_CURVE('',#7082,#7083,#4990,.T.);
#9207=EDGE_CURVE('',#7082,#7080,#1258,.T.);
#9208=EDGE_CURVE('',#7083,#7081,#1259,.T.);
#9209=EDGE_CURVE('',#7084,#7085,#4991,.T.);
#9210=EDGE_CURVE('',#7084,#7082,#1260,.T.);
#9211=EDGE_CURVE('',#7085,#7083,#1261,.T.);
#9212=EDGE_CURVE('',#7086,#7087,#4992,.T.);
#9213=EDGE_CURVE('',#7086,#7084,#1262,.T.);
#9214=EDGE_CURVE('',#7087,#7085,#1263,.T.);
#9215=EDGE_CURVE('',#7088,#7089,#4993,.T.);
#9216=EDGE_CURVE('',#7088,#7086,#1264,.T.);
#9217=EDGE_CURVE('',#7089,#7087,#1265,.T.);
#9218=EDGE_CURVE('',#7090,#7091,#4994,.T.);
#9219=EDGE_CURVE('',#7090,#7088,#1266,.T.);
#9220=EDGE_CURVE('',#7091,#7089,#1267,.T.);
#9221=EDGE_CURVE('',#7092,#7093,#4995,.T.);
#9222=EDGE_CURVE('',#7092,#7090,#1268,.T.);
#9223=EDGE_CURVE('',#7093,#7091,#1269,.T.);
#9224=EDGE_CURVE('',#7094,#7095,#4996,.T.);
#9225=EDGE_CURVE('',#7094,#7092,#1270,.T.);
#9226=EDGE_CURVE('',#7095,#7093,#1271,.T.);
#9227=EDGE_CURVE('',#7096,#7097,#4997,.T.);
#9228=EDGE_CURVE('',#7096,#7094,#1272,.T.);
#9229=EDGE_CURVE('',#7097,#7095,#1273,.T.);
#9230=EDGE_CURVE('',#7098,#7099,#4998,.T.);
#9231=EDGE_CURVE('',#7098,#7096,#1274,.T.);
#9232=EDGE_CURVE('',#7099,#7097,#1275,.T.);
#9233=EDGE_CURVE('',#7100,#7101,#4999,.T.);
#9234=EDGE_CURVE('',#7100,#7098,#1276,.T.);
#9235=EDGE_CURVE('',#7101,#7099,#1277,.T.);
#9236=EDGE_CURVE('',#7102,#7103,#5000,.T.);
#9237=EDGE_CURVE('',#7102,#7100,#1278,.T.);
#9238=EDGE_CURVE('',#7103,#7101,#1279,.T.);
#9239=EDGE_CURVE('',#7104,#7105,#5001,.T.);
#9240=EDGE_CURVE('',#7104,#7102,#1280,.T.);
#9241=EDGE_CURVE('',#7105,#7103,#1281,.T.);
#9242=EDGE_CURVE('',#7106,#7107,#5002,.T.);
#9243=EDGE_CURVE('',#7106,#7104,#1282,.T.);
#9244=EDGE_CURVE('',#7107,#7105,#1283,.T.);
#9245=EDGE_CURVE('',#7108,#7109,#5003,.T.);
#9246=EDGE_CURVE('',#7108,#7106,#1284,.T.);
#9247=EDGE_CURVE('',#7109,#7107,#1285,.T.);
#9248=EDGE_CURVE('',#7110,#7111,#5004,.T.);
#9249=EDGE_CURVE('',#7110,#7108,#1286,.T.);
#9250=EDGE_CURVE('',#7111,#7109,#1287,.T.);
#9251=EDGE_CURVE('',#7112,#7113,#5005,.T.);
#9252=EDGE_CURVE('',#7112,#7110,#1288,.T.);
#9253=EDGE_CURVE('',#7113,#7111,#1289,.T.);
#9254=EDGE_CURVE('',#7114,#7115,#5006,.T.);
#9255=EDGE_CURVE('',#7114,#7112,#1290,.T.);
#9256=EDGE_CURVE('',#7115,#7113,#1291,.T.);
#9257=EDGE_CURVE('',#7116,#7117,#5007,.T.);
#9258=EDGE_CURVE('',#7116,#7114,#1292,.T.);
#9259=EDGE_CURVE('',#7117,#7115,#1293,.T.);
#9260=EDGE_CURVE('',#7118,#7119,#5008,.T.);
#9261=EDGE_CURVE('',#7118,#7116,#1294,.T.);
#9262=EDGE_CURVE('',#7119,#7117,#1295,.T.);
#9263=EDGE_CURVE('',#7120,#7121,#5009,.T.);
#9264=EDGE_CURVE('',#7120,#7118,#1296,.T.);
#9265=EDGE_CURVE('',#7121,#7119,#1297,.T.);
#9266=EDGE_CURVE('',#7122,#7123,#5010,.T.);
#9267=EDGE_CURVE('',#7122,#7120,#1298,.T.);
#9268=EDGE_CURVE('',#7123,#7121,#1299,.T.);
#9269=EDGE_CURVE('',#7124,#7125,#5011,.T.);
#9270=EDGE_CURVE('',#7124,#7122,#1300,.T.);
#9271=EDGE_CURVE('',#7125,#7123,#1301,.T.);
#9272=EDGE_CURVE('',#7126,#7127,#5012,.T.);
#9273=EDGE_CURVE('',#7126,#7124,#1302,.T.);
#9274=EDGE_CURVE('',#7127,#7125,#1303,.T.);
#9275=EDGE_CURVE('',#7128,#7129,#5013,.T.);
#9276=EDGE_CURVE('',#7128,#7126,#1304,.T.);
#9277=EDGE_CURVE('',#7129,#7127,#1305,.T.);
#9278=EDGE_CURVE('',#7130,#7131,#5014,.T.);
#9279=EDGE_CURVE('',#7130,#7128,#1306,.T.);
#9280=EDGE_CURVE('',#7131,#7129,#1307,.T.);
#9281=EDGE_CURVE('',#7132,#7133,#5015,.T.);
#9282=EDGE_CURVE('',#7132,#7130,#1308,.T.);
#9283=EDGE_CURVE('',#7133,#7131,#1309,.T.);
#9284=EDGE_CURVE('',#7134,#7135,#5016,.T.);
#9285=EDGE_CURVE('',#7134,#7132,#1310,.T.);
#9286=EDGE_CURVE('',#7135,#7133,#1311,.T.);
#9287=EDGE_CURVE('',#7136,#7137,#5017,.T.);
#9288=EDGE_CURVE('',#7136,#7134,#1312,.T.);
#9289=EDGE_CURVE('',#7137,#7135,#1313,.T.);
#9290=EDGE_CURVE('',#7138,#7139,#5018,.T.);
#9291=EDGE_CURVE('',#7138,#7136,#1314,.T.);
#9292=EDGE_CURVE('',#7139,#7137,#1315,.T.);
#9293=EDGE_CURVE('',#7140,#7141,#5019,.T.);
#9294=EDGE_CURVE('',#7140,#7138,#1316,.T.);
#9295=EDGE_CURVE('',#7141,#7139,#1317,.T.);
#9296=EDGE_CURVE('',#7142,#7143,#5020,.T.);
#9297=EDGE_CURVE('',#7142,#7140,#1318,.T.);
#9298=EDGE_CURVE('',#7143,#7141,#1319,.T.);
#9299=EDGE_CURVE('',#7144,#7145,#5021,.T.);
#9300=EDGE_CURVE('',#7144,#7142,#1320,.T.);
#9301=EDGE_CURVE('',#7145,#7143,#1321,.T.);
#9302=EDGE_CURVE('',#7146,#7147,#5022,.T.);
#9303=EDGE_CURVE('',#7146,#7144,#1322,.T.);
#9304=EDGE_CURVE('',#7147,#7145,#1323,.T.);
#9305=EDGE_CURVE('',#7148,#7149,#5023,.T.);
#9306=EDGE_CURVE('',#7148,#7146,#1324,.T.);
#9307=EDGE_CURVE('',#7149,#7147,#1325,.T.);
#9308=EDGE_CURVE('',#7150,#7151,#5024,.T.);
#9309=EDGE_CURVE('',#7150,#7148,#1326,.T.);
#9310=EDGE_CURVE('',#7151,#7149,#1327,.T.);
#9311=EDGE_CURVE('',#7152,#7153,#5025,.T.);
#9312=EDGE_CURVE('',#7152,#7150,#1328,.T.);
#9313=EDGE_CURVE('',#7153,#7151,#1329,.T.);
#9314=EDGE_CURVE('',#7154,#7155,#5026,.T.);
#9315=EDGE_CURVE('',#7154,#7152,#1330,.T.);
#9316=EDGE_CURVE('',#7155,#7153,#1331,.T.);
#9317=EDGE_CURVE('',#7156,#7157,#5027,.T.);
#9318=EDGE_CURVE('',#7156,#7154,#1332,.T.);
#9319=EDGE_CURVE('',#7157,#7155,#1333,.T.);
#9320=EDGE_CURVE('',#7158,#7159,#5028,.T.);
#9321=EDGE_CURVE('',#7158,#7156,#1334,.T.);
#9322=EDGE_CURVE('',#7159,#7157,#1335,.T.);
#9323=EDGE_CURVE('',#7160,#7161,#5029,.T.);
#9324=EDGE_CURVE('',#7160,#7158,#1336,.T.);
#9325=EDGE_CURVE('',#7161,#7159,#1337,.T.);
#9326=EDGE_CURVE('',#7162,#7163,#5030,.T.);
#9327=EDGE_CURVE('',#7162,#7160,#1338,.T.);
#9328=EDGE_CURVE('',#7163,#7161,#1339,.T.);
#9329=EDGE_CURVE('',#7164,#7165,#5031,.T.);
#9330=EDGE_CURVE('',#7164,#7162,#1340,.T.);
#9331=EDGE_CURVE('',#7165,#7163,#1341,.T.);
#9332=EDGE_CURVE('',#7166,#7167,#5032,.T.);
#9333=EDGE_CURVE('',#7166,#7164,#1342,.T.);
#9334=EDGE_CURVE('',#7167,#7165,#1343,.T.);
#9335=EDGE_CURVE('',#7168,#7169,#5033,.T.);
#9336=EDGE_CURVE('',#7168,#7166,#1344,.T.);
#9337=EDGE_CURVE('',#7169,#7167,#1345,.T.);
#9338=EDGE_CURVE('',#7170,#7171,#5034,.T.);
#9339=EDGE_CURVE('',#7170,#7168,#1346,.T.);
#9340=EDGE_CURVE('',#7171,#7169,#1347,.T.);
#9341=EDGE_CURVE('',#7172,#7173,#5035,.T.);
#9342=EDGE_CURVE('',#7172,#7170,#1348,.T.);
#9343=EDGE_CURVE('',#7173,#7171,#1349,.T.);
#9344=EDGE_CURVE('',#7174,#7175,#5036,.T.);
#9345=EDGE_CURVE('',#7174,#7172,#1350,.T.);
#9346=EDGE_CURVE('',#7175,#7173,#1351,.T.);
#9347=EDGE_CURVE('',#7176,#7177,#5037,.T.);
#9348=EDGE_CURVE('',#7176,#7174,#1352,.T.);
#9349=EDGE_CURVE('',#7177,#7175,#1353,.T.);
#9350=EDGE_CURVE('',#7178,#7179,#5038,.T.);
#9351=EDGE_CURVE('',#7178,#7176,#1354,.T.);
#9352=EDGE_CURVE('',#7179,#7177,#1355,.T.);
#9353=EDGE_CURVE('',#7180,#7181,#5039,.T.);
#9354=EDGE_CURVE('',#7180,#7178,#1356,.T.);
#9355=EDGE_CURVE('',#7181,#7179,#1357,.T.);
#9356=EDGE_CURVE('',#6859,#7182,#1358,.T.);
#9357=EDGE_CURVE('',#7183,#6858,#1359,.T.);
#9358=EDGE_CURVE('',#7182,#7183,#2516,.T.);
#9359=EDGE_CURVE('',#7183,#7184,#1360,.T.);
#9360=EDGE_CURVE('',#7184,#7185,#2517,.T.);
#9361=EDGE_CURVE('',#7185,#7182,#1361,.T.);
#9362=EDGE_CURVE('',#7186,#7186,#2518,.T.);
#9363=EDGE_CURVE('',#7186,#7187,#5040,.T.);
#9364=EDGE_CURVE('',#7187,#7187,#2519,.T.);
#9365=EDGE_CURVE('',#7188,#7188,#2520,.T.);
#9366=EDGE_CURVE('',#7189,#7189,#2521,.T.);
#9367=EDGE_CURVE('',#7189,#7188,#5041,.T.);
#9368=EDGE_CURVE('',#7022,#7016,#1362,.T.);
#9369=EDGE_CURVE('',#7019,#7023,#1363,.T.);
#9370=EDGE_CURVE('',#7185,#7181,#1364,.T.);
#9371=EDGE_CURVE('',#7013,#7018,#1365,.T.);
#9372=EDGE_CURVE('',#7184,#7180,#1366,.T.);
#9373=EDGE_CURVE('',#7017,#7012,#1367,.T.);
#9374=EDGE_CURVE('',#7190,#7190,#2522,.T.);
#9375=EDGE_CURVE('',#7190,#7191,#5042,.T.);
#9376=EDGE_CURVE('',#7191,#7191,#2523,.T.);
#9377=EDGE_CURVE('',#7192,#7192,#2524,.T.);
#9378=EDGE_CURVE('',#7192,#7193,#5043,.T.);
#9379=EDGE_CURVE('',#7193,#7193,#2525,.T.);
#9380=EDGE_CURVE('',#7194,#7194,#2526,.T.);
#9381=EDGE_CURVE('',#7194,#7195,#5044,.T.);
#9382=EDGE_CURVE('',#7195,#7195,#2527,.T.);
#9383=EDGE_CURVE('',#7196,#7196,#2528,.T.);
#9384=EDGE_CURVE('',#7196,#7197,#5045,.T.);
#9385=EDGE_CURVE('',#7197,#7197,#2529,.T.);
#9386=EDGE_CURVE('',#7198,#7198,#2530,.T.);
#9387=EDGE_CURVE('',#7198,#7199,#5046,.T.);
#9388=EDGE_CURVE('',#7199,#7199,#2531,.T.);
#9389=EDGE_CURVE('',#7200,#7200,#2532,.T.);
#9390=EDGE_CURVE('',#7200,#7201,#5047,.T.);
#9391=EDGE_CURVE('',#7201,#7201,#2533,.T.);
#9392=EDGE_CURVE('',#7202,#7202,#2534,.T.);
#9393=EDGE_CURVE('',#7203,#7203,#2535,.T.);
#9394=EDGE_CURVE('',#7204,#7204,#2536,.T.);
#9395=EDGE_CURVE('',#7204,#7202,#5048,.T.);
#9396=EDGE_CURVE('',#7205,#7205,#2537,.T.);
#9397=EDGE_CURVE('',#7203,#7205,#5049,.T.);
#12568=ORIENTED_EDGE('',*,*,#8873,.F.);
#12569=ORIENTED_EDGE('',*,*,#8874,.T.);
#12570=ORIENTED_EDGE('',*,*,#8875,.T.);
#12571=ORIENTED_EDGE('',*,*,#8876,.T.);
#12572=ORIENTED_EDGE('',*,*,#8877,.F.);
#12573=ORIENTED_EDGE('',*,*,#8878,.T.);
#12574=ORIENTED_EDGE('',*,*,#8873,.T.);
#12575=ORIENTED_EDGE('',*,*,#8879,.T.);
#12576=ORIENTED_EDGE('',*,*,#8880,.F.);
#12577=ORIENTED_EDGE('',*,*,#8881,.T.);
#12578=ORIENTED_EDGE('',*,*,#8877,.T.);
#12579=ORIENTED_EDGE('',*,*,#8882,.T.);
#12580=ORIENTED_EDGE('',*,*,#8883,.F.);
#12581=ORIENTED_EDGE('',*,*,#8884,.T.);
#12582=ORIENTED_EDGE('',*,*,#8880,.T.);
#12583=ORIENTED_EDGE('',*,*,#8885,.T.);
#12584=ORIENTED_EDGE('',*,*,#8886,.F.);
#12585=ORIENTED_EDGE('',*,*,#8887,.T.);
#12586=ORIENTED_EDGE('',*,*,#8883,.T.);
#12587=ORIENTED_EDGE('',*,*,#8888,.T.);
#12588=ORIENTED_EDGE('',*,*,#8889,.F.);
#12589=ORIENTED_EDGE('',*,*,#8890,.T.);
#12590=ORIENTED_EDGE('',*,*,#8886,.T.);
#12591=ORIENTED_EDGE('',*,*,#8891,.T.);
#12592=ORIENTED_EDGE('',*,*,#8892,.F.);
#12593=ORIENTED_EDGE('',*,*,#8893,.T.);
#12594=ORIENTED_EDGE('',*,*,#8889,.T.);
#12595=ORIENTED_EDGE('',*,*,#8894,.T.);
#12596=ORIENTED_EDGE('',*,*,#8895,.F.);
#12597=ORIENTED_EDGE('',*,*,#8896,.T.);
#12598=ORIENTED_EDGE('',*,*,#8892,.T.);
#12599=ORIENTED_EDGE('',*,*,#8897,.T.);
#12600=ORIENTED_EDGE('',*,*,#8898,.F.);
#12601=ORIENTED_EDGE('',*,*,#8899,.T.);
#12602=ORIENTED_EDGE('',*,*,#8895,.T.);
#12603=ORIENTED_EDGE('',*,*,#8900,.T.);
#12604=ORIENTED_EDGE('',*,*,#8901,.F.);
#12605=ORIENTED_EDGE('',*,*,#8902,.T.);
#12606=ORIENTED_EDGE('',*,*,#8898,.T.);
#12607=ORIENTED_EDGE('',*,*,#8903,.T.);
#12608=ORIENTED_EDGE('',*,*,#8904,.F.);
#12609=ORIENTED_EDGE('',*,*,#8905,.T.);
#12610=ORIENTED_EDGE('',*,*,#8901,.T.);
#12611=ORIENTED_EDGE('',*,*,#8906,.T.);
#12612=ORIENTED_EDGE('',*,*,#8907,.F.);
#12613=ORIENTED_EDGE('',*,*,#8908,.T.);
#12614=ORIENTED_EDGE('',*,*,#8904,.T.);
#12615=ORIENTED_EDGE('',*,*,#8909,.T.);
#12616=ORIENTED_EDGE('',*,*,#8910,.F.);
#12617=ORIENTED_EDGE('',*,*,#8911,.T.);
#12618=ORIENTED_EDGE('',*,*,#8907,.T.);
#12619=ORIENTED_EDGE('',*,*,#8912,.T.);
#12620=ORIENTED_EDGE('',*,*,#8913,.F.);
#12621=ORIENTED_EDGE('',*,*,#8914,.T.);
#12622=ORIENTED_EDGE('',*,*,#8910,.T.);
#12623=ORIENTED_EDGE('',*,*,#8915,.T.);
#12624=ORIENTED_EDGE('',*,*,#8916,.F.);
#12625=ORIENTED_EDGE('',*,*,#8917,.T.);
#12626=ORIENTED_EDGE('',*,*,#8913,.T.);
#12627=ORIENTED_EDGE('',*,*,#8918,.T.);
#12628=ORIENTED_EDGE('',*,*,#8919,.F.);
#12629=ORIENTED_EDGE('',*,*,#8920,.T.);
#12630=ORIENTED_EDGE('',*,*,#8916,.T.);
#12631=ORIENTED_EDGE('',*,*,#8921,.T.);
#12632=ORIENTED_EDGE('',*,*,#8922,.F.);
#12633=ORIENTED_EDGE('',*,*,#8923,.T.);
#12634=ORIENTED_EDGE('',*,*,#8919,.T.);
#12635=ORIENTED_EDGE('',*,*,#8924,.T.);
#12636=ORIENTED_EDGE('',*,*,#8925,.F.);
#12637=ORIENTED_EDGE('',*,*,#8926,.T.);
#12638=ORIENTED_EDGE('',*,*,#8922,.T.);
#12639=ORIENTED_EDGE('',*,*,#8927,.T.);
#12640=ORIENTED_EDGE('',*,*,#8928,.F.);
#12641=ORIENTED_EDGE('',*,*,#8929,.T.);
#12642=ORIENTED_EDGE('',*,*,#8925,.T.);
#12643=ORIENTED_EDGE('',*,*,#8930,.T.);
#12644=ORIENTED_EDGE('',*,*,#8931,.F.);
#12645=ORIENTED_EDGE('',*,*,#8932,.T.);
#12646=ORIENTED_EDGE('',*,*,#8928,.T.);
#12647=ORIENTED_EDGE('',*,*,#8933,.T.);
#12648=ORIENTED_EDGE('',*,*,#8934,.F.);
#12649=ORIENTED_EDGE('',*,*,#8935,.T.);
#12650=ORIENTED_EDGE('',*,*,#8931,.T.);
#12651=ORIENTED_EDGE('',*,*,#8936,.T.);
#12652=ORIENTED_EDGE('',*,*,#8937,.F.);
#12653=ORIENTED_EDGE('',*,*,#8938,.T.);
#12654=ORIENTED_EDGE('',*,*,#8934,.T.);
#12655=ORIENTED_EDGE('',*,*,#8939,.T.);
#12656=ORIENTED_EDGE('',*,*,#8940,.F.);
#12657=ORIENTED_EDGE('',*,*,#8941,.T.);
#12658=ORIENTED_EDGE('',*,*,#8937,.T.);
#12659=ORIENTED_EDGE('',*,*,#8942,.T.);
#12660=ORIENTED_EDGE('',*,*,#8943,.F.);
#12661=ORIENTED_EDGE('',*,*,#8944,.T.);
#12662=ORIENTED_EDGE('',*,*,#8940,.T.);
#12663=ORIENTED_EDGE('',*,*,#8945,.T.);
#12664=ORIENTED_EDGE('',*,*,#8946,.F.);
#12665=ORIENTED_EDGE('',*,*,#8947,.T.);
#12666=ORIENTED_EDGE('',*,*,#8943,.T.);
#12667=ORIENTED_EDGE('',*,*,#8948,.T.);
#12668=ORIENTED_EDGE('',*,*,#8949,.F.);
#12669=ORIENTED_EDGE('',*,*,#8950,.T.);
#12670=ORIENTED_EDGE('',*,*,#8946,.T.);
#12671=ORIENTED_EDGE('',*,*,#8951,.T.);
#12672=ORIENTED_EDGE('',*,*,#8952,.F.);
#12673=ORIENTED_EDGE('',*,*,#8953,.T.);
#12674=ORIENTED_EDGE('',*,*,#8949,.T.);
#12675=ORIENTED_EDGE('',*,*,#8954,.T.);
#12676=ORIENTED_EDGE('',*,*,#8955,.F.);
#12677=ORIENTED_EDGE('',*,*,#8956,.T.);
#12678=ORIENTED_EDGE('',*,*,#8952,.T.);
#12679=ORIENTED_EDGE('',*,*,#8957,.T.);
#12680=ORIENTED_EDGE('',*,*,#8958,.F.);
#12681=ORIENTED_EDGE('',*,*,#8959,.T.);
#12682=ORIENTED_EDGE('',*,*,#8955,.T.);
#12683=ORIENTED_EDGE('',*,*,#8960,.T.);
#12684=ORIENTED_EDGE('',*,*,#8961,.F.);
#12685=ORIENTED_EDGE('',*,*,#8962,.T.);
#12686=ORIENTED_EDGE('',*,*,#8958,.T.);
#12687=ORIENTED_EDGE('',*,*,#8963,.T.);
#12688=ORIENTED_EDGE('',*,*,#8964,.F.);
#12689=ORIENTED_EDGE('',*,*,#8965,.T.);
#12690=ORIENTED_EDGE('',*,*,#8961,.T.);
#12691=ORIENTED_EDGE('',*,*,#8966,.T.);
#12692=ORIENTED_EDGE('',*,*,#8967,.F.);
#12693=ORIENTED_EDGE('',*,*,#8968,.T.);
#12694=ORIENTED_EDGE('',*,*,#8964,.T.);
#12695=ORIENTED_EDGE('',*,*,#8969,.T.);
#12696=ORIENTED_EDGE('',*,*,#8970,.F.);
#12697=ORIENTED_EDGE('',*,*,#8971,.T.);
#12698=ORIENTED_EDGE('',*,*,#8967,.T.);
#12699=ORIENTED_EDGE('',*,*,#8972,.T.);
#12700=ORIENTED_EDGE('',*,*,#8973,.F.);
#12701=ORIENTED_EDGE('',*,*,#8974,.T.);
#12702=ORIENTED_EDGE('',*,*,#8970,.T.);
#12703=ORIENTED_EDGE('',*,*,#8975,.T.);
#12704=ORIENTED_EDGE('',*,*,#8976,.F.);
#12705=ORIENTED_EDGE('',*,*,#8977,.T.);
#12706=ORIENTED_EDGE('',*,*,#8973,.T.);
#12707=ORIENTED_EDGE('',*,*,#8978,.T.);
#12708=ORIENTED_EDGE('',*,*,#8979,.F.);
#12709=ORIENTED_EDGE('',*,*,#8980,.T.);
#12710=ORIENTED_EDGE('',*,*,#8976,.T.);
#12711=ORIENTED_EDGE('',*,*,#8981,.T.);
#12712=ORIENTED_EDGE('',*,*,#8982,.F.);
#12713=ORIENTED_EDGE('',*,*,#8983,.T.);
#12714=ORIENTED_EDGE('',*,*,#8979,.T.);
#12715=ORIENTED_EDGE('',*,*,#8984,.T.);
#12716=ORIENTED_EDGE('',*,*,#8985,.F.);
#12717=ORIENTED_EDGE('',*,*,#8986,.T.);
#12718=ORIENTED_EDGE('',*,*,#8982,.T.);
#12719=ORIENTED_EDGE('',*,*,#8987,.T.);
#12720=ORIENTED_EDGE('',*,*,#8988,.F.);
#12721=ORIENTED_EDGE('',*,*,#8989,.T.);
#12722=ORIENTED_EDGE('',*,*,#8985,.T.);
#12723=ORIENTED_EDGE('',*,*,#8990,.T.);
#12724=ORIENTED_EDGE('',*,*,#8991,.F.);
#12725=ORIENTED_EDGE('',*,*,#8992,.T.);
#12726=ORIENTED_EDGE('',*,*,#8988,.T.);
#12727=ORIENTED_EDGE('',*,*,#8993,.T.);
#12728=ORIENTED_EDGE('',*,*,#8994,.F.);
#12729=ORIENTED_EDGE('',*,*,#8995,.T.);
#12730=ORIENTED_EDGE('',*,*,#8991,.T.);
#12731=ORIENTED_EDGE('',*,*,#8996,.T.);
#12732=ORIENTED_EDGE('',*,*,#8997,.F.);
#12733=ORIENTED_EDGE('',*,*,#8998,.T.);
#12734=ORIENTED_EDGE('',*,*,#8994,.T.);
#12735=ORIENTED_EDGE('',*,*,#8999,.T.);
#12736=ORIENTED_EDGE('',*,*,#9000,.F.);
#12737=ORIENTED_EDGE('',*,*,#9001,.T.);
#12738=ORIENTED_EDGE('',*,*,#8997,.T.);
#12739=ORIENTED_EDGE('',*,*,#9002,.T.);
#12740=ORIENTED_EDGE('',*,*,#9003,.F.);
#12741=ORIENTED_EDGE('',*,*,#9004,.T.);
#12742=ORIENTED_EDGE('',*,*,#9000,.T.);
#12743=ORIENTED_EDGE('',*,*,#9005,.T.);
#12744=ORIENTED_EDGE('',*,*,#9006,.F.);
#12745=ORIENTED_EDGE('',*,*,#9007,.T.);
#12746=ORIENTED_EDGE('',*,*,#9003,.T.);
#12747=ORIENTED_EDGE('',*,*,#9008,.T.);
#12748=ORIENTED_EDGE('',*,*,#9009,.F.);
#12749=ORIENTED_EDGE('',*,*,#9010,.T.);
#12750=ORIENTED_EDGE('',*,*,#9006,.T.);
#12751=ORIENTED_EDGE('',*,*,#9011,.T.);
#12752=ORIENTED_EDGE('',*,*,#9012,.F.);
#12753=ORIENTED_EDGE('',*,*,#9013,.T.);
#12754=ORIENTED_EDGE('',*,*,#9009,.T.);
#12755=ORIENTED_EDGE('',*,*,#9014,.T.);
#12756=ORIENTED_EDGE('',*,*,#9015,.F.);
#12757=ORIENTED_EDGE('',*,*,#9016,.T.);
#12758=ORIENTED_EDGE('',*,*,#9012,.T.);
#12759=ORIENTED_EDGE('',*,*,#9017,.T.);
#12760=ORIENTED_EDGE('',*,*,#9018,.F.);
#12761=ORIENTED_EDGE('',*,*,#9019,.T.);
#12762=ORIENTED_EDGE('',*,*,#9015,.T.);
#12763=ORIENTED_EDGE('',*,*,#9020,.T.);
#12764=ORIENTED_EDGE('',*,*,#9021,.F.);
#12765=ORIENTED_EDGE('',*,*,#9022,.T.);
#12766=ORIENTED_EDGE('',*,*,#9018,.T.);
#12767=ORIENTED_EDGE('',*,*,#9023,.T.);
#12768=ORIENTED_EDGE('',*,*,#9024,.F.);
#12769=ORIENTED_EDGE('',*,*,#9025,.T.);
#12770=ORIENTED_EDGE('',*,*,#9021,.T.);
#12771=ORIENTED_EDGE('',*,*,#9026,.T.);
#12772=ORIENTED_EDGE('',*,*,#9027,.F.);
#12773=ORIENTED_EDGE('',*,*,#9028,.T.);
#12774=ORIENTED_EDGE('',*,*,#9024,.T.);
#12775=ORIENTED_EDGE('',*,*,#9029,.T.);
#12776=ORIENTED_EDGE('',*,*,#9030,.F.);
#12777=ORIENTED_EDGE('',*,*,#9031,.T.);
#12778=ORIENTED_EDGE('',*,*,#9027,.T.);
#12779=ORIENTED_EDGE('',*,*,#9032,.T.);
#12780=ORIENTED_EDGE('',*,*,#9033,.F.);
#12781=ORIENTED_EDGE('',*,*,#9034,.T.);
#12782=ORIENTED_EDGE('',*,*,#9030,.T.);
#12783=ORIENTED_EDGE('',*,*,#9035,.T.);
#12784=ORIENTED_EDGE('',*,*,#9036,.F.);
#12785=ORIENTED_EDGE('',*,*,#9037,.T.);
#12786=ORIENTED_EDGE('',*,*,#9033,.T.);
#12787=ORIENTED_EDGE('',*,*,#9038,.T.);
#12788=ORIENTED_EDGE('',*,*,#9039,.F.);
#12789=ORIENTED_EDGE('',*,*,#9040,.T.);
#12790=ORIENTED_EDGE('',*,*,#9036,.T.);
#12791=ORIENTED_EDGE('',*,*,#9041,.T.);
#12792=ORIENTED_EDGE('',*,*,#9042,.F.);
#12793=ORIENTED_EDGE('',*,*,#9043,.T.);
#12794=ORIENTED_EDGE('',*,*,#9039,.T.);
#12795=ORIENTED_EDGE('',*,*,#9044,.T.);
#12796=ORIENTED_EDGE('',*,*,#9045,.F.);
#12797=ORIENTED_EDGE('',*,*,#9046,.T.);
#12798=ORIENTED_EDGE('',*,*,#9042,.T.);
#12799=ORIENTED_EDGE('',*,*,#9047,.T.);
#12800=ORIENTED_EDGE('',*,*,#9048,.F.);
#12801=ORIENTED_EDGE('',*,*,#9049,.T.);
#12802=ORIENTED_EDGE('',*,*,#9045,.T.);
#12803=ORIENTED_EDGE('',*,*,#9050,.T.);
#12804=ORIENTED_EDGE('',*,*,#9051,.F.);
#12805=ORIENTED_EDGE('',*,*,#9052,.T.);
#12806=ORIENTED_EDGE('',*,*,#9048,.T.);
#12807=ORIENTED_EDGE('',*,*,#9053,.T.);
#12808=ORIENTED_EDGE('',*,*,#9054,.F.);
#12809=ORIENTED_EDGE('',*,*,#9055,.T.);
#12810=ORIENTED_EDGE('',*,*,#9051,.T.);
#12811=ORIENTED_EDGE('',*,*,#9056,.T.);
#12812=ORIENTED_EDGE('',*,*,#9057,.F.);
#12813=ORIENTED_EDGE('',*,*,#9058,.T.);
#12814=ORIENTED_EDGE('',*,*,#9054,.T.);
#12815=ORIENTED_EDGE('',*,*,#9059,.T.);
#12816=ORIENTED_EDGE('',*,*,#9060,.F.);
#12817=ORIENTED_EDGE('',*,*,#9061,.T.);
#12818=ORIENTED_EDGE('',*,*,#9057,.T.);
#12819=ORIENTED_EDGE('',*,*,#9062,.T.);
#12820=ORIENTED_EDGE('',*,*,#9063,.F.);
#12821=ORIENTED_EDGE('',*,*,#9064,.T.);
#12822=ORIENTED_EDGE('',*,*,#9060,.T.);
#12823=ORIENTED_EDGE('',*,*,#9065,.T.);
#12824=ORIENTED_EDGE('',*,*,#9066,.F.);
#12825=ORIENTED_EDGE('',*,*,#9067,.T.);
#12826=ORIENTED_EDGE('',*,*,#9063,.T.);
#12827=ORIENTED_EDGE('',*,*,#9068,.T.);
#12828=ORIENTED_EDGE('',*,*,#9069,.F.);
#12829=ORIENTED_EDGE('',*,*,#9070,.T.);
#12830=ORIENTED_EDGE('',*,*,#9066,.T.);
#12831=ORIENTED_EDGE('',*,*,#9071,.T.);
#12832=ORIENTED_EDGE('',*,*,#9072,.F.);
#12833=ORIENTED_EDGE('',*,*,#9073,.T.);
#12834=ORIENTED_EDGE('',*,*,#9069,.T.);
#12835=ORIENTED_EDGE('',*,*,#9074,.T.);
#12836=ORIENTED_EDGE('',*,*,#9075,.F.);
#12837=ORIENTED_EDGE('',*,*,#9076,.T.);
#12838=ORIENTED_EDGE('',*,*,#9072,.T.);
#12839=ORIENTED_EDGE('',*,*,#9077,.T.);
#12840=ORIENTED_EDGE('',*,*,#9078,.F.);
#12841=ORIENTED_EDGE('',*,*,#9079,.T.);
#12842=ORIENTED_EDGE('',*,*,#9075,.T.);
#12843=ORIENTED_EDGE('',*,*,#9080,.T.);
#12844=ORIENTED_EDGE('',*,*,#9081,.F.);
#12845=ORIENTED_EDGE('',*,*,#9082,.T.);
#12846=ORIENTED_EDGE('',*,*,#9078,.T.);
#12847=ORIENTED_EDGE('',*,*,#9083,.T.);
#12848=ORIENTED_EDGE('',*,*,#9084,.F.);
#12849=ORIENTED_EDGE('',*,*,#9085,.T.);
#12850=ORIENTED_EDGE('',*,*,#9081,.T.);
#12851=ORIENTED_EDGE('',*,*,#9086,.T.);
#12852=ORIENTED_EDGE('',*,*,#9087,.F.);
#12853=ORIENTED_EDGE('',*,*,#9088,.T.);
#12854=ORIENTED_EDGE('',*,*,#9084,.T.);
#12855=ORIENTED_EDGE('',*,*,#9089,.T.);
#12856=ORIENTED_EDGE('',*,*,#9090,.F.);
#12857=ORIENTED_EDGE('',*,*,#9091,.T.);
#12858=ORIENTED_EDGE('',*,*,#9087,.T.);
#12859=ORIENTED_EDGE('',*,*,#9092,.T.);
#12860=ORIENTED_EDGE('',*,*,#9093,.F.);
#12861=ORIENTED_EDGE('',*,*,#9094,.T.);
#12862=ORIENTED_EDGE('',*,*,#9090,.T.);
#12863=ORIENTED_EDGE('',*,*,#9095,.T.);
#12864=ORIENTED_EDGE('',*,*,#9096,.F.);
#12865=ORIENTED_EDGE('',*,*,#9097,.T.);
#12866=ORIENTED_EDGE('',*,*,#9093,.T.);
#12867=ORIENTED_EDGE('',*,*,#9098,.T.);
#12868=ORIENTED_EDGE('',*,*,#9099,.F.);
#12869=ORIENTED_EDGE('',*,*,#9100,.T.);
#12870=ORIENTED_EDGE('',*,*,#9096,.T.);
#12871=ORIENTED_EDGE('',*,*,#9101,.T.);
#12872=ORIENTED_EDGE('',*,*,#9102,.F.);
#12873=ORIENTED_EDGE('',*,*,#9103,.T.);
#12874=ORIENTED_EDGE('',*,*,#9099,.T.);
#12875=ORIENTED_EDGE('',*,*,#9104,.T.);
#12876=ORIENTED_EDGE('',*,*,#9105,.F.);
#12877=ORIENTED_EDGE('',*,*,#9106,.T.);
#12878=ORIENTED_EDGE('',*,*,#9102,.T.);
#12879=ORIENTED_EDGE('',*,*,#9107,.T.);
#12880=ORIENTED_EDGE('',*,*,#9108,.T.);
#12881=ORIENTED_EDGE('',*,*,#9109,.T.);
#12882=ORIENTED_EDGE('',*,*,#9110,.T.);
#12883=ORIENTED_EDGE('',*,*,#9111,.T.);
#12884=ORIENTED_EDGE('',*,*,#9112,.T.);
#12885=ORIENTED_EDGE('',*,*,#9113,.T.);
#12886=ORIENTED_EDGE('',*,*,#9114,.T.);
#12887=ORIENTED_EDGE('',*,*,#9109,.F.);
#12888=ORIENTED_EDGE('',*,*,#9115,.F.);
#12889=ORIENTED_EDGE('',*,*,#9116,.T.);
#12890=ORIENTED_EDGE('',*,*,#9117,.F.);
#12891=ORIENTED_EDGE('',*,*,#9118,.F.);
#12892=ORIENTED_EDGE('',*,*,#9119,.F.);
#12893=ORIENTED_EDGE('',*,*,#9120,.T.);
#12894=ORIENTED_EDGE('',*,*,#9115,.T.);
#12895=ORIENTED_EDGE('',*,*,#9121,.F.);
#12896=ORIENTED_EDGE('',*,*,#9122,.F.);
#12897=ORIENTED_EDGE('',*,*,#9123,.T.);
#12898=ORIENTED_EDGE('',*,*,#9119,.T.);
#12899=ORIENTED_EDGE('',*,*,#9124,.F.);
#12900=ORIENTED_EDGE('',*,*,#9125,.F.);
#12901=ORIENTED_EDGE('',*,*,#9126,.T.);
#12902=ORIENTED_EDGE('',*,*,#9122,.T.);
#12903=ORIENTED_EDGE('',*,*,#9127,.F.);
#12904=ORIENTED_EDGE('',*,*,#9128,.F.);
#12905=ORIENTED_EDGE('',*,*,#9129,.T.);
#12906=ORIENTED_EDGE('',*,*,#9125,.T.);
#12907=ORIENTED_EDGE('',*,*,#9130,.F.);
#12908=ORIENTED_EDGE('',*,*,#9131,.F.);
#12909=ORIENTED_EDGE('',*,*,#9132,.T.);
#12910=ORIENTED_EDGE('',*,*,#9128,.T.);
#12911=ORIENTED_EDGE('',*,*,#9133,.F.);
#12912=ORIENTED_EDGE('',*,*,#9134,.F.);
#12913=ORIENTED_EDGE('',*,*,#9135,.T.);
#12914=ORIENTED_EDGE('',*,*,#9131,.T.);
#12915=ORIENTED_EDGE('',*,*,#9136,.F.);
#12916=ORIENTED_EDGE('',*,*,#9137,.F.);
#12917=ORIENTED_EDGE('',*,*,#9138,.T.);
#12918=ORIENTED_EDGE('',*,*,#9134,.T.);
#12919=ORIENTED_EDGE('',*,*,#9139,.F.);
#12920=ORIENTED_EDGE('',*,*,#9140,.F.);
#12921=ORIENTED_EDGE('',*,*,#9141,.T.);
#12922=ORIENTED_EDGE('',*,*,#9137,.T.);
#12923=ORIENTED_EDGE('',*,*,#9142,.F.);
#12924=ORIENTED_EDGE('',*,*,#9143,.F.);
#12925=ORIENTED_EDGE('',*,*,#9144,.T.);
#12926=ORIENTED_EDGE('',*,*,#9140,.T.);
#12927=ORIENTED_EDGE('',*,*,#9145,.F.);
#12928=ORIENTED_EDGE('',*,*,#9146,.F.);
#12929=ORIENTED_EDGE('',*,*,#9147,.T.);
#12930=ORIENTED_EDGE('',*,*,#9143,.T.);
#12931=ORIENTED_EDGE('',*,*,#9148,.F.);
#12932=ORIENTED_EDGE('',*,*,#9149,.F.);
#12933=ORIENTED_EDGE('',*,*,#9150,.T.);
#12934=ORIENTED_EDGE('',*,*,#9146,.T.);
#12935=ORIENTED_EDGE('',*,*,#9151,.F.);
#12936=ORIENTED_EDGE('',*,*,#9152,.F.);
#12937=ORIENTED_EDGE('',*,*,#9153,.T.);
#12938=ORIENTED_EDGE('',*,*,#9149,.T.);
#12939=ORIENTED_EDGE('',*,*,#9154,.F.);
#12940=ORIENTED_EDGE('',*,*,#9155,.F.);
#12941=ORIENTED_EDGE('',*,*,#9156,.T.);
#12942=ORIENTED_EDGE('',*,*,#9152,.T.);
#12943=ORIENTED_EDGE('',*,*,#9157,.F.);
#12944=ORIENTED_EDGE('',*,*,#9158,.F.);
#12945=ORIENTED_EDGE('',*,*,#9159,.T.);
#12946=ORIENTED_EDGE('',*,*,#9155,.T.);
#12947=ORIENTED_EDGE('',*,*,#9160,.F.);
#12948=ORIENTED_EDGE('',*,*,#9161,.F.);
#12949=ORIENTED_EDGE('',*,*,#9162,.T.);
#12950=ORIENTED_EDGE('',*,*,#9158,.T.);
#12951=ORIENTED_EDGE('',*,*,#9163,.F.);
#12952=ORIENTED_EDGE('',*,*,#9164,.F.);
#12953=ORIENTED_EDGE('',*,*,#9165,.T.);
#12954=ORIENTED_EDGE('',*,*,#9161,.T.);
#12955=ORIENTED_EDGE('',*,*,#9166,.F.);
#12956=ORIENTED_EDGE('',*,*,#9167,.F.);
#12957=ORIENTED_EDGE('',*,*,#9168,.T.);
#12958=ORIENTED_EDGE('',*,*,#9164,.T.);
#12959=ORIENTED_EDGE('',*,*,#9169,.F.);
#12960=ORIENTED_EDGE('',*,*,#9170,.F.);
#12961=ORIENTED_EDGE('',*,*,#9171,.T.);
#12962=ORIENTED_EDGE('',*,*,#9167,.T.);
#12963=ORIENTED_EDGE('',*,*,#9172,.F.);
#12964=ORIENTED_EDGE('',*,*,#9173,.F.);
#12965=ORIENTED_EDGE('',*,*,#9174,.T.);
#12966=ORIENTED_EDGE('',*,*,#9170,.T.);
#12967=ORIENTED_EDGE('',*,*,#9175,.F.);
#12968=ORIENTED_EDGE('',*,*,#9176,.F.);
#12969=ORIENTED_EDGE('',*,*,#9177,.T.);
#12970=ORIENTED_EDGE('',*,*,#9173,.T.);
#12971=ORIENTED_EDGE('',*,*,#9178,.F.);
#12972=ORIENTED_EDGE('',*,*,#9179,.F.);
#12973=ORIENTED_EDGE('',*,*,#9180,.T.);
#12974=ORIENTED_EDGE('',*,*,#9176,.T.);
#12975=ORIENTED_EDGE('',*,*,#9181,.F.);
#12976=ORIENTED_EDGE('',*,*,#9182,.F.);
#12977=ORIENTED_EDGE('',*,*,#9183,.T.);
#12978=ORIENTED_EDGE('',*,*,#9179,.T.);
#12979=ORIENTED_EDGE('',*,*,#9184,.F.);
#12980=ORIENTED_EDGE('',*,*,#9185,.F.);
#12981=ORIENTED_EDGE('',*,*,#9186,.T.);
#12982=ORIENTED_EDGE('',*,*,#9182,.T.);
#12983=ORIENTED_EDGE('',*,*,#9187,.F.);
#12984=ORIENTED_EDGE('',*,*,#9188,.F.);
#12985=ORIENTED_EDGE('',*,*,#9189,.T.);
#12986=ORIENTED_EDGE('',*,*,#9185,.T.);
#12987=ORIENTED_EDGE('',*,*,#9190,.F.);
#12988=ORIENTED_EDGE('',*,*,#9191,.F.);
#12989=ORIENTED_EDGE('',*,*,#9192,.T.);
#12990=ORIENTED_EDGE('',*,*,#9188,.T.);
#12991=ORIENTED_EDGE('',*,*,#9193,.F.);
#12992=ORIENTED_EDGE('',*,*,#9194,.F.);
#12993=ORIENTED_EDGE('',*,*,#9195,.T.);
#12994=ORIENTED_EDGE('',*,*,#9191,.T.);
#12995=ORIENTED_EDGE('',*,*,#9196,.F.);
#12996=ORIENTED_EDGE('',*,*,#9197,.F.);
#12997=ORIENTED_EDGE('',*,*,#9198,.T.);
#12998=ORIENTED_EDGE('',*,*,#9194,.T.);
#12999=ORIENTED_EDGE('',*,*,#9199,.F.);
#13000=ORIENTED_EDGE('',*,*,#9200,.F.);
#13001=ORIENTED_EDGE('',*,*,#9201,.T.);
#13002=ORIENTED_EDGE('',*,*,#9197,.T.);
#13003=ORIENTED_EDGE('',*,*,#9202,.F.);
#13004=ORIENTED_EDGE('',*,*,#9203,.F.);
#13005=ORIENTED_EDGE('',*,*,#9204,.T.);
#13006=ORIENTED_EDGE('',*,*,#9200,.T.);
#13007=ORIENTED_EDGE('',*,*,#9205,.F.);
#13008=ORIENTED_EDGE('',*,*,#9206,.F.);
#13009=ORIENTED_EDGE('',*,*,#9207,.T.);
#13010=ORIENTED_EDGE('',*,*,#9203,.T.);
#13011=ORIENTED_EDGE('',*,*,#9208,.F.);
#13012=ORIENTED_EDGE('',*,*,#9209,.F.);
#13013=ORIENTED_EDGE('',*,*,#9210,.T.);
#13014=ORIENTED_EDGE('',*,*,#9206,.T.);
#13015=ORIENTED_EDGE('',*,*,#9211,.F.);
#13016=ORIENTED_EDGE('',*,*,#9212,.F.);
#13017=ORIENTED_EDGE('',*,*,#9213,.T.);
#13018=ORIENTED_EDGE('',*,*,#9209,.T.);
#13019=ORIENTED_EDGE('',*,*,#9214,.F.);
#13020=ORIENTED_EDGE('',*,*,#9215,.F.);
#13021=ORIENTED_EDGE('',*,*,#9216,.T.);
#13022=ORIENTED_EDGE('',*,*,#9212,.T.);
#13023=ORIENTED_EDGE('',*,*,#9217,.F.);
#13024=ORIENTED_EDGE('',*,*,#9218,.F.);
#13025=ORIENTED_EDGE('',*,*,#9219,.T.);
#13026=ORIENTED_EDGE('',*,*,#9215,.T.);
#13027=ORIENTED_EDGE('',*,*,#9220,.F.);
#13028=ORIENTED_EDGE('',*,*,#9221,.F.);
#13029=ORIENTED_EDGE('',*,*,#9222,.T.);
#13030=ORIENTED_EDGE('',*,*,#9218,.T.);
#13031=ORIENTED_EDGE('',*,*,#9223,.F.);
#13032=ORIENTED_EDGE('',*,*,#9224,.F.);
#13033=ORIENTED_EDGE('',*,*,#9225,.T.);
#13034=ORIENTED_EDGE('',*,*,#9221,.T.);
#13035=ORIENTED_EDGE('',*,*,#9226,.F.);
#13036=ORIENTED_EDGE('',*,*,#9227,.F.);
#13037=ORIENTED_EDGE('',*,*,#9228,.T.);
#13038=ORIENTED_EDGE('',*,*,#9224,.T.);
#13039=ORIENTED_EDGE('',*,*,#9229,.F.);
#13040=ORIENTED_EDGE('',*,*,#9230,.F.);
#13041=ORIENTED_EDGE('',*,*,#9231,.T.);
#13042=ORIENTED_EDGE('',*,*,#9227,.T.);
#13043=ORIENTED_EDGE('',*,*,#9232,.F.);
#13044=ORIENTED_EDGE('',*,*,#9233,.F.);
#13045=ORIENTED_EDGE('',*,*,#9234,.T.);
#13046=ORIENTED_EDGE('',*,*,#9230,.T.);
#13047=ORIENTED_EDGE('',*,*,#9235,.F.);
#13048=ORIENTED_EDGE('',*,*,#9236,.F.);
#13049=ORIENTED_EDGE('',*,*,#9237,.T.);
#13050=ORIENTED_EDGE('',*,*,#9233,.T.);
#13051=ORIENTED_EDGE('',*,*,#9238,.F.);
#13052=ORIENTED_EDGE('',*,*,#9239,.F.);
#13053=ORIENTED_EDGE('',*,*,#9240,.T.);
#13054=ORIENTED_EDGE('',*,*,#9236,.T.);
#13055=ORIENTED_EDGE('',*,*,#9241,.F.);
#13056=ORIENTED_EDGE('',*,*,#9242,.F.);
#13057=ORIENTED_EDGE('',*,*,#9243,.T.);
#13058=ORIENTED_EDGE('',*,*,#9239,.T.);
#13059=ORIENTED_EDGE('',*,*,#9244,.F.);
#13060=ORIENTED_EDGE('',*,*,#9245,.F.);
#13061=ORIENTED_EDGE('',*,*,#9246,.T.);
#13062=ORIENTED_EDGE('',*,*,#9242,.T.);
#13063=ORIENTED_EDGE('',*,*,#9247,.F.);
#13064=ORIENTED_EDGE('',*,*,#9248,.F.);
#13065=ORIENTED_EDGE('',*,*,#9249,.T.);
#13066=ORIENTED_EDGE('',*,*,#9245,.T.);
#13067=ORIENTED_EDGE('',*,*,#9250,.F.);
#13068=ORIENTED_EDGE('',*,*,#9251,.F.);
#13069=ORIENTED_EDGE('',*,*,#9252,.T.);
#13070=ORIENTED_EDGE('',*,*,#9248,.T.);
#13071=ORIENTED_EDGE('',*,*,#9253,.F.);
#13072=ORIENTED_EDGE('',*,*,#9254,.F.);
#13073=ORIENTED_EDGE('',*,*,#9255,.T.);
#13074=ORIENTED_EDGE('',*,*,#9251,.T.);
#13075=ORIENTED_EDGE('',*,*,#9256,.F.);
#13076=ORIENTED_EDGE('',*,*,#9257,.F.);
#13077=ORIENTED_EDGE('',*,*,#9258,.T.);
#13078=ORIENTED_EDGE('',*,*,#9254,.T.);
#13079=ORIENTED_EDGE('',*,*,#9259,.F.);
#13080=ORIENTED_EDGE('',*,*,#9260,.F.);
#13081=ORIENTED_EDGE('',*,*,#9261,.T.);
#13082=ORIENTED_EDGE('',*,*,#9257,.T.);
#13083=ORIENTED_EDGE('',*,*,#9262,.F.);
#13084=ORIENTED_EDGE('',*,*,#9263,.F.);
#13085=ORIENTED_EDGE('',*,*,#9264,.T.);
#13086=ORIENTED_EDGE('',*,*,#9260,.T.);
#13087=ORIENTED_EDGE('',*,*,#9265,.F.);
#13088=ORIENTED_EDGE('',*,*,#9266,.F.);
#13089=ORIENTED_EDGE('',*,*,#9267,.T.);
#13090=ORIENTED_EDGE('',*,*,#9263,.T.);
#13091=ORIENTED_EDGE('',*,*,#9268,.F.);
#13092=ORIENTED_EDGE('',*,*,#9269,.F.);
#13093=ORIENTED_EDGE('',*,*,#9270,.T.);
#13094=ORIENTED_EDGE('',*,*,#9266,.T.);
#13095=ORIENTED_EDGE('',*,*,#9271,.F.);
#13096=ORIENTED_EDGE('',*,*,#9272,.F.);
#13097=ORIENTED_EDGE('',*,*,#9273,.T.);
#13098=ORIENTED_EDGE('',*,*,#9269,.T.);
#13099=ORIENTED_EDGE('',*,*,#9274,.F.);
#13100=ORIENTED_EDGE('',*,*,#9275,.F.);
#13101=ORIENTED_EDGE('',*,*,#9276,.T.);
#13102=ORIENTED_EDGE('',*,*,#9272,.T.);
#13103=ORIENTED_EDGE('',*,*,#9277,.F.);
#13104=ORIENTED_EDGE('',*,*,#9278,.F.);
#13105=ORIENTED_EDGE('',*,*,#9279,.T.);
#13106=ORIENTED_EDGE('',*,*,#9275,.T.);
#13107=ORIENTED_EDGE('',*,*,#9280,.F.);
#13108=ORIENTED_EDGE('',*,*,#9281,.F.);
#13109=ORIENTED_EDGE('',*,*,#9282,.T.);
#13110=ORIENTED_EDGE('',*,*,#9278,.T.);
#13111=ORIENTED_EDGE('',*,*,#9283,.F.);
#13112=ORIENTED_EDGE('',*,*,#9284,.F.);
#13113=ORIENTED_EDGE('',*,*,#9285,.T.);
#13114=ORIENTED_EDGE('',*,*,#9281,.T.);
#13115=ORIENTED_EDGE('',*,*,#9286,.F.);
#13116=ORIENTED_EDGE('',*,*,#9287,.F.);
#13117=ORIENTED_EDGE('',*,*,#9288,.T.);
#13118=ORIENTED_EDGE('',*,*,#9284,.T.);
#13119=ORIENTED_EDGE('',*,*,#9289,.F.);
#13120=ORIENTED_EDGE('',*,*,#9290,.F.);
#13121=ORIENTED_EDGE('',*,*,#9291,.T.);
#13122=ORIENTED_EDGE('',*,*,#9287,.T.);
#13123=ORIENTED_EDGE('',*,*,#9292,.F.);
#13124=ORIENTED_EDGE('',*,*,#9293,.F.);
#13125=ORIENTED_EDGE('',*,*,#9294,.T.);
#13126=ORIENTED_EDGE('',*,*,#9290,.T.);
#13127=ORIENTED_EDGE('',*,*,#9295,.F.);
#13128=ORIENTED_EDGE('',*,*,#9296,.F.);
#13129=ORIENTED_EDGE('',*,*,#9297,.T.);
#13130=ORIENTED_EDGE('',*,*,#9293,.T.);
#13131=ORIENTED_EDGE('',*,*,#9298,.F.);
#13132=ORIENTED_EDGE('',*,*,#9299,.F.);
#13133=ORIENTED_EDGE('',*,*,#9300,.T.);
#13134=ORIENTED_EDGE('',*,*,#9296,.T.);
#13135=ORIENTED_EDGE('',*,*,#9301,.F.);
#13136=ORIENTED_EDGE('',*,*,#9302,.F.);
#13137=ORIENTED_EDGE('',*,*,#9303,.T.);
#13138=ORIENTED_EDGE('',*,*,#9299,.T.);
#13139=ORIENTED_EDGE('',*,*,#9304,.F.);
#13140=ORIENTED_EDGE('',*,*,#9305,.F.);
#13141=ORIENTED_EDGE('',*,*,#9306,.T.);
#13142=ORIENTED_EDGE('',*,*,#9302,.T.);
#13143=ORIENTED_EDGE('',*,*,#9307,.F.);
#13144=ORIENTED_EDGE('',*,*,#9308,.F.);
#13145=ORIENTED_EDGE('',*,*,#9309,.T.);
#13146=ORIENTED_EDGE('',*,*,#9305,.T.);
#13147=ORIENTED_EDGE('',*,*,#9310,.F.);
#13148=ORIENTED_EDGE('',*,*,#9311,.F.);
#13149=ORIENTED_EDGE('',*,*,#9312,.T.);
#13150=ORIENTED_EDGE('',*,*,#9308,.T.);
#13151=ORIENTED_EDGE('',*,*,#9313,.F.);
#13152=ORIENTED_EDGE('',*,*,#9314,.F.);
#13153=ORIENTED_EDGE('',*,*,#9315,.T.);
#13154=ORIENTED_EDGE('',*,*,#9311,.T.);
#13155=ORIENTED_EDGE('',*,*,#9316,.F.);
#13156=ORIENTED_EDGE('',*,*,#9317,.F.);
#13157=ORIENTED_EDGE('',*,*,#9318,.T.);
#13158=ORIENTED_EDGE('',*,*,#9314,.T.);
#13159=ORIENTED_EDGE('',*,*,#9319,.F.);
#13160=ORIENTED_EDGE('',*,*,#9320,.F.);
#13161=ORIENTED_EDGE('',*,*,#9321,.T.);
#13162=ORIENTED_EDGE('',*,*,#9317,.T.);
#13163=ORIENTED_EDGE('',*,*,#9322,.F.);
#13164=ORIENTED_EDGE('',*,*,#9323,.F.);
#13165=ORIENTED_EDGE('',*,*,#9324,.T.);
#13166=ORIENTED_EDGE('',*,*,#9320,.T.);
#13167=ORIENTED_EDGE('',*,*,#9325,.F.);
#13168=ORIENTED_EDGE('',*,*,#9326,.F.);
#13169=ORIENTED_EDGE('',*,*,#9327,.T.);
#13170=ORIENTED_EDGE('',*,*,#9323,.T.);
#13171=ORIENTED_EDGE('',*,*,#9328,.F.);
#13172=ORIENTED_EDGE('',*,*,#9329,.F.);
#13173=ORIENTED_EDGE('',*,*,#9330,.T.);
#13174=ORIENTED_EDGE('',*,*,#9326,.T.);
#13175=ORIENTED_EDGE('',*,*,#9331,.F.);
#13176=ORIENTED_EDGE('',*,*,#9332,.F.);
#13177=ORIENTED_EDGE('',*,*,#9333,.T.);
#13178=ORIENTED_EDGE('',*,*,#9329,.T.);
#13179=ORIENTED_EDGE('',*,*,#9334,.F.);
#13180=ORIENTED_EDGE('',*,*,#9335,.F.);
#13181=ORIENTED_EDGE('',*,*,#9336,.T.);
#13182=ORIENTED_EDGE('',*,*,#9332,.T.);
#13183=ORIENTED_EDGE('',*,*,#9337,.F.);
#13184=ORIENTED_EDGE('',*,*,#9338,.F.);
#13185=ORIENTED_EDGE('',*,*,#9339,.T.);
#13186=ORIENTED_EDGE('',*,*,#9335,.T.);
#13187=ORIENTED_EDGE('',*,*,#9340,.F.);
#13188=ORIENTED_EDGE('',*,*,#9341,.F.);
#13189=ORIENTED_EDGE('',*,*,#9342,.T.);
#13190=ORIENTED_EDGE('',*,*,#9338,.T.);
#13191=ORIENTED_EDGE('',*,*,#9343,.F.);
#13192=ORIENTED_EDGE('',*,*,#9344,.F.);
#13193=ORIENTED_EDGE('',*,*,#9345,.T.);
#13194=ORIENTED_EDGE('',*,*,#9341,.T.);
#13195=ORIENTED_EDGE('',*,*,#9346,.F.);
#13196=ORIENTED_EDGE('',*,*,#9347,.F.);
#13197=ORIENTED_EDGE('',*,*,#9348,.T.);
#13198=ORIENTED_EDGE('',*,*,#9344,.T.);
#13199=ORIENTED_EDGE('',*,*,#9349,.F.);
#13200=ORIENTED_EDGE('',*,*,#9350,.F.);
#13201=ORIENTED_EDGE('',*,*,#9351,.T.);
#13202=ORIENTED_EDGE('',*,*,#9347,.T.);
#13203=ORIENTED_EDGE('',*,*,#9352,.F.);
#13204=ORIENTED_EDGE('',*,*,#9353,.F.);
#13205=ORIENTED_EDGE('',*,*,#9354,.T.);
#13206=ORIENTED_EDGE('',*,*,#9350,.T.);
#13207=ORIENTED_EDGE('',*,*,#9355,.F.);
#13208=ORIENTED_EDGE('',*,*,#9356,.F.);
#13209=ORIENTED_EDGE('',*,*,#8875,.F.);
#13210=ORIENTED_EDGE('',*,*,#9357,.F.);
#13211=ORIENTED_EDGE('',*,*,#9358,.F.);
#13212=ORIENTED_EDGE('',*,*,#9358,.T.);
#13213=ORIENTED_EDGE('',*,*,#9359,.T.);
#13214=ORIENTED_EDGE('',*,*,#9360,.T.);
#13215=ORIENTED_EDGE('',*,*,#9361,.T.);
#13216=ORIENTED_EDGE('',*,*,#9362,.T.);
#13217=ORIENTED_EDGE('',*,*,#9363,.T.);
#13218=ORIENTED_EDGE('',*,*,#9364,.F.);
#13219=ORIENTED_EDGE('',*,*,#9363,.F.);
#13220=ORIENTED_EDGE('',*,*,#9108,.F.);
#13221=ORIENTED_EDGE('',*,*,#9362,.F.);
#13222=ORIENTED_EDGE('',*,*,#9365,.F.);
#13223=ORIENTED_EDGE('',*,*,#9364,.T.);
#13224=ORIENTED_EDGE('',*,*,#9366,.T.);
#13225=ORIENTED_EDGE('',*,*,#9367,.T.);
#13226=ORIENTED_EDGE('',*,*,#9365,.T.);
#13227=ORIENTED_EDGE('',*,*,#9367,.F.);
#13228=ORIENTED_EDGE('',*,*,#9117,.T.);
#13229=ORIENTED_EDGE('',*,*,#9368,.T.);
#13230=ORIENTED_EDGE('',*,*,#9110,.F.);
#13231=ORIENTED_EDGE('',*,*,#9114,.F.);
#13232=ORIENTED_EDGE('',*,*,#9369,.T.);
#13233=ORIENTED_EDGE('',*,*,#9356,.T.);
#13234=ORIENTED_EDGE('',*,*,#9361,.F.);
#13235=ORIENTED_EDGE('',*,*,#9370,.T.);
#13236=ORIENTED_EDGE('',*,*,#9355,.T.);
#13237=ORIENTED_EDGE('',*,*,#9352,.T.);
#13238=ORIENTED_EDGE('',*,*,#9349,.T.);
#13239=ORIENTED_EDGE('',*,*,#9346,.T.);
#13240=ORIENTED_EDGE('',*,*,#9343,.T.);
#13241=ORIENTED_EDGE('',*,*,#9340,.T.);
#13242=ORIENTED_EDGE('',*,*,#9337,.T.);
#13243=ORIENTED_EDGE('',*,*,#9334,.T.);
#13244=ORIENTED_EDGE('',*,*,#9331,.T.);
#13245=ORIENTED_EDGE('',*,*,#9328,.T.);
#13246=ORIENTED_EDGE('',*,*,#9325,.T.);
#13247=ORIENTED_EDGE('',*,*,#9322,.T.);
#13248=ORIENTED_EDGE('',*,*,#9319,.T.);
#13249=ORIENTED_EDGE('',*,*,#9316,.T.);
#13250=ORIENTED_EDGE('',*,*,#9313,.T.);
#13251=ORIENTED_EDGE('',*,*,#9310,.T.);
#13252=ORIENTED_EDGE('',*,*,#9307,.T.);
#13253=ORIENTED_EDGE('',*,*,#9304,.T.);
#13254=ORIENTED_EDGE('',*,*,#9301,.T.);
#13255=ORIENTED_EDGE('',*,*,#9298,.T.);
#13256=ORIENTED_EDGE('',*,*,#9295,.T.);
#13257=ORIENTED_EDGE('',*,*,#9292,.T.);
#13258=ORIENTED_EDGE('',*,*,#9289,.T.);
#13259=ORIENTED_EDGE('',*,*,#9286,.T.);
#13260=ORIENTED_EDGE('',*,*,#9283,.T.);
#13261=ORIENTED_EDGE('',*,*,#9280,.T.);
#13262=ORIENTED_EDGE('',*,*,#9277,.T.);
#13263=ORIENTED_EDGE('',*,*,#9274,.T.);
#13264=ORIENTED_EDGE('',*,*,#9271,.T.);
#13265=ORIENTED_EDGE('',*,*,#9268,.T.);
#13266=ORIENTED_EDGE('',*,*,#9265,.T.);
#13267=ORIENTED_EDGE('',*,*,#9262,.T.);
#13268=ORIENTED_EDGE('',*,*,#9259,.T.);
#13269=ORIENTED_EDGE('',*,*,#9256,.T.);
#13270=ORIENTED_EDGE('',*,*,#9253,.T.);
#13271=ORIENTED_EDGE('',*,*,#9250,.T.);
#13272=ORIENTED_EDGE('',*,*,#9247,.T.);
#13273=ORIENTED_EDGE('',*,*,#9244,.T.);
#13274=ORIENTED_EDGE('',*,*,#9241,.T.);
#13275=ORIENTED_EDGE('',*,*,#9238,.T.);
#13276=ORIENTED_EDGE('',*,*,#9235,.T.);
#13277=ORIENTED_EDGE('',*,*,#9232,.T.);
#13278=ORIENTED_EDGE('',*,*,#9229,.T.);
#13279=ORIENTED_EDGE('',*,*,#9226,.T.);
#13280=ORIENTED_EDGE('',*,*,#9223,.T.);
#13281=ORIENTED_EDGE('',*,*,#9220,.T.);
#13282=ORIENTED_EDGE('',*,*,#9217,.T.);
#13283=ORIENTED_EDGE('',*,*,#9214,.T.);
#13284=ORIENTED_EDGE('',*,*,#9211,.T.);
#13285=ORIENTED_EDGE('',*,*,#9208,.T.);
#13286=ORIENTED_EDGE('',*,*,#9205,.T.);
#13287=ORIENTED_EDGE('',*,*,#9202,.T.);
#13288=ORIENTED_EDGE('',*,*,#9199,.T.);
#13289=ORIENTED_EDGE('',*,*,#9196,.T.);
#13290=ORIENTED_EDGE('',*,*,#9193,.T.);
#13291=ORIENTED_EDGE('',*,*,#9190,.T.);
#13292=ORIENTED_EDGE('',*,*,#9187,.T.);
#13293=ORIENTED_EDGE('',*,*,#9184,.T.);
#13294=ORIENTED_EDGE('',*,*,#9181,.T.);
#13295=ORIENTED_EDGE('',*,*,#9178,.T.);
#13296=ORIENTED_EDGE('',*,*,#9175,.T.);
#13297=ORIENTED_EDGE('',*,*,#9172,.T.);
#13298=ORIENTED_EDGE('',*,*,#9169,.T.);
#13299=ORIENTED_EDGE('',*,*,#9166,.T.);
#13300=ORIENTED_EDGE('',*,*,#9163,.T.);
#13301=ORIENTED_EDGE('',*,*,#9160,.T.);
#13302=ORIENTED_EDGE('',*,*,#9157,.T.);
#13303=ORIENTED_EDGE('',*,*,#9154,.T.);
#13304=ORIENTED_EDGE('',*,*,#9151,.T.);
#13305=ORIENTED_EDGE('',*,*,#9148,.T.);
#13306=ORIENTED_EDGE('',*,*,#9145,.T.);
#13307=ORIENTED_EDGE('',*,*,#9142,.T.);
#13308=ORIENTED_EDGE('',*,*,#9139,.T.);
#13309=ORIENTED_EDGE('',*,*,#9136,.T.);
#13310=ORIENTED_EDGE('',*,*,#9133,.T.);
#13311=ORIENTED_EDGE('',*,*,#9130,.T.);
#13312=ORIENTED_EDGE('',*,*,#9127,.T.);
#13313=ORIENTED_EDGE('',*,*,#9124,.T.);
#13314=ORIENTED_EDGE('',*,*,#9121,.T.);
#13315=ORIENTED_EDGE('',*,*,#9118,.T.);
#13316=ORIENTED_EDGE('',*,*,#9369,.F.);
#13317=ORIENTED_EDGE('',*,*,#9113,.F.);
#13318=ORIENTED_EDGE('',*,*,#9371,.F.);
#13319=ORIENTED_EDGE('',*,*,#9107,.F.);
#13320=ORIENTED_EDGE('',*,*,#9104,.F.);
#13321=ORIENTED_EDGE('',*,*,#9101,.F.);
#13322=ORIENTED_EDGE('',*,*,#9098,.F.);
#13323=ORIENTED_EDGE('',*,*,#9095,.F.);
#13324=ORIENTED_EDGE('',*,*,#9092,.F.);
#13325=ORIENTED_EDGE('',*,*,#9089,.F.);
#13326=ORIENTED_EDGE('',*,*,#9086,.F.);
#13327=ORIENTED_EDGE('',*,*,#9083,.F.);
#13328=ORIENTED_EDGE('',*,*,#9080,.F.);
#13329=ORIENTED_EDGE('',*,*,#9077,.F.);
#13330=ORIENTED_EDGE('',*,*,#9074,.F.);
#13331=ORIENTED_EDGE('',*,*,#9071,.F.);
#13332=ORIENTED_EDGE('',*,*,#9068,.F.);
#13333=ORIENTED_EDGE('',*,*,#9065,.F.);
#13334=ORIENTED_EDGE('',*,*,#9062,.F.);
#13335=ORIENTED_EDGE('',*,*,#9059,.F.);
#13336=ORIENTED_EDGE('',*,*,#9056,.F.);
#13337=ORIENTED_EDGE('',*,*,#9053,.F.);
#13338=ORIENTED_EDGE('',*,*,#9050,.F.);
#13339=ORIENTED_EDGE('',*,*,#9047,.F.);
#13340=ORIENTED_EDGE('',*,*,#9044,.F.);
#13341=ORIENTED_EDGE('',*,*,#9041,.F.);
#13342=ORIENTED_EDGE('',*,*,#9038,.F.);
#13343=ORIENTED_EDGE('',*,*,#9035,.F.);
#13344=ORIENTED_EDGE('',*,*,#9032,.F.);
#13345=ORIENTED_EDGE('',*,*,#9029,.F.);
#13346=ORIENTED_EDGE('',*,*,#9026,.F.);
#13347=ORIENTED_EDGE('',*,*,#9023,.F.);
#13348=ORIENTED_EDGE('',*,*,#9020,.F.);
#13349=ORIENTED_EDGE('',*,*,#9017,.F.);
#13350=ORIENTED_EDGE('',*,*,#9014,.F.);
#13351=ORIENTED_EDGE('',*,*,#9011,.F.);
#13352=ORIENTED_EDGE('',*,*,#9008,.F.);
#13353=ORIENTED_EDGE('',*,*,#9005,.F.);
#13354=ORIENTED_EDGE('',*,*,#9002,.F.);
#13355=ORIENTED_EDGE('',*,*,#8999,.F.);
#13356=ORIENTED_EDGE('',*,*,#8996,.F.);
#13357=ORIENTED_EDGE('',*,*,#8993,.F.);
#13358=ORIENTED_EDGE('',*,*,#8990,.F.);
#13359=ORIENTED_EDGE('',*,*,#8987,.F.);
#13360=ORIENTED_EDGE('',*,*,#8984,.F.);
#13361=ORIENTED_EDGE('',*,*,#8981,.F.);
#13362=ORIENTED_EDGE('',*,*,#8978,.F.);
#13363=ORIENTED_EDGE('',*,*,#8975,.F.);
#13364=ORIENTED_EDGE('',*,*,#8972,.F.);
#13365=ORIENTED_EDGE('',*,*,#8969,.F.);
#13366=ORIENTED_EDGE('',*,*,#8966,.F.);
#13367=ORIENTED_EDGE('',*,*,#8963,.F.);
#13368=ORIENTED_EDGE('',*,*,#8960,.F.);
#13369=ORIENTED_EDGE('',*,*,#8957,.F.);
#13370=ORIENTED_EDGE('',*,*,#8954,.F.);
#13371=ORIENTED_EDGE('',*,*,#8951,.F.);
#13372=ORIENTED_EDGE('',*,*,#8948,.F.);
#13373=ORIENTED_EDGE('',*,*,#8945,.F.);
#13374=ORIENTED_EDGE('',*,*,#8942,.F.);
#13375=ORIENTED_EDGE('',*,*,#8939,.F.);
#13376=ORIENTED_EDGE('',*,*,#8936,.F.);
#13377=ORIENTED_EDGE('',*,*,#8933,.F.);
#13378=ORIENTED_EDGE('',*,*,#8930,.F.);
#13379=ORIENTED_EDGE('',*,*,#8927,.F.);
#13380=ORIENTED_EDGE('',*,*,#8924,.F.);
#13381=ORIENTED_EDGE('',*,*,#8921,.F.);
#13382=ORIENTED_EDGE('',*,*,#8918,.F.);
#13383=ORIENTED_EDGE('',*,*,#8915,.F.);
#13384=ORIENTED_EDGE('',*,*,#8912,.F.);
#13385=ORIENTED_EDGE('',*,*,#8909,.F.);
#13386=ORIENTED_EDGE('',*,*,#8906,.F.);
#13387=ORIENTED_EDGE('',*,*,#8903,.F.);
#13388=ORIENTED_EDGE('',*,*,#8900,.F.);
#13389=ORIENTED_EDGE('',*,*,#8897,.F.);
#13390=ORIENTED_EDGE('',*,*,#8894,.F.);
#13391=ORIENTED_EDGE('',*,*,#8891,.F.);
#13392=ORIENTED_EDGE('',*,*,#8888,.F.);
#13393=ORIENTED_EDGE('',*,*,#8885,.F.);
#13394=ORIENTED_EDGE('',*,*,#8882,.F.);
#13395=ORIENTED_EDGE('',*,*,#8879,.F.);
#13396=ORIENTED_EDGE('',*,*,#8876,.F.);
#13397=ORIENTED_EDGE('',*,*,#9353,.T.);
#13398=ORIENTED_EDGE('',*,*,#9370,.F.);
#13399=ORIENTED_EDGE('',*,*,#9360,.F.);
#13400=ORIENTED_EDGE('',*,*,#9372,.T.);
#13401=ORIENTED_EDGE('',*,*,#9357,.T.);
#13402=ORIENTED_EDGE('',*,*,#8874,.F.);
#13403=ORIENTED_EDGE('',*,*,#8878,.F.);
#13404=ORIENTED_EDGE('',*,*,#8881,.F.);
#13405=ORIENTED_EDGE('',*,*,#8884,.F.);
#13406=ORIENTED_EDGE('',*,*,#8887,.F.);
#13407=ORIENTED_EDGE('',*,*,#8890,.F.);
#13408=ORIENTED_EDGE('',*,*,#8893,.F.);
#13409=ORIENTED_EDGE('',*,*,#8896,.F.);
#13410=ORIENTED_EDGE('',*,*,#8899,.F.);
#13411=ORIENTED_EDGE('',*,*,#8902,.F.);
#13412=ORIENTED_EDGE('',*,*,#8905,.F.);
#13413=ORIENTED_EDGE('',*,*,#8908,.F.);
#13414=ORIENTED_EDGE('',*,*,#8911,.F.);
#13415=ORIENTED_EDGE('',*,*,#8914,.F.);
#13416=ORIENTED_EDGE('',*,*,#8917,.F.);
#13417=ORIENTED_EDGE('',*,*,#8920,.F.);
#13418=ORIENTED_EDGE('',*,*,#8923,.F.);
#13419=ORIENTED_EDGE('',*,*,#8926,.F.);
#13420=ORIENTED_EDGE('',*,*,#8929,.F.);
#13421=ORIENTED_EDGE('',*,*,#8932,.F.);
#13422=ORIENTED_EDGE('',*,*,#8935,.F.);
#13423=ORIENTED_EDGE('',*,*,#8938,.F.);
#13424=ORIENTED_EDGE('',*,*,#8941,.F.);
#13425=ORIENTED_EDGE('',*,*,#8944,.F.);
#13426=ORIENTED_EDGE('',*,*,#8947,.F.);
#13427=ORIENTED_EDGE('',*,*,#8950,.F.);
#13428=ORIENTED_EDGE('',*,*,#8953,.F.);
#13429=ORIENTED_EDGE('',*,*,#8956,.F.);
#13430=ORIENTED_EDGE('',*,*,#8959,.F.);
#13431=ORIENTED_EDGE('',*,*,#8962,.F.);
#13432=ORIENTED_EDGE('',*,*,#8965,.F.);
#13433=ORIENTED_EDGE('',*,*,#8968,.F.);
#13434=ORIENTED_EDGE('',*,*,#8971,.F.);
#13435=ORIENTED_EDGE('',*,*,#8974,.F.);
#13436=ORIENTED_EDGE('',*,*,#8977,.F.);
#13437=ORIENTED_EDGE('',*,*,#8980,.F.);
#13438=ORIENTED_EDGE('',*,*,#8983,.F.);
#13439=ORIENTED_EDGE('',*,*,#8986,.F.);
#13440=ORIENTED_EDGE('',*,*,#8989,.F.);
#13441=ORIENTED_EDGE('',*,*,#8992,.F.);
#13442=ORIENTED_EDGE('',*,*,#8995,.F.);
#13443=ORIENTED_EDGE('',*,*,#8998,.F.);
#13444=ORIENTED_EDGE('',*,*,#9001,.F.);
#13445=ORIENTED_EDGE('',*,*,#9004,.F.);
#13446=ORIENTED_EDGE('',*,*,#9007,.F.);
#13447=ORIENTED_EDGE('',*,*,#9010,.F.);
#13448=ORIENTED_EDGE('',*,*,#9013,.F.);
#13449=ORIENTED_EDGE('',*,*,#9016,.F.);
#13450=ORIENTED_EDGE('',*,*,#9019,.F.);
#13451=ORIENTED_EDGE('',*,*,#9022,.F.);
#13452=ORIENTED_EDGE('',*,*,#9025,.F.);
#13453=ORIENTED_EDGE('',*,*,#9028,.F.);
#13454=ORIENTED_EDGE('',*,*,#9031,.F.);
#13455=ORIENTED_EDGE('',*,*,#9034,.F.);
#13456=ORIENTED_EDGE('',*,*,#9037,.F.);
#13457=ORIENTED_EDGE('',*,*,#9040,.F.);
#13458=ORIENTED_EDGE('',*,*,#9043,.F.);
#13459=ORIENTED_EDGE('',*,*,#9046,.F.);
#13460=ORIENTED_EDGE('',*,*,#9049,.F.);
#13461=ORIENTED_EDGE('',*,*,#9052,.F.);
#13462=ORIENTED_EDGE('',*,*,#9055,.F.);
#13463=ORIENTED_EDGE('',*,*,#9058,.F.);
#13464=ORIENTED_EDGE('',*,*,#9061,.F.);
#13465=ORIENTED_EDGE('',*,*,#9064,.F.);
#13466=ORIENTED_EDGE('',*,*,#9067,.F.);
#13467=ORIENTED_EDGE('',*,*,#9070,.F.);
#13468=ORIENTED_EDGE('',*,*,#9073,.F.);
#13469=ORIENTED_EDGE('',*,*,#9076,.F.);
#13470=ORIENTED_EDGE('',*,*,#9079,.F.);
#13471=ORIENTED_EDGE('',*,*,#9082,.F.);
#13472=ORIENTED_EDGE('',*,*,#9085,.F.);
#13473=ORIENTED_EDGE('',*,*,#9088,.F.);
#13474=ORIENTED_EDGE('',*,*,#9091,.F.);
#13475=ORIENTED_EDGE('',*,*,#9094,.F.);
#13476=ORIENTED_EDGE('',*,*,#9097,.F.);
#13477=ORIENTED_EDGE('',*,*,#9100,.F.);
#13478=ORIENTED_EDGE('',*,*,#9103,.F.);
#13479=ORIENTED_EDGE('',*,*,#9106,.F.);
#13480=ORIENTED_EDGE('',*,*,#9373,.F.);
#13481=ORIENTED_EDGE('',*,*,#9111,.F.);
#13482=ORIENTED_EDGE('',*,*,#9368,.F.);
#13483=ORIENTED_EDGE('',*,*,#9116,.F.);
#13484=ORIENTED_EDGE('',*,*,#9120,.F.);
#13485=ORIENTED_EDGE('',*,*,#9123,.F.);
#13486=ORIENTED_EDGE('',*,*,#9126,.F.);
#13487=ORIENTED_EDGE('',*,*,#9129,.F.);
#13488=ORIENTED_EDGE('',*,*,#9132,.F.);
#13489=ORIENTED_EDGE('',*,*,#9135,.F.);
#13490=ORIENTED_EDGE('',*,*,#9138,.F.);
#13491=ORIENTED_EDGE('',*,*,#9141,.F.);
#13492=ORIENTED_EDGE('',*,*,#9144,.F.);
#13493=ORIENTED_EDGE('',*,*,#9147,.F.);
#13494=ORIENTED_EDGE('',*,*,#9150,.F.);
#13495=ORIENTED_EDGE('',*,*,#9153,.F.);
#13496=ORIENTED_EDGE('',*,*,#9156,.F.);
#13497=ORIENTED_EDGE('',*,*,#9159,.F.);
#13498=ORIENTED_EDGE('',*,*,#9162,.F.);
#13499=ORIENTED_EDGE('',*,*,#9165,.F.);
#13500=ORIENTED_EDGE('',*,*,#9168,.F.);
#13501=ORIENTED_EDGE('',*,*,#9171,.F.);
#13502=ORIENTED_EDGE('',*,*,#9174,.F.);
#13503=ORIENTED_EDGE('',*,*,#9177,.F.);
#13504=ORIENTED_EDGE('',*,*,#9180,.F.);
#13505=ORIENTED_EDGE('',*,*,#9183,.F.);
#13506=ORIENTED_EDGE('',*,*,#9186,.F.);
#13507=ORIENTED_EDGE('',*,*,#9189,.F.);
#13508=ORIENTED_EDGE('',*,*,#9192,.F.);
#13509=ORIENTED_EDGE('',*,*,#9195,.F.);
#13510=ORIENTED_EDGE('',*,*,#9198,.F.);
#13511=ORIENTED_EDGE('',*,*,#9201,.F.);
#13512=ORIENTED_EDGE('',*,*,#9204,.F.);
#13513=ORIENTED_EDGE('',*,*,#9207,.F.);
#13514=ORIENTED_EDGE('',*,*,#9210,.F.);
#13515=ORIENTED_EDGE('',*,*,#9213,.F.);
#13516=ORIENTED_EDGE('',*,*,#9216,.F.);
#13517=ORIENTED_EDGE('',*,*,#9219,.F.);
#13518=ORIENTED_EDGE('',*,*,#9222,.F.);
#13519=ORIENTED_EDGE('',*,*,#9225,.F.);
#13520=ORIENTED_EDGE('',*,*,#9228,.F.);
#13521=ORIENTED_EDGE('',*,*,#9231,.F.);
#13522=ORIENTED_EDGE('',*,*,#9234,.F.);
#13523=ORIENTED_EDGE('',*,*,#9237,.F.);
#13524=ORIENTED_EDGE('',*,*,#9240,.F.);
#13525=ORIENTED_EDGE('',*,*,#9243,.F.);
#13526=ORIENTED_EDGE('',*,*,#9246,.F.);
#13527=ORIENTED_EDGE('',*,*,#9249,.F.);
#13528=ORIENTED_EDGE('',*,*,#9252,.F.);
#13529=ORIENTED_EDGE('',*,*,#9255,.F.);
#13530=ORIENTED_EDGE('',*,*,#9258,.F.);
#13531=ORIENTED_EDGE('',*,*,#9261,.F.);
#13532=ORIENTED_EDGE('',*,*,#9264,.F.);
#13533=ORIENTED_EDGE('',*,*,#9267,.F.);
#13534=ORIENTED_EDGE('',*,*,#9270,.F.);
#13535=ORIENTED_EDGE('',*,*,#9273,.F.);
#13536=ORIENTED_EDGE('',*,*,#9276,.F.);
#13537=ORIENTED_EDGE('',*,*,#9279,.F.);
#13538=ORIENTED_EDGE('',*,*,#9282,.F.);
#13539=ORIENTED_EDGE('',*,*,#9285,.F.);
#13540=ORIENTED_EDGE('',*,*,#9288,.F.);
#13541=ORIENTED_EDGE('',*,*,#9291,.F.);
#13542=ORIENTED_EDGE('',*,*,#9294,.F.);
#13543=ORIENTED_EDGE('',*,*,#9297,.F.);
#13544=ORIENTED_EDGE('',*,*,#9300,.F.);
#13545=ORIENTED_EDGE('',*,*,#9303,.F.);
#13546=ORIENTED_EDGE('',*,*,#9306,.F.);
#13547=ORIENTED_EDGE('',*,*,#9309,.F.);
#13548=ORIENTED_EDGE('',*,*,#9312,.F.);
#13549=ORIENTED_EDGE('',*,*,#9315,.F.);
#13550=ORIENTED_EDGE('',*,*,#9318,.F.);
#13551=ORIENTED_EDGE('',*,*,#9321,.F.);
#13552=ORIENTED_EDGE('',*,*,#9324,.F.);
#13553=ORIENTED_EDGE('',*,*,#9327,.F.);
#13554=ORIENTED_EDGE('',*,*,#9330,.F.);
#13555=ORIENTED_EDGE('',*,*,#9333,.F.);
#13556=ORIENTED_EDGE('',*,*,#9336,.F.);
#13557=ORIENTED_EDGE('',*,*,#9339,.F.);
#13558=ORIENTED_EDGE('',*,*,#9342,.F.);
#13559=ORIENTED_EDGE('',*,*,#9345,.F.);
#13560=ORIENTED_EDGE('',*,*,#9348,.F.);
#13561=ORIENTED_EDGE('',*,*,#9351,.F.);
#13562=ORIENTED_EDGE('',*,*,#9354,.F.);
#13563=ORIENTED_EDGE('',*,*,#9372,.F.);
#13564=ORIENTED_EDGE('',*,*,#9359,.F.);
#13565=ORIENTED_EDGE('',*,*,#9112,.F.);
#13566=ORIENTED_EDGE('',*,*,#9373,.T.);
#13567=ORIENTED_EDGE('',*,*,#9105,.T.);
#13568=ORIENTED_EDGE('',*,*,#9371,.T.);
#13569=ORIENTED_EDGE('',*,*,#9374,.F.);
#13570=ORIENTED_EDGE('',*,*,#9375,.T.);
#13571=ORIENTED_EDGE('',*,*,#9376,.F.);
#13572=ORIENTED_EDGE('',*,*,#9375,.F.);
#13573=ORIENTED_EDGE('',*,*,#9377,.F.);
#13574=ORIENTED_EDGE('',*,*,#9378,.T.);
#13575=ORIENTED_EDGE('',*,*,#9379,.F.);
#13576=ORIENTED_EDGE('',*,*,#9378,.F.);
#13577=ORIENTED_EDGE('',*,*,#9380,.F.);
#13578=ORIENTED_EDGE('',*,*,#9381,.T.);
#13579=ORIENTED_EDGE('',*,*,#9382,.F.);
#13580=ORIENTED_EDGE('',*,*,#9381,.F.);
#13581=ORIENTED_EDGE('',*,*,#9383,.F.);
#13582=ORIENTED_EDGE('',*,*,#9384,.T.);
#13583=ORIENTED_EDGE('',*,*,#9385,.F.);
#13584=ORIENTED_EDGE('',*,*,#9384,.F.);
#13585=ORIENTED_EDGE('',*,*,#9386,.F.);
#13586=ORIENTED_EDGE('',*,*,#9387,.T.);
#13587=ORIENTED_EDGE('',*,*,#9388,.F.);
#13588=ORIENTED_EDGE('',*,*,#9387,.F.);
#13589=ORIENTED_EDGE('',*,*,#9389,.F.);
#13590=ORIENTED_EDGE('',*,*,#9390,.T.);
#13591=ORIENTED_EDGE('',*,*,#9391,.F.);
#13592=ORIENTED_EDGE('',*,*,#9390,.F.);
#13593=ORIENTED_EDGE('',*,*,#9392,.F.);
#13594=ORIENTED_EDGE('',*,*,#9393,.T.);
#13595=ORIENTED_EDGE('',*,*,#9391,.T.);
#13596=ORIENTED_EDGE('',*,*,#9388,.T.);
#13597=ORIENTED_EDGE('',*,*,#9385,.T.);
#13598=ORIENTED_EDGE('',*,*,#9382,.T.);
#13599=ORIENTED_EDGE('',*,*,#9379,.T.);
#13600=ORIENTED_EDGE('',*,*,#9376,.T.);
#13601=ORIENTED_EDGE('',*,*,#9394,.F.);
#13602=ORIENTED_EDGE('',*,*,#9395,.T.);
#13603=ORIENTED_EDGE('',*,*,#9392,.T.);
#13604=ORIENTED_EDGE('',*,*,#9395,.F.);
#13605=ORIENTED_EDGE('',*,*,#9394,.T.);
#13606=ORIENTED_EDGE('',*,*,#9389,.T.);
#13607=ORIENTED_EDGE('',*,*,#9386,.T.);
#13608=ORIENTED_EDGE('',*,*,#9383,.T.);
#13609=ORIENTED_EDGE('',*,*,#9380,.T.);
#13610=ORIENTED_EDGE('',*,*,#9377,.T.);
#13611=ORIENTED_EDGE('',*,*,#9374,.T.);
#13612=ORIENTED_EDGE('',*,*,#9396,.F.);
#13613=ORIENTED_EDGE('',*,*,#9366,.F.);
#13614=ORIENTED_EDGE('',*,*,#9393,.F.);
#13615=ORIENTED_EDGE('',*,*,#9397,.T.);
#13616=ORIENTED_EDGE('',*,*,#9396,.T.);
#13617=ORIENTED_EDGE('',*,*,#9397,.F.);
#14583=PLANE('',#16471);
#14584=PLANE('',#16476);
#14585=PLANE('',#16477);
#14586=PLANE('',#16481);
#14587=PLANE('',#16502);
#14588=PLANE('',#16507);
#14589=PLANE('',#16508);
#15130=ADVANCED_FACE('',(#3150),#2112,.T.);
#15131=ADVANCED_FACE('',(#3151),#2113,.T.);
#15132=ADVANCED_FACE('',(#3152),#2114,.T.);
#15133=ADVANCED_FACE('',(#3153),#2115,.T.);
#15134=ADVANCED_FACE('',(#3154),#2116,.T.);
#15135=ADVANCED_FACE('',(#3155),#2117,.T.);
#15136=ADVANCED_FACE('',(#3156),#2118,.T.);
#15137=ADVANCED_FACE('',(#3157),#2119,.T.);
#15138=ADVANCED_FACE('',(#3158),#2120,.T.);
#15139=ADVANCED_FACE('',(#3159),#2121,.T.);
#15140=ADVANCED_FACE('',(#3160),#2122,.T.);
#15141=ADVANCED_FACE('',(#3161),#2123,.T.);
#15142=ADVANCED_FACE('',(#3162),#2124,.T.);
#15143=ADVANCED_FACE('',(#3163),#2125,.T.);
#15144=ADVANCED_FACE('',(#3164),#2126,.T.);
#15145=ADVANCED_FACE('',(#3165),#2127,.T.);
#15146=ADVANCED_FACE('',(#3166),#2128,.T.);
#15147=ADVANCED_FACE('',(#3167),#2129,.T.);
#15148=ADVANCED_FACE('',(#3168),#2130,.T.);
#15149=ADVANCED_FACE('',(#3169),#2131,.T.);
#15150=ADVANCED_FACE('',(#3170),#2132,.T.);
#15151=ADVANCED_FACE('',(#3171),#2133,.T.);
#15152=ADVANCED_FACE('',(#3172),#2134,.T.);
#15153=ADVANCED_FACE('',(#3173),#2135,.T.);
#15154=ADVANCED_FACE('',(#3174),#2136,.T.);
#15155=ADVANCED_FACE('',(#3175),#2137,.T.);
#15156=ADVANCED_FACE('',(#3176),#2138,.T.);
#15157=ADVANCED_FACE('',(#3177),#2139,.T.);
#15158=ADVANCED_FACE('',(#3178),#2140,.T.);
#15159=ADVANCED_FACE('',(#3179),#2141,.T.);
#15160=ADVANCED_FACE('',(#3180),#2142,.T.);
#15161=ADVANCED_FACE('',(#3181),#2143,.T.);
#15162=ADVANCED_FACE('',(#3182),#2144,.T.);
#15163=ADVANCED_FACE('',(#3183),#2145,.T.);
#15164=ADVANCED_FACE('',(#3184),#2146,.T.);
#15165=ADVANCED_FACE('',(#3185),#2147,.T.);
#15166=ADVANCED_FACE('',(#3186),#2148,.T.);
#15167=ADVANCED_FACE('',(#3187),#2149,.T.);
#15168=ADVANCED_FACE('',(#3188),#2150,.T.);
#15169=ADVANCED_FACE('',(#3189),#2151,.T.);
#15170=ADVANCED_FACE('',(#3190),#2152,.T.);
#15171=ADVANCED_FACE('',(#3191),#2153,.T.);
#15172=ADVANCED_FACE('',(#3192),#2154,.T.);
#15173=ADVANCED_FACE('',(#3193),#2155,.T.);
#15174=ADVANCED_FACE('',(#3194),#2156,.T.);
#15175=ADVANCED_FACE('',(#3195),#2157,.T.);
#15176=ADVANCED_FACE('',(#3196),#2158,.T.);
#15177=ADVANCED_FACE('',(#3197),#2159,.T.);
#15178=ADVANCED_FACE('',(#3198),#2160,.T.);
#15179=ADVANCED_FACE('',(#3199),#2161,.T.);
#15180=ADVANCED_FACE('',(#3200),#2162,.T.);
#15181=ADVANCED_FACE('',(#3201),#2163,.T.);
#15182=ADVANCED_FACE('',(#3202),#2164,.T.);
#15183=ADVANCED_FACE('',(#3203),#2165,.T.);
#15184=ADVANCED_FACE('',(#3204),#2166,.T.);
#15185=ADVANCED_FACE('',(#3205),#2167,.T.);
#15186=ADVANCED_FACE('',(#3206),#2168,.T.);
#15187=ADVANCED_FACE('',(#3207),#2169,.T.);
#15188=ADVANCED_FACE('',(#3208),#2170,.T.);
#15189=ADVANCED_FACE('',(#3209),#2171,.T.);
#15190=ADVANCED_FACE('',(#3210),#2172,.T.);
#15191=ADVANCED_FACE('',(#3211),#2173,.T.);
#15192=ADVANCED_FACE('',(#3212),#2174,.T.);
#15193=ADVANCED_FACE('',(#3213),#2175,.T.);
#15194=ADVANCED_FACE('',(#3214),#2176,.T.);
#15195=ADVANCED_FACE('',(#3215),#2177,.T.);
#15196=ADVANCED_FACE('',(#3216),#2178,.T.);
#15197=ADVANCED_FACE('',(#3217),#2179,.T.);
#15198=ADVANCED_FACE('',(#3218),#2180,.T.);
#15199=ADVANCED_FACE('',(#3219),#2181,.T.);
#15200=ADVANCED_FACE('',(#3220),#2182,.T.);
#15201=ADVANCED_FACE('',(#3221),#2183,.T.);
#15202=ADVANCED_FACE('',(#3222),#2184,.T.);
#15203=ADVANCED_FACE('',(#3223),#2185,.T.);
#15204=ADVANCED_FACE('',(#3224),#2186,.T.);
#15205=ADVANCED_FACE('',(#3225),#2187,.T.);
#15206=ADVANCED_FACE('',(#3226),#2188,.T.);
#15207=ADVANCED_FACE('',(#3227),#2189,.T.);
#15208=ADVANCED_FACE('',(#3228),#2190,.T.);
#15209=ADVANCED_FACE('',(#3229),#2191,.T.);
#15210=ADVANCED_FACE('',(#3230),#2192,.T.);
#15211=ADVANCED_FACE('',(#3231),#2193,.T.);
#15212=ADVANCED_FACE('',(#3232),#2194,.T.);
#15213=ADVANCED_FACE('',(#3233),#2195,.T.);
#15214=ADVANCED_FACE('',(#3234),#2196,.T.);
#15215=ADVANCED_FACE('',(#3235),#2197,.T.);
#15216=ADVANCED_FACE('',(#3236),#2198,.T.);
#15217=ADVANCED_FACE('',(#3237),#2199,.T.);
#15218=ADVANCED_FACE('',(#3238),#2200,.T.);
#15219=ADVANCED_FACE('',(#3239),#2201,.T.);
#15220=ADVANCED_FACE('',(#3240),#2202,.T.);
#15221=ADVANCED_FACE('',(#3241),#2203,.T.);
#15222=ADVANCED_FACE('',(#3242),#2204,.T.);
#15223=ADVANCED_FACE('',(#3243),#2205,.T.);
#15224=ADVANCED_FACE('',(#3244),#2206,.T.);
#15225=ADVANCED_FACE('',(#3245),#2207,.T.);
#15226=ADVANCED_FACE('',(#3246),#2208,.T.);
#15227=ADVANCED_FACE('',(#3247),#2209,.T.);
#15228=ADVANCED_FACE('',(#3248),#2210,.T.);
#15229=ADVANCED_FACE('',(#3249),#2211,.T.);
#15230=ADVANCED_FACE('',(#3250),#2212,.T.);
#15231=ADVANCED_FACE('',(#3251),#2213,.T.);
#15232=ADVANCED_FACE('',(#3252),#2214,.T.);
#15233=ADVANCED_FACE('',(#3253),#2215,.T.);
#15234=ADVANCED_FACE('',(#3254),#2216,.T.);
#15235=ADVANCED_FACE('',(#3255),#2217,.T.);
#15236=ADVANCED_FACE('',(#3256),#2218,.T.);
#15237=ADVANCED_FACE('',(#3257),#2219,.T.);
#15238=ADVANCED_FACE('',(#3258),#2220,.T.);
#15239=ADVANCED_FACE('',(#3259),#2221,.T.);
#15240=ADVANCED_FACE('',(#3260),#2222,.T.);
#15241=ADVANCED_FACE('',(#3261),#2223,.T.);
#15242=ADVANCED_FACE('',(#3262),#2224,.T.);
#15243=ADVANCED_FACE('',(#3263),#2225,.T.);
#15244=ADVANCED_FACE('',(#3264),#2226,.T.);
#15245=ADVANCED_FACE('',(#3265),#2227,.T.);
#15246=ADVANCED_FACE('',(#3266),#2228,.T.);
#15247=ADVANCED_FACE('',(#3267),#2229,.T.);
#15248=ADVANCED_FACE('',(#3268),#2230,.T.);
#15249=ADVANCED_FACE('',(#3269),#2231,.T.);
#15250=ADVANCED_FACE('',(#3270),#2232,.T.);
#15251=ADVANCED_FACE('',(#3271),#2233,.T.);
#15252=ADVANCED_FACE('',(#3272),#2234,.T.);
#15253=ADVANCED_FACE('',(#3273),#2235,.T.);
#15254=ADVANCED_FACE('',(#3274),#2236,.T.);
#15255=ADVANCED_FACE('',(#3275),#2237,.T.);
#15256=ADVANCED_FACE('',(#3276),#2238,.T.);
#15257=ADVANCED_FACE('',(#3277),#2239,.T.);
#15258=ADVANCED_FACE('',(#3278),#2240,.T.);
#15259=ADVANCED_FACE('',(#3279),#2241,.T.);
#15260=ADVANCED_FACE('',(#3280),#2242,.T.);
#15261=ADVANCED_FACE('',(#3281),#2243,.T.);
#15262=ADVANCED_FACE('',(#3282),#2244,.T.);
#15263=ADVANCED_FACE('',(#3283),#2245,.T.);
#15264=ADVANCED_FACE('',(#3284),#2246,.T.);
#15265=ADVANCED_FACE('',(#3285),#2247,.T.);
#15266=ADVANCED_FACE('',(#3286),#2248,.T.);
#15267=ADVANCED_FACE('',(#3287),#2249,.T.);
#15268=ADVANCED_FACE('',(#3288),#2250,.T.);
#15269=ADVANCED_FACE('',(#3289),#2251,.T.);
#15270=ADVANCED_FACE('',(#3290),#2252,.T.);
#15271=ADVANCED_FACE('',(#3291),#2253,.T.);
#15272=ADVANCED_FACE('',(#3292),#2254,.T.);
#15273=ADVANCED_FACE('',(#3293),#2255,.T.);
#15274=ADVANCED_FACE('',(#3294),#2256,.T.);
#15275=ADVANCED_FACE('',(#3295),#2257,.T.);
#15276=ADVANCED_FACE('',(#3296),#2258,.T.);
#15277=ADVANCED_FACE('',(#3297),#2259,.T.);
#15278=ADVANCED_FACE('',(#3298),#2260,.T.);
#15279=ADVANCED_FACE('',(#3299),#2261,.T.);
#15280=ADVANCED_FACE('',(#3300),#2262,.T.);
#15281=ADVANCED_FACE('',(#3301),#2263,.T.);
#15282=ADVANCED_FACE('',(#3302),#2264,.T.);
#15283=ADVANCED_FACE('',(#3303),#2265,.T.);
#15284=ADVANCED_FACE('',(#3304),#2266,.T.);
#15285=ADVANCED_FACE('',(#3305),#2267,.T.);
#15286=ADVANCED_FACE('',(#3306),#2268,.T.);
#15287=ADVANCED_FACE('',(#3307),#2269,.T.);
#15288=ADVANCED_FACE('',(#3308),#2270,.T.);
#15289=ADVANCED_FACE('',(#3309),#238,.T.);
#15290=ADVANCED_FACE('',(#3310),#14583,.F.);
#15291=ADVANCED_FACE('',(#3311),#2271,.T.);
#15292=ADVANCED_FACE('',(#3312,#1673),#14584,.F.);
#15293=ADVANCED_FACE('',(#3313,#1674),#14585,.F.);
#15294=ADVANCED_FACE('',(#3314),#2272,.T.);
#15295=ADVANCED_FACE('',(#3315),#14586,.F.);
#15296=ADVANCED_FACE('',(#3316),#260,.F.);
#15297=ADVANCED_FACE('',(#3317),#2273,.T.);
#15298=ADVANCED_FACE('',(#3318),#261,.F.);
#15299=ADVANCED_FACE('',(#3319),#2274,.T.);
#15300=ADVANCED_FACE('',(#3320),#2275,.F.);
#15301=ADVANCED_FACE('',(#3321),#2276,.F.);
#15302=ADVANCED_FACE('',(#3322),#2277,.F.);
#15303=ADVANCED_FACE('',(#3323),#2278,.F.);
#15304=ADVANCED_FACE('',(#3324),#2279,.F.);
#15305=ADVANCED_FACE('',(#3325),#2280,.F.);
#15306=ADVANCED_FACE('',(#3326,#1675,#1676,#1677,#1678,#1679,#1680,#1681),
#14587,.F.);
#15307=ADVANCED_FACE('',(#3327),#2281,.T.);
#15308=ADVANCED_FACE('',(#3328,#1682,#1683,#1684,#1685,#1686,#1687),#14588,
 .T.);
#15309=ADVANCED_FACE('',(#3329,#1688),#14589,.F.);
#15310=ADVANCED_FACE('',(#3330),#2282,.T.);
#15485=CLOSED_SHELL('',(#15130,#15131,#15132,#15133,#15134,#15135,#15136,
#15137,#15138,#15139,#15140,#15141,#15142,#15143,#15144,#15145,#15146,#15147,
#15148,#15149,#15150,#15151,#15152,#15153,#15154,#15155,#15156,#15157,#15158,
#15159,#15160,#15161,#15162,#15163,#15164,#15165,#15166,#15167,#15168,#15169,
#15170,#15171,#15172,#15173,#15174,#15175,#15176,#15177,#15178,#15179,#15180,
#15181,#15182,#15183,#15184,#15185,#15186,#15187,#15188,#15189,#15190,#15191,
#15192,#15193,#15194,#15195,#15196,#15197,#15198,#15199,#15200,#15201,#15202,
#15203,#15204,#15205,#15206,#15207,#15208,#15209,#15210,#15211,#15212,#15213,
#15214,#15215,#15216,#15217,#15218,#15219,#15220,#15221,#15222,#15223,#15224,
#15225,#15226,#15227,#15228,#15229,#15230,#15231,#15232,#15233,#15234,#15235,
#15236,#15237,#15238,#15239,#15240,#15241,#15242,#15243,#15244,#15245,#15246,
#15247,#15248,#15249,#15250,#15251,#15252,#15253,#15254,#15255,#15256,#15257,
#15258,#15259,#15260,#15261,#15262,#15263,#15264,#15265,#15266,#15267,#15268,
#15269,#15270,#15271,#15272,#15273,#15274,#15275,#15276,#15277,#15278,#15279,
#15280,#15281,#15282,#15283,#15284,#15285,#15286,#15287,#15288,#15289,#15290,
#15291,#15292,#15293,#15294,#15295,#15296,#15297,#15298,#15299,#15300,#15301,
#15302,#15303,#15304,#15305,#15306,#15307,#15308,#15309,#15310));
#16304=AXIS2_PLACEMENT_3D('',#46839,#18534,#18535);
#16305=AXIS2_PLACEMENT_3D('',#46840,#18536,#18537);
#16306=AXIS2_PLACEMENT_3D('',#46865,#18539,#18540);
#16307=AXIS2_PLACEMENT_3D('',#46882,#18541,#18542);
#16308=AXIS2_PLACEMENT_3D('',#46930,#18544,#18545);
#16309=AXIS2_PLACEMENT_3D('',#46981,#18547,#18548);
#16310=AXIS2_PLACEMENT_3D('',#47032,#18550,#18551);
#16311=AXIS2_PLACEMENT_3D('',#47080,#18553,#18554);
#16312=AXIS2_PLACEMENT_3D('',#47128,#18556,#18557);
#16313=AXIS2_PLACEMENT_3D('',#47182,#18559,#18560);
#16314=AXIS2_PLACEMENT_3D('',#47230,#18562,#18563);
#16315=AXIS2_PLACEMENT_3D('',#47278,#18565,#18566);
#16316=AXIS2_PLACEMENT_3D('',#47329,#18568,#18569);
#16317=AXIS2_PLACEMENT_3D('',#47380,#18571,#18572);
#16318=AXIS2_PLACEMENT_3D('',#47428,#18574,#18575);
#16319=AXIS2_PLACEMENT_3D('',#47476,#18577,#18578);
#16320=AXIS2_PLACEMENT_3D('',#47530,#18580,#18581);
#16321=AXIS2_PLACEMENT_3D('',#47578,#18583,#18584);
#16322=AXIS2_PLACEMENT_3D('',#47626,#18586,#18587);
#16323=AXIS2_PLACEMENT_3D('',#47677,#18589,#18590);
#16324=AXIS2_PLACEMENT_3D('',#47728,#18592,#18593);
#16325=AXIS2_PLACEMENT_3D('',#47776,#18595,#18596);
#16326=AXIS2_PLACEMENT_3D('',#47824,#18598,#18599);
#16327=AXIS2_PLACEMENT_3D('',#47878,#18601,#18602);
#16328=AXIS2_PLACEMENT_3D('',#47926,#18604,#18605);
#16329=AXIS2_PLACEMENT_3D('',#47974,#18607,#18608);
#16330=AXIS2_PLACEMENT_3D('',#48025,#18610,#18611);
#16331=AXIS2_PLACEMENT_3D('',#48076,#18613,#18614);
#16332=AXIS2_PLACEMENT_3D('',#48124,#18616,#18617);
#16333=AXIS2_PLACEMENT_3D('',#48172,#18619,#18620);
#16334=AXIS2_PLACEMENT_3D('',#48226,#18622,#18623);
#16335=AXIS2_PLACEMENT_3D('',#48274,#18625,#18626);
#16336=AXIS2_PLACEMENT_3D('',#48322,#18628,#18629);
#16337=AXIS2_PLACEMENT_3D('',#48373,#18631,#18632);
#16338=AXIS2_PLACEMENT_3D('',#48424,#18634,#18635);
#16339=AXIS2_PLACEMENT_3D('',#48472,#18637,#18638);
#16340=AXIS2_PLACEMENT_3D('',#48520,#18640,#18641);
#16341=AXIS2_PLACEMENT_3D('',#48574,#18643,#18644);
#16342=AXIS2_PLACEMENT_3D('',#48622,#18646,#18647);
#16343=AXIS2_PLACEMENT_3D('',#48670,#18649,#18650);
#16344=AXIS2_PLACEMENT_3D('',#48721,#18652,#18653);
#16345=AXIS2_PLACEMENT_3D('',#48772,#18655,#18656);
#16346=AXIS2_PLACEMENT_3D('',#48820,#18658,#18659);
#16347=AXIS2_PLACEMENT_3D('',#48868,#18661,#18662);
#16348=AXIS2_PLACEMENT_3D('',#48922,#18664,#18665);
#16349=AXIS2_PLACEMENT_3D('',#48970,#18667,#18668);
#16350=AXIS2_PLACEMENT_3D('',#49018,#18670,#18671);
#16351=AXIS2_PLACEMENT_3D('',#49069,#18673,#18674);
#16352=AXIS2_PLACEMENT_3D('',#49120,#18676,#18677);
#16353=AXIS2_PLACEMENT_3D('',#49168,#18679,#18680);
#16354=AXIS2_PLACEMENT_3D('',#49216,#18682,#18683);
#16355=AXIS2_PLACEMENT_3D('',#49270,#18685,#18686);
#16356=AXIS2_PLACEMENT_3D('',#49318,#18688,#18689);
#16357=AXIS2_PLACEMENT_3D('',#49366,#18691,#18692);
#16358=AXIS2_PLACEMENT_3D('',#49417,#18694,#18695);
#16359=AXIS2_PLACEMENT_3D('',#49465,#18697,#18698);
#16360=AXIS2_PLACEMENT_3D('',#49513,#18700,#18701);
#16361=AXIS2_PLACEMENT_3D('',#49561,#18703,#18704);
#16362=AXIS2_PLACEMENT_3D('',#49615,#18706,#18707);
#16363=AXIS2_PLACEMENT_3D('',#49663,#18709,#18710);
#16364=AXIS2_PLACEMENT_3D('',#49711,#18712,#18713);
#16365=AXIS2_PLACEMENT_3D('',#49765,#18715,#18716);
#16366=AXIS2_PLACEMENT_3D('',#49813,#18718,#18719);
#16367=AXIS2_PLACEMENT_3D('',#49861,#18721,#18722);
#16368=AXIS2_PLACEMENT_3D('',#49909,#18724,#18725);
#16369=AXIS2_PLACEMENT_3D('',#49963,#18727,#18728);
#16370=AXIS2_PLACEMENT_3D('',#50011,#18730,#18731);
#16371=AXIS2_PLACEMENT_3D('',#50059,#18733,#18734);
#16372=AXIS2_PLACEMENT_3D('',#50113,#18736,#18737);
#16373=AXIS2_PLACEMENT_3D('',#50161,#18739,#18740);
#16374=AXIS2_PLACEMENT_3D('',#50209,#18742,#18743);
#16375=AXIS2_PLACEMENT_3D('',#50257,#18745,#18746);
#16376=AXIS2_PLACEMENT_3D('',#50311,#18748,#18749);
#16377=AXIS2_PLACEMENT_3D('',#50359,#18751,#18752);
#16378=AXIS2_PLACEMENT_3D('',#50407,#18754,#18755);
#16379=AXIS2_PLACEMENT_3D('',#50461,#18757,#18758);
#16380=AXIS2_PLACEMENT_3D('',#50509,#18760,#18761);
#16381=AXIS2_PLACEMENT_3D('',#50557,#18763,#18764);
#16382=AXIS2_PLACEMENT_3D('',#50605,#18766,#18767);
#16383=AXIS2_PLACEMENT_3D('',#50659,#18769,#18770);
#16384=AXIS2_PLACEMENT_3D('',#50707,#18772,#18773);
#16385=AXIS2_PLACEMENT_3D('',#50709,#18774,#18775);
#16386=AXIS2_PLACEMENT_3D('',#50713,#18777,#18778);
#16387=AXIS2_PLACEMENT_3D('',#50756,#18780,#18781);
#16388=AXIS2_PLACEMENT_3D('',#50757,#18782,#18783);
#16389=AXIS2_PLACEMENT_3D('',#50773,#18785,#18786);
#16390=AXIS2_PLACEMENT_3D('',#50781,#18787,#18788);
#16391=AXIS2_PLACEMENT_3D('',#50806,#18790,#18791);
#16392=AXIS2_PLACEMENT_3D('',#50830,#18793,#18794);
#16393=AXIS2_PLACEMENT_3D('',#50855,#18796,#18797);
#16394=AXIS2_PLACEMENT_3D('',#50880,#18799,#18800);
#16395=AXIS2_PLACEMENT_3D('',#50904,#18802,#18803);
#16396=AXIS2_PLACEMENT_3D('',#50928,#18805,#18806);
#16397=AXIS2_PLACEMENT_3D('',#50953,#18808,#18809);
#16398=AXIS2_PLACEMENT_3D('',#50978,#18811,#18812);
#16399=AXIS2_PLACEMENT_3D('',#51002,#18814,#18815);
#16400=AXIS2_PLACEMENT_3D('',#51027,#18817,#18818);
#16401=AXIS2_PLACEMENT_3D('',#51052,#18820,#18821);
#16402=AXIS2_PLACEMENT_3D('',#51076,#18823,#18824);
#16403=AXIS2_PLACEMENT_3D('',#51100,#18826,#18827);
#16404=AXIS2_PLACEMENT_3D('',#51125,#18829,#18830);
#16405=AXIS2_PLACEMENT_3D('',#51150,#18832,#18833);
#16406=AXIS2_PLACEMENT_3D('',#51174,#18835,#18836);
#16407=AXIS2_PLACEMENT_3D('',#51199,#18838,#18839);
#16408=AXIS2_PLACEMENT_3D('',#51224,#18841,#18842);
#16409=AXIS2_PLACEMENT_3D('',#51248,#18844,#18845);
#16410=AXIS2_PLACEMENT_3D('',#51272,#18847,#18848);
#16411=AXIS2_PLACEMENT_3D('',#51297,#18850,#18851);
#16412=AXIS2_PLACEMENT_3D('',#51322,#18853,#18854);
#16413=AXIS2_PLACEMENT_3D('',#51346,#18856,#18857);
#16414=AXIS2_PLACEMENT_3D('',#51371,#18859,#18860);
#16415=AXIS2_PLACEMENT_3D('',#51408,#18862,#18863);
#16416=AXIS2_PLACEMENT_3D('',#51444,#18865,#18866);
#16417=AXIS2_PLACEMENT_3D('',#51469,#18868,#18869);
#16418=AXIS2_PLACEMENT_3D('',#51493,#18871,#18872);
#16419=AXIS2_PLACEMENT_3D('',#51518,#18874,#18875);
#16420=AXIS2_PLACEMENT_3D('',#51542,#18877,#18878);
#16421=AXIS2_PLACEMENT_3D('',#51567,#18880,#18881);
#16422=AXIS2_PLACEMENT_3D('',#51592,#18883,#18884);
#16423=AXIS2_PLACEMENT_3D('',#51616,#18886,#18887);
#16424=AXIS2_PLACEMENT_3D('',#51641,#18889,#18890);
#16425=AXIS2_PLACEMENT_3D('',#51665,#18892,#18893);
#16426=AXIS2_PLACEMENT_3D('',#51690,#18895,#18896);
#16427=AXIS2_PLACEMENT_3D('',#51714,#18898,#18899);
#16428=AXIS2_PLACEMENT_3D('',#51739,#18901,#18902);
#16429=AXIS2_PLACEMENT_3D('',#51764,#18904,#18905);
#16430=AXIS2_PLACEMENT_3D('',#51788,#18907,#18908);
#16431=AXIS2_PLACEMENT_3D('',#51813,#18910,#18911);
#16432=AXIS2_PLACEMENT_3D('',#51837,#18913,#18914);
#16433=AXIS2_PLACEMENT_3D('',#51862,#18916,#18917);
#16434=AXIS2_PLACEMENT_3D('',#51886,#18919,#18920);
#16435=AXIS2_PLACEMENT_3D('',#51911,#18922,#18923);
#16436=AXIS2_PLACEMENT_3D('',#51936,#18925,#18926);
#16437=AXIS2_PLACEMENT_3D('',#51960,#18928,#18929);
#16438=AXIS2_PLACEMENT_3D('',#51985,#18931,#18932);
#16439=AXIS2_PLACEMENT_3D('',#52009,#18934,#18935);
#16440=AXIS2_PLACEMENT_3D('',#52034,#18937,#18938);
#16441=AXIS2_PLACEMENT_3D('',#52058,#18940,#18941);
#16442=AXIS2_PLACEMENT_3D('',#52083,#18943,#18944);
#16443=AXIS2_PLACEMENT_3D('',#52108,#18946,#18947);
#16444=AXIS2_PLACEMENT_3D('',#52132,#18949,#18950);
#16445=AXIS2_PLACEMENT_3D('',#52157,#18952,#18953);
#16446=AXIS2_PLACEMENT_3D('',#52181,#18955,#18956);
#16447=AXIS2_PLACEMENT_3D('',#52206,#18958,#18959);
#16448=AXIS2_PLACEMENT_3D('',#52230,#18961,#18962);
#16449=AXIS2_PLACEMENT_3D('',#52255,#18964,#18965);
#16450=AXIS2_PLACEMENT_3D('',#52280,#18967,#18968);
#16451=AXIS2_PLACEMENT_3D('',#52304,#18970,#18971);
#16452=AXIS2_PLACEMENT_3D('',#52329,#18973,#18974);
#16453=AXIS2_PLACEMENT_3D('',#52353,#18976,#18977);
#16454=AXIS2_PLACEMENT_3D('',#52378,#18979,#18980);
#16455=AXIS2_PLACEMENT_3D('',#52402,#18982,#18983);
#16456=AXIS2_PLACEMENT_3D('',#52427,#18985,#18986);
#16457=AXIS2_PLACEMENT_3D('',#52452,#18988,#18989);
#16458=AXIS2_PLACEMENT_3D('',#52476,#18991,#18992);
#16459=AXIS2_PLACEMENT_3D('',#52501,#18994,#18995);
#16460=AXIS2_PLACEMENT_3D('',#52525,#18997,#18998);
#16461=AXIS2_PLACEMENT_3D('',#52550,#19000,#19001);
#16462=AXIS2_PLACEMENT_3D('',#52574,#19003,#19004);
#16463=AXIS2_PLACEMENT_3D('',#52599,#19006,#19007);
#16464=AXIS2_PLACEMENT_3D('',#52624,#19009,#19010);
#16465=AXIS2_PLACEMENT_3D('',#52648,#19012,#19013);
#16466=AXIS2_PLACEMENT_3D('',#52673,#19015,#19016);
#16467=AXIS2_PLACEMENT_3D('',#52697,#19018,#19019);
#16468=AXIS2_PLACEMENT_3D('',#52722,#19021,#19022);
#16469=AXIS2_PLACEMENT_3D('',#52746,#19024,#19025);
#16470=AXIS2_PLACEMENT_3D('',#53102,#19026,#19027);
#16471=AXIS2_PLACEMENT_3D('',#53103,#19028,#19029);
#16472=AXIS2_PLACEMENT_3D('',#53113,#19030,#19031);
#16473=AXIS2_PLACEMENT_3D('',#53121,#19032,#19033);
#16474=AXIS2_PLACEMENT_3D('',#53123,#19034,#19035);
#16475=AXIS2_PLACEMENT_3D('',#53126,#19037,#19038);
#16476=AXIS2_PLACEMENT_3D('',#53127,#19039,#19040);
#16477=AXIS2_PLACEMENT_3D('',#53128,#19041,#19042);
#16478=AXIS2_PLACEMENT_3D('',#53130,#19043,#19044);
#16479=AXIS2_PLACEMENT_3D('',#53131,#19045,#19046);
#16480=AXIS2_PLACEMENT_3D('',#53133,#19047,#19048);
#16481=AXIS2_PLACEMENT_3D('',#53135,#19050,#19051);
#16482=AXIS2_PLACEMENT_3D('',#55424,#19052,#19053);
#16483=AXIS2_PLACEMENT_3D('',#57496,#19054,#19055);
#16484=AXIS2_PLACEMENT_3D('',#57497,#19056,#19057);
#16485=AXIS2_PLACEMENT_3D('',#57499,#19058,#19059);
#16486=AXIS2_PLACEMENT_3D('',#57502,#19061,#19062);
#16487=AXIS2_PLACEMENT_3D('',#57503,#19063,#19064);
#16488=AXIS2_PLACEMENT_3D('',#57505,#19065,#19066);
#16489=AXIS2_PLACEMENT_3D('',#57508,#19068,#19069);
#16490=AXIS2_PLACEMENT_3D('',#57509,#19070,#19071);
#16491=AXIS2_PLACEMENT_3D('',#57511,#19072,#19073);
#16492=AXIS2_PLACEMENT_3D('',#57514,#19075,#19076);
#16493=AXIS2_PLACEMENT_3D('',#57515,#19077,#19078);
#16494=AXIS2_PLACEMENT_3D('',#57517,#19079,#19080);
#16495=AXIS2_PLACEMENT_3D('',#57520,#19082,#19083);
#16496=AXIS2_PLACEMENT_3D('',#57521,#19084,#19085);
#16497=AXIS2_PLACEMENT_3D('',#57523,#19086,#19087);
#16498=AXIS2_PLACEMENT_3D('',#57526,#19089,#19090);
#16499=AXIS2_PLACEMENT_3D('',#57527,#19091,#19092);
#16500=AXIS2_PLACEMENT_3D('',#57529,#19093,#19094);
#16501=AXIS2_PLACEMENT_3D('',#57532,#19096,#19097);
#16502=AXIS2_PLACEMENT_3D('',#57533,#19098,#19099);
#16503=AXIS2_PLACEMENT_3D('',#57535,#19100,#19101);
#16504=AXIS2_PLACEMENT_3D('',#57537,#19102,#19103);
#16505=AXIS2_PLACEMENT_3D('',#57538,#19104,#19105);
#16506=AXIS2_PLACEMENT_3D('',#57540,#19106,#19107);
#16507=AXIS2_PLACEMENT_3D('',#57542,#19109,#19110);
#16508=AXIS2_PLACEMENT_3D('',#57543,#19111,#19112);
#16509=AXIS2_PLACEMENT_3D('',#57545,#19113,#19114);
#16510=AXIS2_PLACEMENT_3D('',#57546,#19115,#19116);
#18534=DIRECTION('axis',(0.,0.,1.));
#18535=DIRECTION('refdir',(1.,0.,0.));
#18536=DIRECTION('center_axis',(0.,0.,1.));
#18537=DIRECTION('ref_axis',(1.,0.,0.));
#18538=DIRECTION('',(0.,0.,-1.));
#18539=DIRECTION('center_axis',(0.,0.,1.));
#18540=DIRECTION('ref_axis',(1.,0.,0.));
#18541=DIRECTION('center_axis',(0.,0.,1.));
#18542=DIRECTION('ref_axis',(1.,0.,0.));
#18543=DIRECTION('',(0.,0.,-1.));
#18544=DIRECTION('center_axis',(0.,0.,1.));
#18545=DIRECTION('ref_axis',(1.,0.,0.));
#18546=DIRECTION('',(0.,0.,-1.));
#18547=DIRECTION('center_axis',(0.,0.,1.));
#18548=DIRECTION('ref_axis',(1.,0.,0.));
#18549=DIRECTION('',(0.,0.,-1.));
#18550=DIRECTION('center_axis',(0.,0.,1.));
#18551=DIRECTION('ref_axis',(1.,0.,0.));
#18552=DIRECTION('',(0.,0.,-1.));
#18553=DIRECTION('center_axis',(0.,0.,1.));
#18554=DIRECTION('ref_axis',(1.,0.,0.));
#18555=DIRECTION('',(0.,0.,-1.));
#18556=DIRECTION('center_axis',(0.,0.,1.));
#18557=DIRECTION('ref_axis',(1.,0.,0.));
#18558=DIRECTION('',(0.,0.,-1.));
#18559=DIRECTION('center_axis',(0.,0.,1.));
#18560=DIRECTION('ref_axis',(1.,0.,0.));
#18561=DIRECTION('',(0.,0.,-1.));
#18562=DIRECTION('center_axis',(0.,0.,1.));
#18563=DIRECTION('ref_axis',(1.,0.,0.));
#18564=DIRECTION('',(0.,0.,-1.));
#18565=DIRECTION('center_axis',(0.,0.,1.));
#18566=DIRECTION('ref_axis',(1.,0.,0.));
#18567=DIRECTION('',(0.,0.,-1.));
#18568=DIRECTION('center_axis',(0.,0.,1.));
#18569=DIRECTION('ref_axis',(1.,0.,0.));
#18570=DIRECTION('',(0.,0.,-1.));
#18571=DIRECTION('center_axis',(0.,0.,1.));
#18572=DIRECTION('ref_axis',(1.,0.,0.));
#18573=DIRECTION('',(0.,0.,-1.));
#18574=DIRECTION('center_axis',(0.,0.,1.));
#18575=DIRECTION('ref_axis',(1.,0.,0.));
#18576=DIRECTION('',(0.,0.,-1.));
#18577=DIRECTION('center_axis',(0.,0.,1.));
#18578=DIRECTION('ref_axis',(1.,0.,0.));
#18579=DIRECTION('',(0.,0.,-1.));
#18580=DIRECTION('center_axis',(0.,0.,1.));
#18581=DIRECTION('ref_axis',(1.,0.,0.));
#18582=DIRECTION('',(0.,0.,-1.));
#18583=DIRECTION('center_axis',(0.,0.,1.));
#18584=DIRECTION('ref_axis',(1.,0.,0.));
#18585=DIRECTION('',(0.,0.,-1.));
#18586=DIRECTION('center_axis',(0.,0.,1.));
#18587=DIRECTION('ref_axis',(1.,0.,0.));
#18588=DIRECTION('',(0.,0.,-1.));
#18589=DIRECTION('center_axis',(0.,0.,1.));
#18590=DIRECTION('ref_axis',(1.,0.,0.));
#18591=DIRECTION('',(0.,0.,-1.));
#18592=DIRECTION('center_axis',(0.,0.,1.));
#18593=DIRECTION('ref_axis',(1.,0.,0.));
#18594=DIRECTION('',(0.,0.,-1.));
#18595=DIRECTION('center_axis',(0.,0.,1.));
#18596=DIRECTION('ref_axis',(1.,0.,0.));
#18597=DIRECTION('',(0.,0.,-1.));
#18598=DIRECTION('center_axis',(0.,0.,1.));
#18599=DIRECTION('ref_axis',(1.,0.,0.));
#18600=DIRECTION('',(0.,0.,-1.));
#18601=DIRECTION('center_axis',(0.,0.,1.));
#18602=DIRECTION('ref_axis',(1.,0.,0.));
#18603=DIRECTION('',(0.,0.,-1.));
#18604=DIRECTION('center_axis',(0.,0.,1.));
#18605=DIRECTION('ref_axis',(1.,0.,0.));
#18606=DIRECTION('',(0.,0.,-1.));
#18607=DIRECTION('center_axis',(0.,0.,1.));
#18608=DIRECTION('ref_axis',(1.,0.,0.));
#18609=DIRECTION('',(0.,0.,-1.));
#18610=DIRECTION('center_axis',(0.,0.,1.));
#18611=DIRECTION('ref_axis',(1.,0.,0.));
#18612=DIRECTION('',(0.,0.,-1.));
#18613=DIRECTION('center_axis',(0.,0.,1.));
#18614=DIRECTION('ref_axis',(1.,0.,0.));
#18615=DIRECTION('',(0.,0.,-1.));
#18616=DIRECTION('center_axis',(0.,0.,1.));
#18617=DIRECTION('ref_axis',(1.,0.,0.));
#18618=DIRECTION('',(0.,0.,-1.));
#18619=DIRECTION('center_axis',(0.,0.,1.));
#18620=DIRECTION('ref_axis',(1.,0.,0.));
#18621=DIRECTION('',(0.,0.,-1.));
#18622=DIRECTION('center_axis',(0.,0.,1.));
#18623=DIRECTION('ref_axis',(1.,0.,0.));
#18624=DIRECTION('',(0.,0.,-1.));
#18625=DIRECTION('center_axis',(0.,0.,1.));
#18626=DIRECTION('ref_axis',(1.,0.,0.));
#18627=DIRECTION('',(0.,0.,-1.));
#18628=DIRECTION('center_axis',(0.,0.,1.));
#18629=DIRECTION('ref_axis',(1.,0.,0.));
#18630=DIRECTION('',(0.,0.,-1.));
#18631=DIRECTION('center_axis',(0.,0.,1.));
#18632=DIRECTION('ref_axis',(1.,0.,0.));
#18633=DIRECTION('',(0.,0.,-1.));
#18634=DIRECTION('center_axis',(0.,0.,1.));
#18635=DIRECTION('ref_axis',(1.,0.,0.));
#18636=DIRECTION('',(0.,0.,-1.));
#18637=DIRECTION('center_axis',(0.,0.,1.));
#18638=DIRECTION('ref_axis',(1.,0.,0.));
#18639=DIRECTION('',(0.,0.,-1.));
#18640=DIRECTION('center_axis',(0.,0.,1.));
#18641=DIRECTION('ref_axis',(1.,0.,0.));
#18642=DIRECTION('',(0.,0.,-1.));
#18643=DIRECTION('center_axis',(0.,0.,1.));
#18644=DIRECTION('ref_axis',(1.,0.,0.));
#18645=DIRECTION('',(0.,0.,-1.));
#18646=DIRECTION('center_axis',(0.,0.,1.));
#18647=DIRECTION('ref_axis',(1.,0.,0.));
#18648=DIRECTION('',(0.,0.,-1.));
#18649=DIRECTION('center_axis',(0.,0.,1.));
#18650=DIRECTION('ref_axis',(1.,0.,0.));
#18651=DIRECTION('',(0.,0.,-1.));
#18652=DIRECTION('center_axis',(0.,0.,1.));
#18653=DIRECTION('ref_axis',(1.,0.,0.));
#18654=DIRECTION('',(0.,0.,-1.));
#18655=DIRECTION('center_axis',(0.,0.,1.));
#18656=DIRECTION('ref_axis',(1.,0.,0.));
#18657=DIRECTION('',(0.,0.,-1.));
#18658=DIRECTION('center_axis',(0.,0.,1.));
#18659=DIRECTION('ref_axis',(1.,0.,0.));
#18660=DIRECTION('',(0.,0.,-1.));
#18661=DIRECTION('center_axis',(0.,0.,1.));
#18662=DIRECTION('ref_axis',(1.,0.,0.));
#18663=DIRECTION('',(0.,0.,-1.));
#18664=DIRECTION('center_axis',(0.,0.,1.));
#18665=DIRECTION('ref_axis',(1.,0.,0.));
#18666=DIRECTION('',(0.,0.,-1.));
#18667=DIRECTION('center_axis',(0.,0.,1.));
#18668=DIRECTION('ref_axis',(1.,0.,0.));
#18669=DIRECTION('',(0.,0.,-1.));
#18670=DIRECTION('center_axis',(0.,0.,1.));
#18671=DIRECTION('ref_axis',(1.,0.,0.));
#18672=DIRECTION('',(0.,0.,-1.));
#18673=DIRECTION('center_axis',(0.,0.,1.));
#18674=DIRECTION('ref_axis',(1.,0.,0.));
#18675=DIRECTION('',(0.,0.,-1.));
#18676=DIRECTION('center_axis',(0.,0.,1.));
#18677=DIRECTION('ref_axis',(1.,0.,0.));
#18678=DIRECTION('',(0.,0.,-1.));
#18679=DIRECTION('center_axis',(0.,0.,1.));
#18680=DIRECTION('ref_axis',(1.,0.,0.));
#18681=DIRECTION('',(0.,0.,-1.));
#18682=DIRECTION('center_axis',(0.,0.,1.));
#18683=DIRECTION('ref_axis',(1.,0.,0.));
#18684=DIRECTION('',(0.,0.,-1.));
#18685=DIRECTION('center_axis',(0.,0.,1.));
#18686=DIRECTION('ref_axis',(1.,0.,0.));
#18687=DIRECTION('',(0.,0.,-1.));
#18688=DIRECTION('center_axis',(0.,0.,1.));
#18689=DIRECTION('ref_axis',(1.,0.,0.));
#18690=DIRECTION('',(0.,0.,-1.));
#18691=DIRECTION('center_axis',(0.,0.,1.));
#18692=DIRECTION('ref_axis',(1.,0.,0.));
#18693=DIRECTION('',(0.,0.,-1.));
#18694=DIRECTION('center_axis',(0.,0.,1.));
#18695=DIRECTION('ref_axis',(1.,0.,0.));
#18696=DIRECTION('',(0.,0.,-1.));
#18697=DIRECTION('center_axis',(0.,0.,1.));
#18698=DIRECTION('ref_axis',(1.,0.,0.));
#18699=DIRECTION('',(0.,0.,-1.));
#18700=DIRECTION('center_axis',(0.,0.,1.));
#18701=DIRECTION('ref_axis',(1.,0.,0.));
#18702=DIRECTION('',(0.,0.,-1.));
#18703=DIRECTION('center_axis',(0.,0.,1.));
#18704=DIRECTION('ref_axis',(1.,0.,0.));
#18705=DIRECTION('',(0.,0.,-1.));
#18706=DIRECTION('center_axis',(0.,0.,1.));
#18707=DIRECTION('ref_axis',(1.,0.,0.));
#18708=DIRECTION('',(0.,0.,-1.));
#18709=DIRECTION('center_axis',(0.,0.,1.));
#18710=DIRECTION('ref_axis',(1.,0.,0.));
#18711=DIRECTION('',(0.,0.,-1.));
#18712=DIRECTION('center_axis',(0.,0.,1.));
#18713=DIRECTION('ref_axis',(1.,0.,0.));
#18714=DIRECTION('',(0.,0.,-1.));
#18715=DIRECTION('center_axis',(0.,0.,1.));
#18716=DIRECTION('ref_axis',(1.,0.,0.));
#18717=DIRECTION('',(0.,0.,-1.));
#18718=DIRECTION('center_axis',(0.,0.,1.));
#18719=DIRECTION('ref_axis',(1.,0.,0.));
#18720=DIRECTION('',(0.,0.,-1.));
#18721=DIRECTION('center_axis',(0.,0.,1.));
#18722=DIRECTION('ref_axis',(1.,0.,0.));
#18723=DIRECTION('',(0.,0.,-1.));
#18724=DIRECTION('center_axis',(0.,0.,1.));
#18725=DIRECTION('ref_axis',(1.,0.,0.));
#18726=DIRECTION('',(0.,0.,-1.));
#18727=DIRECTION('center_axis',(0.,0.,1.));
#18728=DIRECTION('ref_axis',(1.,0.,0.));
#18729=DIRECTION('',(0.,0.,-1.));
#18730=DIRECTION('center_axis',(0.,0.,1.));
#18731=DIRECTION('ref_axis',(1.,0.,0.));
#18732=DIRECTION('',(0.,0.,-1.));
#18733=DIRECTION('center_axis',(0.,0.,1.));
#18734=DIRECTION('ref_axis',(1.,0.,0.));
#18735=DIRECTION('',(0.,0.,-1.));
#18736=DIRECTION('center_axis',(0.,0.,1.));
#18737=DIRECTION('ref_axis',(1.,0.,0.));
#18738=DIRECTION('',(0.,0.,-1.));
#18739=DIRECTION('center_axis',(0.,0.,1.));
#18740=DIRECTION('ref_axis',(1.,0.,0.));
#18741=DIRECTION('',(0.,0.,-1.));
#18742=DIRECTION('center_axis',(0.,0.,1.));
#18743=DIRECTION('ref_axis',(1.,0.,0.));
#18744=DIRECTION('',(0.,0.,-1.));
#18745=DIRECTION('center_axis',(0.,0.,1.));
#18746=DIRECTION('ref_axis',(1.,0.,0.));
#18747=DIRECTION('',(0.,0.,-1.));
#18748=DIRECTION('center_axis',(0.,0.,1.));
#18749=DIRECTION('ref_axis',(1.,0.,0.));
#18750=DIRECTION('',(0.,0.,-1.));
#18751=DIRECTION('center_axis',(0.,0.,1.));
#18752=DIRECTION('ref_axis',(1.,0.,0.));
#18753=DIRECTION('',(0.,0.,-1.));
#18754=DIRECTION('center_axis',(0.,0.,1.));
#18755=DIRECTION('ref_axis',(1.,0.,0.));
#18756=DIRECTION('',(0.,0.,-1.));
#18757=DIRECTION('center_axis',(0.,0.,1.));
#18758=DIRECTION('ref_axis',(1.,0.,0.));
#18759=DIRECTION('',(0.,0.,-1.));
#18760=DIRECTION('center_axis',(0.,0.,1.));
#18761=DIRECTION('ref_axis',(1.,0.,0.));
#18762=DIRECTION('',(0.,0.,-1.));
#18763=DIRECTION('center_axis',(0.,0.,1.));
#18764=DIRECTION('ref_axis',(1.,0.,0.));
#18765=DIRECTION('',(0.,0.,-1.));
#18766=DIRECTION('center_axis',(0.,0.,1.));
#18767=DIRECTION('ref_axis',(1.,0.,0.));
#18768=DIRECTION('',(0.,0.,-1.));
#18769=DIRECTION('center_axis',(0.,0.,1.));
#18770=DIRECTION('ref_axis',(1.,0.,0.));
#18771=DIRECTION('',(0.,0.,-1.));
#18772=DIRECTION('center_axis',(0.,0.,1.));
#18773=DIRECTION('ref_axis',(1.,0.,0.));
#18774=DIRECTION('center_axis',(0.,0.,-1.));
#18775=DIRECTION('ref_axis',(1.,0.,0.));
#18776=DIRECTION('',(0.,0.,-1.));
#18777=DIRECTION('center_axis',(0.,0.,1.));
#18778=DIRECTION('ref_axis',(1.,0.,0.));
#18779=DIRECTION('',(0.,0.,-1.));
#18780=DIRECTION('center_axis',(0.,0.,1.));
#18781=DIRECTION('ref_axis',(1.,0.,0.));
#18782=DIRECTION('center_axis',(0.,0.,1.));
#18783=DIRECTION('ref_axis',(-0.45747178569478,-0.889224136701894,0.));
#18784=DIRECTION('',(0.,0.,1.));
#18785=DIRECTION('center_axis',(0.,0.,1.));
#18786=DIRECTION('ref_axis',(1.,-1.39943489555162E-12,0.));
#18787=DIRECTION('center_axis',(0.,0.,1.));
#18788=DIRECTION('ref_axis',(1.,-1.39943489555162E-12,0.));
#18789=DIRECTION('',(0.,0.,1.));
#18790=DIRECTION('center_axis',(0.,0.,1.));
#18791=DIRECTION('ref_axis',(1.,-1.39943489555162E-12,0.));
#18792=DIRECTION('',(0.,0.,1.));
#18793=DIRECTION('center_axis',(0.,0.,1.));
#18794=DIRECTION('ref_axis',(1.,-1.39943489555162E-12,0.));
#18795=DIRECTION('',(0.,0.,1.));
#18796=DIRECTION('center_axis',(0.,0.,1.));
#18797=DIRECTION('ref_axis',(1.,-1.39943489555162E-12,0.));
#18798=DIRECTION('',(0.,0.,1.));
#18799=DIRECTION('center_axis',(0.,0.,1.));
#18800=DIRECTION('ref_axis',(1.,-1.39943489555162E-12,0.));
#18801=DIRECTION('',(0.,0.,1.));
#18802=DIRECTION('center_axis',(0.,0.,1.));
#18803=DIRECTION('ref_axis',(1.,-1.39943489555162E-12,0.));
#18804=DIRECTION('',(0.,0.,1.));
#18805=DIRECTION('center_axis',(0.,0.,1.));
#18806=DIRECTION('ref_axis',(1.,-1.39943489555162E-12,0.));
#18807=DIRECTION('',(0.,0.,1.));
#18808=DIRECTION('center_axis',(0.,0.,1.));
#18809=DIRECTION('ref_axis',(1.,-1.39943489555162E-12,0.));
#18810=DIRECTION('',(0.,0.,1.));
#18811=DIRECTION('center_axis',(0.,0.,1.));
#18812=DIRECTION('ref_axis',(1.,-1.39943489555162E-12,0.));
#18813=DIRECTION('',(0.,0.,1.));
#18814=DIRECTION('center_axis',(0.,0.,1.));
#18815=DIRECTION('ref_axis',(1.,-1.39943489555162E-12,0.));
#18816=DIRECTION('',(0.,0.,1.));
#18817=DIRECTION('center_axis',(0.,0.,1.));
#18818=DIRECTION('ref_axis',(1.,-1.39943489555162E-12,0.));
#18819=DIRECTION('',(0.,0.,1.));
#18820=DIRECTION('center_axis',(0.,0.,1.));
#18821=DIRECTION('ref_axis',(1.,-1.39943489555162E-12,0.));
#18822=DIRECTION('',(0.,0.,1.));
#18823=DIRECTION('center_axis',(0.,0.,1.));
#18824=DIRECTION('ref_axis',(1.,-1.39943489555162E-12,0.));
#18825=DIRECTION('',(0.,0.,1.));
#18826=DIRECTION('center_axis',(0.,0.,1.));
#18827=DIRECTION('ref_axis',(1.,-1.39943489555162E-12,0.));
#18828=DIRECTION('',(0.,0.,1.));
#18829=DIRECTION('center_axis',(0.,0.,1.));
#18830=DIRECTION('ref_axis',(1.,-1.39943489555162E-12,0.));
#18831=DIRECTION('',(0.,0.,1.));
#18832=DIRECTION('center_axis',(0.,0.,1.));
#18833=DIRECTION('ref_axis',(1.,-1.39943489555162E-12,0.));
#18834=DIRECTION('',(0.,0.,1.));
#18835=DIRECTION('center_axis',(0.,0.,1.));
#18836=DIRECTION('ref_axis',(1.,-1.39943489555162E-12,0.));
#18837=DIRECTION('',(0.,0.,1.));
#18838=DIRECTION('center_axis',(0.,0.,1.));
#18839=DIRECTION('ref_axis',(1.,-1.39943489555162E-12,0.));
#18840=DIRECTION('',(0.,0.,1.));
#18841=DIRECTION('center_axis',(0.,0.,1.));
#18842=DIRECTION('ref_axis',(1.,-1.39943489555162E-12,0.));
#18843=DIRECTION('',(0.,0.,1.));
#18844=DIRECTION('center_axis',(0.,0.,1.));
#18845=DIRECTION('ref_axis',(1.,-1.39943489555162E-12,0.));
#18846=DIRECTION('',(0.,0.,1.));
#18847=DIRECTION('center_axis',(0.,0.,1.));
#18848=DIRECTION('ref_axis',(1.,-1.39943489555162E-12,0.));
#18849=DIRECTION('',(0.,0.,1.));
#18850=DIRECTION('center_axis',(0.,0.,1.));
#18851=DIRECTION('ref_axis',(1.,-1.39943489555162E-12,0.));
#18852=DIRECTION('',(0.,0.,1.));
#18853=DIRECTION('center_axis',(0.,0.,1.));
#18854=DIRECTION('ref_axis',(1.,-1.39943489555162E-12,0.));
#18855=DIRECTION('',(0.,0.,1.));
#18856=DIRECTION('center_axis',(0.,0.,1.));
#18857=DIRECTION('ref_axis',(1.,-1.39943489555162E-12,0.));
#18858=DIRECTION('',(0.,0.,1.));
#18859=DIRECTION('center_axis',(0.,0.,1.));
#18860=DIRECTION('ref_axis',(1.,-1.39943489555162E-12,0.));
#18861=DIRECTION('',(0.,0.,1.));
#18862=DIRECTION('center_axis',(0.,0.,1.));
#18863=DIRECTION('ref_axis',(1.,-1.39943489555162E-12,0.));
#18864=DIRECTION('',(0.,0.,1.));
#18865=DIRECTION('center_axis',(0.,0.,1.));
#18866=DIRECTION('ref_axis',(1.,-1.39943489555162E-12,0.));
#18867=DIRECTION('',(0.,0.,1.));
#18868=DIRECTION('center_axis',(0.,0.,1.));
#18869=DIRECTION('ref_axis',(1.,-1.39943489555162E-12,0.));
#18870=DIRECTION('',(0.,0.,1.));
#18871=DIRECTION('center_axis',(0.,0.,1.));
#18872=DIRECTION('ref_axis',(1.,-1.39943489555162E-12,0.));
#18873=DIRECTION('',(0.,0.,1.));
#18874=DIRECTION('center_axis',(0.,0.,1.));
#18875=DIRECTION('ref_axis',(1.,-1.39943489555162E-12,0.));
#18876=DIRECTION('',(0.,0.,1.));
#18877=DIRECTION('center_axis',(0.,0.,1.));
#18878=DIRECTION('ref_axis',(1.,-1.39943489555162E-12,0.));
#18879=DIRECTION('',(0.,0.,1.));
#18880=DIRECTION('center_axis',(0.,0.,1.));
#18881=DIRECTION('ref_axis',(1.,-1.39943489555162E-12,0.));
#18882=DIRECTION('',(0.,0.,1.));
#18883=DIRECTION('center_axis',(0.,0.,1.));
#18884=DIRECTION('ref_axis',(1.,-1.39943489555162E-12,0.));
#18885=DIRECTION('',(0.,0.,1.));
#18886=DIRECTION('center_axis',(0.,0.,1.));
#18887=DIRECTION('ref_axis',(1.,-1.39943489555162E-12,0.));
#18888=DIRECTION('',(0.,0.,1.));
#18889=DIRECTION('center_axis',(0.,0.,1.));
#18890=DIRECTION('ref_axis',(1.,-1.39943489555162E-12,0.));
#18891=DIRECTION('',(0.,0.,1.));
#18892=DIRECTION('center_axis',(0.,0.,1.));
#18893=DIRECTION('ref_axis',(1.,-1.39943489555162E-12,0.));
#18894=DIRECTION('',(0.,0.,1.));
#18895=DIRECTION('center_axis',(0.,0.,1.));
#18896=DIRECTION('ref_axis',(1.,-1.39943489555162E-12,0.));
#18897=DIRECTION('',(0.,0.,1.));
#18898=DIRECTION('center_axis',(0.,0.,1.));
#18899=DIRECTION('ref_axis',(1.,-1.39943489555162E-12,0.));
#18900=DIRECTION('',(0.,0.,1.));
#18901=DIRECTION('center_axis',(0.,0.,1.));
#18902=DIRECTION('ref_axis',(1.,-1.39943489555162E-12,0.));
#18903=DIRECTION('',(0.,0.,1.));
#18904=DIRECTION('center_axis',(0.,0.,1.));
#18905=DIRECTION('ref_axis',(1.,-1.39943489555162E-12,0.));
#18906=DIRECTION('',(0.,0.,1.));
#18907=DIRECTION('center_axis',(0.,0.,1.));
#18908=DIRECTION('ref_axis',(1.,-1.39943489555162E-12,0.));
#18909=DIRECTION('',(0.,0.,1.));
#18910=DIRECTION('center_axis',(0.,0.,1.));
#18911=DIRECTION('ref_axis',(1.,-1.39943489555162E-12,0.));
#18912=DIRECTION('',(0.,0.,1.));
#18913=DIRECTION('center_axis',(0.,0.,1.));
#18914=DIRECTION('ref_axis',(1.,-1.39943489555162E-12,0.));
#18915=DIRECTION('',(0.,0.,1.));
#18916=DIRECTION('center_axis',(0.,0.,1.));
#18917=DIRECTION('ref_axis',(1.,-1.39943489555162E-12,0.));
#18918=DIRECTION('',(0.,0.,1.));
#18919=DIRECTION('center_axis',(0.,0.,1.));
#18920=DIRECTION('ref_axis',(1.,-1.39943489555162E-12,0.));
#18921=DIRECTION('',(0.,0.,1.));
#18922=DIRECTION('center_axis',(0.,0.,1.));
#18923=DIRECTION('ref_axis',(1.,-1.39943489555162E-12,0.));
#18924=DIRECTION('',(0.,0.,1.));
#18925=DIRECTION('center_axis',(0.,0.,1.));
#18926=DIRECTION('ref_axis',(1.,-1.39943489555162E-12,0.));
#18927=DIRECTION('',(0.,0.,1.));
#18928=DIRECTION('center_axis',(0.,0.,1.));
#18929=DIRECTION('ref_axis',(1.,-1.39943489555162E-12,0.));
#18930=DIRECTION('',(0.,0.,1.));
#18931=DIRECTION('center_axis',(0.,0.,1.));
#18932=DIRECTION('ref_axis',(1.,-1.39943489555162E-12,0.));
#18933=DIRECTION('',(0.,0.,1.));
#18934=DIRECTION('center_axis',(0.,0.,1.));
#18935=DIRECTION('ref_axis',(1.,-1.39943489555162E-12,0.));
#18936=DIRECTION('',(0.,0.,1.));
#18937=DIRECTION('center_axis',(0.,0.,1.));
#18938=DIRECTION('ref_axis',(1.,-1.39943489555162E-12,0.));
#18939=DIRECTION('',(0.,0.,1.));
#18940=DIRECTION('center_axis',(0.,0.,1.));
#18941=DIRECTION('ref_axis',(1.,-1.39943489555162E-12,0.));
#18942=DIRECTION('',(0.,0.,1.));
#18943=DIRECTION('center_axis',(0.,0.,1.));
#18944=DIRECTION('ref_axis',(1.,-1.39943489555162E-12,0.));
#18945=DIRECTION('',(0.,0.,1.));
#18946=DIRECTION('center_axis',(0.,0.,1.));
#18947=DIRECTION('ref_axis',(1.,-1.39943489555162E-12,0.));
#18948=DIRECTION('',(0.,0.,1.));
#18949=DIRECTION('center_axis',(0.,0.,1.));
#18950=DIRECTION('ref_axis',(1.,-1.39943489555162E-12,0.));
#18951=DIRECTION('',(0.,0.,1.));
#18952=DIRECTION('center_axis',(0.,0.,1.));
#18953=DIRECTION('ref_axis',(1.,-1.39943489555162E-12,0.));
#18954=DIRECTION('',(0.,0.,1.));
#18955=DIRECTION('center_axis',(0.,0.,1.));
#18956=DIRECTION('ref_axis',(1.,-1.39943489555162E-12,0.));
#18957=DIRECTION('',(0.,0.,1.));
#18958=DIRECTION('center_axis',(0.,0.,1.));
#18959=DIRECTION('ref_axis',(1.,-1.39943489555162E-12,0.));
#18960=DIRECTION('',(0.,0.,1.));
#18961=DIRECTION('center_axis',(0.,0.,1.));
#18962=DIRECTION('ref_axis',(1.,-1.39943489555162E-12,0.));
#18963=DIRECTION('',(0.,0.,1.));
#18964=DIRECTION('center_axis',(0.,0.,1.));
#18965=DIRECTION('ref_axis',(1.,-1.39943489555162E-12,0.));
#18966=DIRECTION('',(0.,0.,1.));
#18967=DIRECTION('center_axis',(0.,0.,1.));
#18968=DIRECTION('ref_axis',(1.,-1.39943489555162E-12,0.));
#18969=DIRECTION('',(0.,0.,1.));
#18970=DIRECTION('center_axis',(0.,0.,1.));
#18971=DIRECTION('ref_axis',(1.,-1.39943489555162E-12,0.));
#18972=DIRECTION('',(0.,0.,1.));
#18973=DIRECTION('center_axis',(0.,0.,1.));
#18974=DIRECTION('ref_axis',(1.,-1.39943489555162E-12,0.));
#18975=DIRECTION('',(0.,0.,1.));
#18976=DIRECTION('center_axis',(0.,0.,1.));
#18977=DIRECTION('ref_axis',(1.,-1.39943489555162E-12,0.));
#18978=DIRECTION('',(0.,0.,1.));
#18979=DIRECTION('center_axis',(0.,0.,1.));
#18980=DIRECTION('ref_axis',(1.,-1.39943489555162E-12,0.));
#18981=DIRECTION('',(0.,0.,1.));
#18982=DIRECTION('center_axis',(0.,0.,1.));
#18983=DIRECTION('ref_axis',(1.,-1.39943489555162E-12,0.));
#18984=DIRECTION('',(0.,0.,1.));
#18985=DIRECTION('center_axis',(0.,0.,1.));
#18986=DIRECTION('ref_axis',(1.,-1.39943489555162E-12,0.));
#18987=DIRECTION('',(0.,0.,1.));
#18988=DIRECTION('center_axis',(0.,0.,1.));
#18989=DIRECTION('ref_axis',(1.,-1.39943489555162E-12,0.));
#18990=DIRECTION('',(0.,0.,1.));
#18991=DIRECTION('center_axis',(0.,0.,1.));
#18992=DIRECTION('ref_axis',(1.,-1.39943489555162E-12,0.));
#18993=DIRECTION('',(0.,0.,1.));
#18994=DIRECTION('center_axis',(0.,0.,1.));
#18995=DIRECTION('ref_axis',(1.,-1.39943489555162E-12,0.));
#18996=DIRECTION('',(0.,0.,1.));
#18997=DIRECTION('center_axis',(0.,0.,1.));
#18998=DIRECTION('ref_axis',(1.,-1.39943489555162E-12,0.));
#18999=DIRECTION('',(0.,0.,1.));
#19000=DIRECTION('center_axis',(0.,0.,1.));
#19001=DIRECTION('ref_axis',(1.,-1.39943489555162E-12,0.));
#19002=DIRECTION('',(0.,0.,1.));
#19003=DIRECTION('center_axis',(0.,0.,1.));
#19004=DIRECTION('ref_axis',(1.,-1.39943489555162E-12,0.));
#19005=DIRECTION('',(0.,0.,1.));
#19006=DIRECTION('center_axis',(0.,0.,1.));
#19007=DIRECTION('ref_axis',(1.,-1.39943489555162E-12,0.));
#19008=DIRECTION('',(0.,0.,1.));
#19009=DIRECTION('center_axis',(0.,0.,1.));
#19010=DIRECTION('ref_axis',(1.,-1.39943489555162E-12,0.));
#19011=DIRECTION('',(0.,0.,1.));
#19012=DIRECTION('center_axis',(0.,0.,1.));
#19013=DIRECTION('ref_axis',(1.,-1.39943489555162E-12,0.));
#19014=DIRECTION('',(0.,0.,1.));
#19015=DIRECTION('center_axis',(0.,0.,1.));
#19016=DIRECTION('ref_axis',(1.,-1.39943489555162E-12,0.));
#19017=DIRECTION('',(0.,0.,1.));
#19018=DIRECTION('center_axis',(0.,0.,1.));
#19019=DIRECTION('ref_axis',(1.,-1.39943489555162E-12,0.));
#19020=DIRECTION('',(0.,0.,1.));
#19021=DIRECTION('center_axis',(0.,0.,1.));
#19022=DIRECTION('ref_axis',(1.,-1.39943489555162E-12,0.));
#19023=DIRECTION('',(0.,0.,1.));
#19024=DIRECTION('center_axis',(0.,0.,1.));
#19025=DIRECTION('ref_axis',(-0.640826195965856,0.767685994768649,0.));
#19026=DIRECTION('center_axis',(0.,0.,-1.));
#19027=DIRECTION('ref_axis',(1.,0.,0.));
#19028=DIRECTION('center_axis',(0.,0.,1.));
#19029=DIRECTION('ref_axis',(1.,0.,0.));
#19030=DIRECTION('center_axis',(0.,0.,-1.));
#19031=DIRECTION('ref_axis',(1.,-1.39943489555162E-12,0.));
#19032=DIRECTION('center_axis',(0.,0.,1.));
#19033=DIRECTION('ref_axis',(1.,0.,0.));
#19034=DIRECTION('center_axis',(0.,0.,1.));
#19035=DIRECTION('ref_axis',(1.,0.,0.));
#19036=DIRECTION('',(0.,0.,1.));
#19037=DIRECTION('center_axis',(0.,0.,1.));
#19038=DIRECTION('ref_axis',(1.,0.,0.));
#19039=DIRECTION('center_axis',(0.,0.,-1.));
#19040=DIRECTION('ref_axis',(-1.,0.,0.));
#19041=DIRECTION('center_axis',(0.,0.,1.));
#19042=DIRECTION('ref_axis',(1.,0.,0.));
#19043=DIRECTION('center_axis',(0.,0.,1.));
#19044=DIRECTION('ref_axis',(1.,0.,0.));
#19045=DIRECTION('center_axis',(0.,0.,1.));
#19046=DIRECTION('ref_axis',(1.,0.,0.));
#19047=DIRECTION('center_axis',(0.,0.,-1.));
#19048=DIRECTION('ref_axis',(1.,0.,0.));
#19049=DIRECTION('',(0.,0.,-1.));
#19050=DIRECTION('center_axis',(0.,0.,1.));
#19051=DIRECTION('ref_axis',(1.,0.,0.));
#19052=DIRECTION('center_axis',(0.,0.,1.));
#19053=DIRECTION('ref_axis',(1.,-1.39943489555162E-12,0.));
#19054=DIRECTION('center_axis',(0.,0.,1.));
#19055=DIRECTION('ref_axis',(1.,0.,0.));
#19056=DIRECTION('center_axis',(0.,0.,-1.));
#19057=DIRECTION('ref_axis',(1.,0.,0.));
#19058=DIRECTION('center_axis',(0.,0.,-1.));
#19059=DIRECTION('ref_axis',(1.,0.,0.));
#19060=DIRECTION('',(0.,0.,-1.));
#19061=DIRECTION('center_axis',(0.,0.,1.));
#19062=DIRECTION('ref_axis',(1.,0.,0.));
#19063=DIRECTION('center_axis',(0.,0.,-1.));
#19064=DIRECTION('ref_axis',(1.,0.,0.));
#19065=DIRECTION('center_axis',(0.,0.,-1.));
#19066=DIRECTION('ref_axis',(1.,0.,0.));
#19067=DIRECTION('',(0.,0.,-1.));
#19068=DIRECTION('center_axis',(0.,0.,1.));
#19069=DIRECTION('ref_axis',(1.,0.,0.));
#19070=DIRECTION('center_axis',(0.,0.,-1.));
#19071=DIRECTION('ref_axis',(1.,0.,0.));
#19072=DIRECTION('center_axis',(0.,0.,-1.));
#19073=DIRECTION('ref_axis',(1.,0.,0.));
#19074=DIRECTION('',(0.,0.,-1.));
#19075=DIRECTION('center_axis',(0.,0.,1.));
#19076=DIRECTION('ref_axis',(1.,0.,0.));
#19077=DIRECTION('center_axis',(0.,0.,-1.));
#19078=DIRECTION('ref_axis',(1.,0.,0.));
#19079=DIRECTION('center_axis',(0.,0.,-1.));
#19080=DIRECTION('ref_axis',(1.,0.,0.));
#19081=DIRECTION('',(0.,0.,-1.));
#19082=DIRECTION('center_axis',(0.,0.,1.));
#19083=DIRECTION('ref_axis',(1.,0.,0.));
#19084=DIRECTION('center_axis',(0.,0.,-1.));
#19085=DIRECTION('ref_axis',(1.,0.,0.));
#19086=DIRECTION('center_axis',(0.,0.,-1.));
#19087=DIRECTION('ref_axis',(1.,0.,0.));
#19088=DIRECTION('',(0.,0.,-1.));
#19089=DIRECTION('center_axis',(0.,0.,1.));
#19090=DIRECTION('ref_axis',(1.,0.,0.));
#19091=DIRECTION('center_axis',(0.,0.,-1.));
#19092=DIRECTION('ref_axis',(1.,0.,0.));
#19093=DIRECTION('center_axis',(0.,0.,-1.));
#19094=DIRECTION('ref_axis',(1.,0.,0.));
#19095=DIRECTION('',(0.,0.,-1.));
#19096=DIRECTION('center_axis',(0.,0.,1.));
#19097=DIRECTION('ref_axis',(1.,0.,0.));
#19098=DIRECTION('center_axis',(0.,0.,1.));
#19099=DIRECTION('ref_axis',(1.,0.,0.));
#19100=DIRECTION('center_axis',(0.,0.,1.));
#19101=DIRECTION('ref_axis',(1.,0.,0.));
#19102=DIRECTION('center_axis',(0.,0.,1.));
#19103=DIRECTION('ref_axis',(1.,0.,0.));
#19104=DIRECTION('center_axis',(0.,0.,1.));
#19105=DIRECTION('ref_axis',(1.,0.,0.));
#19106=DIRECTION('center_axis',(0.,0.,1.));
#19107=DIRECTION('ref_axis',(1.,0.,0.));
#19108=DIRECTION('',(0.,0.,-1.));
#19109=DIRECTION('center_axis',(0.,0.,1.));
#19110=DIRECTION('ref_axis',(1.,0.,0.));
#19111=DIRECTION('center_axis',(0.,0.,1.));
#19112=DIRECTION('ref_axis',(1.,0.,0.));
#19113=DIRECTION('center_axis',(0.,0.,1.));
#19114=DIRECTION('ref_axis',(1.,0.,0.));
#19115=DIRECTION('center_axis',(0.,0.,1.));
#19116=DIRECTION('ref_axis',(1.,0.,0.));
#19117=DIRECTION('',(0.,0.,-1.));
#46839=CARTESIAN_POINT('',(0.,0.,0.));
#46840=CARTESIAN_POINT('Origin',(0.,0.,-10.));
#46841=CARTESIAN_POINT('',(-5.90914966774444,0.00356580792582911,-7.6866248077951));
#46842=CARTESIAN_POINT('',(-5.90684818604763,7.69732782816217E-5,-7.93837519220449));
#46843=CARTESIAN_POINT('',(-5.91675,-7.2459289488551E-16,-10.));
#46844=CARTESIAN_POINT('',(-1.76006007606278,-5.64890423809343,-9.08325));
#46845=CARTESIAN_POINT('Ctrl Pts',(-5.90914966774444,0.00356580792582911,
-7.6866248077951));
#46846=CARTESIAN_POINT('Ctrl Pts',(-5.91328542926688,0.757557195719996,
-7.72201370069112));
#46847=CARTESIAN_POINT('Ctrl Pts',(-5.77952731968195,1.51013660070763,-7.75740259358713));
#46848=CARTESIAN_POINT('Ctrl Pts',(-5.50114206197789,2.20475331667403,-7.79279148648315));
#46849=CARTESIAN_POINT('Ctrl Pts',(-4.77121527592137,4.02603994373196,-7.88558124505991));
#46850=CARTESIAN_POINT('Ctrl Pts',(-3.04699187872556,5.44883910826404,-7.97837100363666));
#46851=CARTESIAN_POINT('Ctrl Pts',(-1.1202364612261,5.81970068129217,-8.07116076221342));
#46852=CARTESIAN_POINT('Ctrl Pts',(0.806518956273354,6.1905622543203,-8.16395052079018));
#46853=CARTESIAN_POINT('Ctrl Pts',(2.93580639407646,5.50948623584449,-8.25674027936694));
#46854=CARTESIAN_POINT('Ctrl Pts',(4.28964970625473,4.08933490559468,-8.34953003794369));
#46855=CARTESIAN_POINT('Ctrl Pts',(5.64349301843301,2.66918357534486,-8.44231979652045));
#46856=CARTESIAN_POINT('Ctrl Pts',(6.22189220498645,0.509956933321043,-8.53510955509721));
#46857=CARTESIAN_POINT('Ctrl Pts',(5.7594588630459,-1.39690584090804,-8.62789931367396));
#46858=CARTESIAN_POINT('Ctrl Pts',(5.29702552110535,-3.30376861513711,-8.72068907225072));
#46859=CARTESIAN_POINT('Ctrl Pts',(3.79375965067081,-4.95826752157145,-8.81347883082748));
#46860=CARTESIAN_POINT('Ctrl Pts',(1.93957562617669,-5.60028674616276,-8.90626858940423));
#46861=CARTESIAN_POINT('Ctrl Pts',(0.76072388940282,-6.0084692501395,-8.96526239293616));
#46862=CARTESIAN_POINT('Ctrl Pts',(-0.559974320405811,-6.00739201583435,
-9.02425619646808));
#46863=CARTESIAN_POINT('Ctrl Pts',(-1.76205604469195,-5.64092543727167,
-9.08325));
#46864=CARTESIAN_POINT('',(3.34982837776095,-4.87714879843208,-9.08325));
#46865=CARTESIAN_POINT('Origin',(0.,0.,-9.08325));
#46866=CARTESIAN_POINT('Ctrl Pts',(3.3444648754246,-4.86859341898359,-9.08325));
#46867=CARTESIAN_POINT('Ctrl Pts',(4.33259176949258,-4.18349695521928,-9.02678881114205));
#46868=CARTESIAN_POINT('Ctrl Pts',(5.12344724565752,-3.20972013684931,-8.9703276222841));
#46869=CARTESIAN_POINT('Ctrl Pts',(5.54426475499171,-2.09385801960084,-8.91386643342615));
#46870=CARTESIAN_POINT('Ctrl Pts',(6.23598258217496,-0.259662193480346,
-8.82105848221044));
#46871=CARTESIAN_POINT('Ctrl Pts',(5.9278923803199,1.95843484105861,-8.72825053099474));
#46872=CARTESIAN_POINT('Ctrl Pts',(4.75815453645331,3.53476303607018,-8.63544257977903));
#46873=CARTESIAN_POINT('Ctrl Pts',(3.58841669258673,5.11109123108174,-8.54263462856332));
#46874=CARTESIAN_POINT('Ctrl Pts',(1.55703120670862,6.04565058656591,-8.4498266773476));
#46875=CARTESIAN_POINT('Ctrl Pts',(-0.40117185096479,5.91244101960478,-8.35701872613189));
#46876=CARTESIAN_POINT('Ctrl Pts',(-2.3593749086382,5.77923145264365,-8.26421077491618));
#46877=CARTESIAN_POINT('Ctrl Pts',(-4.24439553810691,4.57825296323722,-8.17140282370047));
#46878=CARTESIAN_POINT('Ctrl Pts',(-5.19107535624382,2.85949434106974,-8.07859487248476));
#46879=CARTESIAN_POINT('Ctrl Pts',(-5.66784176719644,1.99389399353369,-8.03185497905801));
#46880=CARTESIAN_POINT('Ctrl Pts',(-5.90661436346097,0.996967727442935,
-7.98511508563125));
#46881=CARTESIAN_POINT('Ctrl Pts',(-5.90684818604763,7.69732782816216E-5,
-7.93837519220449));
#46882=CARTESIAN_POINT('Origin',(0.,0.,-10.));
#46883=CARTESIAN_POINT('',(-5.91124449814648,-0.00463389484992694,-5.93662480779511));
#46884=CARTESIAN_POINT('',(-5.9180539583466,-0.00537329958833666,-6.18837519220452));
#46885=CARTESIAN_POINT('',(-5.91675,-7.2459289488551E-16,-10.));
#46886=CARTESIAN_POINT('Ctrl Pts',(-5.91124449814648,-0.00463389484992693,
-5.93662480779511));
#46887=CARTESIAN_POINT('Ctrl Pts',(-5.90163171584489,1.31481634025305,-5.99860848256392));
#46888=CARTESIAN_POINT('Ctrl Pts',(-5.46550912136613,2.64003051865407,-6.06059215733273));
#46889=CARTESIAN_POINT('Ctrl Pts',(-4.65401854734394,3.66929885831296,-6.12257583210154));
#46890=CARTESIAN_POINT('Ctrl Pts',(-3.43921457304457,5.21011684149748,-6.21536559067829));
#46891=CARTESIAN_POINT('Ctrl Pts',(-1.38320399826394,6.0877147140118,-6.30815534925505));
#46892=CARTESIAN_POINT('Ctrl Pts',(0.56981453680638,5.89906436771486,-6.4009451078318));
#46893=CARTESIAN_POINT('Ctrl Pts',(2.5228330718767,5.71041402141791,-6.49373486640856));
#46894=CARTESIAN_POINT('Ctrl Pts',(4.3728595672367,4.4555154563097,-6.58652462498532));
#46895=CARTESIAN_POINT('Ctrl Pts',(5.27028709003435,2.71066883561754,-6.67931438356208));
#46896=CARTESIAN_POINT('Ctrl Pts',(6.167714612832,0.965822214925369,-6.77210414213884));
#46897=CARTESIAN_POINT('Ctrl Pts',(6.1125431630673,-1.26897246135075,-6.86489390071559));
#46898=CARTESIAN_POINT('Ctrl Pts',(5.13011480377032,-2.96741404802536,-6.95768365929235));
#46899=CARTESIAN_POINT('Ctrl Pts',(4.14768644447333,-4.66585563469996,-7.0504734178691));
#46900=CARTESIAN_POINT('Ctrl Pts',(2.23800117564407,-5.82794413177304,-7.14326317644586));
#46901=CARTESIAN_POINT('Ctrl Pts',(0.278051023782169,-5.91999652376047,
-7.23605293502262));
#46902=CARTESIAN_POINT('Ctrl Pts',(-1.68189912807974,-6.01204891574791,
-7.32884269359937));
#46903=CARTESIAN_POINT('Ctrl Pts',(-3.69211416297429,-5.0340652026497,-7.42163245217613));
#46904=CARTESIAN_POINT('Ctrl Pts',(-4.82940659296296,-3.4351863013087,-7.51442221075289));
#46905=CARTESIAN_POINT('Ctrl Pts',(-5.53294943017705,-2.44610049633029,
-7.57182307643363));
#46906=CARTESIAN_POINT('Ctrl Pts',(-5.90244145304175,-1.21940995744712,
-7.62922394211437));
#46907=CARTESIAN_POINT('Ctrl Pts',(-5.90914966774444,0.00356580792582911,
-7.6866248077951));
#46908=CARTESIAN_POINT('Ctrl Pts',(-5.90684818604763,7.69732782816216E-5,
-7.93837519220449));
#46909=CARTESIAN_POINT('Ctrl Pts',(-5.90707864768639,-0.982484549761922,
-7.89230713441554));
#46910=CARTESIAN_POINT('Ctrl Pts',(-5.67557852724961,-1.96501157443031,
-7.84623907662659));
#46911=CARTESIAN_POINT('Ctrl Pts',(-5.21182602918055,-2.82172617607135,
-7.80017101883763));
#46912=CARTESIAN_POINT('Ctrl Pts',(-4.27755787717527,-4.54764931611639,
-7.70736306762192));
#46913=CARTESIAN_POINT('Ctrl Pts',(-2.40068256635962,-5.76295684127793,
-7.61455511640621));
#46914=CARTESIAN_POINT('Ctrl Pts',(-0.443673941101387,-5.90981951500856,
-7.5217471651905));
#46915=CARTESIAN_POINT('Ctrl Pts',(1.51333468415685,-6.05668218873918,-7.42893921397479));
#46916=CARTESIAN_POINT('Ctrl Pts',(3.55047662385768,-5.13510001103889,-7.33613126275908));
#46917=CARTESIAN_POINT('Ctrl Pts',(4.73200308253274,-3.56819310617019,-7.24332331154337));
#46918=CARTESIAN_POINT('Ctrl Pts',(5.91352954120779,-2.00128620130149,-7.15051536032766));
#46919=CARTESIAN_POINT('Ctrl Pts',(6.23944051885709,0.210945430735604,-7.05770740911195));
#46920=CARTESIAN_POINT('Ctrl Pts',(5.55994672995165,2.0520574898606,-6.96489945789624));
#46921=CARTESIAN_POINT('Ctrl Pts',(4.88045294104622,3.8931695489856,-6.87209150668053));
#46922=CARTESIAN_POINT('Ctrl Pts',(3.19555438558608,5.3631620351985,-6.77928355546483));
#46923=CARTESIAN_POINT('Ctrl Pts',(1.2793340040228,5.78678727197991,-6.68647560424912));
#46924=CARTESIAN_POINT('Ctrl Pts',(-0.63688637754048,6.21041250876132,-6.59366765303341));
#46925=CARTESIAN_POINT('Ctrl Pts',(-2.78442858520689,5.58767049611123,-6.50085970181769));
#46926=CARTESIAN_POINT('Ctrl Pts',(-4.17672173121847,4.20461291148561,-6.40805175060198));
#46927=CARTESIAN_POINT('Ctrl Pts',(-5.27524171285711,3.11337979235374,-6.33482623113616));
#46928=CARTESIAN_POINT('Ctrl Pts',(-5.90360270323821,1.54883366893403,-6.26160071167034));
#46929=CARTESIAN_POINT('Ctrl Pts',(-5.9180539583466,-0.00537329958833666,
-6.18837519220452));
#46930=CARTESIAN_POINT('Origin',(0.,0.,-10.));
#46931=CARTESIAN_POINT('',(-5.92596791550767,-0.00164632128292097,-4.1866248077951));
#46932=CARTESIAN_POINT('',(-5.92512149738253,0.00261993485437684,-4.43837519220451));
#46933=CARTESIAN_POINT('',(-5.91675,-7.2459289488551E-16,-10.));
#46934=CARTESIAN_POINT('Ctrl Pts',(-5.92596791550767,-0.00164632128292097,
-4.1866248077951));
#46935=CARTESIAN_POINT('Ctrl Pts',(-5.91906177124303,1.87187930368298,-4.27520326443671));
#46936=CARTESIAN_POINT('Ctrl Pts',(-4.95561321993308,3.75151790639186,-4.36378172107832));
#46937=CARTESIAN_POINT('Ctrl Pts',(-3.42759171092563,4.83479689493213,-4.45236017771992));
#46938=CARTESIAN_POINT('Ctrl Pts',(-1.82692319290707,5.96957841663579,-4.54514993629668));
#46939=CARTESIAN_POINT('Ctrl Pts',(0.39327761073488,6.2304773245562,-4.63793969487344));
#46940=CARTESIAN_POINT('Ctrl Pts',(2.21340809258917,5.49767866152403,-4.73072945345019));
#46941=CARTESIAN_POINT('Ctrl Pts',(4.03353857444347,4.76487999849185,-4.82351921202695));
#46942=CARTESIAN_POINT('Ctrl Pts',(5.45359873451011,3.03838376450709,-4.91630897060371));
#46943=CARTESIAN_POINT('Ctrl Pts',(5.82144160499229,1.11106428290431,-5.00909872918046));
#46944=CARTESIAN_POINT('Ctrl Pts',(6.18928447547447,-0.816255198698479,
-5.10188848775722));
#46945=CARTESIAN_POINT('Ctrl Pts',(5.50491005637218,-2.94439792791929,-5.19467824633398));
#46946=CARTESIAN_POINT('Ctrl Pts',(4.08260983745286,-4.29603799551428,-5.28746800491073));
#46947=CARTESIAN_POINT('Ctrl Pts',(2.66030961853354,-5.64767806310926,-5.38025776348749));
#46948=CARTESIAN_POINT('Ctrl Pts',(0.500083599797188,-6.22281546907843,
-5.47304752206424));
#46949=CARTESIAN_POINT('Ctrl Pts',(-1.40600855129438,-5.75732457831857,
-5.565837280641));
#46950=CARTESIAN_POINT('Ctrl Pts',(-3.31210070238594,-5.29183368755872,
-5.65862703921776));
#46951=CARTESIAN_POINT('Ctrl Pts',(-4.96405898583272,-3.78571450006987,
-5.75141679779452));
#46952=CARTESIAN_POINT('Ctrl Pts',(-5.60323944064706,-1.93063585939808,
-5.84420655637127));
#46953=CARTESIAN_POINT('Ctrl Pts',(-5.81544655230931,-1.31475207058976,
-5.87501264017922));
#46954=CARTESIAN_POINT('Ctrl Pts',(-5.91602208157172,-0.66040486478031,
-5.90581872398716));
#46955=CARTESIAN_POINT('Ctrl Pts',(-5.91124449814648,-0.00463389484992693,
-5.93662480779511));
#46956=CARTESIAN_POINT('Ctrl Pts',(-5.9180539583466,-0.00537329958833666,
-6.18837519220452));
#46957=CARTESIAN_POINT('Ctrl Pts',(-5.92191860442798,-0.421009161352276,
-6.16879276045463));
#46958=CARTESIAN_POINT('Ctrl Pts',(-5.88187836580504,-0.835905599423084,
-6.14921032870475));
#46959=CARTESIAN_POINT('Ctrl Pts',(-5.79518393962897,-1.24081253117895,
-6.12962789695486));
#46960=CARTESIAN_POINT('Ctrl Pts',(-5.38430891767115,-3.1598072326167,-6.03681994573915));
#46961=CARTESIAN_POINT('Ctrl Pts',(-3.92551478939875,-4.85442347889104,
-5.94401199452343));
#46962=CARTESIAN_POINT('Ctrl Pts',(-2.08898215973251,-5.5461589296916,-5.85120404330772));
#46963=CARTESIAN_POINT('Ctrl Pts',(-0.252449530066264,-6.23789438049217,
-5.75839609209201));
#46964=CARTESIAN_POINT('Ctrl Pts',(1.96182160099383,-5.92674903581894,-5.66558814087631));
#46965=CARTESIAN_POINT('Ctrl Pts',(3.53658941057065,-4.75565854394093,-5.5727801896606));
#46966=CARTESIAN_POINT('Ctrl Pts',(5.11135722014747,-3.58456805206292,-5.47997223844489));
#46967=CARTESIAN_POINT('Ctrl Pts',(6.04662170824101,-1.55353241298013,-5.38716428722918));
#46968=CARTESIAN_POINT('Ctrl Pts',(5.91271741582685,0.404379920195457,-5.29435633601347));
#46969=CARTESIAN_POINT('Ctrl Pts',(5.7788131234127,2.36229225337103,-5.20154838479775));
#46970=CARTESIAN_POINT('Ctrl Pts',(4.57574005049085,4.24708128063941,-5.10874043358204));
#46971=CARTESIAN_POINT('Ctrl Pts',(2.85619526042756,5.19286940926132,-5.01593248236633));
#46972=CARTESIAN_POINT('Ctrl Pts',(1.13665047036426,6.13865753788323,-4.92312453115062));
#46973=CARTESIAN_POINT('Ctrl Pts',(-1.09936603684048,6.14544476785868,-4.83031657993492));
#46974=CARTESIAN_POINT('Ctrl Pts',(-2.82462024052683,5.21011217386649,-4.73750862871921));
#46975=CARTESIAN_POINT('Ctrl Pts',(-4.54987444421319,4.27477957987429,-4.6447006775035));
#46976=CARTESIAN_POINT('Ctrl Pts',(-5.76436634438116,2.39732716191442,-4.55189272628778));
#46977=CARTESIAN_POINT('Ctrl Pts',(-5.91015356810031,0.440264092825153,
-4.45908477507207));
#46978=CARTESIAN_POINT('Ctrl Pts',(-5.92099743995646,0.294694813198242,
-4.45218158078288));
#46979=CARTESIAN_POINT('Ctrl Pts',(-5.92592858883168,0.148685079125095,
-4.4452783864937));
#46980=CARTESIAN_POINT('Ctrl Pts',(-5.92512149738253,0.00261993485437684,
-4.43837519220451));
#46981=CARTESIAN_POINT('Origin',(0.,0.,-10.));
#46982=CARTESIAN_POINT('',(-5.91623372814898,0.00546481507842006,-2.4366248077951));
#46983=CARTESIAN_POINT('',(-5.90999536725745,0.0040860534926895,-2.6883751922045));
#46984=CARTESIAN_POINT('',(-5.91675,-7.2459289488551E-16,-10.));
#46985=CARTESIAN_POINT('Ctrl Pts',(-5.91623372814898,0.00546481507842006,
-2.4366248077951));
#46986=CARTESIAN_POINT('Ctrl Pts',(-5.92059929034551,0.480925655459938,
-2.45900828773275));
#46987=CARTESIAN_POINT('Ctrl Pts',(-5.86811878257571,0.955434629522007,
-2.48139176767039));
#46988=CARTESIAN_POINT('Ctrl Pts',(-5.75510650687943,1.41506011009764,-2.50377524760804));
#46989=CARTESIAN_POINT('Ctrl Pts',(-5.28661895234013,3.32041787828841,-2.5965650061848));
#46990=CARTESIAN_POINT('Ctrl Pts',(-3.77790412893443,4.97000555564954,-2.68935476476155));
#46991=CARTESIAN_POINT('Ctrl Pts',(-1.92182261689083,5.60626826399261,-2.78214452333831));
#46992=CARTESIAN_POINT('Ctrl Pts',(-0.0657411048472262,6.24253097233568,
-2.87493428191507));
#46993=CARTESIAN_POINT('Ctrl Pts',(2.13770709583431,5.86546871166071,-2.96772404049182));
#46994=CARTESIAN_POINT('Ctrl Pts',(3.67661279380201,4.64824315028558,-3.06051379906858));
#46995=CARTESIAN_POINT('Ctrl Pts',(5.21551849176971,3.43101758891044,-3.15330355764534));
#46996=CARTESIAN_POINT('Ctrl Pts',(6.08988168702359,1.37362872683514,-3.24609331622209));
#46997=CARTESIAN_POINT('Ctrl Pts',(5.89816076077324,-0.579090377210239,
-3.33888307479885));
#46998=CARTESIAN_POINT('Ctrl Pts',(5.7064398345229,-2.53180948125562,-3.4316728333756));
#46999=CARTESIAN_POINT('Ctrl Pts',(4.44863478676834,-4.37985882727109,-3.52446259195236));
#47000=CARTESIAN_POINT('Ctrl Pts',(2.70237866321106,-5.27454221436282,-3.61725235052912));
#47001=CARTESIAN_POINT('Ctrl Pts',(0.956122539653778,-6.16922560145455,
-3.71004210910587));
#47002=CARTESIAN_POINT('Ctrl Pts',(-1.27858465970622,-6.11054302962255,
-3.80283186768263));
#47003=CARTESIAN_POINT('Ctrl Pts',(-2.9754783984976,-5.12544381703233,-3.89562162625939));
#47004=CARTESIAN_POINT('Ctrl Pts',(-4.67237213728899,-4.14034460444212,
-3.98841138483614));
#47005=CARTESIAN_POINT('Ctrl Pts',(-5.83145241551177,-2.2288287510937,-4.0812011434129));
#47006=CARTESIAN_POINT('Ctrl Pts',(-5.92042443842556,-0.268738756676046,
-4.17399090198966));
#47007=CARTESIAN_POINT('Ctrl Pts',(-5.92446247083364,-0.179779253890741,
-4.17820220392481));
#47008=CARTESIAN_POINT('Ctrl Pts',(-5.92629625560083,-0.0907196963349705,
-4.18241350585995));
#47009=CARTESIAN_POINT('Ctrl Pts',(-5.92596791550767,-0.00164632128292097,
-4.1866248077951));
#47010=CARTESIAN_POINT('Ctrl Pts',(-5.92512149738253,0.00261993485437684,
-4.43837519220451));
#47011=CARTESIAN_POINT('Ctrl Pts',(-5.91507788686657,-1.8150444953158,-4.35247043527799));
#47012=CARTESIAN_POINT('Ctrl Pts',(-5.01642065476797,-3.64128964946244,
-4.26656567835147));
#47013=CARTESIAN_POINT('Ctrl Pts',(-3.56539308202037,-4.73410171351781,
-4.18066092142495));
#47014=CARTESIAN_POINT('Ctrl Pts',(-1.99776282495092,-5.91473073055283,
-4.08785297020924));
#47015=CARTESIAN_POINT('Ctrl Pts',(0.214580236458331,-6.23931504440418,
-3.99504501899353));
#47016=CARTESIAN_POINT('Ctrl Pts',(2.05527741171376,-5.55873927088791,-3.90223706777781));
#47017=CARTESIAN_POINT('Ctrl Pts',(3.89597458696917,-4.87816349737166,-3.80942911656211));
#47018=CARTESIAN_POINT('Ctrl Pts',(5.36502587607076,-3.19242763648782,-3.7166211653464));
#47019=CARTESIAN_POINT('Ctrl Pts',(5.78754354247752,-1.27596516977657,-3.62381321413069));
#47020=CARTESIAN_POINT('Ctrl Pts',(6.21006120888429,0.640497296934686,-3.53100526291498));
#47021=CARTESIAN_POINT('Ctrl Pts',(5.5860452525962,2.78768636947335,-3.43819731169927));
#47022=CARTESIAN_POINT('Ctrl Pts',(4.20217097506051,4.17917532158192,-3.34538936048356));
#47023=CARTESIAN_POINT('Ctrl Pts',(2.81829669752482,5.5706642736905,-3.25258140926785));
#47024=CARTESIAN_POINT('Ctrl Pts',(0.674564098741514,6.20645310536897,-3.15977345805214));
#47025=CARTESIAN_POINT('Ctrl Pts',(-1.24418798567351,5.7944580097669,-3.06696550683643));
#47026=CARTESIAN_POINT('Ctrl Pts',(-3.1629400700885,5.38246291416483,-2.97415755562072));
#47027=CARTESIAN_POINT('Ctrl Pts',(-4.85671164013523,3.92268389128225,-2.88134960440501));
#47028=CARTESIAN_POINT('Ctrl Pts',(-5.5473776410707,2.08574894203492,-2.7885416531893));
#47029=CARTESIAN_POINT('Ctrl Pts',(-5.79585336658777,1.42488863673007,-2.75515283286103));
#47030=CARTESIAN_POINT('Ctrl Pts',(-5.91449808653743,0.715213396403952,
-2.72176401253277));
#47031=CARTESIAN_POINT('Ctrl Pts',(-5.90999536725745,0.0040860534926895,
-2.6883751922045));
#47032=CARTESIAN_POINT('Origin',(0.,0.,-10.));
#47033=CARTESIAN_POINT('',(-5.90707267146128,-0.000907514317987079,-0.6866248077951));
#47034=CARTESIAN_POINT('',(-5.91020249175295,-0.00419241645486733,-0.93837519220451));
#47035=CARTESIAN_POINT('',(-5.91675,-7.2459289488551E-16,-10.));
#47036=CARTESIAN_POINT('Ctrl Pts',(-5.90707267146128,-0.000907514317987079,
-0.6866248077951));
#47037=CARTESIAN_POINT('Ctrl Pts',(-5.90564731739626,1.04354150490343,-0.735603069605543));
#47038=CARTESIAN_POINT('Ctrl Pts',(-5.64214242329099,2.0886625894451,-0.784581331415985));
#47039=CARTESIAN_POINT('Ctrl Pts',(-5.1207586220131,2.98353433950782,-0.833559593226428));
#47040=CARTESIAN_POINT('Ctrl Pts',(-4.13299230981434,4.6788769379619,-0.926349351803184));
#47041=CARTESIAN_POINT('Ctrl Pts',(-2.21965620168432,5.83494997235119,-1.01913911037994));
#47042=CARTESIAN_POINT('Ctrl Pts',(-0.259428722982098,5.92083970038001,
-1.1119288689567));
#47043=CARTESIAN_POINT('Ctrl Pts',(1.70079875572013,6.00672942840883,-1.20471862753345));
#47044=CARTESIAN_POINT('Ctrl Pts',(3.70791760499457,5.02243585007718,-1.29750838611021));
#47045=CARTESIAN_POINT('Ctrl Pts',(4.84018071389265,3.41998489423038,-1.39029814468697));
#47046=CARTESIAN_POINT('Ctrl Pts',(5.97244382279073,1.81753393838358,-1.48308790326372));
#47047=CARTESIAN_POINT('Ctrl Pts',(6.22985119131246,-0.403074394978366,
-1.57587766184048));
#47048=CARTESIAN_POINT('Ctrl Pts',(5.49419133515994,-2.22205031281952,-1.66866742041724));
#47049=CARTESIAN_POINT('Ctrl Pts',(4.75853147900741,-4.04102623066067,-1.76145717899399));
#47050=CARTESIAN_POINT('Ctrl Pts',(3.02980439818064,-5.45836973298102,-1.85424693757075));
#47051=CARTESIAN_POINT('Ctrl Pts',(1.10190886608084,-5.8231815076133,-1.9470366961475));
#47052=CARTESIAN_POINT('Ctrl Pts',(-0.825986666018957,-6.18799328224558,
-2.03982645472426));
#47053=CARTESIAN_POINT('Ctrl Pts',(-2.95305064939178,-5.50027332918978,
-2.13261621330102));
#47054=CARTESIAN_POINT('Ctrl Pts',(-4.30245249824173,-4.07584942315166,
-2.22540597187777));
#47055=CARTESIAN_POINT('Ctrl Pts',(-5.32634095342796,-2.99503632516554,
-2.29581225051688));
#47056=CARTESIAN_POINT('Ctrl Pts',(-5.90250203900672,-1.49007691941227,
-2.36621852915599));
#47057=CARTESIAN_POINT('Ctrl Pts',(-5.91623372814898,0.00546481507842006,
-2.4366248077951));
#47058=CARTESIAN_POINT('Ctrl Pts',(-5.90999536725745,0.0040860534926895,
-2.6883751922045));
#47059=CARTESIAN_POINT('Ctrl Pts',(-5.90198227594078,-1.26144439204732,
-2.62895606131706));
#47060=CARTESIAN_POINT('Ctrl Pts',(-5.50395911021358,-2.53157367164205,
-2.56953693042961));
#47061=CARTESIAN_POINT('Ctrl Pts',(-4.75359485550615,-3.53936198776295,
-2.51011779954216));
#47062=CARTESIAN_POINT('Ctrl Pts',(-3.58158563718193,-5.1134470927013,-2.41730984832646));
#47063=CARTESIAN_POINT('Ctrl Pts',(-1.55000676870931,-6.0475264269659,-2.32450189711075));
#47064=CARTESIAN_POINT('Ctrl Pts',(0.407826753663942,-5.91248041723304,
-2.23169394589504));
#47065=CARTESIAN_POINT('Ctrl Pts',(2.36566027603722,-5.77743440750018,-2.13888599467933));
#47066=CARTESIAN_POINT('Ctrl Pts',(4.24974845231112,-4.57326305376982,-2.04607804346362));
#47067=CARTESIAN_POINT('Ctrl Pts',(5.19453406473041,-2.85316722089178,-1.95327009224791));
#47068=CARTESIAN_POINT('Ctrl Pts',(6.13931967714968,-1.13307138801377,-1.8604621410322));
#47069=CARTESIAN_POINT('Ctrl Pts',(6.14480272571436,1.10294892401191,-1.76765418981649));
#47070=CARTESIAN_POINT('Ctrl Pts',(5.20846427759294,2.82765754785667,-1.67484623860078));
#47071=CARTESIAN_POINT('Ctrl Pts',(4.2721258294715,4.55236617170145,-1.58203828738507));
#47072=CARTESIAN_POINT('Ctrl Pts',(2.39396588466393,5.7657631073653,-1.48923033616936));
#47073=CARTESIAN_POINT('Ctrl Pts',(0.436818208133945,5.91040922390592,-1.39642238495365));
#47074=CARTESIAN_POINT('Ctrl Pts',(-1.52032946839601,6.05505534044654,-1.30361443373794));
#47075=CARTESIAN_POINT('Ctrl Pts',(-3.55646487664837,5.13095063786397,-1.21080648252223));
#47076=CARTESIAN_POINT('Ctrl Pts',(-4.73617972739577,3.56263230349625,-1.11799853130652));
#47077=CARTESIAN_POINT('Ctrl Pts',(-5.49726509383871,2.55084192596966,-1.05812408493918));
#47078=CARTESIAN_POINT('Ctrl Pts',(-5.90189954520199,1.27092330637285,-0.998249638571847));
#47079=CARTESIAN_POINT('Ctrl Pts',(-5.91020249175295,-0.00419241645486733,
-0.93837519220451));
#47080=CARTESIAN_POINT('Origin',(0.,0.,-10.));
#47081=CARTESIAN_POINT('',(-5.91957494766717,-0.0051333472841536,1.0633751922049));
#47082=CARTESIAN_POINT('',(-5.92528955248489,-0.00246218369985553,0.811624807795514));
#47083=CARTESIAN_POINT('',(-5.91675,-7.2459289488551E-16,-10.));
#47084=CARTESIAN_POINT('Ctrl Pts',(-5.91957494766717,-0.0051333472841536,
1.0633751922049));
#47085=CARTESIAN_POINT('Ctrl Pts',(-5.904918870215,1.59783527582977,0.987802148521663));
#47086=CARTESIAN_POINT('Ctrl Pts',(-5.23093422272582,3.21165545437413,0.912229104838426));
#47087=CARTESIAN_POINT('Ctrl Pts',(-4.0690788967531,4.308856339207,0.836656061155188));
#47088=CARTESIAN_POINT('Ctrl Pts',(-2.64253485480606,5.65601665261946,0.743866302578431));
#47089=CARTESIAN_POINT('Ctrl Pts',(-0.480510622894167,6.2243573463337,0.651076544001675));
#47090=CARTESIAN_POINT('Ctrl Pts',(1.4241081059804,5.75287424879129,0.558286785424919));
#47091=CARTESIAN_POINT('Ctrl Pts',(3.32872683485496,5.28139115124888,0.465497026848162));
#47092=CARTESIAN_POINT('Ctrl Pts',(4.97594006069217,3.77008426244976,0.372707268271405));
#47093=CARTESIAN_POINT('Ctrl Pts',(5.60928334562095,1.91300453958267,0.279917509694649));
#47094=CARTESIAN_POINT('Ctrl Pts',(6.24262663054972,0.0559248167155829,
0.187127751117892));
#47095=CARTESIAN_POINT('Ctrl Pts',(5.8620999745701,-2.1469277402195,0.0943379925411347));
#47096=CARTESIAN_POINT('Ctrl Pts',(4.64245603167641,-3.6839174819585,0.00154823396437833));
#47097=CARTESIAN_POINT('Ctrl Pts',(3.42281208878272,-5.2209072236975,-0.0912415246123782));
#47098=CARTESIAN_POINT('Ctrl Pts',(1.36405085897497,-6.09203415024043,-0.184031283189133));
#47099=CARTESIAN_POINT('Ctrl Pts',(-0.588364355247926,-5.89724286471199,
-0.27682104176589));
#47100=CARTESIAN_POINT('Ctrl Pts',(-2.54077956947082,-5.70245157918356,
-0.369610800342646));
#47101=CARTESIAN_POINT('Ctrl Pts',(-4.38684876810885,-4.44174208158375,
-0.462400558919404));
#47102=CARTESIAN_POINT('Ctrl Pts',(-5.27878510929411,-2.69408125152443,
-0.55519031749616));
#47103=CARTESIAN_POINT('Ctrl Pts',(-5.69992066053354,-1.86890789210222,
-0.599001814262474));
#47104=CARTESIAN_POINT('Ctrl Pts',(-5.90834766352312,-0.935176578526429,
-0.642813311028787));
#47105=CARTESIAN_POINT('Ctrl Pts',(-5.90707267146128,-0.000907514317987079,
-0.6866248077951));
#47106=CARTESIAN_POINT('Ctrl Pts',(-5.91020249175295,-0.00419241645486733,
-0.93837519220451));
#47107=CARTESIAN_POINT('Ctrl Pts',(-5.91476946726725,-0.705560569111268,
-0.905441687356137));
#47108=CARTESIAN_POINT('Ctrl Pts',(-5.79942752644688,-1.40547561965529,
-0.872508182507763));
#47109=CARTESIAN_POINT('Ctrl Pts',(-5.55753998903547,-2.05851806168967,
-0.839574677659389));
#47110=CARTESIAN_POINT('Ctrl Pts',(-4.87589110668532,-3.8988181263549,-0.74676672644368));
#47111=CARTESIAN_POINT('Ctrl Pts',(-3.18929904874264,-5.36688628953246,
-0.653958775227971));
#47112=CARTESIAN_POINT('Ctrl Pts',(-1.27259057030329,-5.78828649780727,
-0.561150824012261));
#47113=CARTESIAN_POINT('Ctrl Pts',(0.644117908136064,-6.20968670608207,
-0.468342872796551));
#47114=CARTESIAN_POINT('Ctrl Pts',(2.79094280707207,-5.58441895945409,-0.375534921580841));
#47115=CARTESIAN_POINT('Ctrl Pts',(4.18162466770078,-4.19973361996379,-0.28272697036513));
#47116=CARTESIAN_POINT('Ctrl Pts',(5.57230652832947,-2.8150482804735,-0.189919019149421));
#47117=CARTESIAN_POINT('Ctrl Pts',(6.2068453506509,-0.670945348120922,-0.0971110679337112));
#47118=CARTESIAN_POINT('Ctrl Pts',(5.79373160551071,1.24756620004122,-0.00430311671800236));
#47119=CARTESIAN_POINT('Ctrl Pts',(5.3806178603705,3.16607774820339,0.088504834497708));
#47120=CARTESIAN_POINT('Ctrl Pts',(3.91985154776864,4.85899791217512,0.181312785713418));
#47121=CARTESIAN_POINT('Ctrl Pts',(2.08251422334955,5.54859278103609,0.274120736929129));
#47122=CARTESIAN_POINT('Ctrl Pts',(0.245176898930466,6.23818764989705,0.366928688144839));
#47123=CARTESIAN_POINT('Ctrl Pts',(-1.96873143730581,5.92445722364727,0.459736639360548));
#47124=CARTESIAN_POINT('Ctrl Pts',(-3.54213294235917,4.75153044385172,0.552544590576258));
#47125=CARTESIAN_POINT('Ctrl Pts',(-5.00622159123967,3.66009333847765,0.638904662982677));
#47126=CARTESIAN_POINT('Ctrl Pts',(-5.91571084630785,1.82469886427711,0.725264735389096));
#47127=CARTESIAN_POINT('Ctrl Pts',(-5.92528955248489,-0.00246218369985553,
0.811624807795514));
#47128=CARTESIAN_POINT('Origin',(0.,0.,-10.));
#47129=CARTESIAN_POINT('',(-5.92405509285564,0.0034173886458154,2.81337519220491));
#47130=CARTESIAN_POINT('',(-5.91775768435869,0.00540196786531037,2.5616248077955));
#47131=CARTESIAN_POINT('',(-5.91675,-7.2459289488551E-16,-10.));
#47132=CARTESIAN_POINT('Ctrl Pts',(-5.92405509285564,0.0034173886458154,
2.81337519220491));
#47133=CARTESIAN_POINT('Ctrl Pts',(-5.92541887861536,0.20194281602732,2.80399712522563));
#47134=CARTESIAN_POINT('Ctrl Pts',(-5.91630780139426,0.40034155480686,2.79461905824635));
#47135=CARTESIAN_POINT('Ctrl Pts',(-5.89631038710755,0.597636878725663,
2.78524099126707));
#47136=CARTESIAN_POINT('Ctrl Pts',(-5.69844922361589,2.54974337521345,2.69245123269031));
#47137=CARTESIAN_POINT('Ctrl Pts',(-4.43483839204534,4.39382786076265,2.59966147411355));
#47138=CARTESIAN_POINT('Ctrl Pts',(-2.68577717751512,5.28301495101653,2.5068717155368));
#47139=CARTESIAN_POINT('Ctrl Pts',(-0.936715962984878,6.17220204127042,
2.41408195696004));
#47140=CARTESIAN_POINT('Ctrl Pts',(1.29779563450503,6.10649173622901,2.32129219838329));
#47141=CARTESIAN_POINT('Ctrl Pts',(2.99158290180955,5.11606076601189,2.22850243980653));
#47142=CARTESIAN_POINT('Ctrl Pts',(4.68537016911407,4.12562979579476,2.13571268122977));
#47143=CARTESIAN_POINT('Ctrl Pts',(5.83843310623318,2.21047816040193,2.04292292265302));
#47144=CARTESIAN_POINT('Ctrl Pts',(5.92124032471242,0.250118045980118,1.95013316407626));
#47145=CARTESIAN_POINT('Ctrl Pts',(6.00404754319166,-1.71024206844168,1.85734340549951));
#47146=CARTESIAN_POINT('Ctrl Pts',(5.01659904303105,-3.71581066189244,1.76455364692275));
#47147=CARTESIAN_POINT('Ctrl Pts',(3.41236961600884,-4.84555256123232,1.67176388834599));
#47148=CARTESIAN_POINT('Ctrl Pts',(1.80814018898661,-5.97529446057221,1.57897412976924));
#47149=CARTESIAN_POINT('Ctrl Pts',(-0.412870164897221,-6.2292096658012,
1.48618437119248));
#47150=CARTESIAN_POINT('Ctrl Pts',(-2.23068702915303,-5.4906904299818,1.39339461261573));
#47151=CARTESIAN_POINT('Ctrl Pts',(-4.04850389340885,-4.7521711941624,1.30060485403897));
#47152=CARTESIAN_POINT('Ctrl Pts',(-5.46312726803664,-3.02121751729461,
1.20781509546221));
#47153=CARTESIAN_POINT('Ctrl Pts',(-5.82490702935946,-1.09275071230537,
1.11502533688545));
#47154=CARTESIAN_POINT('Ctrl Pts',(-5.89203360777153,-0.734932525553136,
1.09780862199194));
#47155=CARTESIAN_POINT('Ctrl Pts',(-5.92291383008679,-0.370314533886649,
1.08059190709842));
#47156=CARTESIAN_POINT('Ctrl Pts',(-5.91957494766717,-0.0051333472841536,
1.0633751922049));
#47157=CARTESIAN_POINT('Ctrl Pts',(-5.92528955248489,-0.00246218369985553,
0.811624807795514));
#47158=CARTESIAN_POINT('Ctrl Pts',(-5.92600472484242,-0.138883016546891,
0.818072686604806));
#47159=CARTESIAN_POINT('Ctrl Pts',(-5.92170332485837,-0.275257951967435,
0.824520565414098));
#47160=CARTESIAN_POINT('Ctrl Pts',(-5.91224163087656,-0.411273921283423,
0.830968444223389));
#47161=CARTESIAN_POINT('Ctrl Pts',(-5.77605414047018,-2.36902837328162,
0.923776395439099));
#47162=CARTESIAN_POINT('Ctrl Pts',(-4.57078448578703,-4.25241414393666,
1.01658434665481));
#47163=CARTESIAN_POINT('Ctrl Pts',(-2.85013809380902,-5.19619670397703,
1.10939229787052));
#47164=CARTESIAN_POINT('Ctrl Pts',(-1.129491701831,-6.13997926401741,1.20220024908623));
#47165=CARTESIAN_POINT('Ctrl Pts',(1.1065314274419,-6.14415861344309,1.29500820030194));
#47166=CARTESIAN_POINT('Ctrl Pts',(2.83069383164873,-5.20681474335945,1.38781615151765));
#47167=CARTESIAN_POINT('Ctrl Pts',(4.55485623585553,-4.26947087327583,1.48062410273336));
#47168=CARTESIAN_POINT('Ctrl Pts',(5.7671579149963,-2.3906037836829,1.57343205394907));
#47169=CARTESIAN_POINT('Ctrl Pts',(5.91066290352019,-0.433372104721073,
1.66624000516478));
#47170=CARTESIAN_POINT('Ctrl Pts',(6.05416789204407,1.5238595742408,1.75904795638049));
#47171=CARTESIAN_POINT('Ctrl Pts',(5.12887618995105,3.55945584257158,1.8518559075962));
#47172=CARTESIAN_POINT('Ctrl Pts',(3.55987029641463,4.73825609406093,1.94466385881191));
#47173=CARTESIAN_POINT('Ctrl Pts',(1.99086440287824,5.91705634555026,2.03747181002762));
#47174=CARTESIAN_POINT('Ctrl Pts',(-0.221855682101526,6.23906058019818,
2.13027976124333));
#47175=CARTESIAN_POINT('Ctrl Pts',(-2.06175800263737,5.55633883764849,2.22308771245903));
#47176=CARTESIAN_POINT('Ctrl Pts',(-3.90166032317325,4.87361709509879,2.31589566367475));
#47177=CARTESIAN_POINT('Ctrl Pts',(-5.36874487926518,3.18616937535148,2.40870361489046));
#47178=CARTESIAN_POINT('Ctrl Pts',(-5.78902749036571,1.26921552779285,2.50151156610617));
#47179=CARTESIAN_POINT('Ctrl Pts',(-5.87976881819363,0.855334646409641,
2.52154931333595));
#47180=CARTESIAN_POINT('Ctrl Pts',(-5.92171327919293,0.430755294309258,
2.54158706056572));
#47181=CARTESIAN_POINT('Ctrl Pts',(-5.91775768435869,0.00540196786531037,
2.5616248077955));
#47182=CARTESIAN_POINT('Origin',(0.,0.,-10.));
#47183=CARTESIAN_POINT('',(-5.90893794266972,0.00341325037688023,4.5633751922049));
#47184=CARTESIAN_POINT('',(-5.90693841009768,-4.21682523413384E-5,4.31162480779551));
#47185=CARTESIAN_POINT('',(-5.91675,-7.2459289488551E-16,-10.));
#47186=CARTESIAN_POINT('Ctrl Pts',(-5.90893794266972,0.00341325037688023,
4.5633751922049));
#47187=CARTESIAN_POINT('Ctrl Pts',(-5.91294750478057,0.769920258362169,
4.52740234335283));
#47188=CARTESIAN_POINT('Ctrl Pts',(-5.77459382265735,1.53503581594222,4.49142949450076));
#47189=CARTESIAN_POINT('Ctrl Pts',(-5.48717594814371,2.23931822973835,4.45545664564868));
#47190=CARTESIAN_POINT('Ctrl Pts',(-4.74579915876471,4.05597154554143,4.36266688707193));
#47191=CARTESIAN_POINT('Ctrl Pts',(-3.01262316590221,5.46787129455723,4.26987712849517));
#47192=CARTESIAN_POINT('Ctrl Pts',(-1.0835898565008,5.8266181480181,4.17708736991841));
#47193=CARTESIAN_POINT('Ctrl Pts',(0.845443452900566,6.18536500147897,4.08429761134166));
#47194=CARTESIAN_POINT('Ctrl Pts',(2.97033407884086,5.49095895938497,3.9915078527649));
#47195=CARTESIAN_POINT('Ctrl Pts',(4.31524952575888,4.06229830888417,3.89871809418815));
#47196=CARTESIAN_POINT('Ctrl Pts',(5.6601649726769,2.63363765838336,3.80592833561139));
#47197=CARTESIAN_POINT('Ctrl Pts',(6.22510524057266,0.470722399475758,3.71313857703463));
#47198=CARTESIAN_POINT('Ctrl Pts',(5.75062776579904,-1.43315258055328,3.62034881845788));
#47199=CARTESIAN_POINT('Ctrl Pts',(5.27615029102541,-3.33702756058232,3.52755905988112));
#47200=CARTESIAN_POINT('Ctrl Pts',(3.76225507358237,-4.98186226173277,3.43476930130436));
#47201=CARTESIAN_POINT('Ctrl Pts',(1.90418173193351,-5.61228455726329,3.34197954272761));
#47202=CARTESIAN_POINT('Ctrl Pts',(0.046108390284639,-6.24270685279381,
3.24918978415085));
#47203=CARTESIAN_POINT('Ctrl Pts',(-2.15614307557003,-5.85871674270441,
3.1564000255741));
#47204=CARTESIAN_POINT('Ctrl Pts',(-3.691213060791,-4.63665743394649,3.06361026699734));
#47205=CARTESIAN_POINT('Ctrl Pts',(-5.07113673072789,-3.53810910555936,
2.98019857539986));
#47206=CARTESIAN_POINT('Ctrl Pts',(-5.91192512220749,-1.76233473912115,
2.89678688380238));
#47207=CARTESIAN_POINT('Ctrl Pts',(-5.92405509285564,0.0034173886458154,
2.81337519220491));
#47208=CARTESIAN_POINT('Ctrl Pts',(-5.91775768435869,0.00540196786531037,
2.5616248077955));
#47209=CARTESIAN_POINT('Ctrl Pts',(-5.90339232483635,-1.53933497169563,
2.63439501178143));
#47210=CARTESIAN_POINT('Ctrl Pts',(-5.28365457365082,-3.09427980078845,
2.70716521576736));
#47211=CARTESIAN_POINT('Ctrl Pts',(-4.19729483461209,-4.18407258679137,
2.77993541975329));
#47212=CARTESIAN_POINT('Ctrl Pts',(-2.81179890164883,-5.5739468784471,2.872743370969));
#47213=CARTESIAN_POINT('Ctrl Pts',(-0.66732636961311,-6.20723548638865,
2.96555132218472));
#47214=CARTESIAN_POINT('Ctrl Pts',(1.25094398893609,-5.79300323465687,3.05835927340043));
#47215=CARTESIAN_POINT('Ctrl Pts',(3.16921434748529,-5.37877098292509,3.15116722461614));
#47216=CARTESIAN_POINT('Ctrl Pts',(4.86128253254801,-3.91701787152002,3.24397517583184));
#47217=CARTESIAN_POINT('Ctrl Pts',(5.54980603553847,-2.07927879518383,3.33678312704755));
#47218=CARTESIAN_POINT('Ctrl Pts',(6.23832953852894,-0.241539718847621,
3.42959107826326));
#47219=CARTESIAN_POINT('Ctrl Pts',(5.9233083594471,1.9721853224197,3.52239902947898));
#47220=CARTESIAN_POINT('Ctrl Pts',(4.74946441657433,3.54490269202056,3.61520698069469));
#47221=CARTESIAN_POINT('Ctrl Pts',(3.57562047370158,5.11762006162138,3.7080149319104));
#47222=CARTESIAN_POINT('Ctrl Pts',(1.5429537670379,6.04932975955577,3.8008228831261));
#47223=CARTESIAN_POINT('Ctrl Pts',(-0.414720948889979,5.91200083514474,
3.89363083434181));
#47224=CARTESIAN_POINT('Ctrl Pts',(-2.37239566481789,5.77467191073371,3.98643878555752));
#47225=CARTESIAN_POINT('Ctrl Pts',(-4.25507839001002,4.56830436397723,4.07924673677324));
#47226=CARTESIAN_POINT('Ctrl Pts',(-5.19785757693449,2.84710799761883,4.17205468798895));
#47227=CARTESIAN_POINT('Ctrl Pts',(-5.67046005817503,1.98429549101611,4.2185780612578));
#47228=CARTESIAN_POINT('Ctrl Pts',(-5.90687591097582,0.992112598863517,
4.26510143452666));
#47229=CARTESIAN_POINT('Ctrl Pts',(-5.90693872189066,-4.21669123174065E-5,
4.31162480779551));
#47230=CARTESIAN_POINT('Origin',(0.,0.,-10.));
#47231=CARTESIAN_POINT('',(-5.91154939285259,-0.00474152141923923,6.31337519220491));
#47232=CARTESIAN_POINT('',(-5.91791297517326,-0.00538731180401663,6.0616248077955));
#47233=CARTESIAN_POINT('',(-5.91675,-7.2459289488551E-16,-10.));
#47234=CARTESIAN_POINT('Ctrl Pts',(-5.91154939285259,-0.00474152141923923,
6.31337519220491));
#47235=CARTESIAN_POINT('Ctrl Pts',(-5.90158645275689,1.3269665387579,6.25080756148004));
#47236=CARTESIAN_POINT('Ctrl Pts',(-5.45650196275694,2.66470719166618,6.18823993075516));
#47237=CARTESIAN_POINT('Ctrl Pts',(-4.63084737129029,3.69849951246977,6.12567230003029));
#47238=CARTESIAN_POINT('Ctrl Pts',(-3.40637571841808,5.23164594545016,6.03288254145354));
#47239=CARTESIAN_POINT('Ctrl Pts',(-1.34488502739145,6.09629388207883,5.94009278287678));
#47240=CARTESIAN_POINT('Ctrl Pts',(0.606907924444632,5.89536332986964,5.84730302430003));
#47241=CARTESIAN_POINT('Ctrl Pts',(2.55870087628076,5.69443277766045,5.75451326572327));
#47242=CARTESIAN_POINT('Ctrl Pts',(4.40079608892635,4.42792373661338,5.66172350714651));
#47243=CARTESIAN_POINT('Ctrl Pts',(5.28723172958268,2.677466462464,5.56893374856975));
#47244=CARTESIAN_POINT('Ctrl Pts',(6.17366737023899,0.927009188314677,5.476143989993));
#47245=CARTESIAN_POINT('Ctrl Pts',(6.10444343890609,-1.30739631893691,5.38335423141625));
#47246=CARTESIAN_POINT('Ctrl Pts',(5.11135025967902,-2.99962406691314,5.29056447283949));
#47247=CARTESIAN_POINT('Ctrl Pts',(4.11825708045197,-4.69185181488935,5.19777471426274));
#47248=CARTESIAN_POINT('Ctrl Pts',(2.20129465333077,-5.84190180359021,5.10498495568598));
#47249=CARTESIAN_POINT('Ctrl Pts',(0.240806750516323,-5.9216263077664,5.01219519710923));
#47250=CARTESIAN_POINT('Ctrl Pts',(-1.71968115229822,-6.00135081194258,
4.91940543853247));
#47251=CARTESIAN_POINT('Ctrl Pts',(-3.72369453080605,-5.01074983159395,
4.82661567995571));
#47252=CARTESIAN_POINT('Ctrl Pts',(-4.85091242711216,-3.40474590012443,
4.73382592137895));
#47253=CARTESIAN_POINT('Ctrl Pts',(-5.54112908934749,-2.42135956750124,
4.67700901165427));
#47254=CARTESIAN_POINT('Ctrl Pts',(-5.90260508509081,-1.20723758395451,
4.62019210192958));
#47255=CARTESIAN_POINT('Ctrl Pts',(-5.90893794266972,0.00341325037688023,
4.5633751922049));
#47256=CARTESIAN_POINT('Ctrl Pts',(-5.90693872189066,-4.21669123174065E-5,
4.31162480779551));
#47257=CARTESIAN_POINT('Ctrl Pts',(-5.90700121040943,-0.987104397471501,
4.35790938574237));
#47258=CARTESIAN_POINT('Ctrl Pts',(-5.67313073749119,-1.97413878964724,
4.40419396368922));
#47259=CARTESIAN_POINT('Ctrl Pts',(-5.20516343906184,-2.83372915305156,
4.45047854163608));
#47260=CARTESIAN_POINT('Ctrl Pts',(-4.26681446560791,-4.55734475140324,
4.54328649285178));
#47261=CARTESIAN_POINT('Ctrl Pts',(-2.38724087004325,-5.76855076214631,
4.6360944440675));
#47262=CARTESIAN_POINT('Ctrl Pts',(-0.429925854017753,-5.91091457392572,
4.72890239528321));
#47263=CARTESIAN_POINT('Ctrl Pts',(1.52738916200774,-6.05327838570513,4.82171034649892));
#47264=CARTESIAN_POINT('Ctrl Pts',(3.56244559849406,-5.12679999852089,4.91451829771462));
#47265=CARTESIAN_POINT('Ctrl Pts',(4.74033085001728,-3.55710707915503,5.00732624893033));
#47266=CARTESIAN_POINT('Ctrl Pts',(5.9182161015405,-1.98741415978915,5.10013420014604));
#47267=CARTESIAN_POINT('Ctrl Pts',(6.23893016810059,0.22549329175838,5.19294215136175));
#47268=CARTESIAN_POINT('Ctrl Pts',(5.55513579742875,2.06499724269212,5.28575010257746));
#47269=CARTESIAN_POINT('Ctrl Pts',(4.87134142675691,3.90450119362583,5.37855805379317));
#47270=CARTESIAN_POINT('Ctrl Pts',(3.18303861885318,5.37060164394576,5.47136600500888));
#47271=CARTESIAN_POINT('Ctrl Pts',(1.26584005382931,5.7897665150092,5.56417395622459));
#47272=CARTESIAN_POINT('Ctrl Pts',(-0.651358511194623,6.20893138607266,
5.6569819074403));
#47273=CARTESIAN_POINT('Ctrl Pts',(-2.79745283333869,5.58116067787958,5.74978985865602));
#47274=CARTESIAN_POINT('Ctrl Pts',(-4.18651908354902,4.19485462242498,5.84259780987173));
#47275=CARTESIAN_POINT('Ctrl Pts',(-5.27925236309908,3.10429269839319,5.91560680917965));
#47276=CARTESIAN_POINT('Ctrl Pts',(-5.90350202906922,1.54431438983364,5.98861580848757));
#47277=CARTESIAN_POINT('Ctrl Pts',(-5.91791297517326,-0.00538731180401663,
6.0616248077955));
#47278=CARTESIAN_POINT('Origin',(0.,0.,-10.));
#47279=CARTESIAN_POINT('',(-5.92610585757929,-0.00142481640334258,8.06337519220491));
#47280=CARTESIAN_POINT('',(-5.92520251234299,0.00254533425411539,7.81162480779552));
#47281=CARTESIAN_POINT('',(-5.91675,-7.2459289488551E-16,-10.));
#47282=CARTESIAN_POINT('Ctrl Pts',(-5.92610585757929,-0.00142481640334258,
8.06337519220491));
#47283=CARTESIAN_POINT('Ctrl Pts',(-5.92000527951757,1.88433477380826,7.97421277960724));
#47284=CARTESIAN_POINT('Ctrl Pts',(-4.94203695946198,3.77553572286442,7.88505036700958));
#47285=CARTESIAN_POINT('Ctrl Pts',(-3.39711376542502,4.85626029828357,7.79588795441191));
#47286=CARTESIAN_POINT('Ctrl Pts',(-1.78933930062697,5.98095140431731,7.70309819583515));
#47287=CARTESIAN_POINT('Ctrl Pts',(0.43245861786239,6.22788040808508,7.6103084372584));
#47288=CARTESIAN_POINT('Ctrl Pts',(2.24794389322745,5.48364789832706,7.51751867868164));
#47289=CARTESIAN_POINT('Ctrl Pts',(4.0634291685925,4.73941538856904,7.42472892010489));
#47290=CARTESIAN_POINT('Ctrl Pts',(5.47260180083323,3.00402136528525,7.33193916152813));
#47291=CARTESIAN_POINT('Ctrl Pts',(5.82831485936943,1.07442632133564,7.23914940295137));
#47292=CARTESIAN_POINT('Ctrl Pts',(6.18402791790564,-0.855168722614004,
7.14635964437462));
#47293=CARTESIAN_POINT('Ctrl Pts',(5.48628140273722,-2.97896478722948,7.05356988579786));
#47294=CARTESIAN_POINT('Ctrl Pts',(4.05550767628976,-4.32163204212022,6.9607801272211));
#47295=CARTESIAN_POINT('Ctrl Pts',(2.6247339498423,-5.66429929701095,6.86799036864435));
#47296=CARTESIAN_POINT('Ctrl Pts',(0.460933012115797,-6.22583774217698,
6.77520061006759));
#47297=CARTESIAN_POINT('Ctrl Pts',(-1.44219351141203,-5.74836706339865,
6.68241085149083));
#47298=CARTESIAN_POINT('Ctrl Pts',(-3.34532003493986,-5.27089638462031,
6.58962109291407));
#47299=CARTESIAN_POINT('Ctrl Pts',(-4.987772144269,-3.75441658189762,6.49683133433732));
#47300=CARTESIAN_POINT('Ctrl Pts',(-5.61527189157466,-1.8953542158702,6.40404157576057));
#47301=CARTESIAN_POINT('Ctrl Pts',(-5.81965196412772,-1.28984751585831,
6.37381944790868));
#47302=CARTESIAN_POINT('Ctrl Pts',(-5.91636180537109,-0.647998278783763,
6.34359732005679));
#47303=CARTESIAN_POINT('Ctrl Pts',(-5.91154939285259,-0.00474152141923923,
6.31337519220491));
#47304=CARTESIAN_POINT('Ctrl Pts',(-5.91791297517326,-0.00538731180401663,
6.0616248077955));
#47305=CARTESIAN_POINT('Ctrl Pts',(-5.92182100886177,-0.425643304256778,
6.08142375970328));
#47306=CARTESIAN_POINT('Ctrl Pts',(-5.880880678592,-0.84514354114256,6.10122271161106));
#47307=CARTESIAN_POINT('Ctrl Pts',(-5.79227289452576,-1.25432135258176,
6.12102166351885));
#47308=CARTESIAN_POINT('Ctrl Pts',(-5.37692227701563,-3.17234986941806,
6.21382961473456));
#47309=CARTESIAN_POINT('Ctrl Pts',(-3.9141828637187,-4.86356550037465,6.30663756595028));
#47310=CARTESIAN_POINT('Ctrl Pts',(-2.07604266018777,-5.55101740343884,
6.39944551716599));
#47311=CARTESIAN_POINT('Ctrl Pts',(-0.237902456656868,-6.23846930650301,
6.4922534683817));
#47312=CARTESIAN_POINT('Ctrl Pts',(1.97563853710807,-5.92215748167482,6.58506141959739));
#47313=CARTESIAN_POINT('Ctrl Pts',(3.54767123662648,-4.74739677476125,6.6778693708131));
#47314=CARTESIAN_POINT('Ctrl Pts',(5.11970393614489,-3.57263606784768,6.77067732202881));
#47315=CARTESIAN_POINT('Ctrl Pts',(6.05022834141679,-1.53942647884874,6.86348527324453));
#47316=CARTESIAN_POINT('Ctrl Pts',(5.91175802968461,0.418167835515719,6.95629322446024));
#47317=CARTESIAN_POINT('Ctrl Pts',(5.77328771795243,2.37576214988019,7.04910117567596));
#47318=CARTESIAN_POINT('Ctrl Pts',(4.56582268921612,4.25774118961017,7.14190912689166));
#47319=CARTESIAN_POINT('Ctrl Pts',(2.84407693358168,5.19951668293015,7.23471707810737));
#47320=CARTESIAN_POINT('Ctrl Pts',(1.12233117794723,6.14129217625015,7.32752502932308));
#47321=CARTESIAN_POINT('Ctrl Pts',(-1.11369530458533,6.14286412316017,7.42033298053879));
#47322=CARTESIAN_POINT('Ctrl Pts',(-2.83676351115532,5.2035103653186,7.5131409317545));
#47323=CARTESIAN_POINT('Ctrl Pts',(-4.55983171772526,4.26415660747706,7.60594888297021));
#47324=CARTESIAN_POINT('Ctrl Pts',(-5.76994164833263,2.38387714488395,7.69875683418592));
#47325=CARTESIAN_POINT('Ctrl Pts',(-5.91116423497235,0.426479457165389,
7.79156478540163));
#47326=CARTESIAN_POINT('Ctrl Pts',(-5.92133911120299,0.285451880199395,
7.79825145953293));
#47327=CARTESIAN_POINT('Ctrl Pts',(-5.92596540705868,0.144023983524415,
7.80493813366422));
#47328=CARTESIAN_POINT('Ctrl Pts',(-5.92520251234299,0.00254533425411539,
7.81162480779552));
#47329=CARTESIAN_POINT('Origin',(0.,0.,-10.));
#47330=CARTESIAN_POINT('',(-5.91585872307276,0.00546062239083878,9.81337519220492));
#47331=CARTESIAN_POINT('',(-5.91009314746035,0.00413707980402536,9.5616248077955));
#47332=CARTESIAN_POINT('',(-5.91675,-7.2459289488551E-16,-10.));
#47333=CARTESIAN_POINT('Ctrl Pts',(-5.91585872307276,0.00546062239083878,
9.81337519220492));
#47334=CARTESIAN_POINT('Ctrl Pts',(-5.92031005889638,0.493404501843675,
9.79040775631121));
#47335=CARTESIAN_POINT('Ctrl Pts',(-5.86501686991171,0.9803530671637,9.7674403204175));
#47336=CARTESIAN_POINT('Ctrl Pts',(-5.74609214718014,1.45123087620132,9.7444728845238));
#47337=CARTESIAN_POINT('Ctrl Pts',(-5.2656294450248,3.35360423742296,9.65168312594704));
#47338=CARTESIAN_POINT('Ctrl Pts',(-3.74656880677743,4.99366969368778,9.55889336737027));
#47339=CARTESIAN_POINT('Ctrl Pts',(-1.88652201322028,5.61824534116842,9.46610360879351));
#47340=CARTESIAN_POINT('Ctrl Pts',(-0.0264752196631479,6.24282098864905,
9.37331385021676));
#47341=CARTESIAN_POINT('Ctrl Pts',(2.17455772920379,5.85190682734555,9.28052409164001));
#47342=CARTESIAN_POINT('Ctrl Pts',(3.70577681897754,4.6250258580741,9.18773433306326));
#47343=CARTESIAN_POINT('Ctrl Pts',(5.23699590875136,3.3981448888026,9.0949445744865));
#47344=CARTESIAN_POINT('Ctrl Pts',(6.09840113943194,1.33529711156315,9.00215481590974));
#47345=CARTESIAN_POINT('Ctrl Pts',(5.89440169534027,-0.616177469480281,
8.90936505733298));
#47346=CARTESIAN_POINT('Ctrl Pts',(5.6904022512486,-2.56765205052362,8.81657529875622));
#47347=CARTESIAN_POINT('Ctrl Pts',(4.42099813238473,-4.40775343537091,8.72378554017947));
#47348=CARTESIAN_POINT('Ctrl Pts',(2.66914912692053,-5.29143543456638,8.63099578160272));
#47349=CARTESIAN_POINT('Ctrl Pts',(0.917300121456278,-6.17511743376187,
8.53820602302596));
#47350=CARTESIAN_POINT('Ctrl Pts',(-1.31699377060835,-6.10238004730551,
8.44541626444921));
#47351=CARTESIAN_POINT('Ctrl Pts',(-3.00765781493459,-5.10662711466074,
8.35262650587245));
#47352=CARTESIAN_POINT('Ctrl Pts',(-4.69832185926076,-4.11087418201601,
8.25983674729569));
#47353=CARTESIAN_POINT('Ctrl Pts',(-5.84535605584862,-2.19210570318293,
8.16704698871894));
#47354=CARTESIAN_POINT('Ctrl Pts',(-5.92199764858924,-0.231494859616551,
8.07425723014218));
#47355=CARTESIAN_POINT('Ctrl Pts',(-5.924993728949,-0.154850475914561,8.07062988416309));
#47356=CARTESIAN_POINT('Ctrl Pts',(-5.9263540440814,-0.0781421490528213,
8.067002538184));
#47357=CARTESIAN_POINT('Ctrl Pts',(-5.92610585757929,-0.00142481640334258,
8.06337519220491));
#47358=CARTESIAN_POINT('Ctrl Pts',(-5.92520251234299,0.00254533425411539,
7.81162480779552));
#47359=CARTESIAN_POINT('Ctrl Pts',(-5.91537678046098,-1.81963437961978,
7.89774608487994));
#47360=CARTESIAN_POINT('Ctrl Pts',(-5.01157857549601,-3.65023306152754,
7.98386736196435));
#47361=CARTESIAN_POINT('Ctrl Pts',(-3.55434265269086,-4.74240399454357,
8.06998863904876));
#47362=CARTESIAN_POINT('Ctrl Pts',(-1.98396324109763,-5.91937384568984,
8.16279659026447));
#47363=CARTESIAN_POINT('Ctrl Pts',(0.229130824760936,-6.23879763513836,
8.25560454148017));
#47364=CARTESIAN_POINT('Ctrl Pts',(2.06823578077075,-5.55393086879374,8.34841249269589));
#47365=CARTESIAN_POINT('Ctrl Pts',(3.90734073678059,-4.86906410244912,8.44122044391159));
#47366=CARTESIAN_POINT('Ctrl Pts',(5.37245658294166,-3.1799067803114,8.53402839512731));
#47367=CARTESIAN_POINT('Ctrl Pts',(5.79050357147695,-1.26246414955556,8.62683634634302));
#47368=CARTESIAN_POINT('Ctrl Pts',(6.20855056001223,0.654978481200288,8.71964429755873));
#47369=CARTESIAN_POINT('Ctrl Pts',(5.57952869092166,2.80070642057423,8.81245224877443));
#47370=CARTESIAN_POINT('Ctrl Pts',(4.19241298423735,4.18896415713938,8.90526019999014));
#47371=CARTESIAN_POINT('Ctrl Pts',(2.80529727755305,5.57722189370453,8.99806815120585));
#47372=CARTESIAN_POINT('Ctrl Pts',(0.660087733274977,6.20800942746091,9.09087610242157));
#47373=CARTESIAN_POINT('Ctrl Pts',(-1.25769828983296,5.79154058536687,9.18368405363728));
#47374=CARTESIAN_POINT('Ctrl Pts',(-3.17548431294089,5.37507174327283,9.27649200485299));
#47375=CARTESIAN_POINT('Ctrl Pts',(-4.86584681487867,3.91134652532842,9.3692999560687));
#47376=CARTESIAN_POINT('Ctrl Pts',(-5.55222688432391,2.07280581946095,9.46210790728441));
#47377=CARTESIAN_POINT('Ctrl Pts',(-5.79755937358089,1.41565712291544,9.49528020745477));
#47378=CARTESIAN_POINT('Ctrl Pts',(-5.91462723191149,0.710623554415929,
9.52845250762514));
#47379=CARTESIAN_POINT('Ctrl Pts',(-5.91009314746035,0.00413707980402536,
9.5616248077955));
#47380=CARTESIAN_POINT('Origin',(0.,0.,-10.));
#47381=CARTESIAN_POINT('',(-5.90713571469763,-0.00111013332615595,11.5633751922049));
#47382=CARTESIAN_POINT('',(-5.91010328083002,-0.00414228348423679,11.3116248077955));
#47383=CARTESIAN_POINT('',(-5.91675,-7.2459289488551E-16,-10.));
#47384=CARTESIAN_POINT('Ctrl Pts',(-5.90713571469763,-0.00111013332615595,
11.5633751922049));
#47385=CARTESIAN_POINT('Ctrl Pts',(-5.90537029125798,1.05576347433266,11.5138129744384));
#47386=CARTESIAN_POINT('Ctrl Pts',(-5.63517675792205,2.11347947535037,11.4642507566719));
#47387=CARTESIAN_POINT('Ctrl Pts',(-5.10189134263591,3.01568412600891,11.4146885389054));
#47388=CARTESIAN_POINT('Ctrl Pts',(-4.10348111874248,4.70478028622991,11.3218987803286));
#47389=CARTESIAN_POINT('Ctrl Pts',(-2.18291133267984,5.8487958544671,11.2291090217519));
#47390=CARTESIAN_POINT('Ctrl Pts',(-0.222182396306169,5.92235434626272,
11.1363192631751));
#47391=CARTESIAN_POINT('Ctrl Pts',(1.73854654006744,5.99591283805835,11.0435295045984));
#47392=CARTESIAN_POINT('Ctrl Pts',(3.73943462675207,4.99901425341247,10.9507397460216));
#47393=CARTESIAN_POINT('Ctrl Pts',(4.86159616152291,3.38947323078248,10.8579499874449));
#47394=CARTESIAN_POINT('Ctrl Pts',(5.98375769629379,1.77993220815245,10.7651602288681));
#47395=CARTESIAN_POINT('Ctrl Pts',(6.22719267915082,-0.442251252461718,
10.6723704702913));
#47396=CARTESIAN_POINT('Ctrl Pts',(5.48010628925558,-2.25656399829182,10.5795807117146));
#47397=CARTESIAN_POINT('Ctrl Pts',(4.73301989936036,-4.07087674412186,10.4867909531378));
#47398=CARTESIAN_POINT('Ctrl Pts',(2.99541213671292,-5.47731877516786,10.3940011945611));
#47399=CARTESIAN_POINT('Ctrl Pts',(1.06526012946797,-5.82999715921811,10.3012114359843));
#47400=CARTESIAN_POINT('Ctrl Pts',(-0.864891877777048,-6.18267554326837,
10.2084216774076));
#47401=CARTESIAN_POINT('Ctrl Pts',(-2.98758812961958,-5.48159028032283,
10.1156319188308));
#47402=CARTESIAN_POINT('Ctrl Pts',(-4.3280038725092,-4.0487070157608,10.0228421602541));
#47403=CARTESIAN_POINT('Ctrl Pts',(-5.33663825161536,-2.97049279039852,
9.953019837571));
#47404=CARTESIAN_POINT('Ctrl Pts',(-5.90232640681047,-1.4779167628797,9.88319751488796));
#47405=CARTESIAN_POINT('Ctrl Pts',(-5.91585872307276,0.00546062239083878,
9.81337519220492));
#47406=CARTESIAN_POINT('Ctrl Pts',(-5.91009314746035,0.00413707980402536,
9.5616248077955));
#47407=CARTESIAN_POINT('Ctrl Pts',(-5.90194197685264,-1.26595214077577,
9.62126045884084));
#47408=CARTESIAN_POINT('Ctrl Pts',(-5.50078291561905,-2.54073703934775,
9.68089610988619));
#47409=CARTESIAN_POINT('Ctrl Pts',(-4.74532751911606,-3.55043857523549,
9.74053176093154));
#47410=CARTESIAN_POINT('Ctrl Pts',(-3.56965044751031,-5.12178607027405,
9.83333971214725));
#47411=CARTESIAN_POINT('Ctrl Pts',(-1.53589866734621,-6.05112486656059,
9.92614766336295));
#47412=CARTESIAN_POINT('Ctrl Pts',(0.421614579989387,-5.91151321457888,
10.0189556145787));
#47413=CARTESIAN_POINT('Ctrl Pts',(2.37912782732493,-5.77190156259718,10.1117635657944));
#47414=CARTESIAN_POINT('Ctrl Pts',(4.26040254183193,-4.56333946234723,10.2045715170101));
#47415=CARTESIAN_POINT('Ctrl Pts',(5.20117402139986,-2.84104490272778,10.2973794682258));
#47416=CARTESIAN_POINT('Ctrl Pts',(6.1419455009678,-1.11875034310833,10.3901874194415));
#47417=CARTESIAN_POINT('Ctrl Pts',(6.14221374559667,1.11727667588066,10.4829953706572));
#47418=CARTESIAN_POINT('Ctrl Pts',(5.20185552269185,2.83979690492835,10.5758033218729));
#47419=CARTESIAN_POINT('Ctrl Pts',(4.26149729978703,4.56231713397607,10.6686112730886));
#47420=CARTESIAN_POINT('Ctrl Pts',(2.38051260934848,5.77133057308248,10.7614192243043));
#47421=CARTESIAN_POINT('Ctrl Pts',(0.423032915335419,5.91141188657525,10.8542271755201));
#47422=CARTESIAN_POINT('Ctrl Pts',(-1.53444677867767,6.05149320006802,10.9470351267358));
#47423=CARTESIAN_POINT('Ctrl Pts',(-3.56842147626521,5.12264238794716,11.0398430779515));
#47424=CARTESIAN_POINT('Ctrl Pts',(-4.74447552693495,3.55157701796197,11.1326510291672));
#47425=CARTESIAN_POINT('Ctrl Pts',(-5.50045542794686,2.54167969036188,11.1923089553766));
#47426=CARTESIAN_POINT('Ctrl Pts',(-5.9019379291562,1.26641587263688,11.2519668815861));
#47427=CARTESIAN_POINT('Ctrl Pts',(-5.91010328083002,-0.00414228348423679,
11.3116248077955));
#47428=CARTESIAN_POINT('Origin',(0.,0.,-10.));
#47429=CARTESIAN_POINT('',(-5.91994540799989,-0.00505429986354111,13.3133751922049));
#47430=CARTESIAN_POINT('',(-5.92521073655459,-0.00253761243528721,13.0616248077955));
#47431=CARTESIAN_POINT('',(-5.91675,-7.2459289488551E-16,-10.));
#47432=CARTESIAN_POINT('Ctrl Pts',(-5.91994540799989,-0.00505429986354111,
13.3133751922049));
#47433=CARTESIAN_POINT('Ctrl Pts',(-5.90529546049876,1.610039595349,13.2372181925656));
#47434=CARTESIAN_POINT('Ctrl Pts',(-5.21966076773228,3.23607223700127,13.1610611929263));
#47435=CARTESIAN_POINT('Ctrl Pts',(-4.04189634411325,4.33436500117022,13.084904193287));
#47436=CARTESIAN_POINT('Ctrl Pts',(-2.606907084485,5.67252591765216,12.9921144347103));
#47437=CARTESIAN_POINT('Ctrl Pts',(-0.441350842398215,6.22725656027499,
12.8993246761335));
#47438=CARTESIAN_POINT('Ctrl Pts',(1.46026465257464,5.74380302276866,12.8065349175568));
#47439=CARTESIAN_POINT('Ctrl Pts',(3.36188014754744,5.26034948526234,12.71374515898));
#47440=CARTESIAN_POINT('Ctrl Pts',(4.99955489540633,3.73871176762691,12.6209554004032));
#47441=CARTESIAN_POINT('Ctrl Pts',(5.62120489869217,1.87768514582304,12.5281656418265));
#47442=CARTESIAN_POINT('Ctrl Pts',(6.24285490197803,0.0166585240191056,
12.4353758832497));
#47443=CARTESIAN_POINT('Ctrl Pts',(5.84848016069077,-2.18375700195329,12.342586124673));
#47444=CARTESIAN_POINT('Ctrl Pts',(4.61919290869249,-3.71304496232006,12.2497963660962));
#47445=CARTESIAN_POINT('Ctrl Pts',(3.38990565669422,-5.24233292268681,12.1570066075195));
#47446=CARTESIAN_POINT('Ctrl Pts',(1.32570589398494,-6.10049331744795,12.0642168489427));
#47447=CARTESIAN_POINT('Ctrl Pts',(-0.625445490911942,-5.89342548589725,
11.9714270903659));
#47448=CARTESIAN_POINT('Ctrl Pts',(-2.57659687580883,-5.68635765434655,
11.8786373317892));
#47449=CARTESIAN_POINT('Ctrl Pts',(-4.41469988289332,-4.41406159648403,
11.7858475732124));
#47450=CARTESIAN_POINT('Ctrl Pts',(-5.29562605557344,-2.66082519145039,
11.6930578146357));
#47451=CARTESIAN_POINT('Ctrl Pts',(-5.70601910610445,-1.84405295913638,
11.6498302738254));
#47452=CARTESIAN_POINT('Ctrl Pts',(-5.90867549474026,-0.922901955104379,
11.6066027330152));
#47453=CARTESIAN_POINT('Ctrl Pts',(-5.90713571469763,-0.00111013332615595,
11.5633751922049));
#47454=CARTESIAN_POINT('Ctrl Pts',(-5.91010328083002,-0.00414228348423679,
11.3116248077955));
#47455=CARTESIAN_POINT('Ctrl Pts',(-5.91464050881247,-0.710151314027206,
11.3447748328018));
#47456=CARTESIAN_POINT('Ctrl Pts',(-5.7977342302467,-1.41470738975629,11.377924857808));
#47457=CARTESIAN_POINT('Ctrl Pts',(-5.55272405215304,-2.07147361577248,
11.4110748828143));
#47458=CARTESIAN_POINT('Ctrl Pts',(-4.86678512294952,-3.91017895167227,
11.50388283403));
#47459=CARTESIAN_POINT('Ctrl Pts',(-3.17677386079062,-5.37430969562241,
11.5966907852457));
#47460=CARTESIAN_POINT('Ctrl Pts',(-1.25908781611912,-5.79123865951843,
11.6894987364614));
#47461=CARTESIAN_POINT('Ctrl Pts',(0.658598228552384,-6.20816762341444,
11.7823066876772));
#47462=CARTESIAN_POINT('Ctrl Pts',(2.80395905573648,-5.57789480725632,11.8751146388929));
#47463=CARTESIAN_POINT('Ctrl Pts',(4.19140780673151,-4.18996992087897,11.9679225901086));
#47464=CARTESIAN_POINT('Ctrl Pts',(5.57885655772655,-2.80204503450161,12.0607305413243));
#47465=CARTESIAN_POINT('Ctrl Pts',(6.2083932325325,-0.656468077904998,12.15353849254));
#47466=CARTESIAN_POINT('Ctrl Pts',(5.79080630742918,1.26107479954157,12.2463464437557));
#47467=CARTESIAN_POINT('Ctrl Pts',(5.37321938232585,3.17861767698814,12.3391543949714));
#47468=CARTESIAN_POINT('Ctrl Pts',(3.90850885731324,4.86812647528467,12.4319623461871));
#47469=CARTESIAN_POINT('Ctrl Pts',(2.06956827410354,5.5534344777826,12.5247702974028));
#47470=CARTESIAN_POINT('Ctrl Pts',(0.230627690893864,6.2387424802805,12.6175782486185));
#47471=CARTESIAN_POINT('Ctrl Pts',(-1.9825429505129,5.91984968697983,12.7103861998343));
#47472=CARTESIAN_POINT('Ctrl Pts',(-3.55320470690695,4.74325665034211,12.80319415105));
#47473=CARTESIAN_POINT('Ctrl Pts',(-5.01107961206679,3.65115298466299,12.8893377032985));
#47474=CARTESIAN_POINT('Ctrl Pts',(-5.91540774870406,1.8201067002357,12.975481255547));
#47475=CARTESIAN_POINT('Ctrl Pts',(-5.92521073655459,-0.00253761243528721,
13.0616248077955));
#47476=CARTESIAN_POINT('Origin',(0.,0.,-10.));
#47477=CARTESIAN_POINT('',(-5.92377318385666,0.00359036632908968,15.0633751922049));
#47478=CARTESIAN_POINT('',(-5.91789849188119,0.00538873909439685,14.8116248077955));
#47479=CARTESIAN_POINT('',(-5.91675,-7.2459289488551E-16,-10.));
#47480=CARTESIAN_POINT('Ctrl Pts',(-5.92377318385666,0.00359036632908968,
15.0633751922049));
#47481=CARTESIAN_POINT('Ctrl Pts',(-5.92527934221041,0.214504010083895,
15.0534131692696));
#47482=CARTESIAN_POINT('Ctrl Pts',(-5.91499513265657,0.425269163136507,
15.0434511463342));
#47483=CARTESIAN_POINT('Ctrl Pts',(-5.89243470395443,0.634711965822937,
15.0334891233989));
#47484=CARTESIAN_POINT('Ctrl Pts',(-5.68229899695524,2.58553533001874,14.9406993648221));
#47485=CARTESIAN_POINT('Ctrl Pts',(-4.40711414606309,4.42163541431722,14.8479096062454));
#47486=CARTESIAN_POINT('Ctrl Pts',(-2.65249467663608,5.29980358224176,14.7551198476686));
#47487=CARTESIAN_POINT('Ctrl Pts',(-0.897875207209115,6.17797175016628,
14.6623300890919));
#47488=CARTESIAN_POINT('Ctrl Pts',(1.33617888075265,6.0982080017169,14.5695403305151));
#47489=CARTESIAN_POINT('Ctrl Pts',(3.02370298028995,5.09714295531438,14.4767505719384));
#47490=CARTESIAN_POINT('Ctrl Pts',(4.71122707982726,4.09607790891186,14.3839608133616));
#47491=CARTESIAN_POINT('Ctrl Pts',(5.85222119094007,2.17371156455622,14.2911710547849));
#47492=CARTESIAN_POINT('Ctrl Pts',(5.92269639990486,0.212869383612165,14.1983812962081));
#47493=CARTESIAN_POINT('Ctrl Pts',(5.99317160886964,-1.74797279733192,14.1055915376314));
#47494=CARTESIAN_POINT('Ctrl Pts',(4.99312791568633,-3.74729081486445,14.0128017790546));
#47495=CARTESIAN_POINT('Ctrl Pts',(3.38182431508907,-4.86692000363656,13.9200120204778));
#47496=CARTESIAN_POINT('Ctrl Pts',(1.77052071449184,-5.98654919240866,13.8272222619011));
#47497=CARTESIAN_POINT('Ctrl Pts',(-0.452042793519305,-6.22648955242042,
13.7344325033243));
#47498=CARTESIAN_POINT('Ctrl Pts',(-2.26517852361662,-5.47655112968658,
13.6416427447476));
#47499=CARTESIAN_POINT('Ctrl Pts',(-4.07831425371399,-4.72661270695272,
13.5488529861708));
#47500=CARTESIAN_POINT('Ctrl Pts',(-5.48202220589748,-2.9867955014732,13.456063227594));
#47501=CARTESIAN_POINT('Ctrl Pts',(-5.83166504340434,-1.05609130356291,
13.3632734690173));
#47502=CARTESIAN_POINT('Ctrl Pts',(-5.89433925572756,-0.710008524644843,
13.3466407100798));
#47503=CARTESIAN_POINT('Ctrl Pts',(-5.92314497004129,-0.357792295683551,
13.3300079511424));
#47504=CARTESIAN_POINT('Ctrl Pts',(-5.91994540799989,-0.00505429986354111,
13.3133751922049));
#47505=CARTESIAN_POINT('Ctrl Pts',(-5.92521073655459,-0.00253761243528721,
13.0616248077955));
#47506=CARTESIAN_POINT('Ctrl Pts',(-5.92596913367662,-0.143544438342343,
13.0682892067627));
#47507=CARTESIAN_POINT('Ctrl Pts',(-5.92137364653565,-0.284500977027824,
13.0749536057299));
#47508=CARTESIAN_POINT('Ctrl Pts',(-5.91126638991079,-0.425061181139209,
13.0816180046971));
#47509=CARTESIAN_POINT('Ctrl Pts',(-5.7705134451392,-2.38249269600794,13.1744259559128));
#47510=CARTESIAN_POINT('Ctrl Pts',(-4.56085468421472,-4.26306244577067,
13.2672339071285));
#47511=CARTESIAN_POINT('Ctrl Pts',(-2.83801190608778,-5.20282959178026,
13.3600418583442));
#47512=CARTESIAN_POINT('Ctrl Pts',(-1.11516912796078,-6.14259673778988,
13.4528498095599));
#47513=CARTESIAN_POINT('Ctrl Pts',(1.12085766736865,-6.14156128004636,13.5456577607757));
#47514=CARTESIAN_POINT('Ctrl Pts',(2.84282933333981,-5.20019891174396,13.6384657119914));
#47515=CARTESIAN_POINT('Ctrl Pts',(4.56480099931093,-4.25883654344159,13.7312736632071));
#47516=CARTESIAN_POINT('Ctrl Pts',(5.77271753592375,-2.37714726458037,13.8240816144228));
#47517=CARTESIAN_POINT('Ctrl Pts',(5.91165752865023,-0.419586229699372,
13.9168895656385));
#47518=CARTESIAN_POINT('Ctrl Pts',(6.05059752137672,1.53797480518165,14.0096975168542));
#47519=CARTESIAN_POINT('Ctrl Pts',(5.12056097021688,3.57140759608242,14.1025054680699));
#47520=CARTESIAN_POINT('Ctrl Pts',(3.54881017590845,4.74654544648726,14.1953134192856));
#47521=CARTESIAN_POINT('Ctrl Pts',(1.97705938160005,5.92168329689209,14.2881213705013));
#47522=CARTESIAN_POINT('Ctrl Pts',(-0.236405655857032,6.23852620680096,
14.380929321717));
#47523=CARTESIAN_POINT('Ctrl Pts',(-2.0747107465965,5.55151534791694,14.4737372729327));
#47524=CARTESIAN_POINT('Ctrl Pts',(-3.91301583733602,4.8645044890329,14.5665452241485));
#47525=CARTESIAN_POINT('Ctrl Pts',(-5.37616098135797,3.17363986135601,14.6593531753642));
#47526=CARTESIAN_POINT('Ctrl Pts',(-5.79197177888372,1.25571105466782,14.7521611265799));
#47527=CARTESIAN_POINT('Ctrl Pts',(-5.88077753451924,0.846094185777964,
14.7719823536518));
#47528=CARTESIAN_POINT('Ctrl Pts',(-5.92181100139047,0.426120189229642,
14.7918035807236));
#47529=CARTESIAN_POINT('Ctrl Pts',(-5.91789849188119,0.00538873909439685,
14.8116248077955));
#47530=CARTESIAN_POINT('Origin',(0.,0.,-10.));
#47531=CARTESIAN_POINT('',(-5.9087266087589,0.0032487932499714,16.8133751922049));
#47532=CARTESIAN_POINT('',(-5.90693834692481,3.43012228386451E-5,16.5616248077955));
#47533=CARTESIAN_POINT('',(-5.91675,-7.2459289488551E-16,-10.));
#47534=CARTESIAN_POINT('Ctrl Pts',(-5.9087266087589,0.0032487932499714,
16.8133751922049));
#47535=CARTESIAN_POINT('Ctrl Pts',(-5.91259668880297,0.782268437741723,
16.7768183873968));
#47536=CARTESIAN_POINT('Ctrl Pts',(-5.7695619904093,1.55992356720195,16.7402615825886));
#47537=CARTESIAN_POINT('Ctrl Pts',(-5.47298242841067,2.27378744790129,16.7037047777805));
#47538=CARTESIAN_POINT('Ctrl Pts',(-4.72019382718881,4.08574167897852,16.6109150192038));
#47539=CARTESIAN_POINT('Ctrl Pts',(-2.97817148087205,5.4867120813921,16.518125260627));
#47540=CARTESIAN_POINT('Ctrl Pts',(-1.04691986629196,5.83331850780399,16.4253355020502));
#47541=CARTESIAN_POINT('Ctrl Pts',(0.884331748288081,6.17992493421588,16.3325457434735));
#47542=CARTESIAN_POINT('Ctrl Pts',(3.00481263113146,5.47216738462615,16.2397559848967));
#47543=CARTESIAN_POINT('Ctrl Pts',(4.34071541237453,4.0350756781874,16.14696622632));
#47544=CARTESIAN_POINT('Ctrl Pts',(5.67661819361766,2.59798397174859,16.0541764677432));
#47545=CARTESIAN_POINT('Ctrl Pts',(6.22794287326043,0.431558108460773,15.9613867091665));
#47546=CARTESIAN_POINT('Ctrl Pts',(5.74149969582441,-1.46929481819459,15.8685969505897));
#47547=CARTESIAN_POINT('Ctrl Pts',(5.25505651838841,-3.37014774484988,15.775807192013));
#47548=CARTESIAN_POINT('Ctrl Pts',(3.73084548387367,-5.0054277348727,15.6830174334362));
#47549=CARTESIAN_POINT('Ctrl Pts',(1.86884363552882,-5.62415055682801,15.5902276748594));
#47550=CARTESIAN_POINT('Ctrl Pts',(0.0068417871839091,-6.24287337878334,
15.4974379162827));
#47551=CARTESIAN_POINT('Ctrl Pts',(-2.19295087499116,-5.84503903267113,
15.4046481577059));
#47552=CARTESIAN_POINT('Ctrl Pts',(-3.72030392452555,-4.61334853756847,
15.3118583991292));
#47553=CARTESIAN_POINT('Ctrl Pts',(-5.08367846669871,-3.51389385328867,
15.2290306634878));
#47554=CARTESIAN_POINT('Ctrl Pts',(-5.9112504576224,-1.75001928117738,15.1462029278463));
#47555=CARTESIAN_POINT('Ctrl Pts',(-5.92377318385666,0.00359036632908968,
15.0633751922049));
#47556=CARTESIAN_POINT('Ctrl Pts',(-5.91789849188119,0.00538873909439685,
14.8116248077955));
#47557=CARTESIAN_POINT('Ctrl Pts',(-5.90349165161704,-1.54384987152742,
14.8846115319393));
#47558=CARTESIAN_POINT('Ctrl Pts',(-5.27966370824949,-3.10335877189863,
14.9575982560832));
#47559=CARTESIAN_POINT('Ctrl Pts',(-4.18752543318034,-4.19385003149471,
15.030584980227));
#47560=CARTESIAN_POINT('Ctrl Pts',(-2.79879183892172,-5.58048932526967,
15.1233929314427));
#47561=CARTESIAN_POINT('Ctrl Pts',(-0.652848199374933,-6.2087749271202,
15.2162008826584));
#47562=CARTESIAN_POINT('Ctrl Pts',(1.26445088055988,-5.79007006096228,15.3090088338741));
#47563=CARTESIAN_POINT('Ctrl Pts',(3.18174996049471,-5.37136519480435,15.4018167850898));
#47564=CARTESIAN_POINT('Ctrl Pts',(4.8704044808176,-3.90566986063792,15.4946247363055));
#47565=CARTESIAN_POINT('Ctrl Pts',(5.55464018340432,-2.06633002521627,15.5874326875213));
#47566=CARTESIAN_POINT('Ctrl Pts',(6.23887588599105,-0.226990189794622,
15.680240638737));
#47567=CARTESIAN_POINT('Ctrl Pts',(5.91869277084165,1.98599414688221,15.7730485899527));
#47568=CARTESIAN_POINT('Ctrl Pts',(4.74118416914349,3.55596963070039,15.8658565411684));
#47569=CARTESIAN_POINT('Ctrl Pts',(3.56367556744535,5.12594511451855,15.9586644923841));
#47570=CARTESIAN_POINT('Ctrl Pts',(1.52884147919836,6.05291174547805,16.0514724435998));
#47571=CARTESIAN_POINT('Ctrl Pts',(-0.428507637793467,5.91101755576424,
16.1442803948155));
#47572=CARTESIAN_POINT('Ctrl Pts',(-2.38585675478535,5.76912336605042,16.2370883460312));
#47573=CARTESIAN_POINT('Ctrl Pts',(-4.26572090052208,4.55836835566334,16.3298962972469));
#47574=CARTESIAN_POINT('Ctrl Pts',(-5.20448339350851,2.83497794469277,16.4227042484627));
#47575=CARTESIAN_POINT('Ctrl Pts',(-5.67288223541112,1.97508624825669,16.4690111015736));
#47576=CARTESIAN_POINT('Ctrl Pts',(-5.90698948598436,0.987571607557929,
16.5153179546846));
#47577=CARTESIAN_POINT('Ctrl Pts',(-5.90693863091242,3.43002300271205E-5,
16.5616248077955));
#47578=CARTESIAN_POINT('Origin',(0.,0.,-10.));
#47579=CARTESIAN_POINT('',(-5.91186200022437,-0.00484233898808362,18.5633751922049));
#47580=CARTESIAN_POINT('',(-5.91777217212816,-0.00540066091151231,18.3116248077955));
#47581=CARTESIAN_POINT('',(-5.91675,-7.2459289488551E-16,-10.));
#47582=CARTESIAN_POINT('Ctrl Pts',(-5.91186200022437,-0.00484233898808362,
18.5633751922049));
#47583=CARTESIAN_POINT('Ctrl Pts',(-5.90155532688764,1.33911565951482,18.500223605524));
#47584=CARTESIAN_POINT('Ctrl Pts',(-5.44739994873886,2.68937513445512,18.4370720188431));
#47585=CARTESIAN_POINT('Ctrl Pts',(-4.60749275915341,3.72755368764478,18.3739204321621));
#47586=CARTESIAN_POINT('Ctrl Pts',(-3.37340206651128,5.2529680497059,18.2811306735854));
#47587=CARTESIAN_POINT('Ctrl Pts',(-1.30651364845072,6.104632414813,18.1883409150086));
#47588=CARTESIAN_POINT('Ctrl Pts',(0.643976871300414,5.89142935196167,18.0955511564318));
#47589=CARTESIAN_POINT('Ctrl Pts',(2.59446739105152,5.67822628911034,18.0027613978551));
#47590=CARTESIAN_POINT('Ctrl Pts',(4.42856001249322,4.40015579830073,17.9099716392784));
#47591=CARTESIAN_POINT('Ctrl Pts',(5.30396800424161,2.64415760307637,17.8171818807016));
#47592=CARTESIAN_POINT('Ctrl Pts',(6.17937599599001,0.888159407852008,17.7243921221248));
#47593=CARTESIAN_POINT('Ctrl Pts',(6.09609935804498,-1.34576649178713,17.6316023635481));
#47594=CARTESIAN_POINT('Ctrl Pts',(5.09238196443743,-3.0317143579496,17.5388126049713));
#47595=CARTESIAN_POINT('Ctrl Pts',(4.0886645708299,-4.71766222411203,17.4460228463946));
#47596=CARTESIAN_POINT('Ctrl Pts',(2.1645064215599,-5.8556320567979,17.3532330878178));
#47597=CARTESIAN_POINT('Ctrl Pts',(0.203555844562213,-5.92302380866985,
17.2604433292411));
#47598=CARTESIAN_POINT('Ctrl Pts',(-1.75739473243558,-5.99041556054181,
17.1676535706643));
#47599=CARTESIAN_POINT('Ctrl Pts',(-3.75513773716107,-4.9872292315997,17.0748638120876));
#47600=CARTESIAN_POINT('Ctrl Pts',(-4.8722318114603,-3.37416703725817,16.9820740535108));
#47601=CARTESIAN_POINT('Ctrl Pts',(-5.54921923333517,-2.39661031988311,
16.9258410997422));
#47602=CARTESIAN_POINT('Ctrl Pts',(-5.90277351648673,-1.1950664283202,16.8696081459735));
#47603=CARTESIAN_POINT('Ctrl Pts',(-5.9087266087589,0.0032487932499714,
16.8133751922049));
#47604=CARTESIAN_POINT('Ctrl Pts',(-5.90693863091242,3.43002300271205E-5,
16.5616248077955));
#47605=CARTESIAN_POINT('Ctrl Pts',(-5.90688756251691,-0.991645464752838,
16.6081259059003));
#47606=CARTESIAN_POINT('Ctrl Pts',(-5.67070980570828,-1.98334808692469,
16.654627004005));
#47607=CARTESIAN_POINT('Ctrl Pts',(-5.19854053303828,-2.84586079535849,
16.7011281021098));
#47608=CARTESIAN_POINT('Ctrl Pts',(-4.2561743393455,-4.56728331288531,16.7939360533255));
#47609=CARTESIAN_POINT('Ctrl Pts',(-2.37378111172378,-5.77410253638496,
16.8867440045412));
#47610=CARTESIAN_POINT('Ctrl Pts',(-0.416139401428914,-5.91190116111381,
16.9795519557569));
#47611=CARTESIAN_POINT('Ctrl Pts',(1.54150230886587,-6.04969978584265,17.0723599069726));
#47612=CARTESIAN_POINT('Ctrl Pts',(3.5743925018338,-5.11847781180086,17.1651678581883));
#47613=CARTESIAN_POINT('Ctrl Pts',(4.74861375249686,-3.54604212747086,17.257975809404));
#47614=CARTESIAN_POINT('Ctrl Pts',(5.92283500315997,-1.9736064431408,17.3507837606197));
#47615=CARTESIAN_POINT('Ctrl Pts',(6.23838731151808,0.240042951477567,17.4435917118355));
#47616=CARTESIAN_POINT('Ctrl Pts',(5.55030475649628,2.07794717214253,17.5363996630512));
#47617=CARTESIAN_POINT('Ctrl Pts',(4.8622222014745,3.91585139280746,17.6292076142669));
#47618=CARTESIAN_POINT('Ctrl Pts',(3.1705047830729,5.37801043951901,17.7220155654826));
#47619=CARTESIAN_POINT('Ctrl Pts',(1.25233386634964,5.79270292932359,17.8148235166983));
#47620=CARTESIAN_POINT('Ctrl Pts',(-0.665837050373649,6.20739541912817,
17.907631467914));
#47621=CARTESIAN_POINT('Ctrl Pts',(-2.81046146541861,5.5746213520257,18.0004394191297));
#47622=CARTESIAN_POINT('Ctrl Pts',(-4.19629083059877,4.18507952197244,18.0932473703454));
#47623=CARTESIAN_POINT('Ctrl Pts',(-5.28324462980405,3.09521390844165,18.1660398494955));
#47624=CARTESIAN_POINT('Ctrl Pts',(-5.90340241438398,1.53979942792063,18.2388323286455));
#47625=CARTESIAN_POINT('Ctrl Pts',(-5.91777217212816,-0.00540066091151231,
18.3116248077955));
#47626=CARTESIAN_POINT('Origin',(0.,0.,-10.));
#47627=CARTESIAN_POINT('',(-5.92622532488715,-0.00120034675680336,20.3133751922049));
#47628=CARTESIAN_POINT('',(-5.92528153879606,0.00246997438850003,20.0616248077955));
#47629=CARTESIAN_POINT('',(-5.91675,-7.2459289488551E-16,-10.));
#47630=CARTESIAN_POINT('Ctrl Pts',(-5.92622532488715,-0.00120034675680336,
20.3133751922049));
#47631=CARTESIAN_POINT('Ctrl Pts',(-5.92097756735111,1.89680731405714,20.2236288236512));
#47632=CARTESIAN_POINT('Ctrl Pts',(-4.92835420966625,3.7995314474951,20.1338824550975));
#47633=CARTESIAN_POINT('Ctrl Pts',(-3.36650141622386,4.8775315718597,20.0441360865437));
#47634=CARTESIAN_POINT('Ctrl Pts',(-1.75168461670958,5.9920877694804,19.951346327967));
#47635=CARTESIAN_POINT('Ctrl Pts',(0.471622498167445,6.22503711256374,19.8585565693902));
#47636=CARTESIAN_POINT('Ctrl Pts',(2.28239074985864,5.46940019425212,19.7657668108135));
#47637=CARTESIAN_POINT('Ctrl Pts',(4.09315900154977,4.71376327594051,19.6729770522367));
#47638=CARTESIAN_POINT('Ctrl Pts',(5.4913883900551,2.96954009623401,19.58018729366));
#47639=CARTESIAN_POINT('Ctrl Pts',(5.83495754832857,1.03774584033322,19.4873975350832));
#47640=CARTESIAN_POINT('Ctrl Pts',(6.17852670660203,-0.894048415567604,
19.3946077765065));
#47641=CARTESIAN_POINT('Ctrl Pts',(5.46743563464361,-3.01341374766271,19.3018180179297));
#47642=CARTESIAN_POINT('Ctrl Pts',(4.0282450348487,-4.3470550904195,19.2090282593529));
#47643=CARTESIAN_POINT('Ctrl Pts',(2.5890544350538,-5.68069643317628,19.1162385007762));
#47644=CARTESIAN_POINT('Ctrl Pts',(0.421764307422399,-6.22861378659473,
19.0234487421994));
#47645=CARTESIAN_POINT('Ctrl Pts',(-1.47832135073232,-5.73918217204283,
18.9306589836227));
#47646=CARTESIAN_POINT('Ctrl Pts',(-3.37840700888707,-5.24975055749093,
18.8378692250459));
#47647=CARTESIAN_POINT('Ctrl Pts',(-5.01128819756513,-3.72296997496864,
18.7450794664691));
#47648=CARTESIAN_POINT('Ctrl Pts',(-5.62708230829223,-1.85999750419993,
18.6522897078924));
#47649=CARTESIAN_POINT('Ctrl Pts',(-5.82377440002851,-1.26494155004352,
18.6226515359966));
#47650=CARTESIAN_POINT('Ctrl Pts',(-5.91669910681317,-0.63558592396959,
18.5930133641007));
#47651=CARTESIAN_POINT('Ctrl Pts',(-5.91186200022437,-0.00484233898808362,
18.5633751922049));
#47652=CARTESIAN_POINT('Ctrl Pts',(-5.91777217212816,-0.00540066091151231,
18.3116248077955));
#47653=CARTESIAN_POINT('Ctrl Pts',(-5.92172336994527,-0.430278472122732,
18.3316402798612));
#47654=CARTESIAN_POINT('Ctrl Pts',(-5.8798731060043,-0.854384009783482,
18.3516557519269));
#47655=CARTESIAN_POINT('Ctrl Pts',(-5.78933184621644,-1.26782653174028,
18.3716712239925));
#47656=CARTESIAN_POINT('Ctrl Pts',(-5.3695091813386,-3.18488116239587,18.4644791752083));
#47657=CARTESIAN_POINT('Ctrl Pts',(-3.90282953626755,-4.87268083070307,
18.557287126424));
#47658=CARTESIAN_POINT('Ctrl Pts',(-2.06309107389996,-5.55584400077924,
18.6500950776397));
#47659=CARTESIAN_POINT('Ctrl Pts',(-0.223352611532319,-6.23900717085543,
18.7429030288554));
#47660=CARTESIAN_POINT('Ctrl Pts',(1.98944466813189,-5.91753384270046,18.8357109800711));
#47661=CARTESIAN_POINT('Ctrl Pts',(3.55873334567604,-4.73911007622462,18.9285189312868));
#47662=CARTESIAN_POINT('Ctrl Pts',(5.12802202322017,-3.5606863097488,19.0213268825025));
#47663=CARTESIAN_POINT('Ctrl Pts',(6.05380209864429,-1.52531210495216,19.1141348337182));
#47664=CARTESIAN_POINT('Ctrl Pts',(5.91076671222382,0.43195394878065,19.2069427849339));
#47665=CARTESIAN_POINT('Ctrl Pts',(5.76773132580335,2.38922000251349,19.2997507361496));
#47666=CARTESIAN_POINT('Ctrl Pts',(4.55588047753819,4.26837790518251,19.3925586873654));
#47667=CARTESIAN_POINT('Ctrl Pts',(2.83194301957413,5.20613542602243,19.4853666385811));
#47668=CARTESIAN_POINT('Ctrl Pts',(1.10800556161013,6.14389294686232,19.5781745897968));
#47669=CARTESIAN_POINT('Ctrl Pts',(-1.12801850605279,6.14025008587321,19.6709825410125));
#47670=CARTESIAN_POINT('Ctrl Pts',(-2.84889128995409,5.19688038713843,19.7637904922282));
#47671=CARTESIAN_POINT('Ctrl Pts',(-4.56976407385542,4.25351068840363,19.8565984434439));
#47672=CARTESIAN_POINT('Ctrl Pts',(-5.77548557399514,2.37041415192319,19.9494063946596));
#47673=CARTESIAN_POINT('Ctrl Pts',(-5.91214278388311,0.412692431696099,
20.0422143458753));
#47674=CARTESIAN_POINT('Ctrl Pts',(-5.92166991144025,0.276208856732997,
20.0486844998487));
#47675=CARTESIAN_POINT('Ctrl Pts',(-5.9260011162672,0.139362584510233,20.0551546538221));
#47676=CARTESIAN_POINT('Ctrl Pts',(-5.92528153879606,0.00246997438850003,
20.0616248077955));
#47677=CARTESIAN_POINT('Origin',(0.,0.,-10.));
#47678=CARTESIAN_POINT('',(-5.91548613894553,0.00544808287233939,22.0633751922049));
#47679=CARTESIAN_POINT('',(-5.91019222577512,0.00418729649785822,21.8116248077955));
#47680=CARTESIAN_POINT('',(-5.91675,-7.2459289488551E-16,-10.));
#47681=CARTESIAN_POINT('Ctrl Pts',(-5.91548613894553,0.00544808287233939,
22.0633751922049));
#47682=CARTESIAN_POINT('Ctrl Pts',(-5.92001583191384,0.505878420791942,
22.0398238003552));
#47683=CARTESIAN_POINT('Ctrl Pts',(-5.86183352928881,1.00527075686111,22.0162724085054));
#47684=CARTESIAN_POINT('Ctrl Pts',(-5.73685045715431,1.4873442278685,21.9927210166556));
#47685=CARTESIAN_POINT('Ctrl Pts',(-5.24443161568961,3.38665791923673,21.8999312580789));
#47686=CARTESIAN_POINT('Ctrl Pts',(-3.71508526038522,5.01713626899271,21.8071414995021));
#47687=CARTESIAN_POINT('Ctrl Pts',(-1.85114677370993,5.63000014583558,21.7143517409254));
#47688=CARTESIAN_POINT('Ctrl Pts',(0.0127917129653046,6.24286402267844,
21.6215619823486));
#47689=CARTESIAN_POINT('Ctrl Pts',(2.21132233101142,5.83811342660825,21.5287722237718));
#47690=CARTESIAN_POINT('Ctrl Pts',(3.73479423375194,4.60162558792636,21.4359824651951));
#47691=CARTESIAN_POINT('Ctrl Pts',(5.25826613649246,3.36513774924446,21.3431927066183));
#47692=CARTESIAN_POINT('Ctrl Pts',(6.10667932392737,1.29691266795085,21.2504029480416));
#47693=CARTESIAN_POINT('Ctrl Pts',(5.8904094324049,-0.65324018443506,21.1576131894648));
#47694=CARTESIAN_POINT('Ctrl Pts',(5.67413954088243,-2.603393036821,21.0648234308881));
#47695=CARTESIAN_POINT('Ctrl Pts',(4.39318657040249,-4.43547366029928,20.9720336723113));
#47696=CARTESIAN_POINT('Ctrl Pts',(2.6358139913858,-5.30811931127591,20.8792439137345));
#47697=CARTESIAN_POINT('Ctrl Pts',(0.878441412369118,-6.18076496225253,
20.7864541551578));
#47698=CARTESIAN_POINT('Ctrl Pts',(-1.35535077518424,-6.09397564072757,
20.6936643965811));
#47699=CARTESIAN_POINT('Ctrl Pts',(-3.03971823917821,-5.0876083817775,20.6008746380043));
#47700=CARTESIAN_POINT('Ctrl Pts',(-4.7240857031722,-4.08124112282742,20.5080848794275));
#47701=CARTESIAN_POINT('Ctrl Pts',(-5.85902844360669,-2.15529592645219,
20.4152951208508));
#47702=CARTESIAN_POINT('Ctrl Pts',(-5.92333657174814,-0.194241802185547,
20.322505362274));
#47703=CARTESIAN_POINT('Ctrl Pts',(-5.92544579930286,-0.129921637460919,
20.319461972251));
#47704=CARTESIAN_POINT('Ctrl Pts',(-5.92640328164669,-0.0655637039783095,
20.3164185822279));
#47705=CARTESIAN_POINT('Ctrl Pts',(-5.92622532488715,-0.00120034675680336,
20.3133751922049));
#47706=CARTESIAN_POINT('Ctrl Pts',(-5.92528153879606,0.00246997438850003,
20.0616248077955));
#47707=CARTESIAN_POINT('Ctrl Pts',(-5.91567949005679,-1.82422633999111,
20.1479626050378));
#47708=CARTESIAN_POINT('Ctrl Pts',(-5.00672204207656,-3.65917370087608,
20.2343004022801));
#47709=CARTESIAN_POINT('Ctrl Pts',(-3.54327287359004,-4.75068044426073,
20.3206381995225));
#47710=CARTESIAN_POINT('Ctrl Pts',(-1.97015283377279,-5.92398469601676,
20.4134461507382));
#47711=CARTESIAN_POINT('Ctrl Pts',(0.243680165497836,-6.23824629555509,
20.5062541019539));
#47712=CARTESIAN_POINT('Ctrl Pts',(2.08118289131029,-5.54909227830262,20.5990620531696));
#47713=CARTESIAN_POINT('Ctrl Pts',(3.91868561712269,-4.85993826105017,20.6918700043853));
#47714=CARTESIAN_POINT('Ctrl Pts',(5.3798580694769,-3.16736862700695,20.784677955601));
#47715=CARTESIAN_POINT('Ctrl Pts',(5.79343211058954,-1.24895625231246,20.8774859068167));
#47716=CARTESIAN_POINT('Ctrl Pts',(6.20700615170218,0.669456122382023,20.9702938580324));
#47717=CARTESIAN_POINT('Ctrl Pts',(5.57298178157328,2.81371123772783,21.0631018092481));
#47718=CARTESIAN_POINT('Ctrl Pts',(4.18263218808697,4.19873020321373,21.1559097604638));
#47719=CARTESIAN_POINT('Ctrl Pts',(2.79228259460061,5.58374916869967,21.2487177116796));
#47720=CARTESIAN_POINT('Ctrl Pts',(0.645607777756869,6.20953198432568,21.3415256628953));
#47721=CARTESIAN_POINT('Ctrl Pts',(-1.27120175193518,5.78859166344261,21.434333614111));
#47722=CARTESIAN_POINT('Ctrl Pts',(-3.18801128162718,5.36765134255955,21.5271415653267));
#47723=CARTESIAN_POINT('Ctrl Pts',(-4.87495552416746,3.89998788516743,21.6199495165424));
#47724=CARTESIAN_POINT('Ctrl Pts',(-5.55704592949822,2.05985142125534,21.7127574677581));
#47725=CARTESIAN_POINT('Ctrl Pts',(-5.79925385513654,1.40642537636112,21.7457132477706));
#47726=CARTESIAN_POINT('Ctrl Pts',(-5.91475620853708,0.706032893476995,
21.7786690277831));
#47727=CARTESIAN_POINT('Ctrl Pts',(-5.91019222577512,0.00418729649785822,
21.8116248077955));
#47728=CARTESIAN_POINT('Origin',(0.,0.,-10.));
#47729=CARTESIAN_POINT('',(-5.90721141655292,-0.00131122188027244,23.8133751922049));
#47730=CARTESIAN_POINT('',(-5.91000536569632,-0.00409134141470152,23.5616248077955));
#47731=CARTESIAN_POINT('',(-5.91675,-7.2459289488551E-16,-10.));
#47732=CARTESIAN_POINT('Ctrl Pts',(-5.90721141655292,-0.00131122188027244,
23.8133751922049));
#47733=CARTESIAN_POINT('Ctrl Pts',(-5.90510013293806,1.06798059387856,23.7632290184824));
#47734=CARTESIAN_POINT('Ctrl Pts',(-5.62812187284361,2.13829178876222,23.7130828447598));
#47735=CARTESIAN_POINT('Ctrl Pts',(-5.08282221913792,3.0477146041851,23.6629366710372));
#47736=CARTESIAN_POINT('Ctrl Pts',(-4.07380758326,4.73049750112469,23.5701469124605));
#47737=CARTESIAN_POINT('Ctrl Pts',(-2.14608010200764,5.86241034296819,23.4773571538837));
#47738=CARTESIAN_POINT('Ctrl Pts',(-0.184927279512977,5.92363468836636,
23.384567395307));
#47739=CARTESIAN_POINT('Ctrl Pts',(1.77622554298163,5.98485903376453,23.2917776367302));
#47740=CARTESIAN_POINT('Ctrl Pts',(3.77080370671858,4.97539488271743,23.1989878781534));
#47741=CARTESIAN_POINT('Ctrl Pts',(4.88281927173037,3.35882747094039,23.1061981195767));
#47742=CARTESIAN_POINT('Ctrl Pts',(5.99483483674221,1.74226005916329,23.0134083609999));
#47743=CARTESIAN_POINT('Ctrl Pts',(6.22428780302885,-0.481410613343747,
22.9206186024232));
#47744=CARTESIAN_POINT('Ctrl Pts',(5.46580443606862,-2.29098840821553,22.8278288438465));
#47745=CARTESIAN_POINT('Ctrl Pts',(4.70732106910843,-4.10056620308723,22.7350390852697));
#47746=CARTESIAN_POINT('Ctrl Pts',(2.96090136890143,-5.49605112032366,22.6422493266929));
#47747=CARTESIAN_POINT('Ctrl Pts',(1.0285692483707,-5.8365821609253,22.5494595681161));
#47748=CARTESIAN_POINT('Ctrl Pts',(-0.903762872160078,-6.17711320152695,
22.4566698095394));
#47749=CARTESIAN_POINT('Ctrl Pts',(-3.02200741301463,-5.46269036549375,
22.3638800509627));
#47750=CARTESIAN_POINT('Ctrl Pts',(-4.35338401962936,-4.0214044309869,22.2710902923859));
#47751=CARTESIAN_POINT('Ctrl Pts',(-5.34683785714821,-2.94593785339808,
22.2018519256589));
#47752=CARTESIAN_POINT('Ctrl Pts',(-5.90216936578403,-1.46575920199717,
22.1326135589319));
#47753=CARTESIAN_POINT('Ctrl Pts',(-5.91548613894553,0.00544808287233939,
22.0633751922049));
#47754=CARTESIAN_POINT('Ctrl Pts',(-5.91019222577512,0.00418729649785822,
21.8116248077955));
#47755=CARTESIAN_POINT('Ctrl Pts',(-5.90190341338669,-1.2704596034613,21.8714769789988));
#47756=CARTESIAN_POINT('Ctrl Pts',(-5.49759390107015,-2.54989938108599,
21.931329150202));
#47757=CARTESIAN_POINT('Ctrl Pts',(-4.73703437229062,-3.56149585089434,
21.9911813214053));
#47758=CARTESIAN_POINT('Ctrl Pts',(-3.55769584163102,-5.13009718869973,
22.083989272621));
#47759=CARTESIAN_POINT('Ctrl Pts',(-1.52178221219059,-6.05469039387844,
22.1767972238367));
#47760=CARTESIAN_POINT('Ctrl Pts',(0.435400112929308,-5.91051385937479,
22.2696051750524));
#47761=CARTESIAN_POINT('Ctrl Pts',(2.39258243804923,-5.76633732487114,22.3624131262681));
#47762=CARTESIAN_POINT('Ctrl Pts',(4.27103345884864,-4.55339105068509,22.4552210774838));
#47763=CARTESIAN_POINT('Ctrl Pts',(5.20778568876036,-2.82890713176364,22.5480290286995));
#47764=CARTESIAN_POINT('Ctrl Pts',(6.14453791867207,-1.1044232128422,22.6408369799152));
#47765=CARTESIAN_POINT('Ctrl Pts',(6.13959135769615,1.13159835081458,22.7336449311309));
#47766=CARTESIAN_POINT('Ctrl Pts',(5.19521847460889,2.85192081609621,22.8264528823466));
#47767=CARTESIAN_POINT('Ctrl Pts',(4.25084559152163,4.57224328137783,22.9192608335623));
#47768=CARTESIAN_POINT('Ctrl Pts',(2.36704638632299,5.77686664828424,23.0120687847781));
#47769=CARTESIAN_POINT('Ctrl Pts',(0.409245321672443,5.91238239687603,23.1048767359938));
#47770=CARTESIAN_POINT('Ctrl Pts',(-1.54855574297816,6.04789814546782,23.1976846872095));
#47771=CARTESIAN_POINT('Ctrl Pts',(-3.58035866708069,5.11430627574492,23.2904926384252));
#47772=CARTESIAN_POINT('Ctrl Pts',(-4.75274552107614,3.54050241520763,23.3833005896409));
#47773=CARTESIAN_POINT('Ctrl Pts',(-5.50363294101133,2.53251642807758,23.4427419956924));
#47774=CARTESIAN_POINT('Ctrl Pts',(-5.901978050059,1.26190815291944,23.502183401744));
#47775=CARTESIAN_POINT('Ctrl Pts',(-5.91000536569632,-0.00409134141470152,
23.5616248077955));
#47776=CARTESIAN_POINT('Origin',(0.,0.,-10.));
#47777=CARTESIAN_POINT('',(-5.92031232679181,-0.00496695537298586,25.5633751922049));
#47778=CARTESIAN_POINT('',(-5.9251298904235,-0.0026123641298589,25.3116248077955));
#47779=CARTESIAN_POINT('',(-5.91675,-7.2459289488551E-16,-10.));
#47780=CARTESIAN_POINT('Ctrl Pts',(-5.92031232679181,-0.00496695537298586,
25.5633751922049));
#47781=CARTESIAN_POINT('Ctrl Pts',(-5.90569424287378,1.62225043238685,25.4866342366096));
#47782=CARTESIAN_POINT('Ctrl Pts',(-5.20828674903878,3.26047459758013,25.4098932810142));
#47783=CARTESIAN_POINT('Ctrl Pts',(-4.01455388351686,4.35970218435446,25.3331523254189));
#47784=CARTESIAN_POINT('Ctrl Pts',(-2.57117617812347,5.68881076277143,25.2403625668421));
#47785=CARTESIAN_POINT('Ctrl Pts',(-0.402173600912262,6.22990940771235,
25.1475728082653));
#47786=CARTESIAN_POINT('Ctrl Pts',(1.49636342729237,5.73450455692444,25.0547830496886));
#47787=CARTESIAN_POINT('Ctrl Pts',(3.39490045549694,5.23909970613655,24.9619932911118));
#47788=CARTESIAN_POINT('Ctrl Pts',(5.02297193469495,3.70719135961988,24.8692035325351));
#47789=CARTESIAN_POINT('Ctrl Pts',(5.63290406224316,1.84229146594393,24.7764137739583));
#47790=CARTESIAN_POINT('Ctrl Pts',(6.24283618979139,-0.0226084277320635,
24.6836240153816));
#47791=CARTESIAN_POINT('Ctrl Pts',(5.83462896568976,-2.22049986856735,24.5908342568048));
#47792=CARTESIAN_POINT('Ctrl Pts',(4.59574703839515,-3.74202554494321,24.4980444982281));
#47793=CARTESIAN_POINT('Ctrl Pts',(3.35686511110057,-5.26355122131904,24.4052547396513));
#47794=CARTESIAN_POINT('Ctrl Pts',(1.28730848061306,-6.10871113323548,24.3124649810745));
#47795=CARTESIAN_POINT('Ctrl Pts',(-0.662501882322089,-5.88937494780601,
24.2196752224978));
#47796=CARTESIAN_POINT('Ctrl Pts',(-2.61231224525729,-5.67003876237653,
24.126885463921));
#47797=CARTESIAN_POINT('Ctrl Pts',(-4.44237634064012,-4.38620647960109,
24.0340957053443));
#47798=CARTESIAN_POINT('Ctrl Pts',(-5.31225749307975,-2.62746386219553,
23.9413059467675));
#47799=CARTESIAN_POINT('Ctrl Pts',(-5.71203060711839,-1.81919481189961,
23.8986623619133));
#47800=CARTESIAN_POINT('Ctrl Pts',(-5.90900682177127,-0.910621601800537,
23.8560187770591));
#47801=CARTESIAN_POINT('Ctrl Pts',(-5.90721141655292,-0.00131122188027244,
23.8133751922049));
#47802=CARTESIAN_POINT('Ctrl Pts',(-5.91000536569632,-0.00409134141470152,
23.5616248077955));
#47803=CARTESIAN_POINT('Ctrl Pts',(-5.91451137939202,-0.71474124207285,
23.5949913529597));
#47804=CARTESIAN_POINT('Ctrl Pts',(-5.79602940848674,-1.42393892949713,
23.6283578981239));
#47805=CARTESIAN_POINT('Ctrl Pts',(-5.54787791374812,-2.08441790299983,
23.661724443288));
#47806=CARTESIAN_POINT('Ctrl Pts',(-4.8576526685363,-3.92151850931827,23.7545323945037));
#47807=CARTESIAN_POINT('Ctrl Pts',(-3.16423139422438,-5.38170387060348,
23.8473403457194));
#47808=CARTESIAN_POINT('Ctrl Pts',(-1.24557821370455,-5.79415932243367,
23.9401482969352));
#47809=CARTESIAN_POINT('Ctrl Pts',(0.673074966815246,-6.20661477426384,
24.0329562481509));
#47810=CARTESIAN_POINT('Ctrl Pts',(2.81696005354294,-5.57134031663897,24.1257641993666));
#47811=CARTESIAN_POINT('Ctrl Pts',(4.20116814851063,-4.18018343235558,24.2185721505823));
#47812=CARTESIAN_POINT('Ctrl Pts',(5.58537624347835,-2.78902654807216,24.311380101798));
#47813=CARTESIAN_POINT('Ctrl Pts',(6.20990734668606,-0.641987237130237,
24.4041880530137));
#47814=CARTESIAN_POINT('Ctrl Pts',(5.78784951289245,1.27457653999713,24.4969960042294));
#47815=CARTESIAN_POINT('Ctrl Pts',(5.36579167909883,3.19114031712452,24.5898039554451));
#47816=CARTESIAN_POINT('Ctrl Pts',(3.89714490830379,4.87722856043733,24.6826119066608));
#47817=CARTESIAN_POINT('Ctrl Pts',(2.05661106838393,5.5582459691526,24.7754198578766));
#47818=CARTESIAN_POINT('Ctrl Pts',(0.216077228464096,6.23926337786785,24.8682278090923));
#47819=CARTESIAN_POINT('Ctrl Pts',(-1.99634368058052,5.91520995198563,24.961035760308));
#47820=CARTESIAN_POINT('Ctrl Pts',(-3.56425714541619,4.73495705804709,25.0538437115237));
#47821=CARTESIAN_POINT('Ctrl Pts',(-5.01592318095989,3.64220986382467,25.1397707436143));
#47822=CARTESIAN_POINT('Ctrl Pts',(-5.91510841625453,1.81551650414691,25.2256977757049));
#47823=CARTESIAN_POINT('Ctrl Pts',(-5.9251298904235,-0.0026123641298589,
25.3116248077955));
#47824=CARTESIAN_POINT('Origin',(0.,0.,-10.));
#47825=CARTESIAN_POINT('',(-5.92348042272801,0.00375680996992422,27.3133751922049));
#47826=CARTESIAN_POINT('',(-5.91803924330658,0.00537434068105684,27.0616248077955));
#47827=CARTESIAN_POINT('',(-5.91675,-7.2459289488551E-16,-10.));
#47828=CARTESIAN_POINT('Ctrl Pts',(-5.92348042272801,0.00375680996992422,
27.3133751922049));
#47829=CARTESIAN_POINT('Ctrl Pts',(-5.92513185972389,0.227062797683139,
27.3028292133135));
#47830=CARTESIAN_POINT('Ctrl Pts',(-5.91360289431451,0.450196582758903,
27.2922832344221));
#47831=CARTESIAN_POINT('Ctrl Pts',(-5.88832590072296,0.671761942060206,
27.2817372555307));
#47832=CARTESIAN_POINT('Ctrl Pts',(-5.66592396373262,2.62122499430588,27.188947496954));
#47833=CARTESIAN_POINT('Ctrl Pts',(-4.37921554315603,4.44926803644757,27.0961577383772));
#47834=CARTESIAN_POINT('Ctrl Pts',(-2.61910723615281,5.3163825394207,27.0033679798005));
#47835=CARTESIAN_POINT('Ctrl Pts',(-0.858998929149595,6.18349704239383,
26.9105782212237));
#47836=CARTESIAN_POINT('Ctrl Pts',(1.3745092642802,6.08968300619837,26.817788462647));
#47837=CARTESIAN_POINT('Ctrl Pts',(3.05570343319762,5.07802348835348,26.7249987040702));
#47838=CARTESIAN_POINT('Ctrl Pts',(4.73689760211508,4.06636397050856,26.6322089454934));
#47839=CARTESIAN_POINT('Ctrl Pts',(5.86577774652006,2.13685897101416,26.5394191869167));
#47840=CARTESIAN_POINT('Ctrl Pts',(5.92391815778737,0.175612299576325,26.4466294283399));
#47841=CARTESIAN_POINT('Ctrl Pts',(5.98205856905467,-1.78563437186146,26.3538396697632));
#47842=CARTESIAN_POINT('Ctrl Pts',(4.96945924718425,-3.77862271524274,26.2610499111864));
#47843=CARTESIAN_POINT('Ctrl Pts',(3.35114522038306,-4.88809489799749,26.1682601526097));
#47844=CARTESIAN_POINT('Ctrl Pts',(1.73283119358188,-5.99756708075225,26.0754703940329));
#47845=CARTESIAN_POINT('Ctrl Pts',(-0.491197538150089,-6.22352310288061,
25.9826806354562));
#47846=CARTESIAN_POINT('Ctrl Pts',(-2.29958040171263,-5.46219516275138,
25.8898908768794));
#47847=CARTESIAN_POINT('Ctrl Pts',(-4.10796326527522,-4.70086722262212,
25.7971011183026));
#47848=CARTESIAN_POINT('Ctrl Pts',(-5.50070026066831,-2.95225532023523,
25.7043113597259));
#47849=CARTESIAN_POINT('Ctrl Pts',(-5.83819234157705,-1.01939011309528,
25.6115216011491));
#47850=CARTESIAN_POINT('Ctrl Pts',(-5.89656455848294,-0.685084114515375,
25.5954727981677));
#47851=CARTESIAN_POINT('Ctrl Pts',(-5.92336940038369,-0.345266226622166,
25.5794239951863));
#47852=CARTESIAN_POINT('Ctrl Pts',(-5.92031232679181,-0.00496695537298586,
25.5633751922049));
#47853=CARTESIAN_POINT('Ctrl Pts',(-5.9251298904235,-0.0026123641298589,
25.3116248077955));
#47854=CARTESIAN_POINT('Ctrl Pts',(-5.92593239635899,-0.148205635504764,
25.3185057269206));
#47855=CARTESIAN_POINT('Ctrl Pts',(-5.9210330621433,-0.293743986331754,
25.3253866460457));
#47856=CARTESIAN_POINT('Ctrl Pts',(-5.91025899730312,-0.438846129067858,
25.3322675651708));
#47857=CARTESIAN_POINT('Ctrl Pts',(-5.76494136372773,-2.39594406024946,
25.4250755163865));
#47858=CARTESIAN_POINT('Ctrl Pts',(-4.55090007595029,-4.2736875606178,25.5178834676022));
#47859=CARTESIAN_POINT('Ctrl Pts',(-2.82587028229322,-5.20943418116137,
25.6106914188179));
#47860=CARTESIAN_POINT('Ctrl Pts',(-1.1008404886361,-6.14518080170496,25.7034993700336));
#47861=CARTESIAN_POINT('Ctrl Pts',(1.13517781090063,-6.13893054242372,25.7963073212493));
#47862=CARTESIAN_POINT('Ctrl Pts',(2.85494937275541,-5.19355479601437,25.889115272465));
#47863=CARTESIAN_POINT('Ctrl Pts',(4.57472093461016,-4.24817904960505,25.9819232236808));
#47864=CARTESIAN_POINT('Ctrl Pts',(5.77824575878293,-2.36367781606772,26.0747311748965));
#47865=CARTESIAN_POINT('Ctrl Pts',(5.91262000001114,-0.405798072529415,
26.1675391261122));
#47866=CARTESIAN_POINT('Ctrl Pts',(6.04699424123935,1.55208167100884,26.2603470773279));
#47867=CARTESIAN_POINT('Ctrl Pts',(5.11221789952294,3.58333992454814,26.3531550285436));
#47868=CARTESIAN_POINT('Ctrl Pts',(3.53773075326523,4.75480898224122,26.4459629797593));
#47869=CARTESIAN_POINT('Ctrl Pts',(1.96324360700748,5.92627803993433,26.538770930975));
#47870=CARTESIAN_POINT('Ctrl Pts',(-0.250954343791611,6.2379579017813,26.6315788821908));
#47871=CARTESIAN_POINT('Ctrl Pts',(-2.0876522061113,5.54666166324565,26.7243868334065));
#47872=CARTESIAN_POINT('Ctrl Pts',(-3.92435006843105,4.85536542470998,26.8171947846222));
#47873=CARTESIAN_POINT('Ctrl Pts',(-5.38354784227131,3.16109308579165,26.9100027358379));
#47874=CARTESIAN_POINT('Ctrl Pts',(-5.79488456460875,1.24219975167425,27.0028106870536));
#47875=CARTESIAN_POINT('Ctrl Pts',(-5.88177513571553,0.836853648007722,
27.0224153939676));
#47876=CARTESIAN_POINT('Ctrl Pts',(-5.92190791045004,0.421484476168763,
27.0420201008815));
#47877=CARTESIAN_POINT('Ctrl Pts',(-5.91803924330658,0.00537434068105684,
27.0616248077955));
#47878=CARTESIAN_POINT('Origin',(0.,0.,-10.));
#47879=CARTESIAN_POINT('',(-5.90852622603088,0.0030797858564896,29.0633751922049));
#47880=CARTESIAN_POINT('',(-5.90694030856026,0.000110760884720807,28.8116248077955));
#47881=CARTESIAN_POINT('',(-5.91675,-7.2459289488551E-16,-10.));
#47882=CARTESIAN_POINT('Ctrl Pts',(-5.90852622603088,0.0030797858564896,
29.0633751922049));
#47883=CARTESIAN_POINT('Ctrl Pts',(-5.91224613300031,0.79461059927319,29.0262344314407));
#47884=CARTESIAN_POINT('Ctrl Pts',(-5.76444534826255,1.58480920067904,28.9890936706765));
#47885=CARTESIAN_POINT('Ctrl Pts',(-5.45857238322479,2.30816670910508,28.9519529099124));
#47886=CARTESIAN_POINT('Ctrl Pts',(-4.69440175243967,4.1153501698233,28.8591631513356));
#47887=CARTESIAN_POINT('Ctrl Pts',(-2.94360197161417,5.5053357995932,28.7663733927588));
#47888=CARTESIAN_POINT('Ctrl Pts',(-1.01020845720406,5.83978808630234,28.6735836341821));
#47889=CARTESIAN_POINT('Ctrl Pts',(0.923185057206098,6.17424037301148,28.5807938756053));
#47890=CARTESIAN_POINT('Ctrl Pts',(3.03917230520087,5.4531593166598,28.4880041170286));
#47891=CARTESIAN_POINT('Ctrl Pts',(4.36600956897235,4.00769340937742,28.3952143584518));
#47892=CARTESIAN_POINT('Ctrl Pts',(5.69284683274379,2.56222750209508,28.3024245998751));
#47893=CARTESIAN_POINT('Ctrl Pts',(6.23053411229197,0.392376743882084,28.2096348412983));
#47894=CARTESIAN_POINT('Ctrl Pts',(5.73214447715392,-1.50537892670225,28.1168450827216));
#47895=CARTESIAN_POINT('Ctrl Pts',(5.23375484201585,-3.40313459728663,28.0240553241448));
#47896=CARTESIAN_POINT('Ctrl Pts',(3.69928829219149,-5.02879518024234,27.931265565568));
#47897=CARTESIAN_POINT('Ctrl Pts',(1.83343160279787,-5.63579405033464,27.8384758069913));
#47898=CARTESIAN_POINT('Ctrl Pts',(-0.0324250865956979,-6.24279292042693,
27.7456860484145));
#47899=CARTESIAN_POINT('Ctrl Pts',(-2.2296719155585,-5.83113007765588,27.6528962898378));
#47900=CARTESIAN_POINT('Ctrl Pts',(-3.74924760333789,-4.58985712509556,
27.560106531261));
#47901=CARTESIAN_POINT('Ctrl Pts',(-5.09611658972049,-3.48966049989016,
27.4778627515756));
#47902=CARTESIAN_POINT('Ctrl Pts',(-5.91060154046853,-1.73771533263892,
27.3956189718903));
#47903=CARTESIAN_POINT('Ctrl Pts',(-5.92348042272801,0.00375680996992422,
27.3133751922049));
#47904=CARTESIAN_POINT('Ctrl Pts',(-5.91803924330658,0.00537434068105684,
27.0616248077955));
#47905=CARTESIAN_POINT('Ctrl Pts',(-5.90359378450591,-1.54836538305896,
27.1348280520972));
#47906=CARTESIAN_POINT('Ctrl Pts',(-5.2756592157719,-3.11243597574232,27.208031296399));
#47907=CARTESIAN_POINT('Ctrl Pts',(-4.17773325561082,-4.20360466566063,
27.2812345407007));
#47908=CARTESIAN_POINT('Ctrl Pts',(-2.7857695534408,-5.58700141956182,27.3740424919164));
#47909=CARTESIAN_POINT('Ctrl Pts',(-0.638366478266117,-6.21028059804786,
27.4668504431321));
#47910=CARTESIAN_POINT('Ctrl Pts',(1.27795089477905,-5.78710539481819,27.5596583943478));
#47911=CARTESIAN_POINT('Ctrl Pts',(3.19426826782428,-5.3639301915885,27.6524663455635));
#47912=CARTESIAN_POINT('Ctrl Pts',(4.87949993873997,-3.89430060664304,27.7452742967793));
#47913=CARTESIAN_POINT('Ctrl Pts',(5.5594441193344,-2.05337001638734,27.838082247995));
#47914=CARTESIAN_POINT('Ctrl Pts',(6.2393882999288,-0.212439426131689,27.9308901992107));
#47915=CARTESIAN_POINT('Ctrl Pts',(5.91404499020199,1.99979216943419,28.0236981504264));
#47916=CARTESIAN_POINT('Ctrl Pts',(4.73287813420022,3.56701722830292,28.1165061016421));
#47917=CARTESIAN_POINT('Ctrl Pts',(3.55171127819844,5.13424228717165,28.2093140528578));
#47918=CARTESIAN_POINT('Ctrl Pts',(1.51472087592169,6.05646080934324,28.3021220040735));
#47919=CARTESIAN_POINT('Ctrl Pts',(-0.44229199602487,5.91000212609545,28.3949299552892));
#47920=CARTESIAN_POINT('Ctrl Pts',(-2.39930486797143,5.76354344284765,28.4877379065049));
#47921=CARTESIAN_POINT('Ctrl Pts',(-4.27634020958782,4.54840755418047,28.5805458577206));
#47922=CARTESIAN_POINT('Ctrl Pts',(-5.2110809026651,2.82283247219515,28.6733538089364));
#47923=CARTESIAN_POINT('Ctrl Pts',(-5.67529231132518,1.96587647842105,28.7194441418894));
#47924=CARTESIAN_POINT('Ctrl Pts',(-5.90710376233207,0.983029875912657,
28.7655344748425));
#47925=CARTESIAN_POINT('Ctrl Pts',(-5.90694030856026,0.000110760884720807,
28.8116248077955));
#47926=CARTESIAN_POINT('Origin',(0.,0.,-10.));
#47927=CARTESIAN_POINT('',(-5.9121820127379,-0.00493613606119603,30.8133751922049));
#47928=CARTESIAN_POINT('',(-5.91763133808765,-0.00541284032780908,30.5616248077955));
#47929=CARTESIAN_POINT('',(-5.91675,-7.2459289488551E-16,-10.));
#47930=CARTESIAN_POINT('Ctrl Pts',(-5.9121820127379,-0.00493613606119603,
30.8133751922049));
#47931=CARTESIAN_POINT('Ctrl Pts',(-5.90153888682002,1.35126409100681,30.7496396495679));
#47932=CARTESIAN_POINT('Ctrl Pts',(-5.43820318556864,2.71403437919626,30.6859041069309));
#47933=CARTESIAN_POINT('Ctrl Pts',(-4.58395586259118,3.75646039107845,30.622168564294));
#47934=CARTESIAN_POINT('Ctrl Pts',(-3.34029495402418,5.27408233285128,30.5293788057172));
#47935=CARTESIAN_POINT('Ctrl Pts',(-1.26809058042409,6.11272943237414,30.4365890471405));
#47936=CARTESIAN_POINT('Ctrl Pts',(0.681020340752165,5.88726229374972,30.3437992885637));
#47937=CARTESIAN_POINT('Ctrl Pts',(2.63013126192847,5.66179515512528,30.2510095299869));
#47938=CARTESIAN_POINT('Ctrl Pts',(4.45614873068094,4.3722137783535,30.1582197714102));
#47939=CARTESIAN_POINT('Ctrl Pts',(5.32049444009904,2.61074413392055,30.0654300128334));
#47940=CARTESIAN_POINT('Ctrl Pts',(6.18484014951711,0.849274489487636,29.9726402542567));
#47941=CARTESIAN_POINT('Ctrl Pts',(6.08751409960087,-1.38408342260643,29.8798504956799));
#47942=CARTESIAN_POINT('Ctrl Pts',(5.07321220128966,-3.0636847064623,29.7870607371032));
#47943=CARTESIAN_POINT('Ctrl Pts',(4.05891030297843,-4.74328599031823,29.6942709785264));
#47944=CARTESIAN_POINT('Ctrl Pts',(2.12763255627217,-5.86913064593594,29.6014812199496));
#47945=CARTESIAN_POINT('Ctrl Pts',(0.166296885408143,-5.92418697931023,
29.5086914613729));
#47946=CARTESIAN_POINT('Ctrl Pts',(-1.79503878545582,-5.97924331268453,
29.4159017027961));
#47947=CARTESIAN_POINT('Ctrl Pts',(-3.78643238047755,-4.96351132381548,
29.3231119442194));
#47948=CARTESIAN_POINT('Ctrl Pts',(-4.89335843761608,-3.34345468354768,
29.2303221856426));
#47949=CARTESIAN_POINT('Ctrl Pts',(-5.55721753884891,-2.37185469435356,
29.1746731878301));
#47950=CARTESIAN_POINT('Ctrl Pts',(-5.90295258966627,-1.18289205742564,
29.1190241900175));
#47951=CARTESIAN_POINT('Ctrl Pts',(-5.90852622603088,0.0030797858564896,
29.0633751922049));
#47952=CARTESIAN_POINT('Ctrl Pts',(-5.90694030856026,0.000110760884720807,
28.8116248077955));
#47953=CARTESIAN_POINT('Ctrl Pts',(-5.90677463019724,-0.996185795395627,
28.8583424260582));
#47954=CARTESIAN_POINT('Ctrl Pts',(-5.66827676300471,-1.99255685140481,
28.9050600443208));
#47955=CARTESIAN_POINT('Ctrl Pts',(-5.19188935192074,-2.8579769589016,28.9517776625835));
#47956=CARTESIAN_POINT('Ctrl Pts',(-4.24551106356089,-4.57719703270963,
29.0445856137992));
#47957=CARTESIAN_POINT('Ctrl Pts',(-2.36030844230297,-5.77962290502219,
29.1373935650149));
#47958=CARTESIAN_POINT('Ctrl Pts',(-0.402350685439387,-5.91285559320764,
29.2302015162306));
#47959=CARTESIAN_POINT('Ctrl Pts',(1.55560707142414,-6.04608828139308,29.3230094674463));
#47960=CARTESIAN_POINT('Ctrl Pts',(3.58631996389338,-5.11012778545148,29.415817418662));
#47961=CARTESIAN_POINT('Ctrl Pts',(4.75687082705447,-3.53495788870511,29.5086253698777));
#47962=CARTESIAN_POINT('Ctrl Pts',(5.92742169021559,-1.95978799195868,29.6014333210935));
#47963=CARTESIAN_POINT('Ctrl Pts',(6.23781052406856,0.254591305592438,29.6942412723092));
#47964=CARTESIAN_POINT('Ctrl Pts',(5.54544352720855,2.09088579954553,29.7870492235249));
#47965=CARTESIAN_POINT('Ctrl Pts',(4.85307653034854,3.92718029349861,29.8798571747406));
#47966=CARTESIAN_POINT('Ctrl Pts',(3.15795370277548,5.38538998385357,29.9726651259563));
#47967=CARTESIAN_POINT('Ctrl Pts',(1.23882086737003,5.79560783686828,30.065473077172));
#47968=CARTESIAN_POINT('Ctrl Pts',(-0.68031196803538,6.20582568988297,30.1582810283877));
#47969=CARTESIAN_POINT('Ctrl Pts',(-2.82345481127323,5.56805170555748,30.2510889796034));
#47970=CARTESIAN_POINT('Ctrl Pts',(-4.20603975383542,4.1752816586856,30.3438969308191));
#47971=CARTESIAN_POINT('Ctrl Pts',(-5.2872232815409,3.08613336392054,30.4164728898112));
#47972=CARTESIAN_POINT('Ctrl Pts',(-5.90330559059264,1.53528506123078,30.4890488488034));
#47973=CARTESIAN_POINT('Ctrl Pts',(-5.91763133808765,-0.00541284032780908,
30.5616248077955));
#47974=CARTESIAN_POINT('Origin',(0.,0.,-10.));
#47975=CARTESIAN_POINT('',(-5.9263255902637,-0.000973344357376172,32.5633751922049));
#47976=CARTESIAN_POINT('',(-5.92535850276232,0.00239395280352964,32.3116248077955));
#47977=CARTESIAN_POINT('',(-5.91675,-7.2459289488551E-16,-10.));
#47978=CARTESIAN_POINT('Ctrl Pts',(-5.9263255902637,-0.000973344357376172,
32.5633751922049));
#47979=CARTESIAN_POINT('Ctrl Pts',(-5.92197889376489,1.90929747733607,32.4730448676951));
#47980=CARTESIAN_POINT('Ctrl Pts',(-4.9145647186513,3.82350469477119,32.3827145431853));
#47981=CARTESIAN_POINT('Ctrl Pts',(-3.33575587944999,4.89860987757141,32.2923842186756));
#47982=CARTESIAN_POINT('Ctrl Pts',(-1.7139606315819,6.00298707203011,32.1995944600988));
#47983=CARTESIAN_POINT('Ctrl Pts',(0.510767719857083,6.22194753834564,32.1068047015221));
#47984=CARTESIAN_POINT('Ctrl Pts',(2.31674730916162,5.45493610644687,32.0140149429453));
#47985=CARTESIAN_POINT('Ctrl Pts',(4.12272689846615,4.6879246745481,31.9212251843686));
#47986=CARTESIAN_POINT('Ctrl Pts',(5.50995772563631,2.93494134443502,31.8284354257918));
#47987=CARTESIAN_POINT('Ctrl Pts',(5.84136939115547,1.00102430339996,31.735645667215));
#47988=CARTESIAN_POINT('Ctrl Pts',(6.17278105667463,-0.932892737635148,
31.6428559086383));
#47989=CARTESIAN_POINT('Ctrl Pts',(5.44837356054283,-3.04774348959217,31.5500661500615));
#47990=CARTESIAN_POINT('Ctrl Pts',(4.00082302553252,-4.37230615788672,31.4572763914848));
#47991=CARTESIAN_POINT('Ctrl Pts',(2.55327249052222,-5.69686882618127,31.364486632908));
#47992=CARTESIAN_POINT('Ctrl Pts',(0.382578916633404,-6.23114341081323,
31.2716968743313));
#47993=CARTESIAN_POINT('Ctrl Pts',(-1.5143907038061,-5.72977022367835,31.1789071157545));
#47994=CARTESIAN_POINT('Ctrl Pts',(-3.41136032424556,-5.22839703654348,
31.0861173571777));
#47995=CARTESIAN_POINT('Ctrl Pts',(-5.03460599123578,-3.6913760776418,30.993327598601));
#47996=CARTESIAN_POINT('Ctrl Pts',(-5.63867010296394,-1.82456720617958,
30.9005378400242));
#47997=CARTESIAN_POINT('Ctrl Pts',(-5.82781392026467,-1.24003429110695,
30.8714836240845));
#47998=CARTESIAN_POINT('Ctrl Pts',(-5.91703374327784,-0.623167857712015,
30.8424294081447));
#47999=CARTESIAN_POINT('Ctrl Pts',(-5.9121820127379,-0.00493613606119603,
30.8133751922049));
#48000=CARTESIAN_POINT('Ctrl Pts',(-5.91763133808765,-0.00541284032780908,
30.5616248077955));
#48001=CARTESIAN_POINT('Ctrl Pts',(-5.92162492516443,-0.434913027388583,
30.5818568000191));
#48002=CARTESIAN_POINT('Ctrl Pts',(-5.87885441369386,-0.863624399853681,
30.6020887922427));
#48003=CARTESIAN_POINT('Ctrl Pts',(-5.78635930947281,-1.2813248151338,30.6223207844663));
#48004=CARTESIAN_POINT('Ctrl Pts',(-5.36206688066144,-3.19739513266305,
30.715128735682));
#48005=CARTESIAN_POINT('Ctrl Pts',(-3.89145498115216,-4.88176965830319,
30.8079366868977));
#48006=CARTESIAN_POINT('Ctrl Pts',(-2.05012826636742,-5.5606403796363,30.9007446381134));
#48007=CARTESIAN_POINT('Ctrl Pts',(-0.20880155158272,-6.23951110096938,
30.9935525893291));
#48008=CARTESIAN_POINT('Ctrl Pts',(2.00323997847749,-5.91287801799537,31.0863605405448));
#48009=CARTESIAN_POINT('Ctrl Pts',(3.56977609861613,-4.73079760145679,31.1791684917605));
#48010=CARTESIAN_POINT('Ctrl Pts',(5.13631221875486,-3.54871718491814,31.2719764429762));
#48011=CARTESIAN_POINT('Ctrl Pts',(6.05734292897206,-1.51118943481486,31.3647843941919));
#48012=CARTESIAN_POINT('Ctrl Pts',(5.90974324583908,0.445737712628944,31.4575923454076));
#48013=CARTESIAN_POINT('Ctrl Pts',(5.76214356270612,2.40266486007264,31.5504002966233));
#48014=CARTESIAN_POINT('Ctrl Pts',(4.54591348622311,4.27899140485678,31.6432082478391));
#48015=CARTESIAN_POINT('Ctrl Pts',(2.81979370250234,5.21272585271166,31.7360161990548));
#48016=CARTESIAN_POINT('Ctrl Pts',(1.09367391878148,6.14646030056659,31.8288241502705));
#48017=CARTESIAN_POINT('Ctrl Pts',(-1.14233557217731,6.13760265149206,31.9216321014862));
#48018=CARTESIAN_POINT('Ctrl Pts',(-2.86100357350615,5.19022214289383,32.0144400527019));
#48019=CARTESIAN_POINT('Ctrl Pts',(-4.57967157483495,4.24284163429563,32.1072480039176));
#48020=CARTESIAN_POINT('Ctrl Pts',(-5.78099808653392,2.35693826617388,32.2000559551333));
#48021=CARTESIAN_POINT('Ctrl Pts',(-5.91308917638543,0.398903161574089,
32.292863906349));
#48022=CARTESIAN_POINT('Ctrl Pts',(-5.92198980715467,0.266965818042131,
32.2991175401645));
#48023=CARTESIAN_POINT('Ctrl Pts',(-5.92603567684633,0.134700967265697,
32.30537117398));
#48024=CARTESIAN_POINT('Ctrl Pts',(-5.92535850276232,0.00239395280352964,
32.3116248077955));
#48025=CARTESIAN_POINT('Origin',(0.,0.,-10.));
#48026=CARTESIAN_POINT('',(-5.91511646839551,0.00542726113904934,34.3133751922049));
#48027=CARTESIAN_POINT('',(-5.91029258610688,0.00423669449690529,34.0616248077955));
#48028=CARTESIAN_POINT('',(-5.91675,-7.2459289488551E-16,-10.));
#48029=CARTESIAN_POINT('Ctrl Pts',(-5.91511646839551,0.00542726113904934,
34.3133751922049));
#48030=CARTESIAN_POINT('Ctrl Pts',(-5.91971679252729,0.518347327012361,
34.2892398443991));
#48031=CARTESIAN_POINT('Ctrl Pts',(-5.85856864434903,1.03018765930209,34.2651044965933));
#48032=CARTESIAN_POINT('Ctrl Pts',(-5.72738180236852,1.52339873632063,34.2409691487875));
#48033=CARTESIAN_POINT('Ctrl Pts',(-5.22302630296755,3.41957761603427,34.1481793902107));
#48034=CARTESIAN_POINT('Ctrl Pts',(-3.68345473553503,5.04040435330718,34.055389631634));
#48035=CARTESIAN_POINT('Ctrl Pts',(-1.81569829800748,5.64153221301962,33.9625998730572));
#48036=CARTESIAN_POINT('Ctrl Pts',(0.0520581395200725,6.24266007273206,
33.8698101144804));
#48037=CARTESIAN_POINT('Ctrl Pts',(2.24799944714261,5.82408905488403,33.7770203559037));
#48038=CARTESIAN_POINT('Ctrl Pts',(3.7636638903298,4.57804326547412,33.6842305973269));
#48039=CARTESIAN_POINT('Ctrl Pts',(5.27932833351703,3.33199747606418,33.5914408387502));
#48040=CARTESIAN_POINT('Ctrl Pts',(6.11471591226884,1.25847691509218,33.4986510801734));
#48041=CARTESIAN_POINT('Ctrl Pts',(5.88618412951617,-0.690277055505497,
33.4058613215966));
#48042=CARTESIAN_POINT('Ctrl Pts',(5.6576523467635,-2.63903102610312,33.3130715630199));
#48043=CARTESIAN_POINT('Ctrl Pts',(4.36520120250652,-4.46301840632649,33.2202818044431));
#48044=CARTESIAN_POINT('Ctrl Pts',(2.60237457617807,-5.32459318494731,33.1274920458664));
#48045=CARTESIAN_POINT('Ctrl Pts',(0.83954794984961,-6.18616796356814,33.0347022872896));
#48046=CARTESIAN_POINT('Ctrl Pts',(-1.39365415855027,-6.08533014058638,
32.9419125287129));
#48047=CARTESIAN_POINT('Ctrl Pts',(-3.07165840424395,-5.06838836984331,
32.8491227701361));
#48048=CARTESIAN_POINT('Ctrl Pts',(-4.74966264993768,-4.05144659910021,
32.7563330115594));
#48049=CARTESIAN_POINT('Ctrl Pts',(-5.87246903292514,-2.11840088059577,
32.6635432529826));
#48050=CARTESIAN_POINT('Ctrl Pts',(-5.92444115227025,-0.156981060042544,
32.5707534944058));
#48051=CARTESIAN_POINT('Ctrl Pts',(-5.92581869654681,-0.104992750122198,
32.5682940603389));
#48052=CARTESIAN_POINT('Ctrl Pts',(-5.92644393826595,-0.0529845062958709,
32.5658346262719));
#48053=CARTESIAN_POINT('Ctrl Pts',(-5.9263255902637,-0.000973344357376172,
32.5633751922049));
#48054=CARTESIAN_POINT('Ctrl Pts',(-5.92535850276232,0.00239395280352964,
32.3116248077955));
#48055=CARTESIAN_POINT('Ctrl Pts',(-5.91598597755038,-1.82882029189141,
32.3981791251957));
#48056=CARTESIAN_POINT('Ctrl Pts',(-5.00185104463509,-3.66811155632826,
32.484733442596));
#48057=CARTESIAN_POINT('Ctrl Pts',(-3.53218382246986,-4.75893105481499,
32.5712877599962));
#48058=CARTESIAN_POINT('Ctrl Pts',(-1.95633171069875,-5.92856332552653,
32.6640957112119));
#48059=CARTESIAN_POINT('Ctrl Pts',(0.258228180847425,-6.23766102587179,
32.7569036624276));
#48060=CARTESIAN_POINT('Ctrl Pts',(2.09411868220313,-5.54422350605098,32.8497116136433));
#48061=CARTESIAN_POINT('Ctrl Pts',(3.93000918355878,-4.85078598623018,32.942519564859));
#48062=CARTESIAN_POINT('Ctrl Pts',(5.38723029472394,-3.15481324624327,33.0353275160747));
#48063=CARTESIAN_POINT('Ctrl Pts',(5.79632913896631,-1.23544156194066,33.1281354672904));
#48064=CARTESIAN_POINT('Ctrl Pts',(6.20542798320869,0.68393012236201,33.2209434185061));
#48065=CARTESIAN_POINT('Ctrl Pts',(5.56640456052833,2.82670075098039,33.3137513697218));
#48066=CARTESIAN_POINT('Ctrl Pts',(4.17282864241345,4.20847341220712,33.4065593209376));
#48067=CARTESIAN_POINT('Ctrl Pts',(2.77925272429858,5.59024607343385,33.4993672721533));
#48068=CARTESIAN_POINT('Ctrl Pts',(0.631124310749118,6.21102076726887,33.592175223369));
#48069=CARTESIAN_POINT('Ctrl Pts',(-1.28469829991443,5.78561125710995,33.6849831745847));
#48070=CARTESIAN_POINT('Ctrl Pts',(-3.20052091057798,5.36020174695103,33.7777911258004));
#48071=CARTESIAN_POINT('Ctrl Pts',(-4.88403771835562,3.88860803279828,33.8705990770161));
#48072=CARTESIAN_POINT('Ctrl Pts',(-5.56183474965175,2.04688581942584,33.9634070282318));
#48073=CARTESIAN_POINT('Ctrl Pts',(-5.80093681844618,1.39719340262678,33.9961462880864));
#48074=CARTESIAN_POINT('Ctrl Pts',(-5.91488500290352,0.701441416885687,
34.0288855479409));
#48075=CARTESIAN_POINT('Ctrl Pts',(-5.91029258610688,0.00423669449690529,
34.0616248077955));
#48076=CARTESIAN_POINT('Origin',(0.,0.,-10.));
#48077=CARTESIAN_POINT('',(-5.90729969700522,-0.00151050143465004,36.0633751922049));
#48078=CARTESIAN_POINT('',(-5.90990876146918,-0.00403960103504912,35.8116248077955));
#48079=CARTESIAN_POINT('',(-5.91675,-7.2459289488551E-16,-10.));
#48080=CARTESIAN_POINT('Ctrl Pts',(-5.90729969700522,-0.00151050143465004,
36.0633751922049));
#48081=CARTESIAN_POINT('Ctrl Pts',(-5.90483716507214,1.08019297671428,36.0126450625263));
#48082=CARTESIAN_POINT('Ctrl Pts',(-5.62097754735415,2.16309938757096,35.9619149328477));
#48083=CARTESIAN_POINT('Ctrl Pts',(-5.06355200594223,3.07962450682608,35.9111848031691));
#48084=CARTESIAN_POINT('Ctrl Pts',(-4.04397287732933,4.7560275652059,35.8183950445923));
#48085=CARTESIAN_POINT('Ctrl Pts',(-2.109163966812,5.87579289923287,35.7256052860156));
#48086=CARTESIAN_POINT('Ctrl Pts',(-0.147664846514664,5.92468067603893,
35.6328155274388));
#48087=CARTESIAN_POINT('Ctrl Pts',(1.81383427378267,5.97356845284499,35.5400257688621));
#48088=CARTESIAN_POINT('Ctrl Pts',(3.80202360386,4.95157867243014,35.4472360102853));
#48089=CARTESIAN_POINT('Ctrl Pts',(4.90384920487803,3.32804882712716,35.3544462517086));
#48090=CARTESIAN_POINT('Ctrl Pts',(6.00567480589603,1.70451898182423,35.2616564931318));
#48091=CARTESIAN_POINT('Ctrl Pts',(6.22113667785476,-0.520550928366797,
35.168866734555));
#48092=CARTESIAN_POINT('Ctrl Pts',(5.45128634140899,-2.32532218066509,35.0760769759783));
#48093=CARTESIAN_POINT('Ctrl Pts',(4.68143600496318,-4.13009343296349,34.9832872174015));
#48094=CARTESIAN_POINT('Ctrl Pts',(2.92627346011274,-5.51456602736912,34.8904974588247));
#48095=CARTESIAN_POINT('Ctrl Pts',(0.991837674392355,-5.84293625222638,
34.797707700248));
#48096=CARTESIAN_POINT('Ctrl Pts',(-0.942598111327868,-6.17130647708362,
34.7049179416712));
#48097=CARTESIAN_POINT('Ctrl Pts',(-3.05630713791801,-5.4435743323927,34.6121281830945));
#48098=CARTESIAN_POINT('Ctrl Pts',(-4.37859193552841,-3.99394274897012,
34.5193384245177));
#48099=CARTESIAN_POINT('Ctrl Pts',(-5.35694003173801,-2.92137177000263,
34.4506840137468));
#48100=CARTESIAN_POINT('Ctrl Pts',(-5.9020305768988,-1.45360391497842,34.3820296029759));
#48101=CARTESIAN_POINT('Ctrl Pts',(-5.91511646839551,0.00542726113904934,
34.3133751922049));
#48102=CARTESIAN_POINT('Ctrl Pts',(-5.91029258610688,0.00423669449690529,
34.0616248077955));
#48103=CARTESIAN_POINT('Ctrl Pts',(-5.90186660249012,-1.27496678996694,
34.1216934991566));
#48104=CARTESIAN_POINT('Ctrl Pts',(-5.49439205420357,-2.55906068723431,
34.1817621905178));
#48105=CARTESIAN_POINT('Ctrl Pts',(-4.72871546052388,-3.57253375541824,
34.2418308818789));
#48106=CARTESIAN_POINT('Ctrl Pts',(-3.54572188528532,-5.13838040429787,
34.3346388330947));
#48107=CARTESIAN_POINT('Ctrl Pts',(-1.5076574799935,-6.05822298946509,34.4274467843104));
#48108=CARTESIAN_POINT('Ctrl Pts',(0.449183277708752,-5.90948235662204,
34.5202547355261));
#48109=CARTESIAN_POINT('Ctrl Pts',(2.406024035411,-5.760741723779,34.6130626867418));
#48110=CARTESIAN_POINT('Ctrl Pts',(4.28164114552377,-4.54341787292579,34.7058706379575));
#48111=CARTESIAN_POINT('Ctrl Pts',(5.21436903074208,-2.81675397424735,34.7986785891732));
#48112=CARTESIAN_POINT('Ctrl Pts',(6.1470969159604,-1.0900900755689,34.8914865403889));
#48113=CARTESIAN_POINT('Ctrl Pts',(6.13693557628423,1.14591387093472,34.9842944916046));
#48114=CARTESIAN_POINT('Ctrl Pts',(5.18855316950071,2.86402921553961,35.0771024428203));
#48115=CARTESIAN_POINT('Ctrl Pts',(4.2401707627172,4.58214456014451,35.1699103940361));
#48116=CARTESIAN_POINT('Ctrl Pts',(2.35356728882637,5.7823713028506,35.2627183452517));
#48117=CARTESIAN_POINT('Ctrl Pts',(0.395455502105646,5.91332074946512,35.3555262964675));
#48118=CARTESIAN_POINT('Ctrl Pts',(-1.56265628461502,6.04427019607964,35.4483342476832));
#48119=CARTESIAN_POINT('Ctrl Pts',(-3.59227638416566,5.10594234660255,35.5411421988989));
#48120=CARTESIAN_POINT('Ctrl Pts',(-4.76098966482233,3.52940855550265,35.6339501501146));
#48121=CARTESIAN_POINT('Ctrl Pts',(-5.5067976455242,2.52335214910344,35.6931750360082));
#48122=CARTESIAN_POINT('Ctrl Pts',(-5.90201989047548,1.25740013647395,35.7523999219019));
#48123=CARTESIAN_POINT('Ctrl Pts',(-5.90990876146918,-0.00403960103504912,
35.8116248077955));
#48124=CARTESIAN_POINT('Origin',(0.,0.,-10.));
#48125=CARTESIAN_POINT('',(-5.92067510213246,-0.00487139356358524,37.8133751922049));
#48126=CARTESIAN_POINT('',(-5.92504705000468,-0.0026864220054185,37.5616248077955));
#48127=CARTESIAN_POINT('',(-5.91675,-7.2459289488551E-16,-10.));
#48128=CARTESIAN_POINT('Ctrl Pts',(-5.92067510213246,-0.00487139356358524,
37.8133751922049));
#48129=CARTESIAN_POINT('Ctrl Pts',(-5.90611554008262,1.63446818848114,37.7360502806535));
#48130=CARTESIAN_POINT('Ctrl Pts',(-5.19681189997422,3.28486223478748,37.6587253691021));
#48131=CARTESIAN_POINT('Ctrl Pts',(-3.98705259670286,4.38486688635475,37.5814004575507));
#48132=CARTESIAN_POINT('Ctrl Pts',(-2.53534354932926,5.70487054370628,37.4886106989739));
#48133=CARTESIAN_POINT('Ctrl Pts',(-0.362980448390255,6.23231578369225,
37.3958209403972));
#48134=CARTESIAN_POINT('Ctrl Pts',(1.53240300197176,5.72497921913026,37.3030311818204));
#48135=CARTESIAN_POINT('Ctrl Pts',(3.42778645233388,5.21764265456824,37.2102414232437));
#48136=CARTESIAN_POINT('Ctrl Pts',(5.04619025211903,3.67552428545812,37.1174516646669));
#48137=CARTESIAN_POINT('Ctrl Pts',(5.64438037342458,1.80682490021162,37.0246619060902));
#48138=CARTESIAN_POINT('Ctrl Pts',(6.24257049473012,-0.0618744850348207,
36.9318721475134));
#48139=CARTESIAN_POINT('Ctrl Pts',(5.82054693755619,-2.25715488641753,36.8390823889367));
#48140=CARTESIAN_POINT('Ctrl Pts',(4.57211934836416,-3.77085808328017,36.7462926303599));
#48141=CARTESIAN_POINT('Ctrl Pts',(3.32369175917207,-5.2845612801429,36.6535028717831));
#48142=CARTESIAN_POINT('Ctrl Pts',(1.24886013796173,-6.11668727248533,36.5607131132064));
#48143=CARTESIAN_POINT('Ctrl Pts',(-0.699532063430729,-5.88509141068834,
36.4679233546296));
#48144=CARTESIAN_POINT('Ctrl Pts',(-2.64792426482302,-5.65349554889138,
36.3751335960529));
#48145=CARTESIAN_POINT('Ctrl Pts',(-4.4698770463975,-4.35817783295517,36.2823438374761));
#48146=CARTESIAN_POINT('Ctrl Pts',(-5.32867876383053,-2.59399858362084,
36.1895540788994));
#48147=CARTESIAN_POINT('Ctrl Pts',(-5.71795536166166,-1.79433355943125,
36.1474944500012));
#48148=CARTESIAN_POINT('Ctrl Pts',(-5.90934134720228,-0.898335468313729,
36.105434821103));
#48149=CARTESIAN_POINT('Ctrl Pts',(-5.90729969700522,-0.00151050143465004,
36.0633751922049));
#48150=CARTESIAN_POINT('Ctrl Pts',(-5.90990876146918,-0.00403960103504912,
35.8116248077955));
#48151=CARTESIAN_POINT('Ctrl Pts',(-5.91438209165634,-0.719330351965569,
35.8452078731176));
#48152=CARTESIAN_POINT('Ctrl Pts',(-5.79431305298316,-1.43317023532246,
35.8787909384397));
#48153=CARTESIAN_POINT('Ctrl Pts',(-5.54300160018766,-2.09735085298511,
35.9123740037618));
#48154=CARTESIAN_POINT('Ctrl Pts',(-4.8484937931335,-3.93283673765,36.0051819549775));
#48155=CARTESIAN_POINT('Ctrl Pts',(-3.15167171726243,-5.38906877425699,
36.0979899061931));
#48156=CARTESIAN_POINT('Ctrl Pts',(-1.23206183653459,-5.79704847065775,
36.1907978574088));
#48157=CARTESIAN_POINT('Ctrl Pts',(0.687548044193256,-6.20502816705852,
36.2836058086245));
#48158=CARTESIAN_POINT('Ctrl Pts',(2.82994572977787,-5.56475552325307,36.3764137598403));
#48159=CARTESIAN_POINT('Ctrl Pts',(4.21090563994866,-4.170374207628,36.469221711056));
#48160=CARTESIAN_POINT('Ctrl Pts',(5.59186555011949,-2.7759928920029,36.5620296622717));
#48161=CARTESIAN_POINT('Ctrl Pts',(6.21138768487646,-0.627502904558124,
36.6548376134874));
#48162=CARTESIAN_POINT('Ctrl Pts',(5.78486123798388,1.28807134797416,36.7476455647031));
#48163=CARTESIAN_POINT('Ctrl Pts',(5.35833479109132,3.2036456005064,36.8404535159188));
#48164=CARTESIAN_POINT('Ctrl Pts',(3.88575976254927,4.88630411812616,36.9332614671345));
#48165=CARTESIAN_POINT('Ctrl Pts',(2.04364267666501,5.56302722897469,37.0260694183503));
#48166=CARTESIAN_POINT('Ctrl Pts',(0.201525590780754,6.23975033982323,37.118877369566));
#48167=CARTESIAN_POINT('Ctrl Pts',(-2.01013355244571,5.91053804390054,37.2116853207817));
#48168=CARTESIAN_POINT('Ctrl Pts',(-3.57529019777168,4.72663171210939,37.3044932719974));
#48169=CARTESIAN_POINT('Ctrl Pts',(-5.02075231139987,3.63326399469971,37.3902037839301));
#48170=CARTESIAN_POINT('Ctrl Pts',(-5.91481283469339,1.81092824985332,37.4759142958628));
#48171=CARTESIAN_POINT('Ctrl Pts',(-5.92504705000468,-0.0026864220054185,
37.5616248077955));
#48172=CARTESIAN_POINT('Origin',(0.,0.,-10.));
#48173=CARTESIAN_POINT('',(-5.92317748384162,0.00391648730000096,39.5633751922049));
#48174=CARTESIAN_POINT('',(-5.91817991048888,0.00535877289898346,39.3116248077955));
#48175=CARTESIAN_POINT('',(-5.91675,-7.2459289488551E-16,-10.));
#48176=CARTESIAN_POINT('Ctrl Pts',(-5.92317748384162,0.00391648730000096,
39.5633751922049));
#48177=CARTESIAN_POINT('Ctrl Pts',(-5.92497651525942,0.239619045790868,
39.5522452573574));
#48178=CARTESIAN_POINT('Ctrl Pts',(-5.91213103375526,0.475123798574987,
39.54111532251));
#48179=CARTESIAN_POINT('Ctrl Pts',(-5.88398413996813,0.708785341643609,
39.5299853876626));
#48180=CARTESIAN_POINT('Ctrl Pts',(-5.64932477178711,2.65681095609875,39.4371956290858));
#48181=CARTESIAN_POINT('Ctrl Pts',(-4.35114368706545,4.47672463393544,39.3444058705091));
#48182=CARTESIAN_POINT('Ctrl Pts',(-2.58561617695903,5.33275116664683,39.2516161119323));
#48183=CARTESIAN_POINT('Ctrl Pts',(-0.820088666852756,6.18877769935815,
39.1588263533556));
#48184=CARTESIAN_POINT('Ctrl Pts',(1.41278526863818,6.08091708694438,39.0660365947788));
#48185=CARTESIAN_POINT('Ctrl Pts',(3.08758299451145,5.05870312154499,38.973246836202));
#48186=CARTESIAN_POINT('Ctrl Pts',(4.76238072038482,4.03648915614554,38.8804570776253));
#48187=CARTESIAN_POINT('Ctrl Pts',(5.87910223664044,2.09992183776038,38.7876673190485));
#48188=CARTESIAN_POINT('Ctrl Pts',(5.92490555002402,0.138348267860097,38.6948775604718));
#48189=CARTESIAN_POINT('Ctrl Pts',(5.9707088634076,-1.82322530204013,38.602087801895));
#48190=CARTESIAN_POINT('Ctrl Pts',(4.94559397391919,-3.80980512345547,38.5092980433183));
#48191=CARTESIAN_POINT('Ctrl Pts',(3.3203335456359,-4.909076406581,38.4165082847415));
#48192=CARTESIAN_POINT('Ctrl Pts',(1.69507311735257,-6.00834768970656,38.3237185261647));
#48193=CARTESIAN_POINT('Ctrl Pts',(-0.53033284972568,-6.22031043454227,
38.230928767588));
#48194=CARTESIAN_POINT('Ctrl Pts',(-2.33389130241298,-5.44762309713571,
38.1381390090112));
#48195=CARTESIAN_POINT('Ctrl Pts',(-4.13744975510023,-4.67493575972916,
38.0453492504345));
#48196=CARTESIAN_POINT('Ctrl Pts',(-5.51916069339655,-2.9175983400804,37.9525594918577));
#48197=CARTESIAN_POINT('Ctrl Pts',(-5.84448866564066,-0.982648592897399,
37.859769733281));
#48198=CARTESIAN_POINT('Ctrl Pts',(-5.89870959908197,-0.660159319286536,
37.8443048862556));
#48199=CARTESIAN_POINT('Ctrl Pts',(-5.92358698906954,-0.33273644184221,
37.8288400392302));
#48200=CARTESIAN_POINT('Ctrl Pts',(-5.92067510213246,-0.00487139356358524,
37.8133751922049));
#48201=CARTESIAN_POINT('Ctrl Pts',(-5.92504705000468,-0.0026864220054185,
37.5616248077955));
#48202=CARTESIAN_POINT('Ctrl Pts',(-5.92589451573722,-0.152866600912679,
37.5687222470785));
#48203=CARTESIAN_POINT('Ctrl Pts',(-5.92068156990396,-0.302986979278675,
37.5758196863615));
#48204=CARTESIAN_POINT('Ctrl Pts',(-5.90921945853301,-0.452628690092833,
37.5829171256445));
#48205=CARTESIAN_POINT('Ctrl Pts',(-5.75933792654291,-2.40938239284423,
37.6757250768602));
#48206=CARTESIAN_POINT('Ctrl Pts',(-4.54092071513729,-4.28428943068747,
37.7685330280759));
#48207=CARTESIAN_POINT('Ctrl Pts',(-2.81371328846423,-5.2160104361974,37.8613409792916));
#48208=CARTESIAN_POINT('Ctrl Pts',(-1.08650586179102,-6.14773144170741,
37.9541489305073));
#48209=CARTESIAN_POINT('Ctrl Pts',(1.14949178014972,-6.13626641488391,38.046956881723));
#48210=CARTESIAN_POINT('Ctrl Pts',(2.86705388397389,-5.18688243230851,38.1397648329388));
#48211=CARTESIAN_POINT('Ctrl Pts',(4.58461598779797,-4.23749844973315,38.2325727841545));
#48212=CARTESIAN_POINT('Ctrl Pts',(5.78374255350553,-2.35019551140599,38.3253807353702));
#48213=CARTESIAN_POINT('Ctrl Pts',(5.913550312368,-0.392007708205717,38.4181886865859));
#48214=CARTESIAN_POINT('Ctrl Pts',(6.04335807123046,1.56618009499456,38.5109966378016));
#48215=CARTESIAN_POINT('Ctrl Pts',(5.10384702324784,3.59525276306796,38.6038045890173));
#48216=CARTESIAN_POINT('Ctrl Pts',(3.52663208874664,4.76304665637687,38.696612540233));
#48217=CARTESIAN_POINT('Ctrl Pts',(1.94941715424539,5.93084054968582,38.7894204914487));
#48218=CARTESIAN_POINT('Ctrl Pts',(-0.265501666774463,6.23735566823023,
38.8822284426645));
#48219=CARTESIAN_POINT('Ctrl Pts',(-2.10058231079274,5.54177781003398,38.9750363938802));
#48220=CARTESIAN_POINT('Ctrl Pts',(-3.93566295481097,4.84619995183775,39.0678443450959));
#48221=CARTESIAN_POINT('Ctrl Pts',(-5.39090542182765,3.1485291169009,39.1606522963116));
#48222=CARTESIAN_POINT('Ctrl Pts',(-5.79776583169802,1.22868169230088,39.2534602475273));
#48223=CARTESIAN_POINT('Ctrl Pts',(-5.88276162685228,0.827613034672763,
39.2728484342833));
#48224=CARTESIAN_POINT('Ctrl Pts',(-5.92200399834135,0.416848160320931,
39.2922366210394));
#48225=CARTESIAN_POINT('Ctrl Pts',(-5.91817991048888,0.00535877289898346,
39.3116248077955));
#48226=CARTESIAN_POINT('Origin',(0.,0.,-10.));
#48227=CARTESIAN_POINT('',(-5.9083370126323,0.00290647373917707,41.3133751922049));
#48228=CARTESIAN_POINT('',(-5.90694375459152,0.000187200592619384,41.0616248077955));
#48229=CARTESIAN_POINT('',(-5.91675,-7.2459289488551E-16,-10.));
#48230=CARTESIAN_POINT('Ctrl Pts',(-5.9083370126323,0.00290647373917707,
41.3133751922049));
#48231=CARTESIAN_POINT('Ctrl Pts',(-5.9118961055199,0.806946743982272,41.2756504754847));
#48232=CARTESIAN_POINT('Ctrl Pts',(-5.75924372095175,1.60969263292704,41.2379257587644));
#48233=CARTESIAN_POINT('Ctrl Pts',(-5.44394638268512,2.34245465321636,41.2002010420442));
#48234=CARTESIAN_POINT('Ctrl Pts',(-4.66842395491908,4.1447958466867,41.1074112834675));
#48235=CARTESIAN_POINT('Ctrl Pts',(-2.90891600578834,5.52374171235785,41.0146215248907));
#48236=CARTESIAN_POINT('Ctrl Pts',(-0.973457081635854,5.84602662755981,
40.9218317663139));
#48237=CARTESIAN_POINT('Ctrl Pts',(0.962001842516637,6.16831154276178,40.8290420077372));
#48238=CARTESIAN_POINT('Ctrl Pts',(3.07341174169088,5.43393550749457,40.7362522491604));
#48239=CARTESIAN_POINT('Ctrl Pts',(4.39113099484952,3.98015258576819,40.6434624905837));
#48240=CARTESIAN_POINT('Ctrl Pts',(5.70885024800813,2.52636966404185,40.5506727320069));
#48241=CARTESIAN_POINT('Ctrl Pts',(6.23287885515117,0.353179855856394,40.4578829734301));
#48242=CARTESIAN_POINT('Ctrl Pts',(5.72256247990427,-1.54140347849522,40.3650932148534));
#48243=CARTESIAN_POINT('Ctrl Pts',(5.21224610465735,-3.4359868128469,40.2723034562766));
#48244=CARTESIAN_POINT('Ctrl Pts',(3.66758474702043,-5.05196367336471,40.1795136976999));
#48245=CARTESIAN_POINT('Ctrl Pts',(1.79794703473299,-5.64721457713625,40.0867239391231));
#48246=CARTESIAN_POINT('Ctrl Pts',(-0.0716906775543941,-6.24246548090778,
39.9939341805464));
#48247=CARTESIAN_POINT('Ctrl Pts',(-2.26630474449228,-5.81699042793309,
39.9011444219696));
#48248=CARTESIAN_POINT('Ctrl Pts',(-3.77804295214096,-4.566184125909,39.8083546633928));
#48249=CARTESIAN_POINT('Ctrl Pts',(-5.10845136633424,-3.46540938837883,
39.7266948396635));
#48250=CARTESIAN_POINT('Ctrl Pts',(-5.90997807248162,-1.72542242103686,
39.6450350159342));
#48251=CARTESIAN_POINT('Ctrl Pts',(-5.92317748384162,0.00391648730000096,
39.5633751922049));
#48252=CARTESIAN_POINT('Ctrl Pts',(-5.91817991048888,0.00535877289898346,
39.3116248077955));
#48253=CARTESIAN_POINT('Ctrl Pts',(-5.90369874043758,-1.55288152477645,
39.3850445722551));
#48254=CARTESIAN_POINT('Ctrl Pts',(-5.27164108271407,-3.1215113980975,39.4584643367148));
#48255=CARTESIAN_POINT('Ctrl Pts',(-4.16791835516374,-4.21333643623311,
39.5318841011744));
#48256=CARTESIAN_POINT('Ctrl Pts',(-2.77273211603503,-5.59348312590389,
39.6246920523901));
#48257=CARTESIAN_POINT('Ctrl Pts',(-0.623881285053837,-6.21175249098218,
39.7175000036058));
#48258=CARTESIAN_POINT('Ctrl Pts',(1.29144395816604,-5.78410925234965,39.8103079548215));
#48259=CARTESIAN_POINT('Ctrl Pts',(3.20676920138586,-5.35646601371713,39.9031159060372));
#48260=CARTESIAN_POINT('Ctrl Pts',(4.88856885684424,-3.88291017137353,39.9959238572529));
#48261=CARTESIAN_POINT('Ctrl Pts',(5.56421781719968,-2.04039883918756,40.0887318084687));
#48262=CARTESIAN_POINT('Ctrl Pts',(6.23986677755516,-0.197887507001491,
40.1815397596844));
#48263=CARTESIAN_POINT('Ctrl Pts',(5.90936504280782,2.01357931502706,40.2743477109001));
#48264=CARTESIAN_POINT('Ctrl Pts',(4.72454635692166,3.57804542473942,40.3671556621158));
#48265=CARTESIAN_POINT('Ctrl Pts',(3.53972767103556,5.14251153445169,40.4599636133315));
#48266=CARTESIAN_POINT('Ctrl Pts',(1.50059203401065,6.05997693184778,40.5527715645472));
#48267=CARTESIAN_POINT('Ctrl Pts',(-0.456073948610288,5.90895455166135,
40.6455795157629));
#48268=CARTESIAN_POINT('Ctrl Pts',(-2.41273993123128,5.75793217147491,40.7383874669786));
#48269=CARTESIAN_POINT('Ctrl Pts',(-4.28693625944829,4.538422013706,40.8311954181944));
#48270=CARTESIAN_POINT('Ctrl Pts',(-5.2176500685201,2.81067164618575,40.9240033694101));
#48271=CARTESIAN_POINT('Ctrl Pts',(-5.67769029658167,1.95666618783744,40.9698771822052));
#48272=CARTESIAN_POINT('Ctrl Pts',(-5.90721872419092,0.978487399899294,
41.0157509950003));
#48273=CARTESIAN_POINT('Ctrl Pts',(-5.90694375459152,0.000187200592619384,
41.0616248077955));
#48274=CARTESIAN_POINT('Origin',(0.,0.,-10.));
#48275=CARTESIAN_POINT('',(-5.91250905277058,-0.00502274925685997,43.0633751922049));
#48276=CARTESIAN_POINT('',(-5.91749050086513,-0.0054238502176924,42.8116248077955));
#48277=CARTESIAN_POINT('',(-5.91675,-7.2459289488551E-16,-10.));
#48278=CARTESIAN_POINT('Ctrl Pts',(-5.91250905277058,-0.00502274925685997,
43.0633751922049));
#48279=CARTESIAN_POINT('Ctrl Pts',(-5.9015374759735,1.3634120868958,42.9990556936118));
#48280=CARTESIAN_POINT('Ctrl Pts',(-5.42891142018307,2.73868470796129,42.9347361950188));
#48281=CARTESIAN_POINT('Ctrl Pts',(-4.5602376127848,3.78521847914597,42.8704166964258));
#48282=CARTESIAN_POINT('Ctrl Pts',(-3.30705569076064,5.29498795955015,42.777626937849));
#48283=CARTESIAN_POINT('Ctrl Pts',(-1.2296173434281,6.12058461442322,42.6848371792723));
#48284=CARTESIAN_POINT('Ctrl Pts',(0.718036867263995,5.88286232009343,42.5920474206956));
#48285=CARTESIAN_POINT('Ctrl Pts',(2.66569107795615,5.64514002576363,42.4992576621188));
#48286=CARTESIAN_POINT('Ctrl Pts',(4.48356115200779,4.34409878223093,42.406467903542));
#48287=CARTESIAN_POINT('Ctrl Pts',(5.336810383326,2.57722737692063,42.3136781449652));
#48288=CARTESIAN_POINT('Ctrl Pts',(6.19005961464416,0.810355971610422,42.2208883863885));
#48289=CARTESIAN_POINT('Ctrl Pts',(6.07868800322892,-1.42234559547743,42.1280986278118));
#48290=CARTESIAN_POINT('Ctrl Pts',(5.05384172864138,-3.09553384762119,42.035308869235));
#48291=CARTESIAN_POINT('Ctrl Pts',(4.02899545405375,-4.7687220997651,41.9425191106583));
#48292=CARTESIAN_POINT('Ctrl Pts',(2.09067451629372,-5.88239703696494,41.8497293520815));
#48293=CARTESIAN_POINT('Ctrl Pts',(0.129031347115672,-5.92511577366947,
41.7569395935047));
#48294=CARTESIAN_POINT('Ctrl Pts',(-1.83261182206221,-5.96783451037401,
41.6641498349279));
#48295=CARTESIAN_POINT('Ctrl Pts',(-3.81757722265803,-4.93959704658343,
41.5713600763512));
#48296=CARTESIAN_POINT('Ctrl Pts',(-4.91429146975527,-3.31261005405344,
41.4785703177745));
#48297=CARTESIAN_POINT('Ctrl Pts',(-5.56512424319231,-2.34709286532634,
41.4235052759179));
#48298=CARTESIAN_POINT('Ctrl Pts',(-5.9031419676892,-1.17071429758749,41.3684402340614));
#48299=CARTESIAN_POINT('Ctrl Pts',(-5.9083370126323,0.00290647373917707,
41.3133751922049));
#48300=CARTESIAN_POINT('Ctrl Pts',(-5.90694375459152,0.000187200592619384,
41.0616248077955));
#48301=CARTESIAN_POINT('Ctrl Pts',(-5.9066624293549,-1.00072539361877,41.108558946216));
#48302=CARTESIAN_POINT('Ctrl Pts',(-5.66583159864754,-2.00176507665916,
41.1554930846366));
#48303=CARTESIAN_POINT('Ctrl Pts',(-5.18520993188531,-2.87007757778048,
41.2024272230572));
#48304=CARTESIAN_POINT('Ctrl Pts',(-4.23482469625214,-4.58708585695503,
41.2952351742729));
#48305=CARTESIAN_POINT('Ctrl Pts',(-2.34682293505921,-5.78511183803251,
41.3880431254886));
#48306=CARTESIAN_POINT('Ctrl Pts',(-0.388559781046523,-5.91377786501602,
41.4808510767043));
#48307=CARTESIAN_POINT('Ctrl Pts',(1.56970337296606,-6.04244389199952,41.57365902792));
#48308=CARTESIAN_POINT('Ctrl Pts',(3.59822791979854,-5.10174996488907,41.6664669791358));
#48309=CARTESIAN_POINT('Ctrl Pts',(4.76510202877927,-3.52385442314578,41.7592749303515));
#48310=CARTESIAN_POINT('Ctrl Pts',(5.93197613776004,-1.94595888140243,41.8520828815672));
#48311=CARTESIAN_POINT('Ctrl Pts',(6.23719980888921,0.269138274973701,41.9448908327828));
#48312=CARTESIAN_POINT('Ctrl Pts',(5.54055213600606,2.1038130545272,42.0376987839985));
#48313=CARTESIAN_POINT('Ctrl Pts',(4.84390446312288,3.93848783408075,42.1305067352143));
#48314=CARTESIAN_POINT('Ctrl Pts',(3.14538544622723,5.3927402368115,42.22331468643));
#48315=CARTESIAN_POINT('Ctrl Pts',(1.22530113038875,5.79848122184322,42.3161226376457));
#48316=CARTESIAN_POINT('Ctrl Pts',(-0.694783185449667,6.20422220687492,
42.4089305888614));
#48317=CARTESIAN_POINT('Ctrl Pts',(-2.83643280023093,5.56145177420767,42.5017385400771));
#48318=CARTESIAN_POINT('Ctrl Pts',(-4.21576580023403,4.16546108585562,42.5945464912928));
#48319=CARTESIAN_POINT('Ctrl Pts',(-5.29118833179891,3.07705107891373,42.666905930127));
#48320=CARTESIAN_POINT('Ctrl Pts',(-5.90321154071277,1.53077127151761,42.7392653689613));
#48321=CARTESIAN_POINT('Ctrl Pts',(-5.91749050086513,-0.0054238502176924,
42.8116248077955));
#48322=CARTESIAN_POINT('Origin',(0.,0.,-10.));
#48323=CARTESIAN_POINT('',(-5.92640592629062,-0.000744257410045246,44.8133751922049));
#48324=CARTESIAN_POINT('',(-5.92543336817915,0.00231728688185692,44.5616248077955));
#48325=CARTESIAN_POINT('',(-5.91675,-7.2459289488551E-16,-10.));
#48326=CARTESIAN_POINT('Ctrl Pts',(-5.92640592629062,-0.000744257410045246,
44.8133751922049));
#48327=CARTESIAN_POINT('Ctrl Pts',(-5.92300951336607,1.92180582290993,44.7224609117391));
#48328=CARTESIAN_POINT('Ctrl Pts',(-4.9006682261132,3.84745506871863,44.6315466312733));
#48329=CARTESIAN_POINT('Ctrl Pts',(-3.30487837147756,4.9194943815056,44.5406323508074));
#48330=CARTESIAN_POINT('Ctrl Pts',(-1.67616883770366,6.01364888076154,44.4478425922307));
#48331=CARTESIAN_POINT('Ctrl Pts',(0.549892734243904,6.21861180766247,44.3550528336539));
#48332=CARTESIAN_POINT('Ctrl Pts',(2.35101221190118,5.44025620714841,44.2622630750772));
#48333=CARTESIAN_POINT('Ctrl Pts',(4.15213168955856,4.66190060663431,44.1694733165004));
#48334=CARTESIAN_POINT('Ctrl Pts',(5.52830907292561,2.90022647870511,44.0766835579236));
#48335=CARTESIAN_POINT('Ctrl Pts',(5.84755013418095,0.964263163335458,43.9838937993469));
#48336=CARTESIAN_POINT('Ctrl Pts',(6.16679119543626,-0.971700152034025,
43.8911040407701));
#48337=CARTESIAN_POINT('Ctrl Pts',(5.42909593457998,-3.08195265484406,43.7983142821934));
#48338=CARTESIAN_POINT('Ctrl Pts',(3.9732427332272,-4.39738424552399,43.7055245236166));
#48339=CARTESIAN_POINT('Ctrl Pts',(2.51738953187434,-5.71281583620399,43.6127347650398));
#48340=CARTESIAN_POINT('Ctrl Pts',(0.343378390025083,-6.23342651475394,
43.5199450064631));
#48341=CARTESIAN_POINT('Ctrl Pts',(-1.55040014363566,-5.72013159066641,
43.4271552478863));
#48342=CARTESIAN_POINT('Ctrl Pts',(-3.44417867729635,-5.20683666657891,
43.3343654893096));
#48343=CARTESIAN_POINT('Ctrl Pts',(-5.05772460276838,-3.65963613985392,
43.2415757307328));
#48344=CARTESIAN_POINT('Ctrl Pts',(-5.65003481714654,-1.78906472352378,
43.1487859721561));
#48345=CARTESIAN_POINT('Ctrl Pts',(-5.8317706687429,-1.2151257958025,43.1203157121723));
#48346=CARTESIAN_POINT('Ctrl Pts',(-5.91736549056436,-0.610744130926478,
43.0918454521886));
#48347=CARTESIAN_POINT('Ctrl Pts',(-5.91250905277058,-0.00502274925685997,
43.0633751922049));
#48348=CARTESIAN_POINT('Ctrl Pts',(-5.91749050086513,-0.0054238502176924,
42.8116248077955));
#48349=CARTESIAN_POINT('Ctrl Pts',(-5.92152568270421,-0.439546964952688,
42.832073320177));
#48350=CARTESIAN_POINT('Ctrl Pts',(-5.87782459649013,-0.872864709734026,
42.8525218325585));
#48351=CARTESIAN_POINT('Ctrl Pts',(-5.7833553004627,-1.29481612934438,42.87297034494));
#48352=CARTESIAN_POINT('Ctrl Pts',(-5.35459541546329,-3.20989171215526,
42.9657782961557));
#48353=CARTESIAN_POINT('Ctrl Pts',(-3.88005926023967,-4.8908319337401,43.0585862473713));
#48354=CARTESIAN_POINT('Ctrl Pts',(-2.03715430809605,-5.56540651392206,
43.1513941985871));
#48355=CARTESIAN_POINT('Ctrl Pts',(-0.194249355952331,-6.23998109410406,
43.2442021498028));
#48356=CARTESIAN_POINT('Ctrl Pts',(2.01702439311145,-5.90819003288294,43.3370101010186));
#48357=CARTESIAN_POINT('Ctrl Pts',(3.58079943538484,-4.72245939566959,43.4298180522343));
#48358=CARTESIAN_POINT('Ctrl Pts',(5.1445744776582,-3.53672875845627,43.52262600345));
#48359=CARTESIAN_POINT('Ctrl Pts',(6.06085081314126,-1.49705854525084,43.6154339546656));
#48360=CARTESIAN_POINT('Ctrl Pts',(5.90868763609711,0.459519052089763,43.7082419058814));
#48361=CARTESIAN_POINT('Ctrl Pts',(5.75652445905297,2.41609664943031,43.8010498570971));
#48362=CARTESIAN_POINT('Ctrl Pts',(4.53592176948156,4.28958163090607,43.8938578083128));
#48363=CARTESIAN_POINT('Ctrl Pts',(2.80762904844648,5.21928792715251,43.9866657595285));
#48364=CARTESIAN_POINT('Ctrl Pts',(1.07933632741135,6.14899422339897,44.0794737107442));
#48365=CARTESIAN_POINT('Ctrl Pts',(-1.15664642508744,6.13492183441616,44.1722816619599));
#48366=CARTESIAN_POINT('Ctrl Pts',(-2.8731002959318,5.18353566879953,44.2650896131756));
#48367=CARTESIAN_POINT('Ctrl Pts',(-4.58955416677612,4.23214950318292,44.3578975643913));
#48368=CARTESIAN_POINT('Ctrl Pts',(-5.786479155966,2.34344956093245,44.450705515607));
#48369=CARTESIAN_POINT('Ctrl Pts',(-5.91400340733182,0.385111721800315,
44.5435134668228));
#48370=CARTESIAN_POINT('Ctrl Pts',(-5.92229880001647,0.257722764713088,
44.5495505804803));
#48371=CARTESIAN_POINT('Ctrl Pts',(-5.92606908611989,0.130039138944288,
44.5555876941379));
#48372=CARTESIAN_POINT('Ctrl Pts',(-5.92543336817915,0.00231728688185692,
44.5616248077955));
#48373=CARTESIAN_POINT('Origin',(0.,0.,-10.));
#48374=CARTESIAN_POINT('',(-5.91475019377533,0.00539823251707206,46.5633751922049));
#48375=CARTESIAN_POINT('',(-5.91039421288723,0.00428526322922202,46.3116248077954));
#48376=CARTESIAN_POINT('',(-5.91675,-7.2459289488551E-16,-10.));
#48377=CARTESIAN_POINT('Ctrl Pts',(-5.91475019377533,0.00539823251707206,
46.5633751922049));
#48378=CARTESIAN_POINT('Ctrl Pts',(-5.91941312805242,0.530811138238026,
46.538655888443));
#48379=CARTESIAN_POINT('Ctrl Pts',(-5.85522209608251,1.055103733712,46.5139365846812));
#48380=CARTESIAN_POINT('Ctrl Pts',(-5.71768655742746,1.55939297514728,46.4892172809193));
#48381=CARTESIAN_POINT('Ctrl Pts',(-5.20141435370859,3.45236202542662,46.3964275223426));
#48382=CARTESIAN_POINT('Ctrl Pts',(-3.65167848361261,5.06347302608539,46.3036377637658));
#48383=CARTESIAN_POINT('Ctrl Pts',(-1.78017798854655,5.65284108648206,46.210848005189));
#48384=CARTESIAN_POINT('Ctrl Pts',(0.0913225065194465,6.24220914687871,
46.1180582466122));
#48385=CARTESIAN_POINT('Ctrl Pts',(2.28458762655536,5.80983426701343,46.0252684880356));
#48386=CARTESIAN_POINT('Ctrl Pts',(3.79238464655248,4.55427982369533,45.9324787294588));
#48387=CARTESIAN_POINT('Ctrl Pts',(5.3001816665496,3.29872538037722,45.839688970882));
#48388=CARTESIAN_POINT('Ctrl Pts',(6.12251058650776,1.21999137360628,45.7468992123053));
#48389=CARTESIAN_POINT('Ctrl Pts',(5.88172595383818,-0.727286617415579,
45.6541094537285));
#48390=CARTESIAN_POINT('Ctrl Pts',(5.64094132116859,-2.67456460843749,45.5613196951517));
#48391=CARTESIAN_POINT('Ctrl Pts',(4.33704313587116,-4.4903865837104,45.468529936575));
#48392=CARTESIAN_POINT('Ctrl Pts',(2.56883220424791,-5.34085640383115,45.3757401779983));
#48393=CARTESIAN_POINT('Ctrl Pts',(0.800621272624648,-6.19132622395189,
45.2829504194215));
#48394=CARTESIAN_POINT('Ctrl Pts',(-1.4319024053245,-6.07644388892052,45.1901606608447));
#48395=CARTESIAN_POINT('Ctrl Pts',(-3.10347704649546,-5.04896783925202,
45.0973709022679));
#48396=CARTESIAN_POINT('Ctrl Pts',(-4.77505168766637,-4.02149178958355,
45.0045811436912));
#48397=CARTESIAN_POINT('Ctrl Pts',(-5.88567729205918,-2.08142202527798,
44.9117913851144));
#48398=CARTESIAN_POINT('Ctrl Pts',(-5.92531134645547,-0.119714107319727,
44.8190016265377));
#48399=CARTESIAN_POINT('Ctrl Pts',(-5.92611243487954,-0.0800638235317725,
44.8171261484268));
#48400=CARTESIAN_POINT('Ctrl Pts',(-5.92647599117001,-0.0404046999098048,
44.8152506703158));
#48401=CARTESIAN_POINT('Ctrl Pts',(-5.92640592629062,-0.000744257410045246,
44.8133751922049));
#48402=CARTESIAN_POINT('Ctrl Pts',(-5.92543336817915,0.00231728688185692,
44.5616248077955));
#48403=CARTESIAN_POINT('Ctrl Pts',(-5.91629625708645,-1.83341626171998,
44.6483956453536));
#48404=CARTESIAN_POINT('Ctrl Pts',(-4.9969655697077,-3.67704660900026,44.7351664829118));
#48405=CARTESIAN_POINT('Ctrl Pts',(-3.52107555964431,-4.76715578133082,
44.8219373204699));
#48406=CARTESIAN_POINT('Ctrl Pts',(-1.94249994704928,-5.93310970931579,
44.9147452716856));
#48407=CARTESIAN_POINT('Ctrl Pts',(0.272774791682385,-6.23704182927182,
45.0075532229013));
#48408=CARTESIAN_POINT('Ctrl Pts',(2.107043083091,-5.53932457852026,45.100361174117));
#48409=CARTESIAN_POINT('Ctrl Pts',(3.94131137449957,-4.84160732776873,45.1931691253327));
#48410=CARTESIAN_POINT('Ctrl Pts',(5.394573218585,-3.1422407063096,45.2859770765484));
#48411=CARTESIAN_POINT('Ctrl Pts',(5.79919464085023,-1.22192015194707,45.3787850277641));
#48412=CARTESIAN_POINT('Ctrl Pts',(6.20381606311547,0.69840040241552,45.4715929789798));
#48413=CARTESIAN_POINT('Ctrl Pts',(5.55979706356047,2.83967488968159,45.5644009301955));
#48414=CARTESIAN_POINT('Ctrl Pts',(4.16300240053861,4.21819373112593,45.6572088814113));
#48415=CARTESIAN_POINT('Ctrl Pts',(2.7662077375168,5.59671257257024,45.750016832627));
#48416=CARTESIAN_POINT('Ctrl Pts',(0.616637411028301,6.21247576819288,45.8428247838427));
#48417=CARTESIAN_POINT('Ctrl Pts',(-1.29818786036205,5.78259938257951,45.9356327350584));
#48418=CARTESIAN_POINT('Ctrl Pts',(-3.21301313175245,5.35272299696613,46.0284406862741));
#48419=CARTESIAN_POINT('Ctrl Pts',(-4.89309334804463,3.87720703011655,46.1212486374898));
#48420=CARTESIAN_POINT('Ctrl Pts',(-5.56659331873784,2.0339090844931,46.2140565887055));
#48421=CARTESIAN_POINT('Ctrl Pts',(-5.80260827161228,1.38796120520504,46.2465793284022));
#48422=CARTESIAN_POINT('Ctrl Pts',(-5.91501360248399,0.696849126068583,
46.2791020680988));
#48423=CARTESIAN_POINT('Ctrl Pts',(-5.91039421288723,0.00428526322922202,
46.3116248077954));
#48424=CARTESIAN_POINT('Origin',(0.,0.,-10.));
#48425=CARTESIAN_POINT('',(-5.90740046258813,-0.00170769527667092,48.3133751922049));
#48426=CARTESIAN_POINT('',(-5.90981348303521,-0.00398707326546309,48.0616248077955));
#48427=CARTESIAN_POINT('',(-5.91675,-7.2459289488551E-16,-10.));
#48428=CARTESIAN_POINT('Ctrl Pts',(-5.90740046258813,-0.00170769527667092,
48.3133751922049));
#48429=CARTESIAN_POINT('Ctrl Pts',(-5.90458171200211,1.09240074162204,48.2620611065702));
#48430=CARTESIAN_POINT('Ctrl Pts',(-5.61374355902189,2.18790212669476,48.2107470209356));
#48431=CARTESIAN_POINT('Ctrl Pts',(-5.04408146542834,3.11141257149349,48.1594329353009));
#48432=CARTESIAN_POINT('Ctrl Pts',(-4.01397818128872,4.78136946843801,48.0666431767242));
#48433=CARTESIAN_POINT('Ctrl Pts',(-2.072164387591,5.88894299381245,47.9738534181474));
#48434=CARTESIAN_POINT('Ctrl Pts',(-0.110396571509901,5.92549226789844,
47.8810636595706));
#48435=CARTESIAN_POINT('Ctrl Pts',(1.85137124457137,5.96204154198443,47.7882739009939));
#48436=CARTESIAN_POINT('Ctrl Pts',(3.83309308303601,4.92756656478179,47.6954841424172));
#48437=CARTESIAN_POINT('Ctrl Pts',(4.92468512896701,3.29713851702603,47.6026943838404));
#48438=CARTESIAN_POINT('Ctrl Pts',(6.0162771748979,1.66671046927041,47.5099046252636));
#48439=CARTESIAN_POINT('Ctrl Pts',(6.21773942829533,-0.559670649038214,
47.4171148666868));
#48440=CARTESIAN_POINT('Ctrl Pts',(5.43655257965025,-2.35956395730728,47.3243251081101));
#48441=CARTESIAN_POINT('Ctrl Pts',(4.65536573100512,-4.15945726557646,47.2315353495333));
#48442=CARTESIAN_POINT('Ctrl Pts',(2.89152978031738,-5.53286276380603,47.1387455909566));
#48443=CARTESIAN_POINT('Ctrl Pts',(0.955066860730234,-5.84905918173686,
47.0459558323798));
#48444=CARTESIAN_POINT('Ctrl Pts',(-0.981396058856855,-6.16525559966767,
46.9531660738031));
#48445=CARTESIAN_POINT('Ctrl Pts',(-3.09048594734334,-5.4242429372998,46.8603763152263));
#48446=CARTESIAN_POINT('Ctrl Pts',(-4.4036266229157,-3.96632305616593,46.7675865566495));
#48447=CARTESIAN_POINT('Ctrl Pts',(-5.36694503642602,-2.89679479232864,
46.6995161018346));
#48448=CARTESIAN_POINT('Ctrl Pts',(-5.90190970036696,-1.44145058663312,
46.6314456470198));
#48449=CARTESIAN_POINT('Ctrl Pts',(-5.91475019377533,0.00539823251707206,
46.5633751922049));
#48450=CARTESIAN_POINT('Ctrl Pts',(-5.91039421288723,0.00428526322922202,
46.3116248077954));
#48451=CARTESIAN_POINT('Ctrl Pts',(-5.90183156159993,-1.27947371129696,
46.3719100193145));
#48452=CARTESIAN_POINT('Ctrl Pts',(-5.49117736245765,-2.5682209477384,46.4321952308336));
#48453=CARTESIAN_POINT('Ctrl Pts',(-4.72037082906262,-3.58355222877175,
46.4924804423527));
#48454=CARTESIAN_POINT('Ctrl Pts',(-3.53372864359993,-5.14663567201572,
46.5852883935684));
#48455=CARTESIAN_POINT('Ctrl Pts',(-1.49352454758038,-6.06172263410644,
46.6780963447841));
#48456=CARTESIAN_POINT('Ctrl Pts',(0.462963999359967,-5.90841871193105,
46.7709042959998));
#48457=CARTESIAN_POINT('Ctrl Pts',(2.41945254630037,-5.75511478975566,46.8637122472155));
#48458=CARTESIAN_POINT('Ctrl Pts',(4.29222554416156,-4.53341998331399,46.9565201984312));
#48459=CARTESIAN_POINT('Ctrl Pts',(5.2209240115379,-2.80458549628057,47.0493281496469));
#48460=CARTESIAN_POINT('Ctrl Pts',(6.14962247891425,-1.07575100924715,47.1421361008626));
#48461=CARTESIAN_POINT('Ctrl Pts',(6.13424641580585,1.16022315837803,47.2349440520783));
#48462=CARTESIAN_POINT('Ctrl Pts',(5.18185964362037,2.87612203740016,47.327752003294));
#48463=CARTESIAN_POINT('Ctrl Pts',(4.2294728714349,4.5920209164223,47.4205599545097));
#48464=CARTESIAN_POINT('Ctrl Pts',(2.34007539017238,5.78784450684132,47.5133679057255));
#48465=CARTESIAN_POINT('Ctrl Pts',(0.381663531638894,5.91422693923875,47.6061758569412));
#48466=CARTESIAN_POINT('Ctrl Pts',(-1.57674832689459,6.04060937163617,47.6989838081569));
#48467=CARTESIAN_POINT('Ctrl Pts',(-3.60417456269912,5.09755064601189,47.7917917593726));
#48468=CARTESIAN_POINT('Ctrl Pts',(-4.76920791333336,3.5182954991869,47.8845997105883));
#48469=CARTESIAN_POINT('Ctrl Pts',(-5.50994955397949,2.51418686330868,47.943608076324));
#48470=CARTESIAN_POINT('Ctrl Pts',(-5.90206343299662,1.25289181263786,48.0026164420597));
#48471=CARTESIAN_POINT('Ctrl Pts',(-5.90981348303521,-0.00398707326546309,
48.0616248077955));
#48472=CARTESIAN_POINT('Origin',(0.,0.,-10.));
#48473=CARTESIAN_POINT('',(-5.92103312412998,-0.00476770783831071,50.0633751922048));
#48474=CARTESIAN_POINT('',(-5.92496225112949,-0.0027597696008211,49.8116248077954));
#48475=CARTESIAN_POINT('',(-5.91675,-7.2459289488551E-16,-10.));
#48476=CARTESIAN_POINT('Ctrl Pts',(-5.92103312412998,-0.00476770783831071,
50.0633751922048));
#48477=CARTESIAN_POINT('Ctrl Pts',(-5.90655967293925,1.64669327195933,49.9854663246974));
#48478=CARTESIAN_POINT('Ctrl Pts',(-5.18523595369446,3.30923484336091,49.90755745719));
#48479=CARTESIAN_POINT('Ctrl Pts',(-3.95939357169421,4.40985811158953,49.8296485896825));
#48480=CARTESIAN_POINT('Ctrl Pts',(-2.49941061573483,5.72070462508994,49.7368588311058));
#48481=CARTESIAN_POINT('Ctrl Pts',(-0.32377293541545,6.23447559301229,49.644069072529));
#48482=CARTESIAN_POINT('Ctrl Pts',(1.56838195079361,5.71522738623322,49.5512793139523));
#48483=CARTESIAN_POINT('Ctrl Pts',(3.46053683700266,5.19597917945415,49.4584895553755));
#48484=CARTESIAN_POINT('Ctrl Pts',(5.06920892910144,3.64371179797354,49.3656997967988));
#48485=CARTESIAN_POINT('Ctrl Pts',(5.65563337820364,1.7712868517759,49.272910038222));
#48486=CARTESIAN_POINT('Ctrl Pts',(6.24205782730584,-0.10113809442173,49.1801202796453));
#48487=CARTESIAN_POINT('Ctrl Pts',(5.8062346334116,-2.29372060533647,49.0873305210685));
#48488=CARTESIAN_POINT('Ctrl Pts',(4.54831077337202,-3.79954143664119,48.9945407624917));
#48489=CARTESIAN_POINT('Ctrl Pts',(3.29038691333237,-5.30536226794598,48.901751003915));
#48490=CARTESIAN_POINT('Ctrl Pts',(1.21036238714734,-6.12442141964063,48.8089612453382));
#48491=CARTESIAN_POINT('Ctrl Pts',(-0.736534569227438,-5.88057504401213,
48.7161714867614));
#48492=CARTESIAN_POINT('Ctrl Pts',(-2.68343152560205,-5.63672866838366,
48.6233817281847));
#48493=CARTESIAN_POINT('Ctrl Pts',(-4.49720091216637,-4.32997676543226,
48.5305919696079));
#48494=CARTESIAN_POINT('Ctrl Pts',(-5.34488921815788,-2.56043067969923,
48.4378022110312));
#48495=CARTESIAN_POINT('Ctrl Pts',(-5.72379356574355,-1.76946930816867,
48.3963265380891));
#48496=CARTESIAN_POINT('Ctrl Pts',(-5.90967877615379,-0.886043509327994,
48.354850865147));
#48497=CARTESIAN_POINT('Ctrl Pts',(-5.90740046258813,-0.00170769527667092,
48.3133751922049));
#48498=CARTESIAN_POINT('Ctrl Pts',(-5.90981348303521,-0.00398707326546309,
48.0616248077955));
#48499=CARTESIAN_POINT('Ctrl Pts',(-5.91425265831972,-0.723918642500199,
48.0954243932754));
#48500=CARTESIAN_POINT('Ctrl Pts',(-5.79258515549998,-1.44240130362546,
48.1292239787554));
#48501=CARTESIAN_POINT('Ctrl Pts',(-5.53809513799413,-2.11027239538551,
48.1630235642354));
#48502=CARTESIAN_POINT('Ctrl Pts',(-4.83930854655658,-3.94413357510722,
48.2558315154511));
#48503=CARTESIAN_POINT('Ctrl Pts',(-3.13909489821737,-5.39640436652492,
48.3486394666669));
#48504=CARTESIAN_POINT('Ctrl Pts',(-1.21853875812531,-5.7999060884765,48.4414474178826));
#48505=CARTESIAN_POINT('Ctrl Pts',(0.702017381966812,-6.20340781042809,
48.5342553690983));
#48506=CARTESIAN_POINT('Ctrl Pts',(2.8429160138118,-5.5581404629135,48.627063320314));
#48507=CARTESIAN_POINT('Ctrl Pts',(4.2206202280831,-4.16054230004888,48.7198712715297));
#48508=CARTESIAN_POINT('Ctrl Pts',(5.59832444235433,-2.76294413718435,48.8126792227454));
#48509=CARTESIAN_POINT('Ctrl Pts',(6.21283423905197,-0.613015158969908,
48.9054871739611));
#48510=CARTESIAN_POINT('Ctrl Pts',(5.78184149895695,1.30155915007333,48.9982951251768));
#48511=CARTESIAN_POINT('Ctrl Pts',(5.35084875886191,3.21613345911667,49.0911030763925));
#48512=CARTESIAN_POINT('Ctrl Pts',(3.87435348197408,4.89535309898879,49.1839110276082));
#48513=CARTESIAN_POINT('Ctrl Pts',(2.03066316948238,5.56777823124342,49.2767189788239));
#48514=CARTESIAN_POINT('Ctrl Pts',(0.186972856990724,6.24020336349805,49.3695269300396));
#48515=CARTESIAN_POINT('Ctrl Pts',(-2.02391249110479,5.90583398813525,49.4623348812554));
#48516=CARTESIAN_POINT('Ctrl Pts',(-3.58630380396423,4.71828065781085,49.5551428324711));
#48517=CARTESIAN_POINT('Ctrl Pts',(-5.02556701687734,3.62431539594555,49.6406368242459));
#48518=CARTESIAN_POINT('Ctrl Pts',(-5.91452098969204,1.80634191132433,49.7261308160207));
#48519=CARTESIAN_POINT('Ctrl Pts',(-5.92496225112949,-0.0027597696008211,
49.8116248077954));
#48520=CARTESIAN_POINT('Origin',(0.,0.,-10.));
#48521=CARTESIAN_POINT('',(-5.92286503569152,0.00406918162620035,51.8133751922048));
#48522=CARTESIAN_POINT('',(-5.91832046510867,0.00534203625220547,51.5616248077954));
#48523=CARTESIAN_POINT('',(-5.91675,-7.2459289488551E-16,-10.));
#48524=CARTESIAN_POINT('Ctrl Pts',(-5.92286503569152,0.00406918162620035,
51.8133751922048));
#48525=CARTESIAN_POINT('Ctrl Pts',(-5.92481339761004,0.25217262273859,51.8016613014014));
#48526=CARTESIAN_POINT('Ctrl Pts',(-5.9105794954103,0.500050794796438,51.7899474105979));
#48527=CARTESIAN_POINT('Ctrl Pts',(-5.8794095934613,0.745780699831111,51.7782335197944));
#48528=CARTESIAN_POINT('Ctrl Pts',(-5.63250207782596,2.69229180752391,51.6854437612177));
#48529=CARTESIAN_POINT('Ctrl Pts',(-4.32289968838734,4.50400412052595,51.5926540026409));
#48530=CARTESIAN_POINT('Ctrl Pts',(-2.55202282404879,5.34890881633436,51.4998642440641));
#48531=CARTESIAN_POINT('Ctrl Pts',(-0.781145959710435,6.19381351214267,
51.4070744854874));
#48532=CARTESIAN_POINT('Ctrl Pts',(1.45100537952779,6.07191059075762,51.3142847269106));
#48533=CARTESIAN_POINT('Ctrl Pts',(3.11934040299276,5.03918261925308,51.2214949683339));
#48534=CARTESIAN_POINT('Ctrl Pts',(4.78767542645788,4.00645464774845,51.1287052097571));
#48535=CARTESIAN_POINT('Ctrl Pts',(5.89219413414971,2.06290162612413,51.0359154511803));
#48536=CARTESIAN_POINT('Ctrl Pts',(5.92565853755101,0.101078762725555,50.9431256926036));
#48537=CARTESIAN_POINT('Ctrl Pts',(5.95912294095232,-1.86074410067291,50.8503359340268));
#48538=CARTESIAN_POINT('Ctrl Pts',(4.92153304006336,-3.84083680584558,50.7575461754501));
#48539=CARTESIAN_POINT('Ctrl Pts',(3.2893905098375,-4.9298636993041,50.6647564168733));
#48540=CARTESIAN_POINT('Ctrl Pts',(1.6572479796116,-6.01889059276266,50.5719666582966));
#48541=CARTESIAN_POINT('Ctrl Pts',(-0.569447179951226,-6.21685167450689,
50.4791768997198));
#48542=CARTESIAN_POINT('Ctrl Pts',(-2.368109868289,-5.43283550934846,50.3863871411431));
#48543=CARTESIAN_POINT('Ctrl Pts',(-4.16677255662673,-4.64881934419006,
50.2935973825663));
#48544=CARTESIAN_POINT('Ctrl Pts',(-5.53740277373949,-2.88282593212903,
50.2008076239896));
#48545=CARTESIAN_POINT('Ctrl Pts',(-5.85055376649621,-0.945868196559284,
50.1080178654128));
#48546=CARTESIAN_POINT('Ctrl Pts',(-5.90077445769035,-0.635234162038707,
50.0931369743435));
#48547=CARTESIAN_POINT('Ctrl Pts',(-5.92379760855206,-0.320203058547937,
50.0782560832742));
#48548=CARTESIAN_POINT('Ctrl Pts',(-5.92103312412998,-0.00476770783831071,
50.0633751922048));
#48549=CARTESIAN_POINT('Ctrl Pts',(-5.92496225112949,-0.0027597696008211,
49.8116248077954));
#48550=CARTESIAN_POINT('Ctrl Pts',(-5.92585549474907,-0.157527327462026,
49.8189387672364));
#48551=CARTESIAN_POINT('Ctrl Pts',(-5.92031916798354,-0.312229955259537,
49.8262527266773));
#48552=CARTESIAN_POINT('Ctrl Pts',(-5.90814777925456,-0.466408789250156,
49.8335666861182));
#48553=CARTESIAN_POINT('Ctrl Pts',(-5.75370316406207,-2.42280762070086,
49.9263746373339));
#48554=CARTESIAN_POINT('Ctrl Pts',(-4.53091665605359,-4.29486799831616,
50.0191825885497));
#48555=CARTESIAN_POINT('Ctrl Pts',(-2.8015409907225,-5.22255832112021,50.1119905397654));
#48556=CARTESIAN_POINT('Ctrl Pts',(-1.07216532539152,-6.15024864392421,
50.2047984909811));
#48557=CARTESIAN_POINT('Ctrl Pts',(1.16379949726205,-6.13356891191712,50.2976064421968));
#48558=CARTESIAN_POINT('Ctrl Pts',(2.87914280115849,-5.18018185691753,50.3904143934125));
#48559=CARTESIAN_POINT('Ctrl Pts',(4.59448610505489,-4.22679480191797,50.4832223446282));
#48560=CARTESIAN_POINT('Ctrl Pts',(5.78920789019427,-2.33670042392594,50.5760302958439));
#48561=CARTESIAN_POINT('Ctrl Pts',(5.9144484606608,-0.378215211734605,50.6688382470596));
#48562=CARTESIAN_POINT('Ctrl Pts',(6.03968903112733,1.58027000045679,50.7616461982753));
#48563=CARTESIAN_POINT('Ctrl Pts',(5.09544838692106,3.60714604684744,50.854454149491));
#48564=CARTESIAN_POINT('Ctrl Pts',(3.51551424271886,4.7712584240891,50.9472621007067));
#48565=CARTESIAN_POINT('Ctrl Pts',(1.93558009851661,5.9353708013308,51.0400700519224));
#48566=CARTESIAN_POINT('Ctrl Pts',(-0.280047545681603,6.23671950942332,
51.1328780031381));
#48567=CARTESIAN_POINT('Ctrl Pts',(-2.11350099031294,5.5368638148456,51.2256859543539));
#48568=CARTESIAN_POINT('Ctrl Pts',(-3.94695443494423,4.8370081202679,51.3184939055696));
#48569=CARTESIAN_POINT('Ctrl Pts',(-5.39823368000872,3.13594802301999,51.4113018567853));
#48570=CARTESIAN_POINT('Ctrl Pts',(-5.80061556448015,1.21515695007312,51.504109808001));
#48571=CARTESIAN_POINT('Ctrl Pts',(-5.88373701294625,0.818372347322348,
51.5232814745991));
#48572=CARTESIAN_POINT('Ctrl Pts',(-5.92209925711613,0.412211246926501,
51.5424531411973));
#48573=CARTESIAN_POINT('Ctrl Pts',(-5.91832046510867,0.00534203625220547,
51.5616248077954));
#48574=CARTESIAN_POINT('Origin',(0.,0.,-10.));
#48575=CARTESIAN_POINT('',(-5.90815917370761,0.00272910693063455,53.5633751922048));
#48576=CARTESIAN_POINT('',(-5.90694896850773,0.00026360489279184,53.3116248077954));
#48577=CARTESIAN_POINT('',(-5.91675,-7.2459289488551E-16,-10.));
#48578=CARTESIAN_POINT('Ctrl Pts',(-5.90815917370761,0.00272910693063455,
53.5633751922048));
#48579=CARTESIAN_POINT('Ctrl Pts',(-5.91154687758133,0.819276877355236,
53.5250665195286));
#48580=CARTESIAN_POINT('Ctrl Pts',(-5.75395693091378,1.63457377819285,53.4867578468523));
#48581=CARTESIAN_POINT('Ctrl Pts',(-5.42910500543416,2.37664992371513,53.448449174176));
#48582=CARTESIAN_POINT('Ctrl Pts',(-4.64226146237614,4.17407754462117,53.3556594155992));
#48583=CARTESIAN_POINT('Ctrl Pts',(-2.87411495566173,5.54192909150009,53.2628696570225));
#48584=CARTESIAN_POINT('Ctrl Pts',(-0.936667193567707,5.85203388476343,
53.1700798984458));
#48585=CARTESIAN_POINT('Ctrl Pts',(1.00078056852626,6.16213867802676,53.077290139869));
#48586=CARTESIAN_POINT('Ctrl Pts',(3.10752958599982,5.41449671767459,52.9845003812922));
#48587=CARTESIAN_POINT('Ctrl Pts',(4.41607869613672,3.95245429694674,52.8917106227155));
#48588=CARTESIAN_POINT('Ctrl Pts',(5.72462780627373,2.49041187621876,52.7989208641387));
#48589=CARTESIAN_POINT('Ctrl Pts',(6.23497700907392,0.31396899511498,52.706131105562));
#48590=CARTESIAN_POINT('Ctrl Pts',(5.71275408316433,-1.57736704834818,52.6133413469852));
#48591=CARTESIAN_POINT('Ctrl Pts',(5.19053115725477,-3.46870309181124,52.5205515884085));
#48592=CARTESIAN_POINT('Ctrl Pts',(3.63573610263556,-5.07493229763371,52.4277618298317));
#48593=CARTESIAN_POINT('Ctrl Pts',(1.76239133519637,-5.65841168540697,52.334972071255));
#48594=CARTESIAN_POINT('Ctrl Pts',(-0.110953432242873,-6.24189107318024,
52.2421823126782));
#48595=CARTESIAN_POINT('Ctrl Pts',(-2.30284791250211,-5.80262064290423,
52.1493925541014));
#48596=CARTESIAN_POINT('Ctrl Pts',(-3.80668883171557,-4.54233047657448,
52.0566027955247));
#48597=CARTESIAN_POINT('Ctrl Pts',(-5.1206830632809,-3.44114085771377,51.9755269277514));
#48598=CARTESIAN_POINT('Ctrl Pts',(-5.90937975262626,-1.71314008071065,
51.8944510599781));
#48599=CARTESIAN_POINT('Ctrl Pts',(-5.92286503569152,0.00406918162620035,
51.8133751922048));
#48600=CARTESIAN_POINT('Ctrl Pts',(-5.91832046510867,0.00534203625220547,
51.5616248077954));
#48601=CARTESIAN_POINT('Ctrl Pts',(-5.90380653631969,-1.55739831529493,
51.635261092413));
#48602=CARTESIAN_POINT('Ctrl Pts',(-5.26760929556394,-3.1305850246698,51.7088973770305));
#48603=CARTESIAN_POINT('Ctrl Pts',(-4.15808078522284,-4.22304529028058,
51.7825336616481));
#48604=CARTESIAN_POINT('Ctrl Pts',(-2.75967959761573,-5.59993440904152,
51.8753416128638));
#48605=CARTESIAN_POINT('Ctrl Pts',(-0.609392698522968,-6.2131905979175,
51.9681495640795));
#48606=CARTESIAN_POINT('Ctrl Pts',(1.30492999733203,-5.78108164985268,52.0609575152952));
#48607=CARTESIAN_POINT('Ctrl Pts',(3.21925269318707,-5.34897270178784,52.153765466511));
#48608=CARTESIAN_POINT('Ctrl Pts',(4.8976111858045,-3.8714986167822,52.2465734177267));
#48609=CARTESIAN_POINT('Ctrl Pts',(5.56896125103606,-2.02741656416713,52.3393813689424));
#48610=CARTESIAN_POINT('Ctrl Pts',(6.24031131626763,-0.183334511552064,
52.4321893201581));
#48611=CARTESIAN_POINT('Ctrl Pts',(5.90465295411334,2.02735550867244,52.5249972713738));
#48612=CARTESIAN_POINT('Ctrl Pts',(4.71618888262451,3.58905416002731,52.6178052225895));
#48613=CARTESIAN_POINT('Ctrl Pts',(3.52772481113574,5.1507528113821,52.7106131738052));
#48614=CARTESIAN_POINT('Ctrl Pts',(1.48645503031256,6.06346009386735,52.803421125021));
#48615=CARTESIAN_POINT('Ctrl Pts',(-0.469853420589139,5.90787483815975,
52.8962290762367));
#48616=CARTESIAN_POINT('Ctrl Pts',(-2.42616187149089,5.75228958245214,52.9890370274524));
#48617=CARTESIAN_POINT('Ctrl Pts',(-4.29750899247115,4.52841178855161,53.081844978668));
#48618=CARTESIAN_POINT('Ctrl Pts',(-5.22419085534354,2.79849553280782,53.1746529298837));
#48619=CARTESIAN_POINT('Ctrl Pts',(-5.68007620180948,1.94745538278016,53.2203102225209));
#48620=CARTESIAN_POINT('Ctrl Pts',(-5.90733435577458,0.973944175586275,
53.2659675151582));
#48621=CARTESIAN_POINT('Ctrl Pts',(-5.90694896850773,0.00026360489279184,
53.3116248077954));
#48622=CARTESIAN_POINT('Origin',(0.,0.,-10.));
#48623=CARTESIAN_POINT('',(-5.91284273101683,-0.00510202345033239,55.3133751922048));
#48624=CARTESIAN_POINT('',(-5.9173496880968,-0.00543369097055152,55.0616248077955));
#48625=CARTESIAN_POINT('',(-5.91675,-7.2459289488551E-16,-10.));
#48626=CARTESIAN_POINT('Ctrl Pts',(-5.91284273101683,-0.00510202345033239,
55.3133751922048));
#48627=CARTESIAN_POINT('Ctrl Pts',(-5.90155143772713,1.37555990727446,55.2484717376557));
#48628=CARTESIAN_POINT('Ctrl Pts',(-5.41952439852393,2.76332589927981,55.1835682831067));
#48629=CARTESIAN_POINT('Ctrl Pts',(-4.53633894809001,3.81382681410247,55.1186648285576));
#48630=CARTESIAN_POINT('Ctrl Pts',(-3.27368559175257,5.3156841027214,55.0258750699808));
#48631=CARTESIAN_POINT('Ctrl Pts',(-1.1910954595644,6.12819765018871,54.9330853114041));
#48632=CARTESIAN_POINT('Ctrl Pts',(0.755024986365453,5.87822960506726,54.8402955528274));
#48633=CARTESIAN_POINT('Ctrl Pts',(2.70114543229536,5.6282615599458,54.7475057942506));
#48634=CARTESIAN_POINT('Ctrl Pts',(4.51079619196693,4.31581192223552,54.6547160356738));
#48635=CARTESIAN_POINT('Ctrl Pts',(5.35291518842123,2.54360865808689,54.5619262770971));
#48636=CARTESIAN_POINT('Ctrl Pts',(6.19503418487551,0.771405393938316,54.4691365185203));
#48637=CARTESIAN_POINT('Ctrl Pts',(6.06962141811261,-1.46055149664842,54.3763467599436));
#48638=CARTESIAN_POINT('Ctrl Pts',(5.03427131283913,-3.12726052139094,54.2835570013668));
#48639=CARTESIAN_POINT('Ctrl Pts',(3.99892120756563,-4.79396954613351,54.1907672427901));
#48640=CARTESIAN_POINT('Ctrl Pts',(2.05363376378125,-5.89543070503176,54.0979774842133));
#48641=CARTESIAN_POINT('Ctrl Pts',(0.0917607040070565,-5.92581015500205,
54.0051877256365));
#48642=CARTESIAN_POINT('Ctrl Pts',(-1.87011235576708,-5.95618960497235,
53.9123979670598));
#48643=CARTESIAN_POINT('Ctrl Pts',(-3.84857103153118,-4.91548734601488,
53.8196082084831));
#48644=CARTESIAN_POINT('Ctrl Pts',(-4.93503007971246,-3.28163436906956,
53.7268184499063));
#48645=CARTESIAN_POINT('Ctrl Pts',(-5.57293958221817,-2.32232500399466,
53.6723373640058));
#48646=CARTESIAN_POINT('Ctrl Pts',(-5.90334131464709,-1.15853298111622,
53.6178562781053));
#48647=CARTESIAN_POINT('Ctrl Pts',(-5.90815917370761,0.00272910693063455,
53.5633751922048));
#48648=CARTESIAN_POINT('Ctrl Pts',(-5.90694896850773,0.00026360489279184,
53.3116248077954));
#48649=CARTESIAN_POINT('Ctrl Pts',(-5.90655097593327,-1.00526426374504,
53.3587754663739));
#48650=CARTESIAN_POINT('Ctrl Pts',(-5.66337430186719,-2.01097275620775,
53.4059261249524));
#48651=CARTESIAN_POINT('Ctrl Pts',(-5.17850230926167,-2.88216258617933,
53.4530767835309));
#48652=CARTESIAN_POINT('Ctrl Pts',(-4.22411529554287,-4.59694973183572,
53.5458847347466));
#48653=CARTESIAN_POINT('Ctrl Pts',(-2.33332466334076,-5.79056930556137,
53.6386926859623));
#48654=CARTESIAN_POINT('Ctrl Pts',(-0.374766763259672,-5.91466797152268,
53.731500637178));
#48655=CARTESIAN_POINT('Ctrl Pts',(1.58379113682131,-6.03876663748399,53.8243085883937));
#48656=CARTESIAN_POINT('Ctrl Pts',(3.61011630478126,-5.09334439568107,53.9171165396094));
#48657=CARTESIAN_POINT('Ctrl Pts',(4.77330731290138,-3.51273179118511,54.0099244908252));
#48658=CARTESIAN_POINT('Ctrl Pts',(5.93649832102157,-1.93211918668906,54.1027324420409));
#48659=CARTESIAN_POINT('Ctrl Pts',(6.2365551693018,0.28368378050013,54.1955403932565));
#48660=CARTESIAN_POINT('Ctrl Pts',(5.53563060949312,2.11672886677609,54.2883483444723));
#48661=CARTESIAN_POINT('Ctrl Pts',(4.83470604968444,3.94977395305205,54.381156295688));
#48662=CARTESIAN_POINT('Ctrl Pts',(3.13280008178686,5.40006115841479,54.4739642469037));
#48663=CARTESIAN_POINT('Ctrl Pts',(1.21177472893962,5.8013230686201,54.5667721981195));
#48664=CARTESIAN_POINT('Ctrl Pts',(-0.709250623907553,6.20258497882539,
54.6595801493352));
#48665=CARTESIAN_POINT('Ctrl Pts',(-2.84939536170436,5.55482159387331,54.7523881005508));
#48666=CARTESIAN_POINT('Ctrl Pts',(-4.22546891689455,4.15561785689665,54.8451960517666));
#48667=CARTESIAN_POINT('Ctrl Pts',(-5.2951397940584,3.06796706743294,54.9173389704428));
#48668=CARTESIAN_POINT('Ctrl Pts',(-5.90312024773647,1.52625804066341,54.9894818891192));
#48669=CARTESIAN_POINT('Ctrl Pts',(-5.9173496880968,-0.00543369097055152,
55.0616248077955));
#48670=CARTESIAN_POINT('Origin',(0.,0.,-10.));
#48671=CARTESIAN_POINT('',(-5.92646560327161,-0.000513552043279186,57.0633751922049));
#48672=CARTESIAN_POINT('',(-5.92550609890763,0.00223999432222687,56.8116248077954));
#48673=CARTESIAN_POINT('',(-5.91675,-7.2459289488551E-16,-10.));
#48674=CARTESIAN_POINT('Ctrl Pts',(-5.92646560327161,-0.000513552043279186,
57.0633751922049));
#48675=CARTESIAN_POINT('Ctrl Pts',(-5.92406967673236,1.93433291671647,56.971876955783));
#48676=CARTESIAN_POINT('Ctrl Pts',(-4.88666447252146,3.87138216918967,56.8803787193611));
#48677=CARTESIAN_POINT('Ctrl Pts',(-3.27387011390087,4.94018425741713,56.7888804829392));
#48678=CARTESIAN_POINT('Ctrl Pts',(-1.63831073021625,6.02407277386586,56.6960907243624));
#48679=CARTESIAN_POINT('Ctrl Pts',(0.588995993440916,6.2150300524844,56.6033009657857));
#48680=CARTESIAN_POINT('Ctrl Pts',(2.38518410246891,5.42536107713163,56.510511207209));
#48681=CARTESIAN_POINT('Ctrl Pts',(4.18137221149686,4.63569210177889,56.4177214486322));
#48682=CARTESIAN_POINT('Ctrl Pts',(5.54644170589567,2.86539687245493,56.3249316900555));
#48683=CARTESIAN_POINT('Ctrl Pts',(5.85349953287863,0.927463874506721,56.2321419314787));
#48684=CARTESIAN_POINT('Ctrl Pts',(6.16055735986159,-1.01046912344149,56.139352172902));
#48685=CARTESIAN_POINT('Ctrl Pts',(5.40960351942869,-3.11603989001394,56.0465624143252));
#48686=CARTESIAN_POINT('Ctrl Pts',(3.94550524908144,-4.42228836117639,55.9537726557485));
#48687=CARTESIAN_POINT('Ctrl Pts',(2.48140697873415,-5.72853683233887,55.8609828971717));
#48688=CARTESIAN_POINT('Ctrl Pts',(0.304164278472461,-6.2354630080913,55.7681931385949));
#48689=CARTESIAN_POINT('Ctrl Pts',(-1.58634824559367,-5.71026665433649,
55.6754033800182));
#48690=CARTESIAN_POINT('Ctrl Pts',(-3.47686076965975,-5.1850703005817,55.5826136214414));
#48691=CARTESIAN_POINT('Ctrl Pts',(-5.0806431175303,-3.62775141731974,55.4898238628647));
#48692=CARTESIAN_POINT('Ctrl Pts',(-5.66117600122224,-1.75349146080347,
55.3970341042879));
#48693=CARTESIAN_POINT('Ctrl Pts',(-5.83564478679751,-1.1902161190413,55.3691478002602));
#48694=CARTESIAN_POINT('Ctrl Pts',(-5.91769412821487,-0.598314798134851,
55.3412614962325));
#48695=CARTESIAN_POINT('Ctrl Pts',(-5.91284273101683,-0.00510202345033239,
55.3133751922048));
#48696=CARTESIAN_POINT('Ctrl Pts',(-5.9173496880968,-0.00543369097055152,
55.0616248077955));
#48697=CARTESIAN_POINT('Ctrl Pts',(-5.92142565083105,-0.444180279760379,
55.0822898403349));
#48698=CARTESIAN_POINT('Ctrl Pts',(-5.8767836491699,-0.882104937779715,
55.1029548728743));
#48699=CARTESIAN_POINT('Ctrl Pts',(-5.78031983552505,-1.30830040099209,
55.1236199054137));
#48700=CARTESIAN_POINT('Ctrl Pts',(-5.34709482638179,-3.22237083290313,
55.2164278566294));
#48701=CARTESIAN_POINT('Ctrl Pts',(-3.8686424355115,-4.89986760772403,55.3092358078451));
#48702=CARTESIAN_POINT('Ctrl Pts',(-2.02416926965118,-5.57014237771353,
55.4020437590608));
#48703=CARTESIAN_POINT('Ctrl Pts',(-0.179696103790855,-6.24041714770303,
55.4948517102765));
#48704=CARTESIAN_POINT('Ctrl Pts',(2.03079783705953,-5.90346991286125,55.5876596614922));
#48705=CARTESIAN_POINT('Ctrl Pts',(3.59180329602535,-4.71409550421518,55.6804676127079));
#48706=CARTESIAN_POINT('Ctrl Pts',(5.15280875499122,-3.52472109556908,55.7732755639237));
#48707=CARTESIAN_POINT('Ctrl Pts',(6.06432573207242,-1.48291951311867,55.8660835151394));
#48708=CARTESIAN_POINT('Ctrl Pts',(5.9075998887394,0.473297892205948,55.9588914663551));
#48709=CARTESIAN_POINT('Ctrl Pts',(5.75087404540639,2.42951529753051,56.0516994175708));
#48710=CARTESIAN_POINT('Ctrl Pts',(4.5259053816591,4.30014852572942,56.1445073687865));
#48711=CARTESIAN_POINT('Ctrl Pts',(2.79544912357091,5.22582161365339,56.2373153200022));
#48712=CARTESIAN_POINT('Ctrl Pts',(1.06499286548277,6.15149470157734,56.3301232712179));
#48713=CARTESIAN_POINT('Ctrl Pts',(-1.17095098694624,6.13220764922659,56.4229312224336));
#48714=CARTESIAN_POINT('Ctrl Pts',(-2.88518139143687,5.17682100122332,56.5157391736493));
#48715=CARTESIAN_POINT('Ctrl Pts',(-4.5994117959276,4.22143435321999,56.608547124865));
#48716=CARTESIAN_POINT('Ctrl Pts',(-5.79192875247984,2.32994810956407,56.7013550760807));
#48717=CARTESIAN_POINT('Ctrl Pts',(-5.91488547174977,0.371318187386364,
56.7941630272965));
#48718=CARTESIAN_POINT('Ctrl Pts',(-5.92259689163941,0.248479697322472,
56.7999836207961));
#48719=CARTESIAN_POINT('Ctrl Pts',(-5.92610134150221,0.12537710671222,56.8058042142958));
#48720=CARTESIAN_POINT('Ctrl Pts',(-5.92550609890763,0.00223999432222687,
56.8116248077954));
#48721=CARTESIAN_POINT('Origin',(0.,0.,-10.));
#48722=CARTESIAN_POINT('',(-5.91438778693357,0.00536108274356934,58.8133751922048));
#48723=CARTESIAN_POINT('',(-5.91049709031373,0.00433299224853631,58.5616248077954));
#48724=CARTESIAN_POINT('',(-5.91675,-7.2459289488551E-16,-10.));
#48725=CARTESIAN_POINT('Ctrl Pts',(-5.91438778693357,0.00536108274356934,
58.8133751922048));
#48726=CARTESIAN_POINT('Ctrl Pts',(-5.91910502988221,0.543269775243645,
58.788071932487));
#48727=CARTESIAN_POINT('Ctrl Pts',(-5.85179376277142,1.08001893776843,58.7627686727691));
#48728=CARTESIAN_POINT('Ctrl Pts',(-5.70776510590029,1.59532552032253,58.7374654130512));
#48729=CARTESIAN_POINT('Ctrl Pts',(-5.17959662293784,3.48500985037694,58.6446756544744));
#48730=CARTESIAN_POINT('Ctrl Pts',(-3.61975776176974,5.08634137467013,58.5518858958976));
#48731=CARTESIAN_POINT('Ctrl Pts',(-1.74458725060383,5.66392631881418,58.4590961373208));
#48732=CARTESIAN_POINT('Ctrl Pts',(0.130583260561965,6.24151126295819,58.3663063787441));
#48733=CARTESIAN_POINT('Ctrl Pts',(2.32108542172547,5.79534962695318,58.2735166201674));
#48734=CARTESIAN_POINT('Ctrl Pts',(3.82095536615163,4.53033620273401,58.1807268615907));
#48735=CARTESIAN_POINT('Ctrl Pts',(5.32082531057801,3.26532277851466,58.0879371030139));
#48736=CARTESIAN_POINT('Ctrl Pts',(6.13006303826679,1.18145756608075,57.9951473444371));
#48737=CARTESIAN_POINT('Ctrl Pts',(5.87703508174782,-0.764267405971718,
57.9023575858603));
#48738=CARTESIAN_POINT('Ctrl Pts',(5.62400712522888,-2.70999237802402,57.8095678272836));
#48739=CARTESIAN_POINT('Ctrl Pts',(4.30871348450246,-4.51757710969499,57.7167780687069));
#48740=CARTESIAN_POINT('Ctrl Pts',(2.53518820261855,-5.35690832451229,57.6239883101301));
#48741=CARTESIAN_POINT('Ctrl Pts',(0.761662920734645,-6.1962395393296,57.5311985515533));
#48742=CARTESIAN_POINT('Ctrl Pts',(-1.4700940023067,-6.06731723729321,57.4384087929765));
#48743=CARTESIAN_POINT('Ctrl Pts',(-3.13517290710431,-5.02934755833045,
57.3456190343997));
#48744=CARTESIAN_POINT('Ctrl Pts',(-4.80025181190193,-3.99137787936768,
57.252829275823));
#48745=CARTESIAN_POINT('Ctrl Pts',(-5.89865269845576,-2.04436082347857,
57.1600395172463));
#48746=CARTESIAN_POINT('Ctrl Pts',(-5.92594711987667,-0.0824424183945678,
57.0672497586696));
#48747=CARTESIAN_POINT('Ctrl Pts',(-5.92632702548814,-0.0551348671611112,
57.0659582365147));
#48748=CARTESIAN_POINT('Ctrl Pts',(-5.92649942241751,-0.0278244290443891,
57.0646667143598));
#48749=CARTESIAN_POINT('Ctrl Pts',(-5.92646560327161,-0.000513552043279186,
57.0633751922049));
#48750=CARTESIAN_POINT('Ctrl Pts',(-5.92550609890763,0.00223999432222687,
56.8116248077954));
#48751=CARTESIAN_POINT('Ctrl Pts',(-5.91661034274359,-1.83801427600624,
56.8986121655115));
#48752=CARTESIAN_POINT('Ctrl Pts',(-4.99206560383895,-3.68597883993112,
56.9855995232275));
#48753=CARTESIAN_POINT('Ctrl Pts',(-3.50994814553166,-4.77535457907361,
57.0725868809436));
#48754=CARTESIAN_POINT('Ctrl Pts',(-1.92865761805595,-5.93762382265653,
57.1653948321593));
#48755=CARTESIAN_POINT('Ctrl Pts',(0.287319918883132,-6.23638870912298,
57.258202783375));
#48756=CARTESIAN_POINT('Ctrl Pts',(2.11995602367751,-5.53439552235597,57.3510107345907));
#48757=CARTESIAN_POINT('Ctrl Pts',(3.95259212847195,-4.83240233558894,57.4438186858064));
#48758=CARTESIAN_POINT('Ctrl Pts',(5.40188680112165,-3.12965107558839,57.5366266370221));
#48759=CARTESIAN_POINT('Ctrl Pts',(5.80202860065573,-1.20839209587507,57.6294345882378));
#48760=CARTESIAN_POINT('Ctrl Pts',(6.20217040018978,0.712866883838148,57.7222425394535));
#48761=CARTESIAN_POINT('Ctrl Pts',(5.55315932660834,2.8526335832641,57.8150504906693));
#48762=CARTESIAN_POINT('Ctrl Pts',(4.15315351590817,4.22789110710056,57.907858441885));
#48763=CARTESIAN_POINT('Ctrl Pts',(2.75314770520792,5.60314863093708,58.0006663931007));
#48764=CARTESIAN_POINT('Ctrl Pts',(0.602147157388864,6.21389697918402,58.0934743443164));
#48765=CARTESIAN_POINT('Ctrl Pts',(-1.31167035990828,5.7795560562329,58.1862822955321));
#48766=CARTESIAN_POINT('Ctrl Pts',(-3.22548787720537,5.3452151332818,58.2790902467478));
#48767=CARTESIAN_POINT('Ctrl Pts',(-4.90212236398056,3.8657849391327,58.3718981979635));
#48768=CARTESIAN_POINT('Ctrl Pts',(-5.57132161087445,2.02092128703809,58.4647061491792));
#48769=CARTESIAN_POINT('Ctrl Pts',(-5.8042682226907,1.37872878754992,58.497012368718));
#48770=CARTESIAN_POINT('Ctrl Pts',(-5.91514199481682,0.692256022528799,
58.5293185882567));
#48771=CARTESIAN_POINT('Ctrl Pts',(-5.91049709031373,0.00433299224853631,
58.5616248077954));
#48772=CARTESIAN_POINT('Origin',(0.,0.,-10.));
#48773=CARTESIAN_POINT('',(-5.90751360641923,-0.00190252881137831,60.5633751922048));
#48774=CARTESIAN_POINT('',(-5.90971954504434,-0.00393376914176207,60.3116248077954));
#48775=CARTESIAN_POINT('',(-5.91675,-7.2459289488551E-16,-10.));
#48776=CARTESIAN_POINT('Ctrl Pts',(-5.90751360641923,-0.00190252881137831,
60.5633751922048));
#48777=CARTESIAN_POINT('Ctrl Pts',(-5.90433409970571,1.10460401303531,60.5114771506141));
#48778=CARTESIAN_POINT('Ctrl Pts',(-5.60641968371212,2.21269985804919,60.4595791090234));
#48779=CARTESIAN_POINT('Ctrl Pts',(-5.0244113679022,3.1430775405676,60.4076810674328));
#48780=CARTESIAN_POINT('Ctrl Pts',(-3.9838246818073,4.80652220822881,60.314891308856));
#48781=CARTESIAN_POINT('Ctrl Pts',(-2.03508282814485,5.9018601064549,60.2221015502792));
#48782=CARTESIAN_POINT('Ctrl Pts',(-0.0731239289288037,5.9260694318362,
60.1293117917025));
#48783=CARTESIAN_POINT('Ctrl Pts',(1.88883497028713,5.9502787572175,60.0365220331257));
#48784=CARTESIAN_POINT('Ctrl Pts',(3.86401091505666,4.90335950975414,59.943732274549));
#48785=CARTESIAN_POINT('Ctrl Pts',(4.94532621967354,3.26609776352986,59.8509425159722));
#48786=CARTESIAN_POINT('Ctrl Pts',(6.02664152429041,1.62883601730559,59.7581527573955));
#48787=CARTESIAN_POINT('Ctrl Pts',(6.21409618875463,-0.598768227679594,
59.6653629988187));
#48788=CARTESIAN_POINT('Ctrl Pts',(5.42160373369846,-2.39371238344798,59.5725732402419));
#48789=CARTESIAN_POINT('Ctrl Pts',(4.6291112786423,-4.18865653921637,59.4797834816652));
#48790=CARTESIAN_POINT('Ctrl Pts',(2.85667170406575,-5.55094060576796,59.3869937230885));
#48791=CARTESIAN_POINT('Ctrl Pts',(0.918258262133265,-5.85495070721773,
59.2942039645117));
#48792=CARTESIAN_POINT('Ctrl Pts',(-1.02015517979933,-6.15896080866752,
59.201414205935));
#48793=CARTESIAN_POINT('Ctrl Pts',(-3.12454248908787,-5.40469694501536,
59.1086244473581));
#48794=CARTESIAN_POINT('Ctrl Pts',(-4.42848709135374,-3.93854644528139,
59.0158346887814));
#48795=CARTESIAN_POINT('Ctrl Pts',(-5.37685313155668,-2.87220716878292,
58.9483481899225));
#48796=CARTESIAN_POINT('Ctrl Pts',(-5.90180639566545,-1.42929890839187,
58.8808616910637));
#48797=CARTESIAN_POINT('Ctrl Pts',(-5.91438778693357,0.00536108274356934,
58.8133751922048));
#48798=CARTESIAN_POINT('Ctrl Pts',(-5.91049709031373,0.00433299224853631,
58.5616248077954));
#48799=CARTESIAN_POINT('Ctrl Pts',(-5.90179830816206,-1.28398037857263,
58.6221265394724));
#48800=CARTESIAN_POINT('Ctrl Pts',(-5.48794981324838,-2.57738015247874,
58.6826282711494));
#48801=CARTESIAN_POINT('Ctrl Pts',(-4.71200052329397,-3.5945512110245,58.7431300028264));
#48802=CARTESIAN_POINT('Ctrl Pts',(-3.52171618180695,-5.15486294695242,
58.8359379540421));
#48803=CARTESIAN_POINT('Ctrl Pts',(-1.47938349182042,-6.06518930876796,
58.9287459052578));
#48804=CARTESIAN_POINT('Ctrl Pts',(0.476742202929665,-5.90732293108699,
59.0215538564735));
#48805=CARTESIAN_POINT('Ctrl Pts',(2.43286789767958,-5.74945655340603,59.1143618076892));
#48806=CARTESIAN_POINT('Ctrl Pts',(4.30278659719299,-4.52339743622863,59.2071697589049));
#48807=CARTESIAN_POINT('Ctrl Pts',(5.22745059549495,-2.79240176404826,59.2999777101206));
#48808=CARTESIAN_POINT('Ctrl Pts',(6.15211459379697,-1.06140609186779,59.3927856613363));
#48809=CARTESIAN_POINT('Ctrl Pts',(6.13152389088747,1.17452613531577,59.4855936125521));
#48810=CARTESIAN_POINT('Ctrl Pts',(5.17513793337419,2.88819921590459,59.5784015637678));
#48811=CARTESIAN_POINT('Ctrl Pts',(4.21875197586095,4.60187229649331,59.6712095149835));
#48812=CARTESIAN_POINT('Ctrl Pts',(2.326570763744,5.79328623048741,59.7640174661991));
#48813=CARTESIAN_POINT('Ctrl Pts',(0.367869485287327,5.9151009612681,59.8568254174148));
#48814=CARTESIAN_POINT('Ctrl Pts',(-1.59083179316951,6.0369156920488,59.9496333686306));
#48815=CARTESIAN_POINT('Ctrl Pts',(-3.61605313796599,5.089131219616,60.0424413198463));
#48816=CARTESIAN_POINT('Ctrl Pts',(-4.77740022190952,3.50716330670518,60.135249271062));
#48817=CARTESIAN_POINT('Ctrl Pts',(-5.51308867884712,2.50502058049953,60.1940411166398));
#48818=CARTESIAN_POINT('Ctrl Pts',(-5.90210866022388,1.24838317086696,60.2528329622176));
#48819=CARTESIAN_POINT('Ctrl Pts',(-5.90971954504434,-0.00393376914176207,
60.3116248077954));
#48820=CARTESIAN_POINT('Origin',(0.,0.,-10.));
#48821=CARTESIAN_POINT('',(-5.92138577511996,-0.00465600546497968,62.3133751922048));
#48822=CARTESIAN_POINT('',(-5.92487552954592,-0.00283239076988535,62.0616248077954));
#48823=CARTESIAN_POINT('',(-5.91675,-7.2459289488551E-16,-10.));
#48824=CARTESIAN_POINT('Ctrl Pts',(-5.92138577511996,-0.00465600546497968,
62.3133751922048));
#48825=CARTESIAN_POINT('Ctrl Pts',(-5.90702696023975,1.65892609794656,62.2348823687413));
#48826=CARTESIAN_POINT('Ctrl Pts',(-5.17355864322008,3.33359211408665,62.1563895452778));
#48827=CARTESIAN_POINT('Ctrl Pts',(-3.93157790275368,4.43467487134112,62.0778967218143));
#48828=CARTESIAN_POINT('Ctrl Pts',(-2.46337879894035,5.73631238048495,61.9851069632376));
#48829=CARTESIAN_POINT('Ctrl Pts',(-0.284552613138903,6.23638875022473,
61.8923172046609));
#48830=CARTESIAN_POINT('Ctrl Pts',(1.60429885033706,5.70524944404121,61.7995274460841));
#48831=CARTESIAN_POINT('Ctrl Pts',(3.49315031381303,5.17411013785769,61.7067376875074));
#48832=CARTESIAN_POINT('Ctrl Pts',(5.09202705496358,3.61175515575085,61.6139479289306));
#48833=CARTESIAN_POINT('Ctrl Pts',(5.66666263138229,1.73567872661414,61.5211581703538));
#48834=CARTESIAN_POINT('Ctrl Pts',(6.24129820780094,-0.140397702522356,
61.428368411777));
#48835=CARTESIAN_POINT('Ctrl Pts',(5.79169261948807,-2.3301955786887,61.3355786532003));
#48836=CARTESIAN_POINT('Ctrl Pts',(4.52432225534832,-3.82807447023764,61.2427888946235));
#48837=CARTESIAN_POINT('Ctrl Pts',(3.2569518912085,-5.32595336178667,61.1499991360468));
#48838=CARTESIAN_POINT('Ctrl Pts',(1.17181675124172,-6.13191326871823,61.05720937747));
#48839=CARTESIAN_POINT('Ctrl Pts',(-0.773507935796127,-5.87582602645669,
60.9644196188933));
#48840=CARTESIAN_POINT('Ctrl Pts',(-2.71883262283403,-5.61973878419514,
60.8716298603165));
#48841=CARTESIAN_POINT('Ctrl Pts',(-4.52434685694288,-4.30160439274053,
60.7788401017398));
#48842=CARTESIAN_POINT('Ctrl Pts',(-5.36088821473366,-2.52676147846508,
60.686050343163));
#48843=CARTESIAN_POINT('Ctrl Pts',(-5.72954541327163,-1.74460216197929,
60.645158626177));
#48844=CARTESIAN_POINT('Ctrl Pts',(-5.91001881634045,-0.873745684460358,
60.6042669091909));
#48845=CARTESIAN_POINT('Ctrl Pts',(-5.90751360641923,-0.00190252881137831,
60.5633751922048));
#48846=CARTESIAN_POINT('Ctrl Pts',(-5.90971954504434,-0.00393376914176207,
60.3116248077954));
#48847=CARTESIAN_POINT('Ctrl Pts',(-5.91412309216056,-0.728506112548232,
60.3456409134333));
#48848=CARTESIAN_POINT('Ctrl Pts',(-5.79084570775551,-1.45163213075908,
60.3796570190712));
#48849=CARTESIAN_POINT('Ctrl Pts',(-5.533158553854,-2.12318245992016,60.4136731247091));
#48850=CARTESIAN_POINT('Ctrl Pts',(-4.83009697876454,-3.95540896024582,
60.5064810759248));
#48851=CARTESIAN_POINT('Ctrl Pts',(-3.12650100549514,-5.40371060750862,
60.5992890271406));
#48852=CARTESIAN_POINT('Ctrl Pts',(-1.2050090520295,-5.80273216034717,60.6920969783563));
#48853=CARTESIAN_POINT('Ctrl Pts',(0.716482901436298,-6.20175371318575,
60.784904929572));
#48854=CARTESIAN_POINT('Ctrl Pts',(2.85587083509837,-5.55149517160003,60.8777128807877));
#48855=CARTESIAN_POINT('Ctrl Pts',(4.23031186007554,-4.15068776309476,60.9705208320034));
#48856=CARTESIAN_POINT('Ctrl Pts',(5.60475288505267,-2.74988035458953,61.0633287832191));
#48857=CARTESIAN_POINT('Ctrl Pts',(6.21424700134487,-0.598524079164734,
61.1561367344349));
#48858=CARTESIAN_POINT('Ctrl Pts',(5.77879031223601,1.31503987293452,61.2489446856506));
#48859=CARTESIAN_POINT('Ctrl Pts',(5.34333362312715,3.22860382503377,61.3417526368663));
#48860=CARTESIAN_POINT('Ctrl Pts',(3.86292612861721,4.90437545380759,61.434560588082));
#48861=CARTESIAN_POINT('Ctrl Pts',(2.01767261743198,5.57249895011794,61.5273685392977));
#48862=CARTESIAN_POINT('Ctrl Pts',(0.172419106246808,6.24062244642827,61.6201764905134));
#48863=CARTESIAN_POINT('Ctrl Pts',(-2.03768042161353,5.90109781027533,61.7129844417291));
#48864=CARTESIAN_POINT('Ctrl Pts',(-3.59729790409035,4.70990394057326,61.8057923929448));
#48865=CARTESIAN_POINT('Ctrl Pts',(-5.03036731089132,3.61536408614182,61.8910698645617));
#48866=CARTESIAN_POINT('Ctrl Pts',(-5.9142328668594,1.80175746265739,61.9763473361785));
#48867=CARTESIAN_POINT('Ctrl Pts',(-5.92487552954592,-0.00283239076988535,
62.0616248077954));
#48868=CARTESIAN_POINT('Origin',(0.,0.,-10.));
#48869=CARTESIAN_POINT('',(-5.92254374065673,0.00421469164317803,64.0633751922048));
#48870=CARTESIAN_POINT('',(-5.9184608786744,0.00532413147862563,63.8116248077953));
#48871=CARTESIAN_POINT('',(-5.91675,-7.2459289488551E-16,-10.));
#48872=CARTESIAN_POINT('Ctrl Pts',(-5.92254374065673,0.00421469164317803,
64.0633751922048));
#48873=CARTESIAN_POINT('Ctrl Pts',(-5.92464260024143,0.264723398301747,
64.0510773454453));
#48874=CARTESIAN_POINT('Ctrl Pts',(-5.90894822076181,0.524977554909748,
64.0387794986858));
#48875=CARTESIAN_POINT('Ctrl Pts',(-5.87460244218337,0.782746552990558,
64.0264816519262));
#48876=CARTESIAN_POINT('Ctrl Pts',(-5.61545654739851,2.72766614486684,63.9336918933495));
#48877=CARTESIAN_POINT('Ctrl Pts',(-4.29448466452766,4.53110541697169,63.8409021347727));
#48878=CARTESIAN_POINT('Ctrl Pts',(-2.51832850646255,5.36485484924461,63.748112376196));
#48879=CARTESIAN_POINT('Ctrl Pts',(-0.742172348397438,6.19860428151754,
63.6553226176192));
#48880=CARTESIAN_POINT('Ctrl Pts',(1.48916808486193,6.06266387395855,63.5625328590425));
#48881=CARTESIAN_POINT('Ctrl Pts',(3.15097440223581,5.01946275375961,63.4697431004657));
#48882=CARTESIAN_POINT('Ctrl Pts',(4.81278071960959,3.97626163356074,63.376953341889));
#48883=CARTESIAN_POINT('Ctrl Pts',(5.90505292109795,2.02579980072203,63.2841635833122));
#48884=CARTESIAN_POINT('Ctrl Pts',(5.92617709057818,0.063805258652316,63.1913738247354));
#48885=CARTESIAN_POINT('Ctrl Pts',(5.94730126005842,-1.89818928341785,63.0985840661587));
#48886=CARTESIAN_POINT('Ctrl Pts',(4.89727739752999,-3.87171653471903,63.0057943075819));
#48887=CARTESIAN_POINT('Ctrl Pts',(3.2583173371746,-4.95045595376757,62.9130045490052));
#48888=CARTESIAN_POINT('Ctrl Pts',(1.61935727681958,-6.02919537281587,62.8202147904284));
#48889=CARTESIAN_POINT('Ctrl Pts',(-0.608538981362105,-6.21314695961199,
62.7274250318516));
#48890=CARTESIAN_POINT('Ctrl Pts',(-2.40223474556518,-5.41783298442511,
62.6346352732749));
#48891=CARTESIAN_POINT('Ctrl Pts',(-4.19593050976836,-4.62251900923819,
62.5418455146981));
#48892=CARTESIAN_POINT('Ctrl Pts',(-5.55542577999287,-2.84793947206817,
62.4490557561214));
#48893=CARTESIAN_POINT('Ctrl Pts',(-5.85638740419252,-0.909050379209287,
62.3562659975446));
#48894=CARTESIAN_POINT('Ctrl Pts',(-5.90275921158555,-0.610308664847524,
62.3419690624314));
#48895=CARTESIAN_POINT('Ctrl Pts',(-5.9240011358063,-0.30766619593341,62.3276721273181));
#48896=CARTESIAN_POINT('Ctrl Pts',(-5.92138577511996,-0.00465600546497968,
62.3133751922048));
#48897=CARTESIAN_POINT('Ctrl Pts',(-5.92487552954592,-0.00283239076988535,
62.0616248077954));
#48898=CARTESIAN_POINT('Ctrl Pts',(-5.92581533642245,-0.162187808066437,
62.0691552873942));
#48899=CARTESIAN_POINT('Ctrl Pts',(-5.91994585449146,-0.3214729136569,62.0766857669931));
#48900=CARTESIAN_POINT('Ctrl Pts',(-5.90704396529663,-0.480186351589765,
62.0842162465919));
#48901=CARTESIAN_POINT('Ctrl Pts',(-5.74803710693276,-2.43621967079874,
62.1770241978076));
#48902=CARTESIAN_POINT('Ctrl Pts',(-4.52088795311218,-4.30542320596569,
62.2698321490233));
#48903=CARTESIAN_POINT('Ctrl Pts',(-2.78935345527504,-5.22907780031484,
62.3626401002391));
#48904=CARTESIAN_POINT('Ctrl Pts',(-1.05781895743761,-6.15273239466415,
62.4554480514548));
#48905=CARTESIAN_POINT('Ctrl Pts',(1.17810088441637,-6.13083804819549,62.5482560026705));
#48906=CARTESIAN_POINT('Ctrl Pts',(2.89121605855662,-5.17345310628643,62.6410639538862));
#48907=CARTESIAN_POINT('Ctrl Pts',(4.60433123269666,-4.21606816437748,62.7338719051019));
#48908=CARTESIAN_POINT('Ctrl Pts',(5.79464173912287,-2.32319262702822,62.8266798563176));
#48909=CARTESIAN_POINT('Ctrl Pts',(5.91531444000447,-0.364420658134239,
62.9194878075333));
#48910=CARTESIAN_POINT('Ctrl Pts',(6.03598714088608,1.59435131075997,63.012295758749));
#48911=CARTESIAN_POINT('Ctrl Pts',(5.08702203622284,3.61901971119909,63.1051037099647));
#48912=CARTESIAN_POINT('Ctrl Pts',(3.50437727565169,4.77944424071423,63.1979116611804));
#48913=CARTESIAN_POINT('Ctrl Pts',(1.92173251508063,5.93986877022931,63.2907196123961));
#48914=CARTESIAN_POINT('Ctrl Pts',(-0.294591901398011,6.23604942882064,
63.3835275636119));
#48915=CARTESIAN_POINT('Ctrl Pts',(-2.12640817440725,5.53191970440772,63.4763355148276));
#48916=CARTESIAN_POINT('Ctrl Pts',(-3.95822444741638,4.82778997999483,63.5691434660433));
#48917=CARTESIAN_POINT('Ctrl Pts',(-5.40553257695601,3.12334987257762,63.661951417259));
#48918=CARTESIAN_POINT('Ctrl Pts',(-5.80343374745539,1.20162559855231,63.7547593684747));
#48919=CARTESIAN_POINT('Ctrl Pts',(-5.88470129896102,0.809131587481785,
63.7737145149149));
#48920=CARTESIAN_POINT('Ctrl Pts',(-5.92219367890825,0.407573741272489,
63.7926696613551));
#48921=CARTESIAN_POINT('Ctrl Pts',(-5.9184608786744,0.00532413147862563,
63.8116248077953));
#48922=CARTESIAN_POINT('Origin',(0.,0.,-10.));
#48923=CARTESIAN_POINT('',(-5.90799290133436,0.00254793967829986,65.8133751922048));
#48924=CARTESIAN_POINT('',(-5.90695594955463,0.000339959333261384,65.5616248077954));
#48925=CARTESIAN_POINT('',(-5.91675,-7.2459289488551E-16,-10.));
#48926=CARTESIAN_POINT('Ctrl Pts',(-5.90799290133436,0.00254793967829986,
65.8133751922048));
#48927=CARTESIAN_POINT('Ctrl Pts',(-5.91119872342175,0.8316010093993,65.7744825635725));
#48928=CARTESIAN_POINT('Ctrl Pts',(-5.7485847983095,1.65945254838475,65.7355899349402));
#48929=CARTESIAN_POINT('Ctrl Pts',(-5.41404883863568,2.41075116774689,65.6966973063079));
#48930=CARTESIAN_POINT('Ctrl Pts',(-4.61591530986757,4.20319410516615,65.6039075477311));
#48931=CARTESIAN_POINT('Ctrl Pts',(-2.83920019805476,5.55989721747976,65.5111177891543));
#48932=CARTESIAN_POINT('Ctrl Pts',(-0.899840248503511,5.85780962025043,
65.4183280305776));
#48933=CARTESIAN_POINT('Ctrl Pts',(1.03951970104785,6.15572202302112,65.3255382720008));
#48934=CARTESIAN_POINT('Ctrl Pts',(3.14152448833767,5.39484371624875,65.2327485134241));
#48935=CARTESIAN_POINT('Ctrl Pts',(4.44085168583864,3.92459963872871,65.1399587548473));
#48936=CARTESIAN_POINT('Ctrl Pts',(5.74017888333953,2.45435556120876,65.0471689962706));
#48937=CARTESIAN_POINT('Ctrl Pts',(6.23682849105167,0.274745712941213,64.9543792376938));
#48938=CARTESIAN_POINT('Ctrl Pts',(5.70271967497977,-1.61326821344872,64.861589479117));
#48939=CARTESIAN_POINT('Ctrl Pts',(5.1686108589079,-3.50128213983854,64.7687997205403));
#48940=CARTESIAN_POINT('Ctrl Pts',(3.60374361905212,-5.09770014435078,64.6760099619635));
#48941=CARTESIAN_POINT('Ctrl Pts',(1.72676591086401,-5.66938493216004,64.5832202033868));
#48942=CARTESIAN_POINT('Ctrl Pts',(-0.150211797324312,-6.24106971996937,
64.49043044481));
#48943=CARTESIAN_POINT('Ctrl Pts',(-2.33929997384504,-5.78802129107543,
64.3976406862333));
#48944=CARTESIAN_POINT('Ctrl Pts',(-3.83518410875603,-4.51829712080455,
64.3048509276565));
#48945=CARTESIAN_POINT('Ctrl Pts',(-5.13281194746251,-3.41685524280773,
64.2243590158393));
#48946=CARTESIAN_POINT('Ctrl Pts',(-5.90880627718756,-1.7008678528067,64.1438671040221));
#48947=CARTESIAN_POINT('Ctrl Pts',(-5.92254374065673,0.00421469164317803,
64.0633751922048));
#48948=CARTESIAN_POINT('Ctrl Pts',(-5.9184608786744,0.00532413147862563,
63.8116248077953));
#48949=CARTESIAN_POINT('Ctrl Pts',(-5.90391718903288,-1.56191577335664,
63.8854776125708));
#48950=CARTESIAN_POINT('Ctrl Pts',(-5.26356384080163,-3.1396568410927,63.9593304173463));
#48951=CARTESIAN_POINT('Ctrl Pts',(-4.14822059929475,-4.23273117499648,
64.0331832221218));
#48952=CARTESIAN_POINT('Ctrl Pts',(-2.74661206917558,-5.60635523388617,
64.1259911733375));
#48953=CARTESIAN_POINT('Ctrl Pts',(-0.594900797478113,-6.21459491103191,
64.2187991245533));
#48954=CARTESIAN_POINT('Ctrl Pts',(1.31840893892553,-5.77802260379462,64.311607075769));
#48955=CARTESIAN_POINT('Ctrl Pts',(3.23171867532906,-5.34145029655737,64.4044150269847));
#48956=CARTESIAN_POINT('Ctrl Pts',(4.90662687643879,-3.86006600493721,64.4972229782003));
#48957=CARTESIAN_POINT('Ctrl Pts',(5.57367439504355,-2.01442326193784,64.590030929416));
#48958=CARTESIAN_POINT('Ctrl Pts',(6.24072191364835,-0.168780518938366,
64.6828388806317));
#48959=CARTESIAN_POINT('Ctrl Pts',(5.89990874974806,2.04112067544036,64.7756468318475));
#48960=CARTESIAN_POINT('Ctrl Pts',(4.70780575676577,3.60004337428919,64.8684547830633));
#48961=CARTESIAN_POINT('Ctrl Pts',(3.51570276378348,5.15896607313801,64.961262734279));
#48962=CARTESIAN_POINT('Ctrl Pts',(1.47230994171919,6.06691027645692,65.0540706854946));
#48963=CARTESIAN_POINT('Ctrl Pts',(-0.48363033701444,5.90676299146323,65.1468786367103));
#48964=CARTESIAN_POINT('Ctrl Pts',(-2.43957061574796,5.74661570646955,65.239686587926));
#48965=CARTESIAN_POINT('Ctrl Pts',(-4.30805835115084,4.51837693316338,65.3324945391418));
#48966=CARTESIAN_POINT('Ctrl Pts',(-5.23070322755976,2.7863041982878,65.4253024903575));
#48967=CARTESIAN_POINT('Ctrl Pts',(-5.68245003760025,1.93824406947249,65.4707432628368));
#48968=CARTESIAN_POINT('Ctrl Pts',(-5.90745064133749,0.969400199144218,
65.5161840353161));
#48969=CARTESIAN_POINT('Ctrl Pts',(-5.90695594955463,0.000339959333261384,
65.5616248077954));
#48970=CARTESIAN_POINT('Origin',(0.,0.,-10.));
#48971=CARTESIAN_POINT('',(-5.91318264661351,-0.00517381203793132,67.5633751922048));
#48972=CARTESIAN_POINT('',(-5.91720892724047,-0.00544236320477147,67.3116248077954));
#48973=CARTESIAN_POINT('',(-5.91675,-7.2459289488551E-16,-10.));
#48974=CARTESIAN_POINT('Ctrl Pts',(-5.91318264661351,-0.00517381203793133,
67.5633751922048));
#48975=CARTESIAN_POINT('Ctrl Pts',(-5.90158111533912,1.3877078186906,67.4978877816997));
#48976=CARTESIAN_POINT('Ctrl Pts',(-5.4100418655732,2.78795772811743,67.4324003711946));
#48977=CARTESIAN_POINT('Ctrl Pts',(-4.51226081400018,3.84228426412776,67.3669129606895));
#48978=CARTESIAN_POINT('Ctrl Pts',(-3.24018597720788,5.33616994357178,67.2741232021127));
#48979=CARTESIAN_POINT('Ctrl Pts',(-1.15252645285901,6.13556823847911,67.1813334435359));
#48980=CARTESIAN_POINT('Ctrl Pts',(0.791983234710277,5.87336433195347,67.0885436849592));
#48981=CARTESIAN_POINT('Ctrl Pts',(2.73649292227957,5.61116042542782,66.9957539263824));
#48982=CARTESIAN_POINT('Ctrl Pts',(4.53785277306916,4.28735431746923,66.9029641678057));
#48983=CARTESIAN_POINT('Ctrl Pts',(5.36880821823668,2.50988930746351,66.8101744092289));
#48984=CARTESIAN_POINT('Ctrl Pts',(6.19976366340414,0.732424297457894,66.7173846506522));
#48985=CARTESIAN_POINT('Ctrl Pts',(6.0603147029495,-1.498699614595,66.6245948920754));
#48986=CARTESIAN_POINT('Ctrl Pts',(5.01450172813933,-3.15886347258204,66.5318051334987));
#48987=CARTESIAN_POINT('Ctrl Pts',(3.96868875332904,-4.81902733056926,66.4390153749219));
#48988=CARTESIAN_POINT('Ctrl Pts',(2.01651176416312,-5.90823113449073,66.3462256163452));
#48989=CARTESIAN_POINT('Ctrl Pts',(0.0544864306054393,-5.92627009583644,
66.2534358577684));
#48990=CARTESIAN_POINT('Ctrl Pts',(-1.90753890295213,-5.94430905718215,
66.1606460991917));
#48991=CARTESIAN_POINT('Ctrl Pts',(-3.87941258090134,-4.89118317595221,
66.0678563406149));
#48992=CARTESIAN_POINT('Ctrl Pts',(-4.95557344701427,-3.25052885407475,
65.9750665820381));
#48993=CARTESIAN_POINT('Ctrl Pts',(-5.58066379029856,-2.29755127835456,
65.9211694520937));
#48994=CARTESIAN_POINT('Ctrl Pts',(-5.9035502957379,-1.14634794627538,65.8672723221492));
#48995=CARTESIAN_POINT('Ctrl Pts',(-5.90799290133436,0.00254793967829986,
65.8133751922048));
#48996=CARTESIAN_POINT('Ctrl Pts',(-5.90695594955463,0.000339959333261384,
65.5616248077954));
#48997=CARTESIAN_POINT('Ctrl Pts',(-5.90644028591556,-1.00980241019597,
65.6089919865318));
#48998=CARTESIAN_POINT('Ctrl Pts',(-5.66090486185914,-2.02017988351609,
65.6563591652682));
#48999=CARTESIAN_POINT('Ctrl Pts',(-5.17176652053277,-2.8942319183674,65.7037263440046));
#49000=CARTESIAN_POINT('Ctrl Pts',(-4.21338291968193,-4.60678860370172,
65.7965342952203));
#49001=CARTESIAN_POINT('Ctrl Pts',(-2.31981370056542,-5.79599527792531,
65.8893422464361));
#49002=CARTESIAN_POINT('Ctrl Pts',(-0.360971707099837,-5.91552590788628,
65.9821501976517));
#49003=CARTESIAN_POINT('Ctrl Pts',(1.59787028636575,-6.03505653784725,66.0749581488675));
#49004=CARTESIAN_POINT('Ctrl Pts',(3.62198505418061,-5.08491112354539,66.1677661000831));
#49005=CARTESIAN_POINT('Ctrl Pts',(4.7814866347922,-3.5015900533192,66.2605740512988));
#49006=CARTESIAN_POINT('Ctrl Pts',(5.94098821540385,-1.91826898309292,66.3533820025146));
#49007=CARTESIAN_POINT('Ctrl Pts',(6.23587660881247,0.298227743057843,66.4461899537303));
#49008=CARTESIAN_POINT('Ctrl Pts',(5.53067897443825,2.12963316604222,66.538997904946));
#49009=CARTESIAN_POINT('Ctrl Pts',(4.82548134006407,3.96103858902649,66.6318058561617));
#49010=CARTESIAN_POINT('Ctrl Pts',(3.12019767790724,5.40735270884429,66.7246138073774));
#49011=CARTESIAN_POINT('Ctrl Pts',(1.19824173659399,5.80413336174183,66.8174217585931));
#49012=CARTESIAN_POINT('Ctrl Pts',(-0.723714204719369,6.2009140146394,66.9102297098088));
#49013=CARTESIAN_POINT('Ctrl Pts',(-2.86234242518905,5.54816120061654,67.0030376610246));
#49014=CARTESIAN_POINT('Ctrl Pts',(-4.23514905104094,4.14575202534684,67.0958456122403));
#49015=CARTESIAN_POINT('Ctrl Pts',(-5.29907768179141,3.05888134341762,67.1677720107587));
#49016=CARTESIAN_POINT('Ctrl Pts',(-5.90303169463259,1.52174535067564,67.239698409277));
#49017=CARTESIAN_POINT('Ctrl Pts',(-5.91720892724047,-0.00544236320477147,
67.3116248077954));
#49018=CARTESIAN_POINT('Origin',(0.,0.,-10.));
#49019=CARTESIAN_POINT('',(-5.92650388951378,-0.000281712456556837,69.3133751922048));
#49020=CARTESIAN_POINT('',(-5.92557665873441,0.00216209314576762,69.0616248077954));
#49021=CARTESIAN_POINT('',(-5.91675,-7.2459289488551E-16,-10.));
#49022=CARTESIAN_POINT('Ctrl Pts',(-5.92650388951378,-0.000281712456556837,
69.3133751922048));
#49023=CARTESIAN_POINT('Ctrl Pts',(-5.92515963032167,1.94687933134679,69.2212929998269));
#49024=CARTESIAN_POINT('Ctrl Pts',(-4.87255319916288,3.89528559185528,69.129210807449));
#49025=CARTESIAN_POINT('Ctrl Pts',(-3.24273233348756,4.96067868676048,69.0371286150711));
#49026=CARTESIAN_POINT('Ctrl Pts',(-1.60038780688532,6.0342583389466,68.9443388564943));
#49027=CARTESIAN_POINT('Ctrl Pts',(0.628075950420943,6.21120241451497,68.8515490979176));
#49028=CARTESIAN_POINT('Ctrl Pts',(2.41926162893542,5.41025130568684,68.7587593393408));
#49029=CARTESIAN_POINT('Ctrl Pts',(4.21044730744979,4.60930019685875,68.6659695807641));
#49030=CARTESIAN_POINT('Ctrl Pts',(5.56435490717254,2.83045390363422,68.5731798221873));
#49031=CARTESIAN_POINT('Ctrl Pts',(5.85921735187489,0.890627892788898,68.4803900636105));
#49032=CARTESIAN_POINT('Ctrl Pts',(6.15407979657726,-1.04919811805653,68.3876003050338));
#49033=CARTESIAN_POINT('Ctrl Pts',(5.3898970862593,-3.15000384652261,68.294810546457));
#49034=CARTESIAN_POINT('Ctrl Pts',(3.91761167046192,-4.44701751957263,68.2020207878803));
#49035=CARTESIAN_POINT('Ctrl Pts',(2.44532625466471,-5.7440311926225,68.1092310293035));
#49036=CARTESIAN_POINT('Ctrl Pts',(0.26493813338821,-6.23725281025625,68.0164412707268));
#49037=CARTESIAN_POINT('Ctrl Pts',(-1.62223358747919,-5.70017580497126,
67.92365151215));
#49038=CARTESIAN_POINT('Ctrl Pts',(-3.5094053083468,-5.16309879968621,67.8308617535733));
#49039=CARTESIAN_POINT('Ctrl Pts',(-5.10336062880535,-3.5957231714821,67.7380719949965));
#49040=CARTESIAN_POINT('Ctrl Pts',(-5.67209321441677,-1.71784882538965,
67.6452822364198));
#49041=CARTESIAN_POINT('Ctrl Pts',(-5.83943641317296,-1.16530531392642,
67.6179798883481));
#49042=CARTESIAN_POINT('Ctrl Pts',(-5.91801943955699,-0.585879917401179,
67.5906775402765));
#49043=CARTESIAN_POINT('Ctrl Pts',(-5.91318264661351,-0.00517381203793133,
67.5633751922048));
#49044=CARTESIAN_POINT('Ctrl Pts',(-5.91720892724047,-0.00544236320477147,
67.3116248077954));
#49045=CARTESIAN_POINT('Ctrl Pts',(-5.92132483789222,-0.44881296680819,
67.3325063604927));
#49046=CARTESIAN_POINT('Ctrl Pts',(-5.87573156645681,-0.891345082322613,
67.3533879131901));
#49047=CARTESIAN_POINT('Ctrl Pts',(-5.77725293116981,-1.3217775567357,67.3742694658874));
#49048=CARTESIAN_POINT('Ctrl Pts',(-5.33956515421279,-3.23483242703241,
67.4670774171031));
#49049=CARTESIAN_POINT('Ctrl Pts',(-3.85720456906464,-4.90887663110927,
67.5598853683188));
#49050=CARTESIAN_POINT('Ctrl Pts',(-2.01117322165947,-5.57484794525198,
67.6526933195345));
#49051=CARTESIAN_POINT('Ctrl Pts',(-0.165141874254405,-6.24081925939465,
67.7455012707502));
#49052=CARTESIAN_POINT('Ctrl Pts',(2.04456023540753,-5.89871768360324,67.8383092219659));
#49053=CARTESIAN_POINT('Ctrl Pts',(3.60278762068745,-4.70570597258494,67.9311171731817));
#49054=CARTESIAN_POINT('Ctrl Pts',(5.16101500596746,-3.51269426156657,68.0239251243974));
#49055=CARTESIAN_POINT('Ctrl Pts',(6.06776766686524,-1.46877241532123,68.1167330756131));
#49056=CARTESIAN_POINT('Ctrl Pts',(5.90648000968226,0.487074158033609,68.2095410268288));
#49057=CARTESIAN_POINT('Ctrl Pts',(5.74519235249929,2.44292073138834,68.3023489780444));
#49058=CARTESIAN_POINT('Ctrl Pts',(4.51586437723545,4.31069203185281,68.3951569292602));
#49059=CARTESIAN_POINT('Ctrl Pts',(2.78325399412311,5.23232687667715,68.4879648804759));
#49060=CARTESIAN_POINT('Ctrl Pts',(1.05064361101067,6.15396172150155,68.5807728316916));
#49061=CARTESIAN_POINT('Ctrl Pts',(-1.18524917995037,6.129460110686,68.6735807829073));
#49062=CARTESIAN_POINT('Ctrl Pts',(-2.89724679431174,5.17007817668657,68.7663887341231));
#49063=CARTESIAN_POINT('Ctrl Pts',(-4.60924440867302,4.21069624268719,68.8591966853388));
#49064=CARTESIAN_POINT('Ctrl Pts',(-5.7973468464346,2.31643398550408,68.9520046365544));
#49065=CARTESIAN_POINT('Ctrl Pts',(-5.91573536484165,0.357522633356556,
69.0448125877702));
#49066=CARTESIAN_POINT('Ctrl Pts',(-5.92288408358054,0.239236616440886,
69.0504166611119));
#49067=CARTESIAN_POINT('Ctrl Pts',(-5.92613244049811,0.120714877752119,
69.0560207344536));
#49068=CARTESIAN_POINT('Ctrl Pts',(-5.92557665873441,0.00216209314576762,
69.0616248077954));
#49069=CARTESIAN_POINT('Origin',(0.,0.,-10.));
#49070=CARTESIAN_POINT('',(-5.91402970906047,0.00531590772330143,71.0633751922048));
#49071=CARTESIAN_POINT('',(-5.91060120235062,0.00437987123653664,70.8116248077954));
#49072=CARTESIAN_POINT('',(-5.91675,-7.2459289488551E-16,-10.));
#49073=CARTESIAN_POINT('Ctrl Pts',(-5.91402970906047,0.00531590772330143,
71.0633751922048));
#49074=CARTESIAN_POINT('Ctrl Pts',(-5.91879269344977,0.555723161917816,
71.0374879765309));
#49075=CARTESIAN_POINT('Ctrl Pts',(-5.84828352000433,1.10493322756756,71.0116007608569));
#49076=CARTESIAN_POINT('Ctrl Pts',(-5.69761784030547,1.63119495026137,70.985713545183));
#49077=CARTESIAN_POINT('Ctrl Pts',(-5.15757397382148,3.5175197992524,70.8929237866062));
#49078=CARTESIAN_POINT('Ctrl Pts',(-3.5876938328729,5.10900849433029,70.8001340280294));
#49079=CARTESIAN_POINT('Ctrl Pts',(-1.70892749224105,5.67478747145548,70.7073442694526));
#49080=CARTESIAN_POINT('Ctrl Pts',(0.16983884839081,6.24056644858066,70.6145545108759));
#49081=CARTESIAN_POINT('Ctrl Pts',(2.35749138870594,5.78063570775315,70.5217647522992));
#49082=CARTESIAN_POINT('Ctrl Pts',(3.84937491879597,4.50621334986148,70.4289749937224));
#49083=CARTESIAN_POINT('Ctrl Pts',(5.341258448886,3.23179099196982,70.3361852351457));
#49084=CARTESIAN_POINT('Ctrl Pts',(6.13737296875093,1.14287701701401,70.2433954765689));
#49085=CARTESIAN_POINT('Ctrl Pts',(5.87211169882839,-0.801217958116352,
70.1506057179922));
#49086=CARTESIAN_POINT('Ctrl Pts',(5.60685042890584,-2.74531293324682,70.0578159594154));
#49087=CARTESIAN_POINT('Ctrl Pts',(4.28021336919569,-4.54458890855182,69.9650262008387));
#49088=CARTESIAN_POINT('Ctrl Pts',(2.50144390233472,-5.37274831193476,69.8722364422619));
#49089=CARTESIAN_POINT('Ctrl Pts',(0.722674435473843,-6.20090771531765,
69.7794466836851));
#49090=CARTESIAN_POINT('Ctrl Pts',(-1.50822743853782,-6.05795054677859,
69.6866569251084));
#49091=CARTESIAN_POINT('Ctrl Pts',(-3.16674473209977,-5.00952830330798,
69.5938671665316));
#49092=CARTESIAN_POINT('Ctrl Pts',(-4.82526202566182,-3.9611060598373,69.5010774079548));
#49093=CARTESIAN_POINT('Ctrl Pts',(-5.91139473877411,-2.00721874143496,
69.4082876493781));
#49094=CARTESIAN_POINT('Ctrl Pts',(-5.92634844738098,-0.0451674678319083,
69.3154978908013));
#49095=CARTESIAN_POINT('Ctrl Pts',(-5.9264624765467,-0.0302058903593066,
69.3147903246025));
#49096=CARTESIAN_POINT('Ctrl Pts',(-5.92651421889824,-0.0152438381698188,
69.3140827584037));
#49097=CARTESIAN_POINT('Ctrl Pts',(-5.92650388951378,-0.000281712456556837,
69.3133751922048));
#49098=CARTESIAN_POINT('Ctrl Pts',(-5.92557665873441,0.00216209314576762,
69.0616248077954));
#49099=CARTESIAN_POINT('Ctrl Pts',(-5.91692824853526,-1.84261436140608,
69.1488286856693));
#49100=CARTESIAN_POINT('Ctrl Pts',(-4.98715113358366,-3.69490823008142,
69.2360325635433));
#49101=CARTESIAN_POINT('Ctrl Pts',(-3.4988016406544,-4.78352740344972,69.3232364414173));
#49102=CARTESIAN_POINT('Ctrl Pts',(-1.91480479900762,-5.94210564099642,
69.416044392633));
#49103=CARTESIAN_POINT('Ctrl Pts',(0.301863483338378,-6.23570166897768,
69.5088523438488));
#49104=CARTESIAN_POINT('Ctrl Pts',(2.13285743372907,-5.52943636436726,69.6016602950645));
#49105=CARTESIAN_POINT('Ctrl Pts',(3.96385138411946,-4.82317105975695,69.6944682462802));
#49106=CARTESIAN_POINT('Ctrl Pts',(5.4091710025548,-3.11704442255529,69.7872761974958));
#49107=CARTESIAN_POINT('Ctrl Pts',(5.80483100296866,-1.19485746730486,69.8800841487115));
#49108=CARTESIAN_POINT('Ctrl Pts',(6.20049100338259,0.727329487945907,69.9728920999272));
#49109=CARTESIAN_POINT('Ctrl Pts',(5.54649138577485,2.86557676124536,70.065700051143));
#49110=CARTESIAN_POINT('Ctrl Pts',(4.14328204209017,4.237565487387,70.1585080023588));
#49111=CARTESIAN_POINT('Ctrl Pts',(2.74007269840573,5.60955421352841,70.2513159535744));
#49112=CARTESIAN_POINT('Ctrl Pts',(0.587653628644554,6.21528439251203,70.34412390479));
#49113=CARTESIAN_POINT('Ctrl Pts',(-1.32514572522024,5.77648129462313,70.4369318560057));
#49114=CARTESIAN_POINT('Ctrl Pts',(-3.23794507908537,5.33767819673415,70.5297398072214));
#49115=CARTESIAN_POINT('Ctrl Pts',(-4.91112471705413,3.85434182197222,70.6225477584372));
#49116=CARTESIAN_POINT('Ctrl Pts',(-5.57601960034418,2.007922497702,70.715355709653));
#49117=CARTESIAN_POINT('Ctrl Pts',(-5.80591667969058,1.3694961530774,70.7474454090338));
#49118=CARTESIAN_POINT('Ctrl Pts',(-5.91527016750582,0.687662107846013,
70.7795351084146));
#49119=CARTESIAN_POINT('Ctrl Pts',(-5.91060120235062,0.00437987123653664,
70.8116248077954));
#49120=CARTESIAN_POINT('Origin',(0.,0.,-10.));
#49121=CARTESIAN_POINT('',(-5.9076390082336,-0.00209472984356585,72.8133751922048));
#49122=CARTESIAN_POINT('',(-5.9096269619093,-0.0038796998163677,72.5616248077954));
#49123=CARTESIAN_POINT('',(-5.91675,-7.2459289488551E-16,-10.));
#49124=CARTESIAN_POINT('Ctrl Pts',(-5.9076390082336,-0.00209472984356585,
72.8133751922048));
#49125=CARTESIAN_POINT('Ctrl Pts',(-5.90409465572661,1.11680292108456,72.760893194658));
#49126=CARTESIAN_POINT('Ctrl Pts',(-5.59900569561517,2.23749243052354,72.7084111971113));
#49127=CARTESIAN_POINT('Ctrl Pts',(-5.00454249156355,3.17461816130069,72.6559291995646));
#49128=CARTESIAN_POINT('Ctrl Pts',(-3.95351357183546,4.83148478947064,72.5631394409879));
#49129=CARTESIAN_POINT('Ctrl Pts',(-1.99792075551665,5.91454372612539,72.4703496824111));
#49130=CARTESIAN_POINT('Ctrl Pts',(-0.035848393374774,5.92641214501808,
72.3775599238344));
#49131=CARTESIAN_POINT('Ctrl Pts',(1.92622396876722,5.93828056391078,72.2847701652576));
#49132=CARTESIAN_POINT('Ctrl Pts',(3.89477587673228,4.87895846504129,72.1919804066808));
#49133=CARTESIAN_POINT('Ctrl Pts',(4.96577166038264,3.23492779469125,72.099190648104));
#49134=CARTESIAN_POINT('Ctrl Pts',(6.03676744403288,1.59089712434139,72.0064008895273));
#49135=CARTESIAN_POINT('Ctrl Pts',(6.21020710336862,-0.637842117488892,
71.9136111309505));
#49136=CARTESIAN_POINT('Ctrl Pts',(5.40644039496903,-2.42776610808628,71.8208213723738));
#49137=CARTESIAN_POINT('Ctrl Pts',(4.60267368656935,-4.21769009868388,71.728031613797));
#49138=CARTESIAN_POINT('Ctrl Pts',(2.82170061043407,-5.56879883804846,71.6352418552203));
#49139=CARTESIAN_POINT('Ctrl Pts',(0.881413334845232,-5.86061059558493,
71.5424520966435));
#49140=CARTESIAN_POINT('Ctrl Pts',(-1.05887394074338,-6.15242235312137,
71.4496623380668));
#49141=CARTESIAN_POINT('Ctrl Pts',(-3.15847541578552,-5.38493712882995,
71.35687257949));
#49142=CARTESIAN_POINT('Ctrl Pts',(-4.45317235729702,-3.91061401523227,
71.2640828209133));
#49143=CARTESIAN_POINT('Ctrl Pts',(-5.38666457674259,-2.84760914408037,
71.1971802780104));
#49144=CARTESIAN_POINT('Ctrl Pts',(-5.90172032162132,-1.41714857828327,
71.1302777351076));
#49145=CARTESIAN_POINT('Ctrl Pts',(-5.91402970906047,0.00531590772330143,
71.0633751922048));
#49146=CARTESIAN_POINT('Ctrl Pts',(-5.91060120235062,0.00437987123653664,
70.8116248077954));
#49147=CARTESIAN_POINT('Ctrl Pts',(-5.90176685963095,-1.28848680303269,
70.8723430596303));
#49148=CARTESIAN_POINT('Ctrl Pts',(-5.48470939396936,-2.58653829127134,
70.9330613114652));
#49149=CARTESIAN_POINT('Ctrl Pts',(-4.70360458874419,-3.6055306423528,70.9937795633001));
#49150=CARTESIAN_POINT('Ctrl Pts',(-3.50968456524259,-5.16306218435938,
71.0865875145158));
#49151=CARTESIAN_POINT('Ctrl Pts',(-1.46523438962779,-6.06862299459407,
71.1793954657315));
#49152=CARTESIAN_POINT('Ctrl Pts',(0.490517813476914,-5.90619502004989,
71.2722034169472));
#49153=CARTESIAN_POINT('Ctrl Pts',(2.44627001658162,-5.74376704550572,71.3650113681629));
#49154=CARTESIAN_POINT('Ctrl Pts',(4.31332424717623,-4.51335028618269,71.4578193193786));
#49155=CARTESIAN_POINT('Ctrl Pts',(5.23394874711508,-2.78020284381785,71.5506272705943));
#49156=CARTESIAN_POINT('Ctrl Pts',(6.15457324705387,-1.04705540145311,71.64343522181));
#49157=CARTESIAN_POINT('Ctrl Pts',(6.12876801633701,1.18882272395339,71.7362431730258));
#49158=CARTESIAN_POINT('Ctrl Pts',(5.16838807532191,2.90026068536445,71.8290511242415));
#49159=CARTESIAN_POINT('Ctrl Pts',(4.20800813430676,4.61169864677561,71.9218590754572));
#49160=CARTESIAN_POINT('Ctrl Pts',(2.31305348299327,5.79869644419127,72.0146670266729));
#49161=CARTESIAN_POINT('Ctrl Pts',(0.354073438076874,5.91594281079937,72.1074749778886));
#49162=CARTESIAN_POINT('Ctrl Pts',(-1.60490660683963,6.03318917740748,72.2002829291043));
#49163=CARTESIAN_POINT('Ctrl Pts',(-3.62791204535904,5.0806841132079,72.29309088032));
#49164=CARTESIAN_POINT('Ctrl Pts',(-4.78556654599306,3.49601203860518,72.3858988315358));
#49165=CARTESIAN_POINT('Ctrl Pts',(-5.51621503257378,2.49585331041722,72.4444741569556));
#49166=CARTESIAN_POINT('Ctrl Pts',(-5.90215555477039,1.24387420073254,72.5030494823755));
#49167=CARTESIAN_POINT('Ctrl Pts',(-5.9096269619093,-0.0038796998163677,
72.5616248077954));
#49168=CARTESIAN_POINT('Origin',(0.,0.,-10.));
#49169=CARTESIAN_POINT('',(-5.92173242987796,-0.00453640779018327,74.5633751922048));
#49170=CARTESIAN_POINT('',(-5.92478692091682,-0.00290426967806841,74.3116248077954));
#49171=CARTESIAN_POINT('',(-5.91675,-7.2459289488551E-16,-10.));
#49172=CARTESIAN_POINT('Ctrl Pts',(-5.92173242987796,-0.00453640779018327,
74.5633751922048));
#49173=CARTESIAN_POINT('Ctrl Pts',(-5.90751771867388,1.67116708836971,74.4842984127853));
#49174=CARTESIAN_POINT('Ctrl Pts',(-5.1617797014763,3.35793373378459,74.4052216333658));
#49175=CARTESIAN_POINT('Ctrl Pts',(-3.90360669034165,4.4593161837938,74.3261448539462));
#49176=CARTESIAN_POINT('Ctrl Pts',(-2.42724952445859,5.75169319240769,74.2333550953694));
#49177=CARTESIAN_POINT('Ctrl Pts',(-0.245321033219509,6.23805517964,74.1405653367927));
#49178=CARTESIAN_POINT('Ctrl Pts',(1.64015227963515,5.69504578730786,74.0477755782159));
#49179=CARTESIAN_POINT('Ctrl Pts',(3.5256255924898,5.15203639497571,73.9549858196392));
#49180=CARTESIAN_POINT('Ctrl Pts',(5.11464372696003,3.5796556230791,73.8621960610624));
#49181=CARTESIAN_POINT('Ctrl Pts',(5.67746769661407,1.70000193347804,73.7694063024857));
#49182=CARTESIAN_POINT('Ctrl Pts',(6.24029166626812,-0.179651756123031,
73.6766165439089));
#49183=CARTESIAN_POINT('Ctrl Pts',(5.77692147110597,-2.36657836342856,73.5838267853321));
#49184=CARTESIAN_POINT('Ctrl Pts',(4.50015474334161,-3.85645605522809,73.4910370267554));
#49185=CARTESIAN_POINT('Ctrl Pts',(3.22338801557717,-5.34633374702771,73.3982472681786));
#49186=CARTESIAN_POINT('Ctrl Pts',(1.13322475521041,-6.13916252332125,73.3054575096019));
#49187=CARTESIAN_POINT('Ctrl Pts',(-0.810450700374689,-5.87084454590543,
73.2126677510251));
#49188=CARTESIAN_POINT('Ctrl Pts',(-2.75412615595968,-5.60252656848963,
73.1198779924484));
#49189=CARTESIAN_POINT('Ctrl Pts',(-4.55131380676303,-4.27306183736458,
73.0270882338716));
#49190=CARTESIAN_POINT('Ctrl Pts',(-5.37667512059602,-2.49299231195949,
72.9342984752948));
#49191=CARTESIAN_POINT('Ctrl Pts',(-5.7352110960279,-1.71973222218887,72.8939907142648));
#49192=CARTESIAN_POINT('Ctrl Pts',(-5.91036117813064,-0.86144195820518,
72.8536829532348));
#49193=CARTESIAN_POINT('Ctrl Pts',(-5.9076390082336,-0.00209472984356585,
72.8133751922048));
#49194=CARTESIAN_POINT('Ctrl Pts',(-5.9096269619093,-0.0038796998163677,
72.5616248077954));
#49195=CARTESIAN_POINT('Ctrl Pts',(-5.91399340602072,-0.733092761060087,
72.5958574335912));
#49196=CARTESIAN_POINT('Ctrl Pts',(-5.78909470142213,-1.46086271303664,
72.630090059387));
#49197=CARTESIAN_POINT('Ctrl Pts',(-5.52819187461763,-2.13608097637051,
72.6643226851828));
#49198=CARTESIAN_POINT('Ctrl Pts',(-4.82085913985954,-3.96666283173856,
72.7571306363985));
#49199=CARTESIAN_POINT('Ctrl Pts',(-3.11389010759454,-5.41098745746912,
72.8499385876142));
#49200=CARTESIAN_POINT('Ctrl Pts',(-1.19147279183569,-5.80552667089866,
72.9427465388299));
#49201=CARTESIAN_POINT('Ctrl Pts',(0.730944523923385,-6.20006588432824,
73.0355544900457));
#49202=CARTESIAN_POINT('Ctrl Pts',(2.86881012317626,-5.54481968545648,73.1283624412614));
#49203=CARTESIAN_POINT('Ctrl Pts',(4.23998048321321,-4.14081065036442,73.2211703924771));
#49204=CARTESIAN_POINT('Ctrl Pts',(5.61115084325,-2.73680161527252,73.3139783436929));
#49205=CARTESIAN_POINT('Ctrl Pts',(6.21562596407094,-0.584029743960555,
73.4067862949085));
#49206=CARTESIAN_POINT('Ctrl Pts',(5.77570769441674,1.32851344323482,73.4995942461242));
#49207=CARTESIAN_POINT('Ctrl Pts',(5.33578942476254,3.2410566304302,73.5924021973399));
#49208=CARTESIAN_POINT('Ctrl Pts',(3.85147776463294,4.9133711335092,73.6852101485556));
#49209=CARTESIAN_POINT('Ctrl Pts',(2.00467109117049,5.57718935992186,73.7780180997714));
#49210=CARTESIAN_POINT('Ctrl Pts',(0.157864417707936,6.24100758633457,73.8708260509871));
#49211=CARTESIAN_POINT('Ctrl Pts',(-2.05143726908759,5.8963295360811,73.9636340022028));
#49212=CARTESIAN_POINT('Ctrl Pts',(-3.60827243835276,4.70150160595785,74.0564419534185));
#49213=CARTESIAN_POINT('Ctrl Pts',(-5.03515320694838,3.6064100837908,74.1415029048774));
#49214=CARTESIAN_POINT('Ctrl Pts',(-5.91394845174191,1.79717487807919,74.2265638563364));
#49215=CARTESIAN_POINT('Ctrl Pts',(-5.92478692091682,-0.00290426967806841,
74.3116248077954));
#49216=CARTESIAN_POINT('Origin',(0.,0.,-10.));
#49217=CARTESIAN_POINT('',(-5.92221425476728,0.00435283123465607,76.3133751922048));
#49218=CARTESIAN_POINT('',(-5.91860112252369,0.00530505955111227,76.0616248077954));
#49219=CARTESIAN_POINT('',(-5.91675,-7.2459289488551E-16,-10.));
#49220=CARTESIAN_POINT('Ctrl Pts',(-5.92221425476728,0.00435283123465607,
76.3133751922048));
#49221=CARTESIAN_POINT('Ctrl Pts',(-5.92446422127454,0.277271243771341,
76.3004933894893));
#49222=CARTESIAN_POINT('Ctrl Pts',(-5.90723714835,0.549904061635848,76.2876115867737));
#49223=CARTESIAN_POINT('Ctrl Pts',(-5.86956287631793,0.819681438655091,
76.2747297840581));
#49224=CARTESIAN_POINT('Ctrl Pts',(-5.59818885487094,2.76293256862564,76.1819400254814));
#49225=CARTESIAN_POINT('Ctrl Pts',(-4.26589973965931,4.55802745107444,76.0891502669046));
#49226=CARTESIAN_POINT('Ctrl Pts',(-2.48453455723552,5.3805886345109,75.9963605083278));
#49227=CARTESIAN_POINT('Ctrl Pts',(-0.703169374811634,6.20314981794741,
75.903570749751));
#49228=CARTESIAN_POINT('Ctrl Pts',(1.52727187482435,6.05317730237141,75.8107809911743));
#49229=CARTESIAN_POINT('Ctrl Pts',(3.18248374071698,4.99954430523397,75.7179912325975));
#49230=CARTESIAN_POINT('Ctrl Pts',(4.83769560660942,3.94591130809665,75.6252014740208));
#49231=CARTESIAN_POINT('Ctrl Pts',(5.91767808875851,1.98861782939818,75.532411715444));
#49232=CARTESIAN_POINT('Ctrl Pts',(5.92646118859023,0.0265292302760358,
75.4396219568673));
#49233=CARTESIAN_POINT('Ctrl Pts',(5.93524428842194,-1.93555936884622,75.3468321982905));
#49234=CARTESIAN_POINT('Ctrl Pts',(4.87282800593588,-3.90244308839225,75.2540424397138));
#49235=CARTESIAN_POINT('Ctrl Pts',(3.22711525698444,-4.97085235528712,75.161252681137));
#49236=CARTESIAN_POINT('Ctrl Pts',(1.58140250803301,-6.039261622182,75.0684629225603));
#49237=CARTESIAN_POINT('Ctrl Pts',(-0.647606707383809,-6.20919643642597,
74.9756731639835));
#49238=CARTESIAN_POINT('Ctrl Pts',(-2.43626458417193,-5.40261611590486,
74.8828834054067));
#49239=CARTESIAN_POINT('Ctrl Pts',(-4.22492246096005,-4.59603579538375,
74.79009364683));
#49240=CARTESIAN_POINT('Ctrl Pts',(-5.57322899911938,-2.8129403400976,74.6973038882532));
#49241=CARTESIAN_POINT('Ctrl Pts',(-5.86198934793559,-0.872196597456742,
74.6045141296765));
#49242=CARTESIAN_POINT('Ctrl Pts',(-5.90466393514745,-0.585382848821439,
74.5908011505193));
#49243=CARTESIAN_POINT('Ctrl Pts',(-5.9241974523523,-0.295125975109717,
74.577088171362));
#49244=CARTESIAN_POINT('Ctrl Pts',(-5.92173242987796,-0.00453640779018327,
74.5633751922048));
#49245=CARTESIAN_POINT('Ctrl Pts',(-5.92478692091682,-0.00290426967806841,
74.3116248077954));
#49246=CARTESIAN_POINT('Ctrl Pts',(-5.92577404387537,-0.166848035655527,
74.3193718075521));
#49247=CARTESIAN_POINT('Ctrl Pts',(-5.91956162748079,-0.330715853842254,
74.3271188073088));
#49248=CARTESIAN_POINT('Ctrl Pts',(-5.90590802266303,-0.493961302173379,
74.3348658070656));
#49249=CARTESIAN_POINT('Ctrl Pts',(-5.74233978597349,-2.44961847018869,
74.4276737582813));
#49250=CARTESIAN_POINT('Ctrl Pts',(-4.51083466085957,-4.3159549962264,74.5204817094971));
#49251=CARTESIAN_POINT('Ctrl Pts',(-2.77715074840922,-5.2355688383222,74.6132896607128));
#49252=CARTESIAN_POINT('Ctrl Pts',(-1.04346683595887,-6.155182680418,74.7060976119285));
#49253=CARTESIAN_POINT('Ctrl Pts',(1.19239586382801,-6.12807383857193,74.7989055631442));
#49254=CARTESIAN_POINT('Ctrl Pts',(2.90327359050187,-5.16669621701284,74.8917135143599));
#49255=CARTESIAN_POINT('Ctrl Pts',(4.61415131717573,-4.20531859545374,74.9845214655756));
#49256=CARTESIAN_POINT('Ctrl Pts',(5.80004407073672,-2.30967219418159,75.0773294167913));
#49257=CARTESIAN_POINT('Ctrl Pts',(5.91614824568895,-0.350624122432983,
75.170137368007));
#49258=CARTESIAN_POINT('Ctrl Pts',(6.03225242064119,1.60842394931563,75.2629453192228));
#49259=CARTESIAN_POINT('Ctrl Pts',(5.07856801698493,3.63087369154057,75.3557532704385));
#49260=CARTESIAN_POINT('Ctrl Pts',(3.49322124812066,4.78760406172844,75.4485612216541));
#49261=CARTESIAN_POINT('Ctrl Pts',(1.90787447925649,5.94433443191625,75.5413691728698));
#49262=CARTESIAN_POINT('Ctrl Pts',(-0.30913465481563,6.23534543006683,75.6341771240855));
#49263=CARTESIAN_POINT('Ctrl Pts',(-2.13930379287229,5.52694550561181,75.7269850753013));
#49264=CARTESIAN_POINT('Ctrl Pts',(-3.96947293092905,4.81854558115675,75.819793026517));
#49265=CARTESIAN_POINT('Ctrl Pts',(-5.4128020729704,3.11073473409595,75.9126009777328));
#49266=CARTESIAN_POINT('Ctrl Pts',(-5.80622036529553,1.18808771133609,76.0054089289485));
#49267=CARTESIAN_POINT('Ctrl Pts',(-5.88565448980684,0.799890756653038,
76.0241475552308));
#49268=CARTESIAN_POINT('Ctrl Pts',(-5.92228725593392,0.402935648692027,
76.0428861815131));
#49269=CARTESIAN_POINT('Ctrl Pts',(-5.91860112252369,0.00530505955111227,
76.0616248077954));
#49270=CARTESIAN_POINT('Origin',(0.,0.,-10.));
#49271=CARTESIAN_POINT('',(-5.90783837446273,0.00236323016111234,78.0633751922048));
#49272=CARTESIAN_POINT('',(-5.9069646967222,0.000416249466083529,77.8116248077954));
#49273=CARTESIAN_POINT('',(-5.91675,-7.2459289488551E-16,-10.));
#49274=CARTESIAN_POINT('Ctrl Pts',(-5.90783837446273,0.00236323016111234,
78.0633751922048));
#49275=CARTESIAN_POINT('Ctrl Pts',(-5.91085192024158,0.843919154698636,
78.0238986076164));
#49276=CARTESIAN_POINT('Ctrl Pts',(-5.74312714104647,1.68432885304078,77.9844220230281));
#49277=CARTESIAN_POINT('Ctrl Pts',(-5.39877847795077,2.44475703617782,77.9449454384397));
#49278=CARTESIAN_POINT('Ctrl Pts',(-4.5893865397156,4.23214437639491,77.8521556798629));
#49279=CARTESIAN_POINT('Ctrl Pts',(-2.80417311428585,5.57764537943121,77.7593659212861));
#49280=CARTESIAN_POINT('Ctrl Pts',(-0.862977703412722,5.86335360551774,
77.6665761627094));
#49281=CARTESIAN_POINT('Ctrl Pts',(1.07821770746029,6.14906183160425,77.5737864041326));
#49282=CARTESIAN_POINT('Ctrl Pts',(3.17539510377643,5.37497728074138,77.480996645556));
#49283=CARTESIAN_POINT('Ctrl Pts',(4.4654489838702,3.89658971311811,77.3882068869792));
#49284=CARTESIAN_POINT('Ctrl Pts',(5.7555028639639,2.41820214549493,77.2954171284024));
#49285=CARTESIAN_POINT('Ctrl Pts',(6.23843322783498,0.235511561111468,77.2026273698256));
#49286=CARTESIAN_POINT('Ctrl Pts',(5.69245965233818,-1.64910555345231,77.1098376112489));
#49287=CARTESIAN_POINT('Ctrl Pts',(5.14648607684132,-3.5337226680163,77.0170478526721));
#49288=CARTESIAN_POINT('Ctrl Pts',(3.57160856197623,-5.12026631276067,76.9242580940954));
#49289=CARTESIAN_POINT('Ctrl Pts',(1.69107217117025,-5.68013388326533,76.8314683355187));
#49290=CARTESIAN_POINT('Ctrl Pts',(-0.189464219635722,-6.24000145377,76.7386785769419));
#49291=CARTESIAN_POINT('Ctrl Pts',(-2.37565948638272,-5.77319295003497,
76.6458888183651));
#49292=CARTESIAN_POINT('Ctrl Pts',(-3.86352765591502,-4.49408500942128,
76.5530990597883));
#49293=CARTESIAN_POINT('Ctrl Pts',(-5.14483828590118,-3.39255287453919,
76.4731911039271));
#49294=CARTESIAN_POINT('Ctrl Pts',(-5.9082573398602,-1.68860528528188,76.393283148066));
#49295=CARTESIAN_POINT('Ctrl Pts',(-5.92221425476728,0.00435283123465607,
76.3133751922048));
#49296=CARTESIAN_POINT('Ctrl Pts',(-5.91860112252369,0.00530505955111227,
76.0616248077954));
#49297=CARTESIAN_POINT('Ctrl Pts',(-5.90403071542999,-1.5664339178317,76.1356941327288));
#49298=CARTESIAN_POINT('Ctrl Pts',(-5.25950470490065,-3.14872683292577,
76.2097634576621));
#49299=CARTESIAN_POINT('Ctrl Pts',(-4.13833785100994,-4.24239403769839,
76.2838327825955));
#49300=CARTESIAN_POINT('Ctrl Pts',(-2.73352960179007,-5.61274556551441,
76.3766407338112));
#49301=CARTESIAN_POINT('Ctrl Pts',(-0.580405660741316,-6.21596542268728,
76.469448685027));
#49302=CARTESIAN_POINT('Ctrl Pts',(1.33188070963397,-5.77493213081377,76.5622566362427));
#49303=CARTESIAN_POINT('Ctrl Pts',(3.24416708000904,-5.33389883894032,76.6550645874584));
#49304=CARTESIAN_POINT('Ctrl Pts',(4.91561587971071,-3.84861239802078,76.7478725386741));
#49305=CARTESIAN_POINT('Ctrl Pts',(5.57835722358738,-2.00141900317022,76.8406804898898));
#49306=CARTESIAN_POINT('Ctrl Pts',(6.24109856746405,-0.154225608319656,
76.9334884411055));
#49307=CARTESIAN_POINT('Ctrl Pts',(5.89513245551572,2.05487474046193,77.0262963923212));
#49308=CARTESIAN_POINT('Ctrl Pts',(4.69939702494141,3.61101300775449,77.1191043435369));
#49309=CARTESIAN_POINT('Ctrl Pts',(3.50366159436703,5.16715127504713,77.2119122947526));
#49310=CARTESIAN_POINT('Ctrl Pts',(1.45815684516657,6.07032746085066,77.3047202459683));
#49311=CARTESIAN_POINT('Ctrl Pts',(-0.49740462295242,5.90561901761923,77.397528197184));
#49312=CARTESIAN_POINT('Ctrl Pts',(-2.45296609107141,5.7409105743878,77.4903361483998));
#49313=CARTESIAN_POINT('Ctrl Pts',(-4.31858427810893,4.5083175021214,77.5831440996155));
#49314=CARTESIAN_POINT('Ctrl Pts',(-5.23718714974778,2.77409770893476,77.6759520508312));
#49315=CARTESIAN_POINT('Ctrl Pts',(-5.68481181450939,1.92903225408464,77.7211763031526));
#49316=CARTESIAN_POINT('Ctrl Pts',(-5.90756756517641,0.964855466841043,
77.766400555474));
#49317=CARTESIAN_POINT('Ctrl Pts',(-5.9069646967222,0.000416249466083529,
77.8116248077954));
#49318=CARTESIAN_POINT('Origin',(0.,0.,-10.));
#49319=CARTESIAN_POINT('',(-5.91352838726915,-0.0052379771925426,79.8133751922048));
#49320=CARTESIAN_POINT('',(-5.91706824557423,-0.00544986776190025,79.5616248077954));
#49321=CARTESIAN_POINT('',(-5.91675,-7.2459289488551E-16,-10.));
#49322=CARTESIAN_POINT('Ctrl Pts',(-5.91352838726915,-0.0052379771925426,
79.8133751922048));
#49323=CARTESIAN_POINT('Ctrl Pts',(-5.90162685186426,1.39985609417491,79.7473038257436));
#49324=CARTESIAN_POINT('Ctrl Pts',(-5.40046356538693,2.81257996585592,79.6812324592824));
#49325=CARTESIAN_POINT('Ctrl Pts',(-4.4880041631094,3.87058970337054,79.6151610928213));
#49326=CARTESIAN_POINT('Ctrl Pts',(-3.20655817245923,5.35644467162761,79.5223713342445));
#49327=CARTESIAN_POINT('Ctrl Pts',(-1.11391184920308,6.14269608769454,79.4295815756678));
#49328=CARTESIAN_POINT('Ctrl Pts',(0.828910150132987,5.86826669323505,79.3367918170911));
#49329=CARTESIAN_POINT('Ctrl Pts',(2.77173214946938,5.59383729877552,79.2440020585143));
#49330=CARTESIAN_POINT('Ctrl Pts',(4.56472982488564,4.25872709378915,79.1512122999375));
#49331=CARTESIAN_POINT('Ctrl Pts',(5.38448884400271,2.47607065907574,79.0584225413607));
#49332=CARTESIAN_POINT('Ctrl Pts',(6.20424786311968,0.693414224362538,78.965632782784));
#49333=CARTESIAN_POINT('Ctrl Pts',(6.05076822593769,-1.53678844007761,78.8728430242073));
#49334=CARTESIAN_POINT('Ctrl Pts',(4.99453375667845,-3.19034145089906,78.7800532656305));
#49335=CARTESIAN_POINT('Ctrl Pts',(3.93829928741921,-4.84389446172052,78.6872635070538));
#49336=CARTESIAN_POINT('Ctrl Pts',(1.97930998608272,-5.92079781892327,78.594473748477));
#49337=CARTESIAN_POINT('Ctrl Pts',(0.017210001578922,-5.92649557797616,
78.5016839899002));
#49338=CARTESIAN_POINT('Ctrl Pts',(-1.94488998292488,-5.93219333702905,
78.4088942313235));
#49339=CARTESIAN_POINT('Ctrl Pts',(-3.91010065059599,-4.86668549793206,
78.3161044727467));
#49340=CARTESIAN_POINT('Ctrl Pts',(-4.97592075891125,-3.21929473968469,
78.22331471417));
#49341=CARTESIAN_POINT('Ctrl Pts',(-5.58829710029315,-2.272771853232,78.1700015401816));
#49342=CARTESIAN_POINT('Ctrl Pts',(-5.90376857733856,-1.13415903724546,
78.1166883661932));
#49343=CARTESIAN_POINT('Ctrl Pts',(-5.90783837446273,0.00236323016111234,
78.0633751922048));
#49344=CARTESIAN_POINT('Ctrl Pts',(-5.9069646967222,0.000416249466083529,
77.8116248077954));
#49345=CARTESIAN_POINT('Ctrl Pts',(-5.90633037532328,-1.01433983749622,
77.8592085066897));
#49346=CARTESIAN_POINT('Ctrl Pts',(-5.65842326778303,-2.0293864519967,77.906792205584));
#49347=CARTESIAN_POINT('Ctrl Pts',(-5.16500260233514,-2.90628550869862,
77.9543759044783));
#49348=CARTESIAN_POINT('Ctrl Pts',(-4.20262762704341,-4.61660241903885,
78.047183855694));
#49349=CARTESIAN_POINT('Ctrl Pts',(-2.3062901202197,-5.80138972561238,78.1399918069097));
#49350=CARTESIAN_POINT('Ctrl Pts',(-0.347174687598445,-5.91635166944049,
78.2327997581254));
#49351=CARTESIAN_POINT('Ctrl Pts',(1.6119407450227,-6.03131361326859,78.3256077093412));
#49352=CARTESIAN_POINT('Ctrl Pts',(3.63383410344128,-5.07645019435141,78.4184156605569));
#49353=CARTESIAN_POINT('Ctrl Pts',(4.78963994996363,-3.49042927014899,78.5112236117726));
#49354=CARTESIAN_POINT('Ctrl Pts',(5.94544579648597,-1.90440834594658,78.6040315629883));
#49355=CARTESIAN_POINT('Ctrl Pts',(6.23516413111195,0.312770083541336,78.696839514204));
#49356=CARTESIAN_POINT('Ctrl Pts',(5.52569725777374,2.1425258821382,78.7896474654197));
#49357=CARTESIAN_POINT('Ctrl Pts',(4.8162303844355,3.97228168073516,78.8824554166354));
#49358=CARTESIAN_POINT('Ctrl Pts',(3.10757830313311,5.41461484844123,78.9752633678512));
#49359=CARTESIAN_POINT('Ctrl Pts',(1.18470222695776,5.80691208592327,79.0680713190669));
#49360=CARTESIAN_POINT('Ctrl Pts',(-0.738173849217586,6.1992093234053,79.1608792702826));
#49361=CARTESIAN_POINT('Ctrl Pts',(-2.87527392026577,5.54147063066327,79.2536872214982));
#49362=CARTESIAN_POINT('Ctrl Pts',(-4.24480615002276,4.13586364486661,79.346495172714));
#49363=CARTESIAN_POINT('Ctrl Pts',(-5.30300200846101,3.04979392073473,79.4182050510744));
#49364=CARTESIAN_POINT('Ctrl Pts',(-5.90294586434624,1.51723318368911,79.4899149294349));
#49365=CARTESIAN_POINT('Ctrl Pts',(-5.91706824557423,-0.00544986776190025,
79.5616248077954));
#49366=CARTESIAN_POINT('Origin',(0.,0.,-10.));
#49367=CARTESIAN_POINT('',(-5.92652005161158,-4.92410581365288E-5,81.5633751922047));
#49368=CARTESIAN_POINT('',(-5.92564501137359,0.00208360169631917,81.3116248077953));
#49369=CARTESIAN_POINT('',(-5.91675,-7.2459289488551E-16,-10.));
#49370=CARTESIAN_POINT('Ctrl Pts',(-5.92652005161158,-4.92410581365288E-5,
81.5633751922047));
#49371=CARTESIAN_POINT('Ctrl Pts',(-5.9262796163795,1.95944564602974,81.4707090438708));
#49372=CARTESIAN_POINT('Ctrl Pts',(-4.85833414818282,3.91916492820066,81.378042895537));
#49373=CARTESIAN_POINT('Ctrl Pts',(-3.21146626212954,4.9809768587225,81.285376747203));
#49374=CARTESIAN_POINT('Ctrl Pts',(-1.56240156804075,6.04420517303622,81.1925869886263));
#49375=CARTESIAN_POINT('Ctrl Pts',(0.667131059078623,6.20712904518559,81.0997972300494));
#49376=CARTESIAN_POINT('Ctrl Pts',(2.45324344310461,5.39492749059611,81.0070074714726));
#49377=CARTESIAN_POINT('Ctrl Pts',(4.2393558271304,4.58272593600671,80.9142177128958));
#49378=CARTESIAN_POINT('Ctrl Pts',(5.58204796806278,2.79539895467876,80.8214279543191));
#49379=CARTESIAN_POINT('Ctrl Pts',(5.86470336495774,0.853756675510454,80.7286381957424));
#49380=CARTESIAN_POINT('Ctrl Pts',(6.14735876185272,-1.08788560365796,80.6358484371657));
#49381=CARTESIAN_POINT('Ctrl Pts',(5.3699774147099,-3.1838431806669,80.5430586785889));
#49382=CARTESIAN_POINT('Ctrl Pts',(3.88956310091184,-4.47157074236229,80.4502689200121));
#49383=CARTESIAN_POINT('Ctrl Pts',(2.40914878711369,-5.75929830405776,80.3574791614354));
#49384=CARTESIAN_POINT('Ctrl Pts',(0.225701506660258,-6.23879585043983,
80.2646894028585));
#49385=CARTESIAN_POINT('Ctrl Pts',(-1.65805474957566,-5.68985944179072,
80.1718996442818));
#49386=CARTESIAN_POINT('Ctrl Pts',(-3.54181100581147,-5.14092303314164,
80.079109885705));
#49387=CARTESIAN_POINT('Ctrl Pts',(-5.12587623782969,-3.56355266946152,
79.9863201271284));
#49388=CARTESIAN_POINT('Ctrl Pts',(-5.68278602481674,-1.68213822739774,
79.8935303685516));
#49389=CARTESIAN_POINT('Ctrl Pts',(-5.84314568400726,-1.14039343178604,
79.866811976436));
#49390=CARTESIAN_POINT('Ctrl Pts',(-5.91834121174604,-0.573439550262532,
79.8400935843204));
#49391=CARTESIAN_POINT('Ctrl Pts',(-5.91352838726915,-0.0052379771925426,
79.8133751922048));
#49392=CARTESIAN_POINT('Ctrl Pts',(-5.91706824557423,-0.00544986776190025,
79.5616248077954));
#49393=CARTESIAN_POINT('Ctrl Pts',(-5.92122325231597,-0.453445021141946,
79.5827228806506));
#49394=CARTESIAN_POINT('Ctrl Pts',(-5.87466834302196,-0.900585141668491,
79.6038209535059));
#49395=CARTESIAN_POINT('Ctrl Pts',(-5.77415460407802,-1.33524752327236,
79.6249190263611));
#49396=CARTESIAN_POINT('Ctrl Pts',(-5.33200643991055,-3.2472764267639,79.7177269775768));
#49397=CARTESIAN_POINT('Ctrl Pts',(-3.84574572310957,-4.91785895489578,
79.8105349287925));
#49398=CARTESIAN_POINT('Ctrl Pts',(-1.99816623480639,-5.57952319094383,
79.9033428800082));
#49399=CARTESIAN_POINT('Ctrl Pts',(-0.150586746503413,-6.24118742699181,
79.9961508312239));
#49400=CARTESIAN_POINT('Ctrl Pts',(2.05831151330152,-5.89393337095641,80.0889587824397));
#49401=CARTESIAN_POINT('Ctrl Pts',(3.61375234962716,-4.69729084640972,80.1817667336554));
#49402=CARTESIAN_POINT('Ctrl Pts',(5.16919318595289,-3.50064832186295,80.2745746848711));
#49403=CARTESIAN_POINT('Ctrl Pts',(6.07117659879901,-1.4546173288047,80.3673826360867));
#49404=CARTESIAN_POINT('Ctrl Pts',(5.90532800501674,0.500847774643518,80.4601905873024));
#49405=CARTESIAN_POINT('Ctrl Pts',(5.73947941123448,2.45631287809162,80.5529985385181));
#49406=CARTESIAN_POINT('Ctrl Pts',(4.50579881082393,4.32121209192987,80.6458064897339));
#49407=CARTESIAN_POINT('Ctrl Pts',(2.77104372643263,5.23880368084153,80.7386144409496));
#49408=CARTESIAN_POINT('Ctrl Pts',(1.03628864204112,6.15639526975329,80.8314223921654));
#49409=CARTESIAN_POINT('Ctrl Pts',(-1.19954092633104,6.12667923373836,80.924230343381));
#49410=CARTESIAN_POINT('Ctrl Pts',(-2.90929643893171,5.16330723186405,81.0170382945967));
#49411=CARTESIAN_POINT('Ctrl Pts',(-4.61905195153228,4.1999352299898,81.1098462458124));
#49412=CARTESIAN_POINT('Ctrl Pts',(-5.80273340836125,2.30290726225611,81.2026541970281));
#49413=CARTESIAN_POINT('Ctrl Pts',(-5.9165530819849,0.343725134744857,81.2954621482438));
#49414=CARTESIAN_POINT('Ctrl Pts',(-5.92316037734029,0.229993522631114,
81.3008497014276));
#49415=CARTESIAN_POINT('Ctrl Pts',(-5.92616238070294,0.116052459261064,
81.3062372546115));
#49416=CARTESIAN_POINT('Ctrl Pts',(-5.92564501137359,0.00208360169631917,
81.3116248077953));
#49417=CARTESIAN_POINT('Origin',(0.,0.,-10.));
#49418=CARTESIAN_POINT('',(-5.91367641053724,0.00526281327289491,83.3133751922047));
#49419=CARTESIAN_POINT('',(-5.91070653272951,0.00442589000008243,83.0616248077953));
#49420=CARTESIAN_POINT('',(-5.91675,-7.2459289488551E-16,-10.));
#49421=CARTESIAN_POINT('Ctrl Pts',(-5.91367641053724,0.00526281327289491,
83.3133751922047));
#49422=CARTESIAN_POINT('Ctrl Pts',(-5.91847631819128,0.568171225327802,
83.2869040205747));
#49423=CARTESIAN_POINT('Ctrl Pts',(-5.84469124069181,1.12984655758661,83.2604328489447));
#49424=CARTESIAN_POINT('Ctrl Pts',(-5.6872451620954,1.66699984587517,83.2339616773148));
#49425=CARTESIAN_POINT('Ctrl Pts',(-5.13534727763322,3.54989058587421,83.141171918738));
#49426=CARTESIAN_POINT('Ctrl Pts',(-3.55548796545528,5.13147348829515,83.0483821601613));
#49427=CARTESIAN_POINT('Ctrl Pts',(-1.67320012425186,5.68542411471026,82.9555924015846));
#49428=CARTESIAN_POINT('Ctrl Pts',(0.209087716951782,6.23937474112543,82.8628026430078));
#49429=CARTESIAN_POINT('Ctrl Pts',(2.39380408718108,5.76569309153457,82.770012884431));
#49430=CARTESIAN_POINT('Ctrl Pts',(3.87764218013329,4.48191221944122,82.6772231258543));
#49431=CARTESIAN_POINT('Ctrl Pts',(5.36148027308533,3.19813134734802,82.5844333672775));
#49432=CARTESIAN_POINT('Ctrl Pts',(6.1444400887605,1.10425125275282,82.4916436087007));
#49433=CARTESIAN_POINT('Ctrl Pts',(5.86695599986163,-0.838136811990138,
82.398853850124));
#49434=CARTESIAN_POINT('Ctrl Pts',(5.58947191096278,-2.78052487673298,82.3060640915472));
#49435=CARTESIAN_POINT('Ctrl Pts',(4.25154391748981,-4.57142091162344,82.2132743329705));
#49436=CARTESIAN_POINT('Ctrl Pts',(2.4676006384095,-5.38837573942708,82.1204845743937));
#49437=CARTESIAN_POINT('Ctrl Pts',(0.683657359328989,-6.20533056723082,
82.027694815817));
#49438=CARTESIAN_POINT('Ctrl Pts',(-1.54630120535912,-6.04834418794753,
81.9349050572403));
#49439=CARTESIAN_POINT('Ctrl Pts',(-3.19819127241771,-4.98951085828627,
81.8421152986635));
#49440=CARTESIAN_POINT('Ctrl Pts',(-4.85228191134336,-3.92926699962938,
81.7492019298439));
#49441=CARTESIAN_POINT('Ctrl Pts',(-5.92676112829165,-1.96477178987861,
81.6562885610243));
#49442=CARTESIAN_POINT('Ctrl Pts',(-5.92652005161158,-4.92410581365288E-5,
81.5633751922047));
#49443=CARTESIAN_POINT('Ctrl Pts',(-5.92564501137359,0.00208360169631917,
81.3116248077953));
#49444=CARTESIAN_POINT('Ctrl Pts',(-5.91724998840898,-1.8472165447024,81.3990452058272));
#49445=CARTESIAN_POINT('Ctrl Pts',(-4.9822221455073,-3.70383476033302,81.4864656038591));
#49446=CARTESIAN_POINT('Ctrl Pts',(-3.48763610563928,-4.79167421000652,
81.573886001891));
#49447=CARTESIAN_POINT('Ctrl Pts',(-1.9009415652512,-5.94655513995829,81.6666939531067));
#49448=CARTESIAN_POINT('Ctrl Pts',(0.316405405943797,-6.23498071257269,
81.7595019043224));
#49449=CARTESIAN_POINT('Ctrl Pts',(2.14574724307293,-5.52444713152776,81.8523098555381));
#49450=CARTESIAN_POINT('Ctrl Pts',(3.97508908020207,-4.81391355048283,81.9451178067538));
#49451=CARTESIAN_POINT('Ctrl Pts',(5.41642578326554,-3.10442081577871,82.0379257579695));
#49452=CARTESIAN_POINT('Ctrl Pts',(5.80760183254679,-1.18131633985124,82.1307337091853));
#49453=CARTESIAN_POINT('Ctrl Pts',(6.19877788182802,0.741788136076126,82.223541660401));
#49454=CARTESIAN_POINT('Ctrl Pts',(5.53979327732711,2.87850435322667,82.3163496116167));
#49455=CARTESIAN_POINT('Ctrl Pts',(4.13338803277648,4.24721681936542,82.4091575628324));
#49456=CARTESIAN_POINT('Ctrl Pts',(2.72698278822586,5.61592928550417,82.5019655140481));
#49457=CARTESIAN_POINT('Ctrl Pts',(0.573156903625285,6.21663800063106,82.5947734652638));
#49458=CARTESIAN_POINT('Ctrl Pts',(-1.33861388300644,5.77337511447358,82.6875814164795));
#49459=CARTESIAN_POINT('Ctrl Pts',(-3.25038466963839,5.33011222831604,82.7803893676952));
#49460=CARTESIAN_POINT('Ctrl Pts',(-4.92010035830155,3.84287774087407,82.873197318911));
#49461=CARTESIAN_POINT('Ctrl Pts',(-5.58068726159464,1.99491278718537,82.9660052701267));
#49462=CARTESIAN_POINT('Ctrl Pts',(-5.80755365057478,1.36026330516377,82.9978784493496));
#49463=CARTESIAN_POINT('Ctrl Pts',(-5.91539810822109,0.683067383672749,
83.0297516285724));
#49464=CARTESIAN_POINT('Ctrl Pts',(-5.91070653272951,0.00442589000008243,
83.0616248077953));
#49465=CARTESIAN_POINT('Origin',(0.,0.,-10.));
#49466=CARTESIAN_POINT('',(-5.90777653442157,-0.00228402886370327,85.0633751922047));
#49467=CARTESIAN_POINT('',(-5.90953574780485,-0.00382487655214481,84.8116248077953));
#49468=CARTESIAN_POINT('',(-5.91675,-7.2459289488551E-16,-10.));
#49469=CARTESIAN_POINT('Ctrl Pts',(-5.90777653442157,-0.00228402886370327,
85.0633751922047));
#49470=CARTESIAN_POINT('Ctrl Pts',(-5.9038637091048,1.12899760163664,85.010309238702));
#49471=CARTESIAN_POINT('Ctrl Pts',(-5.59150136727689,2.26227968995058,84.9572432851992));
#49472=CARTESIAN_POINT('Ctrl Pts',(-4.9844756224772,3.20603318586317,84.9041773316965));
#49473=CARTESIAN_POINT('Ctrl Pts',(-3.92304605055994,4.85625622457871,84.8113875731197));
#49474=CARTESIAN_POINT('Ctrl Pts',(-1.96067963993461,5.92699335102708,84.7185978145429));
#49475=CARTESIAN_POINT('Ctrl Pts',(0.0014285604354887,5.92652039388547,
84.6258080559661));
#49476=CARTESIAN_POINT('Ctrl Pts',(1.96353676080559,5.92604743674386,84.5330182973894));
#49477=CARTESIAN_POINT('Ctrl Pts',(3.92538675092045,4.85436439601227,84.4402285388127));
#49478=CARTESIAN_POINT('Ctrl Pts',(4.98602064221901,3.20362984367597,84.3474387802359));
#49479=CARTESIAN_POINT('Ctrl Pts',(6.04665453351756,1.55289529133967,84.2546490216591));
#49480=CARTESIAN_POINT('Ctrl Pts',(6.2060723259998,-0.67689077260134,84.1618592630823));
#49481=CARTESIAN_POINT('Ctrl Pts',(5.39106316336296,-2.46172378396852,84.0690695045056));
#49482=CARTESIAN_POINT('Ctrl Pts',(4.57605400072608,-4.2465567953358,83.9762797459288));
#49483=CARTESIAN_POINT('Ctrl Pts',(2.78661788297001,-5.58643675412919,83.8834899873521));
#49484=CARTESIAN_POINT('Ctrl Pts',(0.844533536547844,-5.86603862291848,
83.7907002287754));
#49485=CARTESIAN_POINT('Ctrl Pts',(-1.09755080987421,-6.14564049170775,
83.6979104701987));
#49486=CARTESIAN_POINT('Ctrl Pts',(-3.19228338496234,-5.36496427049303,
83.6051207116218));
#49487=CARTESIAN_POINT('Ctrl Pts',(-4.47768144413318,-3.88252687109706,
83.5123309530451));
#49488=CARTESIAN_POINT('Ctrl Pts',(-5.3963796308283,-2.82300095926192,83.4460123660983));
#49489=CARTESIAN_POINT('Ctrl Pts',(-5.90165113649419,-1.40499930091568,
83.3796937791515));
#49490=CARTESIAN_POINT('Ctrl Pts',(-5.91367641053724,0.00526281327289491,
83.3133751922047));
#49491=CARTESIAN_POINT('Ctrl Pts',(-5.91070653272951,0.00442589000008243,
83.0616248077953));
#49492=CARTESIAN_POINT('Ctrl Pts',(-5.90173723346798,-1.29299299603636,
83.1225595797881));
#49493=CARTESIAN_POINT('Ctrl Pts',(-5.48145609199123,-2.59569535386845,
83.183494351781));
#49494=CARTESIAN_POINT('Ctrl Pts',(-4.69518307107893,-3.61649046303929,
83.2444291237738));
#49495=CARTESIAN_POINT('Ctrl Pts',(-3.49763385934694,-5.1712333396409,83.3372370749895));
#49496=CARTESIAN_POINT('Ctrl Pts',(-1.45107731795962,-6.07202367290896,
83.4300450262052));
#49497=CARTESIAN_POINT('Ctrl Pts',(0.504290756076211,-5.90503498495449,
83.522852977421));
#49498=CARTESIAN_POINT('Ctrl Pts',(2.45965883011204,-5.73804629700002,83.6156609286367));
#49499=CARTESIAN_POINT('Ctrl Pts',(4.32383843679622,-4.50327858782326,83.7084688798523));
#49500=CARTESIAN_POINT('Ctrl Pts',(5.24041843105424,-2.76798880194039,83.801276831068));
#49501=CARTESIAN_POINT('Ctrl Pts',(6.15699842531226,-1.03269901605751,83.8940847822837));
#49502=CARTESIAN_POINT('Ctrl Pts',(6.1259788071438,1.20311284653135,83.9868927334994));
#49503=CARTESIAN_POINT('Ctrl Pts',(5.16161010617607,2.9123063801773,84.0797006847152));
#49504=CARTESIAN_POINT('Ctrl Pts',(4.1972414052084,4.62149991382316,84.1725086359309));
#49505=CARTESIAN_POINT('Ctrl Pts',(2.2995236214415,5.80407511852627,84.2653165871466));
#49506=CARTESIAN_POINT('Ctrl Pts',(0.34027546504553,5.91675248325366,84.3581245383623));
#49507=CARTESIAN_POINT('Ctrl Pts',(-1.61897269135055,6.02942984798107,84.450932489578));
#49508=CARTESIAN_POINT('Ctrl Pts',(-3.63975122037582,5.0722093727326,84.5437404407937));
#49509=CARTESIAN_POINT('Ctrl Pts',(-4.793706841166,3.4848417555405,84.6365483920094));
#49510=CARTESIAN_POINT('Ctrl Pts',(-5.51932862758084,2.48668506274214,84.6949071972713));
#49511=CARTESIAN_POINT('Ctrl Pts',(-5.90220409926062,1.23936489192517,84.7532660025333));
#49512=CARTESIAN_POINT('Ctrl Pts',(-5.90953574780485,-0.00382487655214481,
84.8116248077953));
#49513=CARTESIAN_POINT('Origin',(0.,0.,-10.));
#49514=CARTESIAN_POINT('',(-5.92207245583525,-0.00440905045111684,86.8133751922048));
#49515=CARTESIAN_POINT('',(-5.92469646081808,-0.00297539080508188,86.5616248077953));
#49516=CARTESIAN_POINT('',(-5.91675,-7.2459289488551E-16,-10.));
#49517=CARTESIAN_POINT('Ctrl Pts',(-5.92207245583525,-0.00440905045111684,
86.8133751922048));
#49518=CARTESIAN_POINT('Ctrl Pts',(-5.90803226273657,1.68341667196022,86.7337144568292));
#49519=CARTESIAN_POINT('Ctrl Pts',(-5.14989886133249,3.38225938529491,86.6540537214536));
#49520=CARTESIAN_POINT('Ctrl Pts',(-3.87548104107258,4.48378107407268,86.574392986078));
#49521=CARTESIAN_POINT('Ctrl Pts',(-2.39102422165811,5.76684645235311,86.4816032275013));
#49522=CARTESIAN_POINT('Ctrl Pts',(-0.206079747760587,6.23947481532992,
86.3888134689245));
#49523=CARTESIAN_POINT('Ctrl Pts',(1.6759408202332,5.6846168197163,86.2960237103478));
#49524=CARTESIAN_POINT('Ctrl Pts',(3.5579613882271,5.12975882410264,86.203233951771));
#49525=CARTESIAN_POINT('Ctrl Pts',(5.13705805031723,3.54741446989843,86.1104441931943));
#49526=CARTESIAN_POINT('Ctrl Pts',(5.68804814642293,1.66425788383293,86.0176544346175));
#49527=CARTESIAN_POINT('Ctrl Pts',(6.2390382425286,-0.218898702232475,85.9248646760407));
#49528=CARTESIAN_POINT('Ctrl Pts',(5.76192177264996,-2.40286752015914,85.8320749174639));
#49529=CARTESIAN_POINT('Ctrl Pts',(4.47580919348121,-3.88468506876354,85.7392851588872));
#49530=CARTESIAN_POINT('Ctrl Pts',(3.18969661431247,-5.36650261736794,85.6464954003104));
#49531=CARTESIAN_POINT('Ctrl Pts',(1.09458792585362,-6.14616889665008,85.5537056417338));
#49532=CARTESIAN_POINT('Ctrl Pts',(-0.847361401410383,-5.86563079943881,
85.460915883157));
#49533=CARTESIAN_POINT('Ctrl Pts',(-2.7893107286745,-5.58509270222752,85.3681261245802));
#49534=CARTESIAN_POINT('Ctrl Pts',(-4.57810069474375,-4.24435022852271,
85.2753363660034));
#49535=CARTESIAN_POINT('Ctrl Pts',(-5.39224931117372,-2.45912451617885,
85.1825466074266));
#49536=CARTESIAN_POINT('Ctrl Pts',(-5.74079080364409,-1.69485958761427,
85.1428228023527));
#49537=CARTESIAN_POINT('Ctrl Pts',(-5.91070557460482,-0.849132299881903,
85.1030989972787));
#49538=CARTESIAN_POINT('Ctrl Pts',(-5.90777653442157,-0.00228402886370327,
85.0633751922047));
#49539=CARTESIAN_POINT('Ctrl Pts',(-5.90953574780485,-0.00382487655214481,
84.8116248077953));
#49540=CARTESIAN_POINT('Ctrl Pts',(-5.91386361280565,-0.737678587063048,
84.8460739537491));
#49541=CARTESIAN_POINT('Ctrl Pts',(-5.78733212812688,-1.47009304673082,
84.8805230997029));
#49542=CARTESIAN_POINT('Ctrl Pts',(-5.52319512729882,-2.14896787458142,
84.9149722456566));
#49543=CARTESIAN_POINT('Ctrl Pts',(-4.81159508008634,-3.97789512837534,
85.0077801968723));
#49544=CARTESIAN_POINT('Ctrl Pts',(-3.10126227310632,-5.41823487682758,
85.1005881480879));
#49545=CARTESIAN_POINT('Ctrl Pts',(-1.17793005116786,-5.80828960493156,
85.1933960993036));
#49546=CARTESIAN_POINT('Ctrl Pts',(0.745402170770599,-6.19834433303554,
85.2862040505193));
#49547=CARTESIAN_POINT('Ctrl Pts',(2.8817338076675,-5.53811404079126,85.3790120017351));
#49548=CARTESIAN_POINT('Ctrl Pts',(4.24962604490735,-4.13091101558063,85.4718199529508));
#49549=CARTESIAN_POINT('Ctrl Pts',(5.61751828214736,-2.72370799036984,85.5646279041665));
#49550=CARTESIAN_POINT('Ctrl Pts',(6.21697111973009,-0.569532232192492,
85.6574358553822));
#49551=CARTESIAN_POINT('Ctrl Pts',(5.77259366226549,1.34197978769155,85.7502438065979));
#49552=CARTESIAN_POINT('Ctrl Pts',(5.32821620480093,3.25349180757538,85.8430517578136));
#49553=CARTESIAN_POINT('Ctrl Pts',(3.84000845228928,4.92234008916595,85.9358597090294));
#49554=CARTESIAN_POINT('Ctrl Pts',(1.99165866141347,5.58184943514397,86.0286676602451));
#49555=CARTESIAN_POINT('Ctrl Pts',(0.143308870537557,6.24135878112202,86.1214756114608));
#49556=CARTESIAN_POINT('Ctrl Pts',(-2.06518295870255,5.89152919148742,86.2142835626764));
#49557=CARTESIAN_POINT('Ctrl Pts',(-3.61922734706008,4.69307369966558,86.3070915138921));
#49558=CARTESIAN_POINT('Ctrl Pts',(-5.03992471856324,3.5974534073171,86.3919359451932));
#49559=CARTESIAN_POINT('Ctrl Pts',(-5.91366772982529,1.79259413194367,86.4767803764943));
#49560=CARTESIAN_POINT('Ctrl Pts',(-5.92469646081808,-0.00297539080508188,
86.5616248077953));
#49561=CARTESIAN_POINT('Origin',(0.,0.,-10.));
#49562=CARTESIAN_POINT('',(-5.92187722747348,0.00448342927688694,88.5633751922048));
#49563=CARTESIAN_POINT('',(-5.91874116782466,0.00528482168223352,88.3116248077953));
#49564=CARTESIAN_POINT('',(-5.91675,-7.2459289488551E-16,-10.));
#49565=CARTESIAN_POINT('Ctrl Pts',(-5.92187722747348,0.00448342927688694,
88.5633751922048));
#49566=CARTESIAN_POINT('Ctrl Pts',(-5.92427836346706,0.289816032030938,
88.5499094335332));
#49567=CARTESIAN_POINT('Ctrl Pts',(-5.9054462137803,0.574830296895836,88.5364436748616));
#49568=CARTESIAN_POINT('Ctrl Pts',(-5.86429109524329,0.856583895585025,
88.52297791619));
#49569=CARTESIAN_POINT('Ctrl Pts',(-5.58069968339791,2.79808968356919,88.4301881576132));
#49570=CARTESIAN_POINT('Ctrl Pts',(-4.23714604467594,4.58476915772875,88.3373983990364));
#49571=CARTESIAN_POINT('Ctrl Pts',(-2.45064231334397,5.39610954966386,88.2446086404596));
#49572=CARTESIAN_POINT('Ctrl Pts',(-0.664138582012099,6.20744994159892,
88.1518188818829));
#49573=CARTESIAN_POINT('Ctrl Pts',(1.56531524192973,6.04345125130962,88.0590291233061));
#49574=CARTESIAN_POINT('Ctrl Pts',(3.21386717184441,4.97942806170208,87.9662393647294));
#49575=CARTESIAN_POINT('Ctrl Pts',(4.8624191017591,3.91540487209454,87.8734496061526));
#49576=CARTESIAN_POINT('Ctrl Pts',(5.93006913764664,1.95135718316875,87.7806598475759));
#49577=CARTESIAN_POINT('Ctrl Pts',(5.92651082034749,-0.0107478476657502,
87.6878700889991));
#49578=CARTESIAN_POINT('Ctrl Pts',(5.92295250304835,-1.97285287850036,87.5950803304223));
#49579=CARTESIAN_POINT('Ctrl Pts',(4.84818583256239,-3.93301525124367,87.5022905718456));
#49580=CARTESIAN_POINT('Ctrl Pts',(3.19578550370114,-4.99105209692896,87.4095008132688));
#49581=CARTESIAN_POINT('Ctrl Pts',(1.54338517483998,-6.0490889426142,87.316711054692));
#49582=CARTESIAN_POINT('Ctrl Pts',(-0.686648812396377,-6.20500026124158,
87.2239212961153));
#49583=CARTESIAN_POINT('Ctrl Pts',(-2.47019803780075,-5.38718550580641,
87.1311315375386));
#49584=CARTESIAN_POINT('Ctrl Pts',(-4.25374726320513,-4.56937075037125,
87.0383417789618));
#49585=CARTESIAN_POINT('Ctrl Pts',(-5.59081172677752,-2.77782992087354,
86.9455520203851));
#49586=CARTESIAN_POINT('Ctrl Pts',(-5.867359376098,-0.83530830933267,86.8527622618084));
#49587=CARTESIAN_POINT('Ctrl Pts',(-5.90648869984939,-0.560456734138262,
86.8396332386071));
#49588=CARTESIAN_POINT('Ctrl Pts',(-5.92438644427727,-0.282582519031695,
86.826504215406));
#49589=CARTESIAN_POINT('Ctrl Pts',(-5.92207245583525,-0.00440905045111684,
86.8133751922048));
#49590=CARTESIAN_POINT('Ctrl Pts',(-5.92469646081808,-0.00297539080508188,
86.5616248077953));
#49591=CARTESIAN_POINT('Ctrl Pts',(-5.92573162031586,-0.171508003179695,
86.56958832771));
#49592=CARTESIAN_POINT('Ctrl Pts',(-5.9191664849481,-0.339958775180508,
86.5775518476247));
#49593=CARTESIAN_POINT('Ctrl Pts',(-5.90473995753208,-0.507733566080088,
86.5855153675394));
#49594=CARTESIAN_POINT('Ctrl Pts',(-5.73661123217162,-2.46300394599478,
86.6783233187551));
#49595=CARTESIAN_POINT('Ctrl Pts',(-4.5007568339759,-4.32646331181517,86.7711312699708));
#49596=CARTESIAN_POINT('Ctrl Pts',(-2.76493293649683,-5.24203139983684,
86.8639392211865));
#49597=CARTESIAN_POINT('Ctrl Pts',(-1.02910903901766,-6.15759948785856,
86.9567471724022));
#49598=CARTESIAN_POINT('Ctrl Pts',(1.20668435774482,-6.12527629808141,87.0495551236178));
#49599=CARTESIAN_POINT('Ctrl Pts',(2.9153153314122,-5.15991122584811,87.1423630748336));
#49600=CARTESIAN_POINT('Ctrl Pts',(4.62394630507958,-4.19454615361481,87.2351710260493));
#49601=CARTESIAN_POINT('Ctrl Pts',(5.80541485565174,-2.29613919892545,87.327978977265));
#49602=CARTESIAN_POINT('Ctrl Pts',(5.91694987317906,-0.336825679672146,
87.4207869284808));
#49603=CARTESIAN_POINT('Ctrl Pts',(6.02848489070638,1.62248783958105,87.5135948796964));
#49604=CARTESIAN_POINT('Ctrl Pts',(5.07008637518878,3.64270792339829,87.6064028309121));
#49605=CARTESIAN_POINT('Ctrl Pts',(3.4820462208031,4.7957378427507,87.6992107821278));
#49606=CARTESIAN_POINT('Ctrl Pts',(1.89400606641742,5.94876776210311,87.7920187333436));
#49607=CARTESIAN_POINT('Ctrl Pts',(-0.323675726836286,6.23460751699098,
87.8848266845593));
#49608=CARTESIAN_POINT('Ctrl Pts',(-2.15218777556883,5.52194124551253,87.977634635775));
#49609=CARTESIAN_POINT('Ctrl Pts',(-3.98069982430137,4.80927497403408,88.0704425869907));
#49610=CARTESIAN_POINT('Ctrl Pts',(-5.42004212851265,3.09810267618934,88.1632505382064));
#49611=CARTESIAN_POINT('Ctrl Pts',(-5.80897540284391,1.1745433620581,88.2560584894221));
#49612=CARTESIAN_POINT('Ctrl Pts',(-5.88659659034037,0.790649856316099,
88.2745805955465));
#49613=CARTESIAN_POINT('Ctrl Pts',(-5.92237998049169,0.398296974565935,
88.2931027016709));
#49614=CARTESIAN_POINT('Ctrl Pts',(-5.91874116782466,0.00528482168223352,
88.3116248077953));
#49615=CARTESIAN_POINT('Origin',(0.,0.,-10.));
#49616=CARTESIAN_POINT('',(-5.9076957588592,0.00217524021099064,90.3133751922047));
#49617=CARTESIAN_POINT('',(-5.90697520874472,0.000492460854587244,90.0616248077953));
#49618=CARTESIAN_POINT('',(-5.91675,-7.2459289488551E-16,-10.));
#49619=CARTESIAN_POINT('Ctrl Pts',(-5.9076957588592,0.00217524021099064,
90.3133751922047));
#49620=CARTESIAN_POINT('Ctrl Pts',(-5.91050674814863,0.856231332472319,
90.2733146516603));
#49621=CARTESIAN_POINT('Ctrl Pts',(-5.73758377480165,1.70920259929656,90.2332541111159));
#49622=CARTESIAN_POINT('Ctrl Pts',(-5.38329452751489,2.47866618364667,90.1931935705715));
#49623=CARTESIAN_POINT('Ctrl Pts',(-4.56267620146798,4.26092721295859,90.1004038119948));
#49624=CARTESIAN_POINT('Ctrl Pts',(-2.76903509011887,5.59517287519017,90.007614053418));
#49625=CARTESIAN_POINT('Ctrl Pts',(-0.826081016675218,5.86866562123062,
89.9148242948413));
#49626=CARTESIAN_POINT('Ctrl Pts',(1.11687305676854,6.14215836727109,89.8220345362645));
#49627=CARTESIAN_POINT('Ctrl Pts',(3.20914009230686,5.35489819712032,89.7292447776878));
#49628=CARTESIAN_POINT('Ctrl Pts',(4.48986961709886,3.86842562825989,89.636455019111));
#49629=CARTESIAN_POINT('Ctrl Pts',(5.77059914189078,2.38195305939954,89.5436652605342));
#49630=CARTESIAN_POINT('Ctrl Pts',(6.23979115593646,0.196268091829603,89.4508755019574));
#49631=CARTESIAN_POINT('Ctrl Pts',(5.68197442115233,-1.684877650542,89.3580857433807));
#49632=CARTESIAN_POINT('Ctrl Pts',(5.1241576863682,-3.5660233929136,89.265295984804));
#49633=CARTESIAN_POINT('Ctrl Pts',(3.53933220275425,-5.14262991008687,89.1725062262272));
#49634=CARTESIAN_POINT('Ctrl Pts',(1.65531152825281,-5.6906581134662,89.0797164676505));
#49635=CARTESIAN_POINT('Ctrl Pts',(-0.228709146248734,-6.23868631684556,
88.9869267090737));
#49636=CARTESIAN_POINT('Ctrl Pts',(-2.4119250116378,-5.75813620643085,88.8941369504969));
#49637=CARTESIAN_POINT('Ctrl Pts',(-3.89171835184781,-4.46969510031906,
88.8013471919202));
#49638=CARTESIAN_POINT('Ctrl Pts',(-5.15676234569935,-3.3682340797641,88.722023192015));
#49639=CARTESIAN_POINT('Ctrl Pts',(-5.90773263183859,-1.67635193290292,
88.6426991921099));
#49640=CARTESIAN_POINT('Ctrl Pts',(-5.92187722747348,0.00448342927688694,
88.5633751922048));
#49641=CARTESIAN_POINT('Ctrl Pts',(-5.91874116782466,0.00528482168223352,
88.3116248077953));
#49642=CARTESIAN_POINT('Ctrl Pts',(-5.90414713233627,-1.57095276771637,
88.3859106528866));
#49643=CARTESIAN_POINT('Ctrl Pts',(-5.25543187432754,-3.15779498565621,
88.4601964979779));
#49644=CARTESIAN_POINT('Ctrl Pts',(-4.12843259412039,-4.25203382583027,
88.5344823430692));
#49645=CARTESIAN_POINT('Ctrl Pts',(-2.72043226661461,-5.61910536916916,
88.6272902942849));
#49646=CARTESIAN_POINT('Ctrl Pts',(-0.56590736715238,-6.2173021254292,88.7200982455007));
#49647=CARTESIAN_POINT('Ctrl Pts',(1.34534523618347,-5.77181024771941,88.8129061967164));
#49648=CARTESIAN_POINT('Ctrl Pts',(3.2565978395191,-5.32631837000967,88.9057141479321));
#49649=CARTESIAN_POINT('Ctrl Pts',(4.92457814672832,-3.83713785832991,88.9985220991478));
#49650=CARTESIAN_POINT('Ctrl Pts',(5.58300971119721,-1.98840385859563,89.0913300503635));
#49651=CARTESIAN_POINT('Ctrl Pts',(6.24144127566621,-0.13966985886104,89.1841380015792));
#49652=CARTESIAN_POINT('Ctrl Pts',(5.89032409739495,2.06861762892818,89.276945952795));
#49653=CARTESIAN_POINT('Ctrl Pts',(4.69096273288672,3.62196300075916,89.3697539040107));
#49654=CARTESIAN_POINT('Ctrl Pts',(3.49160136837863,5.17530837258996,89.4625618552264));
#49655=CARTESIAN_POINT('Ctrl Pts',(1.44399581763367,6.07371162846243,89.555369806442));
#49656=CARTESIAN_POINT('Ctrl Pts',(-0.511176203484458,5.90444292284984,
89.6481777576577));
#49657=CARTESIAN_POINT('Ctrl Pts',(-2.4663482246027,5.73517421723724,89.7409857088734));
#49658=CARTESIAN_POINT('Ctrl Pts',(-4.32908671609423,4.49823355013946,89.8337936600891));
#49659=CARTESIAN_POINT('Ctrl Pts',(-5.24364258664101,2.76187613114078,89.9266016113049));
#49660=CARTESIAN_POINT('Ctrl Pts',(-5.68716154305487,1.91981994273608,89.9716093434683));
#49661=CARTESIAN_POINT('Ctrl Pts',(-5.90768511163,0.960309975045309,90.0166170756318));
#49662=CARTESIAN_POINT('Ctrl Pts',(-5.90697520874472,0.000492460854587244,
90.0616248077953));
#49663=CARTESIAN_POINT('Origin',(0.,0.,-10.));
#49664=CARTESIAN_POINT('',(-5.91387952939735,-0.00529439012957766,92.0633751922047));
#49665=CARTESIAN_POINT('',(-5.9169276701952,-0.00545620570378101,91.8116248077953));
#49666=CARTESIAN_POINT('',(-5.91675,-7.2459289488551E-16,-10.));
#49667=CARTESIAN_POINT('Ctrl Pts',(-5.91387952939735,-0.00529439012957766,
92.0633751922047));
#49668=CARTESIAN_POINT('Ctrl Pts',(-5.90168899007384,1.41200501326097,91.9967198697875));
#49669=CARTESIAN_POINT('Ctrl Pts',(-5.39078924113146,2.8371923802721,91.9300645473704));
#49670=CARTESIAN_POINT('Ctrl Pts',(-4.46356995507357,3.89874201199438,91.8634092249532));
#49671=CARTESIAN_POINT('Ctrl Pts',(-3.17280350790947,5.37650748476838,91.7706194663764));
#49672=CARTESIAN_POINT('Ctrl Pts',(-1.07525317628989,6.14958091583901,91.6778297077997));
#49673=CARTESIAN_POINT('Ctrl Pts',(0.865804271709872,5.86293689058771,91.5850399492229));
#49674=CARTESIAN_POINT('Ctrl Pts',(2.80686171970985,5.57629286533638,91.4922501906461));
#49675=CARTESIAN_POINT('Ctrl Pts',(4.59142628408996,4.22993138376282,91.3994604320693));
#49676=CARTESIAN_POINT('Ctrl Pts',(5.39995644535267,2.44215405087794,91.3066706734926));
#49677=CARTESIAN_POINT('Ctrl Pts',(6.20848660661528,0.654376717993263,91.2138809149158));
#49678=CARTESIAN_POINT('Ctrl Pts',(6.04098236476071,-1.57481646620264,91.1210911563391));
#49679=CARTESIAN_POINT('Ctrl Pts',(4.97436818844188,-3.22169321099058,91.0283013977624));
#49680=CARTESIAN_POINT('Ctrl Pts',(3.90775401212288,-4.86856995577879,90.9355116391856));
#49681=CARTESIAN_POINT('Ctrl Pts',(1.94202990133927,-5.93313026115881,90.8427218806088));
#49682=CARTESIAN_POINT('Ctrl Pts',(-0.020067108320463,-5.92648659250057,
90.749932122032));
#49683=CARTESIAN_POINT('Ctrl Pts',(-1.98216411797986,-5.91984292384233,
90.6571423634553));
#49684=CARTESIAN_POINT('Ctrl Pts',(-3.94063402651538,-4.84199528114619,
90.5643526048786));
#49685=CARTESIAN_POINT('Ctrl Pts',(-4.99607121041088,-3.18793326160208,
90.4715628463019));
#49686=CARTESIAN_POINT('Ctrl Pts',(-5.59583974351959,-2.24798689030669,
90.4188336282695));
#49687=CARTESIAN_POINT('Ctrl Pts',(-5.90399582707808,-1.12196610408279,
90.3661044102371));
#49688=CARTESIAN_POINT('Ctrl Pts',(-5.9076957588592,0.00217524021099064,
90.3133751922047));
#49689=CARTESIAN_POINT('Ctrl Pts',(-5.90697520874472,0.000492460854587244,
90.0616248077953));
#49690=CARTESIAN_POINT('Ctrl Pts',(-5.90622126021652,-1.01887655027118,
90.1094250268476));
#49691=CARTESIAN_POINT('Ctrl Pts',(-5.6559295087634,-2.03859245500849,90.1572252458998));
#49692=CARTESIAN_POINT('Ctrl Pts',(-5.15821059145769,-2.91832329161354,
90.2050254649521));
#49693=CARTESIAN_POINT('Ctrl Pts',(-4.19184947612554,-4.62639112446941,
90.2978334161678));
#49694=CARTESIAN_POINT('Ctrl Pts',(-2.29275399585916,-5.80675261928172,
90.3906413673834));
#49695=CARTESIAN_POINT('Ctrl Pts',(-0.333375779798765,-5.91714525169392,
90.4834493185991));
#49696=CARTESIAN_POINT('Ctrl Pts',(1.62600243626174,-6.02753788410612,90.5762572698148));
#49697=CARTESIAN_POINT('Ctrl Pts',(3.64566338811639,-5.06796165411809,90.6690652210306));
#49698=CARTESIAN_POINT('Ctrl Pts',(4.79776721406981,-3.47924950237795,90.7618731722463));
#49699=CARTESIAN_POINT('Ctrl Pts',(5.94987104002329,-1.89053735063771,90.854681123462));
#49700=CARTESIAN_POINT('Ctrl Pts',(6.23441774007554,0.327310722854481,90.9474890746777));
#49701=CARTESIAN_POINT('Ctrl Pts',(5.52068548659514,2.1554069449406,91.0402970258934));
#49702=CARTESIAN_POINT('Ctrl Pts',(4.80695323311482,3.98350316702652,91.1331049771091));
#49703=CARTESIAN_POINT('Ctrl Pts',(3.09494202610193,5.42184753770625,91.2259129283248));
#49704=CARTESIAN_POINT('Ctrl Pts',(1.17115627367356,5.80965922605064,91.3187208795405));
#49705=CARTESIAN_POINT('Ctrl Pts',(-0.752629478754913,6.19747091439506,
91.4115288307563));
#49706=CARTESIAN_POINT('Ctrl Pts',(-2.88818977659902,5.53474992040405,91.5043367819719));
#49707=CARTESIAN_POINT('Ctrl Pts',(-4.25444016131426,4.12595276923969,91.5971447331876));
#49708=CARTESIAN_POINT('Ctrl Pts',(-5.30691278752029,3.04070481318033,91.6686380913902));
#49709=CARTESIAN_POINT('Ctrl Pts',(-5.90286273979908,1.51272152196721,91.7401314495928));
#49710=CARTESIAN_POINT('Ctrl Pts',(-5.9169276701952,-0.00545620570378101,
91.8116248077953));
#49711=CARTESIAN_POINT('Origin',(0.,0.,-10.));
#49712=CARTESIAN_POINT('',(-5.92651347487416,0.000183341992167018,93.8133751922047));
#49713=CARTESIAN_POINT('',(-5.92571112046846,0.00200453863705335,93.5616248077953));
#49714=CARTESIAN_POINT('',(-5.91675,-7.2459289488551E-16,-10.));
#49715=CARTESIAN_POINT('Ctrl Pts',(-5.92651347487416,0.000183341992167018,
93.8133751922047));
#49716=CARTESIAN_POINT('Ctrl Pts',(-5.92651787928802,0.00991772496236695,
93.8129148464915));
#49717=CARTESIAN_POINT('Ctrl Pts',(-5.92649597763976,0.0196520875258746,
93.8124545007783));
#49718=CARTESIAN_POINT('Ctrl Pts',(-5.92644771040461,0.0293863193554934,
93.811994155065));
#49719=CARTESIAN_POINT('Ctrl Pts',(-5.91671870681498,1.99147045622047,93.7192043964883));
#49720=CARTESIAN_POINT('Ctrl Pts',(-4.83579275707057,3.94824305789768,93.6264146379115));
#49721=CARTESIAN_POINT('Ctrl Pts',(-3.18007313679368,5.00107797025487,93.5336248793348));
#49722=CARTESIAN_POINT('Ctrl Pts',(-1.52435351651669,6.05391288261212,93.440835120758));
#49723=CARTESIAN_POINT('Ctrl Pts',(0.70615977429284,6.20281010564926,93.3480453621812));
#49724=CARTESIAN_POINT('Ctrl Pts',(2.48712820056795,5.37939023810924,93.2552556036045));
#49725=CARTESIAN_POINT('Ctrl Pts',(4.26809662684306,4.55597037056921,93.1624658450277));
#49726=CARTESIAN_POINT('Ctrl Pts',(5.59952018858376,2.76023341245207,93.069676086451));
#49727=CARTESIAN_POINT('Ctrl Pts',(5.86995735508652,0.816851681390876,92.9768863278743));
#49728=CARTESIAN_POINT('Ctrl Pts',(6.14039452158924,-1.1265300496701,92.8840965692975));
#49729=CARTESIAN_POINT('Ctrl Pts',(5.3498452928543,-3.2175565536751,92.7913068107207));
#49730=CARTESIAN_POINT('Ctrl Pts',(3.86136065010522,-4.49594705815631,92.6985170521439));
#49731=CARTESIAN_POINT('Ctrl Pts',(2.37287600735604,-5.77433756263759,92.6057272935672));
#49732=CARTESIAN_POINT('Ctrl Pts',(0.186455950592636,-6.240092067595,92.5129375349904));
#49733=CARTESIAN_POINT('Ctrl Pts',(-1.69381031470308,-5.67931797293749,
92.4201477764137));
#49734=CARTESIAN_POINT('Ctrl Pts',(-3.57407657999879,-5.11854387827999,
92.3273580178369));
#49735=CARTESIAN_POINT('Ctrl Pts',(-5.14818905382682,-3.53124118400757,
92.2345682592602));
#49736=CARTESIAN_POINT('Ctrl Pts',(-5.69325400938658,-1.64636107963258,
92.1417785006834));
#49737=CARTESIAN_POINT('Ctrl Pts',(-5.84677273281456,-1.11548052221118,
92.1156440645238));
#49738=CARTESIAN_POINT('Ctrl Pts',(-5.91865923580559,-0.560993761667654,
92.0895096283643));
#49739=CARTESIAN_POINT('Ctrl Pts',(-5.91387952939735,-0.00529439012957766,
92.0633751922047));
#49740=CARTESIAN_POINT('Ctrl Pts',(-5.9169276701952,-0.00545620570378101,
91.8116248077953));
#49741=CARTESIAN_POINT('Ctrl Pts',(-5.92112090261132,-0.458076437856095,
91.8329394008085));
#49742=CARTESIAN_POINT('Ctrl Pts',(-5.87359397348391,-0.909825114097263,
91.8542539938217));
#49743=CARTESIAN_POINT('Ctrl Pts',(-5.77102487110158,-1.34871022733847,
91.8755685868349));
#49744=CARTESIAN_POINT('Ctrl Pts',(-5.32441872458721,-3.25970276441396,
91.9683765380506));
#49745=CARTESIAN_POINT('Ctrl Pts',(-3.83426595997241,-4.9268145302274,92.0611844892662));
#49746=CARTESIAN_POINT('Ctrl Pts',(-1.98514837983892,-5.58416808935971,
92.1539924404818));
#49747=CARTESIAN_POINT('Ctrl Pts',(-0.136030799705217,-6.24152164849209,
92.2468003916975));
#49748=CARTESIAN_POINT('Ctrl Pts',(2.07205159594715,-5.88911700094308,92.3396083429134));
#49749=CARTESIAN_POINT('Ctrl Pts',(3.62469742320657,-4.68885017145995,92.4324162941291));
#49750=CARTESIAN_POINT('Ctrl Pts',(5.17734325046581,-3.48858334197697,92.5252242453448));
#49751=CARTESIAN_POINT('Ctrl Pts',(6.07455250933224,-1.44045433055982,92.6180321965605));
#49752=CARTESIAN_POINT('Ctrl Pts',(5.90414388100869,0.514618667119702,92.7108401477762));
#49753=CARTESIAN_POINT('Ctrl Pts',(5.73373525268511,2.46969166479956,92.8036480989918));
#49754=CARTESIAN_POINT('Ctrl Pts',(4.49570873717139,4.33170864874189,92.8964560502076));
#49755=CARTESIAN_POINT('Ctrl Pts',(2.75881838691105,5.2452519909192,92.9892640014233));
#49756=CARTESIAN_POINT('Ctrl Pts',(1.02192803665091,6.15879533309641,93.0820719526391));
#49757=CARTESIAN_POINT('Ctrl Pts',(-1.21382614835559,6.1238650335088,93.1748799038548));
#49758=CARTESIAN_POINT('Ctrl Pts',(-2.9213302597588,5.15650820358292,93.2676878550704));
#49759=CARTESIAN_POINT('Ctrl Pts',(-4.628834371162,4.18915137365705,93.3604958062862));
#49760=CARTESIAN_POINT('Ctrl Pts',(-5.80808840896181,2.28936801339296,93.4533037575018));
#49761=CARTESIAN_POINT('Ctrl Pts',(-5.91733861873187,0.329925766597139,
93.5461117087175));
#49762=CARTESIAN_POINT('Ctrl Pts',(-5.92342577436248,0.220750416448644,
93.5512827417434));
#49763=CARTESIAN_POINT('Ctrl Pts',(-5.92619115980276,0.111389858447922,
93.5564537747694));
#49764=CARTESIAN_POINT('Ctrl Pts',(-5.92571112046846,0.00200453863705335,
93.5616248077953));
#49765=CARTESIAN_POINT('Origin',(0.,0.,-10.));
#49766=CARTESIAN_POINT('',(-5.91332833078945,0.00520191486789418,95.5633751922047));
#49767=CARTESIAN_POINT('',(-5.91081306495006,0.00447103847887896,95.3116248077953));
#49768=CARTESIAN_POINT('',(-5.91675,-7.2459289488551E-16,-10.));
#49769=CARTESIAN_POINT('Ctrl Pts',(-5.91332833078945,0.00520191486789418,
95.5633751922047));
#49770=CARTESIAN_POINT('Ctrl Pts',(-5.91815610750766,0.5806138957877,95.5363200646187));
#49771=CARTESIAN_POINT('Ctrl Pts',(-5.84101679508192,1.15475888064953,95.5092649370326));
#49772=CARTESIAN_POINT('Ctrl Pts',(-5.67664748164019,1.70273879062923,95.4822098094466));
#49773=CARTESIAN_POINT('Ctrl Pts',(-5.11291741371888,3.58212092957008,95.3894200508698));
#49774=CARTESIAN_POINT('Ctrl Pts',(-3.52314143366452,5.15373546779132,95.2966302922931));
#49775=CARTESIAN_POINT('Ctrl Pts',(-1.63740656010343,5.69583582776537,95.2038405337164));
#49776=CARTESIAN_POINT('Ctrl Pts',(0.248328313457552,6.2379361877394,95.1110507751396));
#49777=CARTESIAN_POINT('Ctrl Pts',(2.43002208052523,5.75052236946637,95.0182610165629));
#49778=CARTESIAN_POINT('Ctrl Pts',(3.90575603183626,4.45743377288996,94.9254712579861));
#49779=CARTESIAN_POINT('Ctrl Pts',(5.38148998314738,3.16434517631346,94.8326814994093));
#49780=CARTESIAN_POINT('Ctrl Pts',(6.15126411870176,1.06558180143349,94.7398917408325));
#49781=CARTESIAN_POINT('Ctrl Pts',(5.86156818882048,-0.875022506986626,
94.6471019822558));
#49782=CARTESIAN_POINT('Ctrl Pts',(5.57187225893923,-2.81562681540652,94.554312223679));
#49783=CARTESIAN_POINT('Ctrl Pts',(4.22270626362261,-4.59807205736659,94.4615224651023));
#49784=CARTESIAN_POINT('Ctrl Pts',(2.43365974976944,-5.40378998872806,94.3687327065256));
#49785=CARTESIAN_POINT('Ctrl Pts',(0.644613235916068,-6.20950792008962,
94.2759429479488));
#49786=CARTESIAN_POINT('Ctrl Pts',(-1.58431379647396,-6.03849854085236,
94.183153189372));
#49787=CARTESIAN_POINT('Ctrl Pts',(-3.22951128395157,-4.96929601520727,
94.0903634307953));
#49788=CARTESIAN_POINT('Ctrl Pts',(-4.86654666795568,-3.90539798444189,
93.9980340179318));
#49789=CARTESIAN_POINT('Ctrl Pts',(-5.92563010193588,-1.95219687661127,
93.9057046050682));
#49790=CARTESIAN_POINT('Ctrl Pts',(-5.92651347487416,0.000183341992167018,
93.8133751922047));
#49791=CARTESIAN_POINT('Ctrl Pts',(-5.92571112046846,0.00200453863705335,
93.5616248077953));
#49792=CARTESIAN_POINT('Ctrl Pts',(-5.91757557624406,-1.85182085280855,
93.6492617259851));
#49793=CARTESIAN_POINT('Ctrl Pts',(-4.97727862618378,-3.7127584114918,93.7368986441749));
#49794=CARTESIAN_POINT('Ctrl Pts',(-3.47645160121493,-4.79979495443404,
93.8245355623647));
#49795=CARTESIAN_POINT('Ctrl Pts',(-1.88706799218794,-5.95097229534155,
93.9173435135804));
#49796=CARTESIAN_POINT('Ctrl Pts',(0.33094560760626,-6.23422584382928,94.0101514647961));
#49797=CARTESIAN_POINT('Ctrl Pts',(2.15862538160178,-5.51942785097377,94.1029594160118));
#49798=CARTESIAN_POINT('Ctrl Pts',(3.98630515559761,-4.80462985811814,94.1957673672275));
#49799=CARTESIAN_POINT('Ctrl Pts',(5.4236511037946,-3.09178032391887,94.2885753184432));
#49800=CARTESIAN_POINT('Ctrl Pts',(5.8103410743193,-1.16776878716565,94.3813832696589));
#49801=CARTESIAN_POINT('Ctrl Pts',(6.19703104484399,0.756242749587451,94.4741912208746));
#49802=CARTESIAN_POINT('Ctrl Pts',(5.53306503769651,2.89141628889448,94.5669991720904));
#49803=CARTESIAN_POINT('Ctrl Pts',(4.12347154178058,4.25684505054225,94.6598071233061));
#49804=CARTESIAN_POINT('Ctrl Pts',(2.71387804586473,5.62227381218994,94.7526150745219));
#49805=CARTESIAN_POINT('Ctrl Pts',(0.558657061180529,6.21795779617846,94.8454230257375));
#49806=CARTESIAN_POINT('Ctrl Pts',(-1.35207476001135,5.77023753267928,94.9382309769532));
#49807=CARTESIAN_POINT('Ctrl Pts',(-3.26280658120333,5.32251726918006,95.0310389281689));
#49808=CARTESIAN_POINT('Ctrl Pts',(-4.92904923890296,3.83139275819302,95.1238468793846));
#49809=CARTESIAN_POINT('Ctrl Pts',(-5.58532456923768,1.98189222625001,95.2166548306003));
#49810=CARTESIAN_POINT('Ctrl Pts',(-5.80917914325876,1.35103024714942,95.2483114896653));
#49811=CARTESIAN_POINT('Ctrl Pts',(-5.91552580469876,0.678471851738488,
95.2799681487303));
#49812=CARTESIAN_POINT('Ctrl Pts',(-5.91081306495006,0.00447103847887897,
95.3116248077953));
#49813=CARTESIAN_POINT('Origin',(0.,0.,-10.));
#49814=CARTESIAN_POINT('',(-5.90792603807066,-0.00247015932851979,97.3133751922047));
#49815=CARTESIAN_POINT('',(-5.90944591666731,-0.00376931072489263,97.0616248077952));
#49816=CARTESIAN_POINT('',(-5.91675,-7.2459289488551E-16,-10.));
#49817=CARTESIAN_POINT('Ctrl Pts',(-5.90792603807066,-0.00247015932851979,
97.3133751922047));
#49818=CARTESIAN_POINT('Ctrl Pts',(-5.90364159030541,1.14118819633865,97.2597252827458));
#49819=CARTESIAN_POINT('Ctrl Pts',(-5.58390646962752,2.28706147908161,97.206075373287));
#49820=CARTESIAN_POINT('Ctrl Pts',(-4.96421155454115,3.23732137139418,97.1524254638282));
#49821=CARTESIAN_POINT('Ctrl Pts',(-3.89242332335584,4.88083553353004,97.0596357052514));
#49822=CARTESIAN_POINT('Ctrl Pts',(-1.923360954755,5.93920848862016,96.9668459466748));
#49823=CARTESIAN_POINT('Ctrl Pts',(0.0387054577278374,5.92639417415577,
96.8740561880981));
#49824=CARTESIAN_POINT('Ctrl Pts',(2.00077187021056,5.91357985969138,96.7812664295213));
#49825=CARTESIAN_POINT('Ctrl Pts',(3.95584232657529,4.82957827567259,96.6884766709445));
#49826=CARTESIAN_POINT('Ctrl Pts',(5.00607236408032,3.17220514871227,96.5956869123677));
#49827=CARTESIAN_POINT('Ctrl Pts',(6.0563024015854,1.51483202175186,96.502897153791));
#49828=CARTESIAN_POINT('Ctrl Pts',(6.20169202023064,-0.71591264815017,96.4101073952143));
#49829=CARTESIAN_POINT('Ctrl Pts',(5.37547264724376,-2.49558406764019,96.3173176366375));
#49830=CARTESIAN_POINT('Ctrl Pts',(4.54925327425696,-4.27525548713001,96.2245278780607));
#49831=CARTESIAN_POINT('Ctrl Pts',(2.75142490963826,-5.60385365620792,96.1317381194839));
#49832=CARTESIAN_POINT('Ctrl Pts',(0.807620326302736,-5.87123457447137,
96.0389483609071));
#49833=CARTESIAN_POINT('Ctrl Pts',(-1.13618425703301,-6.13861549273485,
95.9461586023304));
#49834=CARTESIAN_POINT('Ctrl Pts',(-3.22596505908562,-5.34477916018357,
95.8533688437537));
#49835=CARTESIAN_POINT('Ctrl Pts',(-4.50201338221775,-3.85428612407767,
95.7605790851769));
#49836=CARTESIAN_POINT('Ctrl Pts',(-5.40599855185311,-2.79838285171782,
95.6948444541862));
#49837=CARTESIAN_POINT('Ctrl Pts',(-5.90159849805931,-1.39285078745819,
95.6291098231954));
#49838=CARTESIAN_POINT('Ctrl Pts',(-5.91332833078945,0.00520191486789418,
95.5633751922047));
#49839=CARTESIAN_POINT('Ctrl Pts',(-5.91081306495006,0.00447103847887897,
95.3116248077953));
#49840=CARTESIAN_POINT('Ctrl Pts',(-5.90170944714215,-1.29749896905956,
95.3727760999461));
#49841=CARTESIAN_POINT('Ctrl Pts',(-5.47818989466327,-2.60485132995615,
95.4339273920968));
#49842=CARTESIAN_POINT('Ctrl Pts',(-4.68673601610343,-3.62743061347276,
95.4950786842475));
#49843=CARTESIAN_POINT('Ctrl Pts',(-3.48556412966475,-5.17937636835338,
95.5878866354632));
#49844=CARTESIAN_POINT('Ctrl Pts',(-1.43691235381768,-6.07539132521594,
95.6806945866788));
#49845=CARTESIAN_POINT('Ctrl Pts',(0.518060955814923,-5.90384283211033,
95.7735025378945));
#49846=CARTESIAN_POINT('Ctrl Pts',(2.47303426544775,-5.7322943390047,95.8663104891102));
#49847=CARTESIAN_POINT('Ctrl Pts',(4.33432910886597,-4.49318239593063,95.9591184403261));
#49848=CARTESIAN_POINT('Ctrl Pts',(5.24685961212369,-2.7557597048483,96.0519263915418));
#49849=CARTESIAN_POINT('Ctrl Pts',(6.15939011538146,-1.01833701376587,96.1447343427575));
#49850=CARTESIAN_POINT('Ctrl Pts',(6.12315627847846,1.21739642532511,96.2375422939731));
#49851=CARTESIAN_POINT('Ctrl Pts',(5.15480406280235,2.92433623482607,96.3303502451888));
#49852=CARTESIAN_POINT('Ctrl Pts',(4.18645184712642,4.63127604432674,96.4231581964045));
#49853=CARTESIAN_POINT('Ctrl Pts',(2.28598125267787,5.80942222423782,96.5159661476203));
#49854=CARTESIAN_POINT('Ctrl Pts',(0.326475641240406,5.91752997422717,96.608774098836));
#49855=CARTESIAN_POINT('Ctrl Pts',(-1.63302997019728,6.02563772421653,96.7015820500518));
#49856=CARTESIAN_POINT('Ctrl Pts',(-3.65157059862376,5.0637070442839,96.7943900012675));
#49857=CARTESIAN_POINT('Ctrl Pts',(-4.80182106315389,3.47365251826545,96.8871979524832));
#49858=CARTESIAN_POINT('Ctrl Pts',(-5.52242947626645,2.47751584708868,96.9453402375872));
#49859=CARTESIAN_POINT('Ctrl Pts',(-5.90225427633181,1.23485523424981,97.0034825226912));
#49860=CARTESIAN_POINT('Ctrl Pts',(-5.90944591666731,-0.00376931072489263,
97.0616248077952));
#49861=CARTESIAN_POINT('Origin',(0.,0.,-10.));
#49862=CARTESIAN_POINT('',(-5.92240521329814,-0.00427408358304571,99.0633751922047));
#49863=CARTESIAN_POINT('',(-5.92460418473688,-0.00304573894302621,98.8116248077953));
#49864=CARTESIAN_POINT('',(-5.91675,-7.2459289488551E-16,-10.));
#49865=CARTESIAN_POINT('Ctrl Pts',(-5.92240521329814,-0.00427408358304571,
99.0633751922047));
#49866=CARTESIAN_POINT('Ctrl Pts',(-5.90857090463864,1.69567528425797,98.9831305008731));
#49867=CARTESIAN_POINT('Ctrl Pts',(-5.13791585564116,3.40656874746623,98.9028858095415));
#49868=CARTESIAN_POINT('Ctrl Pts',(-3.84720206766997,4.50806857428337,98.8226411182099));
#49869=CARTESIAN_POINT('Ctrl Pts',(-2.35470432370565,5.78177156081904,98.7298513596331));
#49870=CARTESIAN_POINT('Ctrl Pts',(-0.166830309248996,6.24064760113001,
98.6370616010563));
#49871=CARTESIAN_POINT('Ctrl Pts',(1.71166305624391,5.67396295386347,98.5442718424796));
#49872=CARTESIAN_POINT('Ctrl Pts',(3.59015642173671,5.10727830659696,98.4514820839028));
#49873=CARTESIAN_POINT('Ctrl Pts',(5.15926913826582,3.5150329717531,98.358692325326));
#49874=CARTESIAN_POINT('Ctrl Pts',(5.69840356221848,1.62844799180725,98.2659025667493));
#49875=CARTESIAN_POINT('Ctrl Pts',(6.23753798617111,-0.258136988138488,
98.1731128081725));
#49876=CARTESIAN_POINT('Ctrl Pts',(5.74669411754747,-2.43906161318616,98.0803230495959));
#49877=CARTESIAN_POINT('Ctrl Pts',(4.45128656894101,-3.91276039403012,97.9875332910191));
#49878=CARTESIAN_POINT('Ctrl Pts',(3.1558790203344,-5.38645917487425,97.8947435324424));
#49879=CARTESIAN_POINT('Ctrl Pts',(1.05590779174478,-6.15293211151451,97.8019537738655));
#49880=CARTESIAN_POINT('Ctrl Pts',(-0.884238578620319,-5.86018499332614,
97.7091640152888));
#49881=CARTESIAN_POINT('Ctrl Pts',(-2.82438494898531,-5.56743787513778,
97.616374256712));
#49882=CARTESIAN_POINT('Ctrl Pts',(-4.60470646112579,-4.21547070212091,
97.5235844981354));
#49883=CARTESIAN_POINT('Ctrl Pts',(-5.40761017031105,-2.42515943102177,
97.4307947395586));
#49884=CARTESIAN_POINT('Ctrl Pts',(-5.74628472357815,-1.66998435459344,
97.3916548904407));
#49885=CARTESIAN_POINT('Ctrl Pts',(-5.91105172161379,-0.836816683578498,
97.3525150413227));
#49886=CARTESIAN_POINT('Ctrl Pts',(-5.90792603807066,-0.00247015932851979,
97.3133751922047));
#49887=CARTESIAN_POINT('Ctrl Pts',(-5.90944591666731,-0.00376931072489263,
97.0616248077952));
#49888=CARTESIAN_POINT('Ctrl Pts',(-5.91373372548356,-0.742263589664,97.0962904739069));
#49889=CARTESIAN_POINT('Ctrl Pts',(-5.78555797945132,-1.4793231280736,97.1309561400185));
#49890=CARTESIAN_POINT('Ctrl Pts',(-5.51816833907535,-2.16184308445984,
97.1656218061302));
#49891=CARTESIAN_POINT('Ctrl Pts',(-4.80230484983295,-3.98910578906286,
97.2584297573459));
#49892=CARTESIAN_POINT('Ctrl Pts',(-3.08861757071432,-5.4254528261647,97.3512377085617));
#49893=CARTESIAN_POINT('Ctrl Pts',(-1.16438090368592,-5.8110209474181,97.4440456597775));
#49894=CARTESIAN_POINT('Ctrl Pts',(0.759855763342594,-6.19658906867151,
97.5368536109932));
#49895=CARTESIAN_POINT('Ctrl Pts',(2.89464181828089,-5.53137827407635,97.6296615622089));
#49896=CARTESIAN_POINT('Ctrl Pts',(4.25924849269672,-4.12098891258653,97.7224695134245));
#49897=CARTESIAN_POINT('Ctrl Pts',(5.62385516711231,-2.71059955109695,97.8152774646402));
#49898=CARTESIAN_POINT('Ctrl Pts',(6.21828246100573,-0.555031622713001,
97.9080854158559));
#49899=CARTESIAN_POINT('Ctrl Pts',(5.76944823271977,1.35543883306,98.0008933670716));
#49900=CARTESIAN_POINT('Ctrl Pts',(5.32061400443376,3.26590928883322,98.0937013182874));
#49901=CARTESIAN_POINT('Ctrl Pts',(3.82851825396813,4.93128227199544,98.1865092695031));
#49902=CARTESIAN_POINT('Ctrl Pts',(1.9786353989358,5.586479150438,98.2793172207188));
#49903=CARTESIAN_POINT('Ctrl Pts',(0.128752543903576,6.24167602888052,98.3721251719345));
#49904=CARTESIAN_POINT('Ctrl Pts',(-2.07891741569531,5.88669680260349,98.4649331231502));
#49905=CARTESIAN_POINT('Ctrl Pts',(-3.63016257062835,4.68462026753603,98.5577410743659));
#49906=CARTESIAN_POINT('Ctrl Pts',(-5.04468185925873,3.58849407506693,98.642368985509));
#49907=CARTESIAN_POINT('Ctrl Pts',(-5.91339068653511,1.7880151987318,98.7269968966522));
#49908=CARTESIAN_POINT('Ctrl Pts',(-5.92460418473688,-0.00304573894302621,
98.8116248077953));
#49909=CARTESIAN_POINT('Origin',(0.,0.,-10.));
#49910=CARTESIAN_POINT('',(-5.92153330141852,0.0046063294329908,100.813375192205));
#49911=CARTESIAN_POINT('',(-5.91888098557728,0.00526341932157319,100.561624807795));
#49912=CARTESIAN_POINT('',(-5.91675,-7.2459289488551E-16,-10.));
#49913=CARTESIAN_POINT('Ctrl Pts',(-5.92153330141852,0.0046063294329908,
100.813375192205));
#49914=CARTESIAN_POINT('Ctrl Pts',(-5.92408513419437,0.302357637627171,
100.799325477577));
#49915=CARTESIAN_POINT('Ctrl Pts',(-5.90357534973135,0.599756241770384,
100.785275762949));
#49916=CARTESIAN_POINT('Ctrl Pts',(-5.85878730752478,0.893452463823286,
100.771226048322));
#49917=CARTESIAN_POINT('Ctrl Pts',(-5.5629897248965,2.83313609879042,100.678436289745));
#49918=CARTESIAN_POINT('Ctrl Pts',(-4.20822471714898,4.61132947896263,100.585646531168));
#49919=CARTESIAN_POINT('Ctrl Pts',(-2.41665311565404,5.41141698065534,100.492856772592));
#49920=CARTESIAN_POINT('Ctrl Pts',(-0.625081514159094,6.21150448234805,
100.400067014015));
#49921=CARTESIAN_POINT('Ctrl Pts',(1.60329668108328,6.03348610556126,100.307277255438));
#49922=CARTESIAN_POINT('Ctrl Pts',(3.24512345400804,4.95911481901481,100.214487496861));
#49923=CARTESIAN_POINT('Ctrl Pts',(4.8869502269329,3.8847435324683,100.121697738284));
#49924=CARTESIAN_POINT('Ctrl Pts',(5.94222557754009,1.91401933616202,100.028907979708));
#49925=CARTESIAN_POINT('Ctrl Pts',(5.92632598388641,-0.0480245003946693,
99.936118221131));
#49926=CARTESIAN_POINT('Ctrl Pts',(5.91042639023273,-2.01006833695136,99.8433284625543));
#49927=CARTESIAN_POINT('Ctrl Pts',(4.82335185231836,-3.96343181375821,99.7505387039774));
#49928=CARTESIAN_POINT('Ctrl Pts',(3.16432931681224,-5.01105437953809,99.6577489454007));
#49929=CARTESIAN_POINT('Ctrl Pts',(1.50530678130631,-6.05867694531785,99.5649591868239));
#49930=CARTESIAN_POINT('Ctrl Pts',(-0.725663751791567,-6.20055860007054,
99.4721694282471));
#49931=CARTESIAN_POINT('Ctrl Pts',(-2.50403376395513,-5.37154176460521,
99.3793796696704));
#49932=CARTESIAN_POINT('Ctrl Pts',(-4.2824037761188,-4.54252492913983,99.2865899110937));
#49933=CARTESIAN_POINT('Ctrl Pts',(-5.60817326734847,-2.74260960345641,
99.1938001525169));
#49934=CARTESIAN_POINT('Ctrl Pts',(-5.87249727622737,-0.798386974234585,
99.1010103939402));
#49935=CARTESIAN_POINT('Ctrl Pts',(-5.90823357424942,-0.535530340084027,
99.088465326695));
#49936=CARTESIAN_POINT('Ctrl Pts',(-5.92456800225705,-0.270035952424749,
99.0759202594499));
#49937=CARTESIAN_POINT('Ctrl Pts',(-5.92240521329814,-0.00427408358304571,
99.0633751922047));
#49938=CARTESIAN_POINT('Ctrl Pts',(-5.92460418473688,-0.00304573894302621,
98.8116248077953));
#49939=CARTESIAN_POINT('Ctrl Pts',(-5.92568806904178,-0.176167703608292,
98.8198048478679));
#49940=CARTESIAN_POINT('Ctrl Pts',(-5.91876042483355,-0.349201677025623,
98.8279848879405));
#49941=CARTESIAN_POINT('Ctrl Pts',(-5.90353977625702,-0.521503068400942,
98.8361649280131));
#49942=CARTESIAN_POINT('Ctrl Pts',(-5.73085147668537,-2.4763760254123,98.9289728792288));
#49943=CARTESIAN_POINT('Ctrl Pts',(-4.49065452727481,-4.3369480955771,99.0217808304444));
#49944=CARTESIAN_POINT('Ctrl Pts',(-2.75270008599051,-5.24846544970891,
99.1145887816601));
#49945=CARTESIAN_POINT('Ctrl Pts',(-1.01474564470621,-6.15998280384072,
99.2073967328758));
#49946=CARTESIAN_POINT('Ctrl Pts',(1.22096628845165,-6.12244544193971,99.3002046840917));
#49947=CARTESIAN_POINT('Ctrl Pts',(2.92734121579234,-5.15309816969595,99.3930126353074));
#49948=CARTESIAN_POINT('Ctrl Pts',(4.63371614313303,-4.1837508974522,99.4858205865231));
#49949=CARTESIAN_POINT('Ctrl Pts',(5.81075406465631,-2.28259371486558,99.5786285377386));
#49950=CARTESIAN_POINT('Ctrl Pts',(5.91771931811476,-0.323025404901408,
99.6714364889544));
#49951=CARTESIAN_POINT('Ctrl Pts',(6.02468457157323,1.63654290506288,99.7642444401701));
#49952=CARTESIAN_POINT('Ctrl Pts',(5.06157715696692,3.65452234240463,99.8570523913859));
#49953=CARTESIAN_POINT('Ctrl Pts',(3.47085225448103,4.80384553954062,99.9498603426016));
#49954=CARTESIAN_POINT('Ctrl Pts',(1.88012735199531,5.95316873667648,100.042668293817));
#49955=CARTESIAN_POINT('Ctrl Pts',(-0.338215038369973,6.23383569360659,
100.135476245033));
#49956=CARTESIAN_POINT('Ctrl Pts',(-2.16506005241971,5.5169069513285,100.228284196249));
#49957=CARTESIAN_POINT('Ctrl Pts',(-3.99190506646955,4.79997820905036,100.321092147464));
#49958=CARTESIAN_POINT('Ctrl Pts',(-5.42725270420401,3.08545376756384,100.41390009868));
#49959=CARTESIAN_POINT('Ctrl Pts',(-5.81169884511591,1.16099262438603,100.506708049896));
#49960=CARTESIAN_POINT('Ctrl Pts',(-5.88752760536498,0.781408887926776,
100.525013635862));
#49961=CARTESIAN_POINT('Ctrl Pts',(-5.92247184496295,0.393657724318832,
100.543319221829));
#49962=CARTESIAN_POINT('Ctrl Pts',(-5.91888098557728,0.00526341932157319,
100.561624807795));
#49963=CARTESIAN_POINT('Origin',(0.,0.,-10.));
#49964=CARTESIAN_POINT('',(-5.90756520705438,0.00198423502760892,102.563375192205));
#49965=CARTESIAN_POINT('',(-5.90698748410082,0.000568579071646174,102.311624807795));
#49966=CARTESIAN_POINT('',(-5.91675,-7.2459289488551E-16,-10.));
#49967=CARTESIAN_POINT('Ctrl Pts',(-5.90756520705438,0.00198423502760892,
102.563375192205));
#49968=CARTESIAN_POINT('Ctrl Pts',(-5.91016349010236,0.868537566628739,
102.522730695704));
#49969=CARTESIAN_POINT('Ctrl Pts',(-5.73195451304473,1.73407369185386,102.482086199204));
#49970=CARTESIAN_POINT('Ctrl Pts',(-5.36759759991338,2.51247726861946,102.441441702703));
#49971=CARTESIAN_POINT('Ctrl Pts',(-4.53578535185495,4.28954147613377,102.348651944127));
#49972=CARTESIAN_POINT('Ctrl Pts',(-2.73378751570448,5.61247901132398,102.25586218555));
#49973=CARTESIAN_POINT('Ctrl Pts',(-0.789151648018449,5.87374545723213,
102.163072426973));
#49974=CARTESIAN_POINT('Ctrl Pts',(1.15548421966758,6.13501190314029,102.070282668396));
#49975=CARTESIAN_POINT('Ctrl Pts',(3.24275811888915,5.3346072597664,101.97749290982));
#49976=CARTESIAN_POINT('Ctrl Pts',(4.51411261938045,3.8401084983989,101.884703151243));
#49977=CARTESIAN_POINT('Ctrl Pts',(5.78546711987161,2.34560973703157,101.791913392666));
#49978=CARTESIAN_POINT('Ctrl Pts',(6.24090222163271,0.157016857670822,101.699123634089));
#49979=CARTESIAN_POINT('Ctrl Pts',(5.67126439624579,-1.72058308947875,101.606333875513));
#49980=CARTESIAN_POINT('Ctrl Pts',(5.10162657085884,-3.59818303662842,101.513544116936));
#49981=CARTESIAN_POINT('Ctrl Pts',(3.50691581832374,-5.16479005156688,101.420754358359));
#49982=CARTESIAN_POINT('Ctrl Pts',(1.61948539689627,-5.70095720639658,101.327964599782));
#49983=CARTESIAN_POINT('Ctrl Pts',(-0.267945024531298,-6.23712436122631,
101.235174841205));
#49984=CARTESIAN_POINT('Ctrl Pts',(-2.44809511485127,-5.74285165594717,
101.142385082629));
#49985=CARTESIAN_POINT('Ctrl Pts',(-3.91975508125673,-4.4451283584265,101.049595324052));
#49986=CARTESIAN_POINT('Ctrl Pts',(-5.16858439399879,-3.34389918132894,
100.970855280103));
#49987=CARTESIAN_POINT('Ctrl Pts',(-5.90723184190519,-1.66410735724864,
100.892115236154));
#49988=CARTESIAN_POINT('Ctrl Pts',(-5.92153330141852,0.0046063294329908,
100.813375192205));
#49989=CARTESIAN_POINT('Ctrl Pts',(-5.91888098557728,0.00526341932157319,
100.561624807795));
#49990=CARTESIAN_POINT('Ctrl Pts',(-5.90426645654772,-1.57547234213497,
100.636127173045));
#49991=CARTESIAN_POINT('Ctrl Pts',(-5.25134533554264,-3.16686128469683,
100.710629538294));
#49992=CARTESIAN_POINT('Ctrl Pts',(-4.1185048825022,-4.26165048695995,100.785131903543));
#49993=CARTESIAN_POINT('Ctrl Pts',(-2.70732013488725,-5.6254346102588,100.877939854759));
#49994=CARTESIAN_POINT('Ctrl Pts',(-0.551405995568029,-6.21860501198742,
100.970747805974));
#49995=CARTESIAN_POINT('Ctrl Pts',(1.35880244534019,-5.76865697149153,101.06355575719));
#49996=CARTESIAN_POINT('Ctrl Pts',(3.26901088624852,-5.31870893099562,101.156363708406));
#49997=CARTESIAN_POINT('Ctrl Pts',(4.93351362874569,-3.82564244827511,101.249171659622));
#49998=CARTESIAN_POINT('Ctrl Pts',(5.58763183256818,-1.97537789900341,101.341979610837));
#49999=CARTESIAN_POINT('Ctrl Pts',(6.24175003639059,-0.12511334973192,101.434787562053));
#50000=CARTESIAN_POINT('Ctrl Pts',(5.88548370153838,2.08234926609087,101.527595513269));
#50001=CARTESIAN_POINT('Ctrl Pts',(4.68250292647658,3.63289329374517,101.620403464484));
#50002=CARTESIAN_POINT('Ctrl Pts',(3.47952215141465,5.18343732139964,101.7132114157));
#50003=CARTESIAN_POINT('Ctrl Pts',(1.42982693614302,6.0770627608857,101.806019366916));
#50004=CARTESIAN_POINT('Ctrl Pts',(-0.524945003706648,5.90323471355187,
101.898827318132));
#50005=CARTESIAN_POINT('Ctrl Pts',(-2.47971694355631,5.72940666621803,101.991635269347));
#50006=CARTESIAN_POINT('Ctrl Pts',(-4.33956560798389,4.4881251320643,102.084443220563));
#50007=CARTESIAN_POINT('Ctrl Pts',(-5.25006950312836,2.74963953137896,102.177251171779));
#50008=CARTESIAN_POINT('Ctrl Pts',(-5.68949923371802,1.91060714149341,102.222042383784));
#50009=CARTESIAN_POINT('Ctrl Pts',(-5.90780326507992,0.955763720222844,
102.26683359579));
#50010=CARTESIAN_POINT('Ctrl Pts',(-5.90698748410082,0.000568579071646174,
102.311624807795));
#50011=CARTESIAN_POINT('Origin',(0.,0.,-10.));
#50012=CARTESIAN_POINT('',(-5.91423563825394,-0.00534293135961927,104.313375192205));
#50013=CARTESIAN_POINT('',(-5.9167872280184,-0.00546137831681672,104.061624807795));
#50014=CARTESIAN_POINT('',(-5.91675,-7.2459289488551E-16,-10.));
#50015=CARTESIAN_POINT('Ctrl Pts',(-5.91423563825394,-0.00534293135961927,
104.313375192205));
#50016=CARTESIAN_POINT('Ctrl Pts',(-5.90176787237235,1.42415486201049,104.246135913831));
#50017=CARTESIAN_POINT('Ctrl Pts',(-5.38101863511829,2.86179473551728,104.178896635458));
#50018=CARTESIAN_POINT('Ctrl Pts',(-4.43895915657409,3.92674007622001,104.111657357085));
#50019=CARTESIAN_POINT('Ctrl Pts',(-3.13892331898171,5.39635758925651,104.018867598508));
#50020=CARTESIAN_POINT('Ctrl Pts',(-1.036551963558,6.15622245053065,103.926077839931));
#50021=CARTESIAN_POINT('Ctrl Pts',(0.902664139812632,5.85737513487242,103.833288081355));
#50022=CARTESIAN_POINT('Ctrl Pts',(2.84188024318338,5.55852781921417,103.740498322778));
#50023=CARTESIAN_POINT('Ctrl Pts',(4.61794109450092,4.20096832662347,103.647708564201));
#50024=CARTESIAN_POINT('Ctrl Pts',(5.41521041034822,2.40814082469893,103.554918805624));
#50025=CARTESIAN_POINT('Ctrl Pts',(6.21247972619543,0.615313322774602,103.462129047048));
#50026=CARTESIAN_POINT('Ctrl Pts',(6.03095750657248,-1.61278218848366,103.369339288471));
#50027=CARTESIAN_POINT('Ctrl Pts',(4.95400582123115,-3.25291751250062,103.276549529894));
#50028=CARTESIAN_POINT('Ctrl Pts',(3.87705413588976,-4.89305283651766,103.183759771317));
#50029=CARTESIAN_POINT('Ctrl Pts',(1.90467298483,-5.94522797329356,103.090970012741));
#50030=CARTESIAN_POINT('Ctrl Pts',(-0.0573434243123933,-5.92624313976515,
102.998180254164));
#50031=CARTESIAN_POINT('Ctrl Pts',(-2.01935983345479,-5.90725830623673,
102.905390495587));
#50032=CARTESIAN_POINT('Ctrl Pts',(-3.9710115006797,-4.81711350240401,102.81260073701));
#50033=CARTESIAN_POINT('Ctrl Pts',(-5.01602400430896,-3.1564456605685,102.719810978434));
#50034=CARTESIAN_POINT('Ctrl Pts',(-5.60329194972236,-2.22319654813983,
102.667665716357));
#50035=CARTESIAN_POINT('Ctrl Pts',(-5.90423171390891,-1.10976900268225,
102.615520454281));
#50036=CARTESIAN_POINT('Ctrl Pts',(-5.90756520705438,0.00198423502760892,
102.563375192205));
#50037=CARTESIAN_POINT('Ctrl Pts',(-5.90698748410082,0.000568579071646174,
102.311624807795));
#50038=CARTESIAN_POINT('Ctrl Pts',(-5.90611295669304,-1.023412553249,102.359641547005));
#50039=CARTESIAN_POINT('Ctrl Pts',(-5.65342357388983,-2.04779788585592,
102.407658286216));
#50040=CARTESIAN_POINT('Ctrl Pts',(-5.1513905248428,-2.93034520163755,102.455675025426));
#50041=CARTESIAN_POINT('Ctrl Pts',(-4.18104852555142,-4.63615466675218,
102.548482976641));
#50042=CARTESIAN_POINT('Ctrl Pts',(-2.27920540110728,-5.81208392976454,
102.641290927857));
#50043=CARTESIAN_POINT('Ctrl Pts',(-0.31957505875301,-5.91790665033028,
102.734098879073));
#50044=CARTESIAN_POINT('Ctrl Pts',(1.64005528360104,-6.02372937089601,102.826906830289));
#50045=CARTESIAN_POINT('Ctrl Pts',(3.65747284386519,-5.05944554901537,102.919714781504));
#50046=CARTESIAN_POINT('Ctrl Pts',(4.80586838290561,-3.46805081081413,103.01252273272));
#50047=CARTESIAN_POINT('Ctrl Pts',(5.95426392194624,-1.87665607261261,103.105330683936));
#50048=CARTESIAN_POINT('Ctrl Pts',(6.23363743976279,0.341849581909771,103.198138635151));
#50049=CARTESIAN_POINT('Ctrl Pts',(5.51564368816192,2.16827628438813,103.290946586367));
#50050=CARTESIAN_POINT('Ctrl Pts',(4.79764993656108,3.99470298686638,103.383754537583));
#50051=CARTESIAN_POINT('Ctrl Pts',(3.08228891554294,5.42905073730067,103.476562488799));
#50052=CARTESIAN_POINT('Ctrl Pts',(1.15760395041781,5.8123747671823,103.569370440014));
#50053=CARTESIAN_POINT('Ctrl Pts',(-0.767081014707224,6.19569879706391,
103.66217839123));
#50054=CARTESIAN_POINT('Ctrl Pts',(-2.90108992393922,5.52799910639299,103.754986342446));
#50055=CARTESIAN_POINT('Ctrl Pts',(-4.26405103251585,4.11601945237153,103.847794293661));
#50056=CARTESIAN_POINT('Ctrl Pts',(-5.31081003241397,3.03161403447703,103.919071131706));
#50057=CARTESIAN_POINT('Ctrl Pts',(-5.90278230389148,1.50821034789738,103.990347969751));
#50058=CARTESIAN_POINT('Ctrl Pts',(-5.9167872280184,-0.00546137831681672,
104.061624807795));
#50059=CARTESIAN_POINT('Origin',(0.,0.,-10.));
#50060=CARTESIAN_POINT('',(-5.92648446538136,0.00041551144474657,106.063375192205));
#50061=CARTESIAN_POINT('',(-5.9257749495935,0.00192492296004073,105.811624807795));
#50062=CARTESIAN_POINT('',(-5.91675,-7.2459289488551E-16,-10.));
#50063=CARTESIAN_POINT('Ctrl Pts',(-5.92648446538136,0.00041551144474657,
106.063375192205));
#50064=CARTESIAN_POINT('Ctrl Pts',(-5.92650674114986,0.0224984077431825,
106.062330890535));
#50065=CARTESIAN_POINT('Ctrl Pts',(-5.9263940289506,0.0445810701819271,
106.061286588866));
#50066=CARTESIAN_POINT('Ctrl Pts',(-5.92614564199684,0.0666622064383869,
106.060242287197));
#50067=CARTESIAN_POINT('Ctrl Pts',(-5.90407561553706,2.0286463367465,105.96745252862));
#50068=CARTESIAN_POINT('Ctrl Pts',(-4.8108632413548,3.97858136859802,105.874662770043));
#50069=CARTESIAN_POINT('Ctrl Pts',(-3.14855419947414,5.02098122610502,105.781873011467));
#50070=CARTESIAN_POINT('Ctrl Pts',(-1.48624515759367,6.06338108361191,105.68908325289));
#50071=CARTESIAN_POINT('Ctrl Pts',(0.745160551985173,6.19824576677453,105.596293494313));
#50072=CARTESIAN_POINT('Ctrl Pts',(2.52091456075547,5.36364016292073,105.503503735736));
#50073=CARTESIAN_POINT('Ctrl Pts',(4.29666856952576,4.52903455906694,105.410713977159));
#50074=CARTESIAN_POINT('Ctrl Pts',(5.61677087748763,2.72495866819665,105.317924218583));
#50075=CARTESIAN_POINT('Ctrl Pts',(5.87497911439927,0.779914370490588,105.225134460006));
#50076=CARTESIAN_POINT('Ctrl Pts',(6.13318735131092,-1.16512992721559,105.132344701429));
#50077=CARTESIAN_POINT('Ctrl Pts',(5.32950151717242,-3.25114263175742,105.039554942853));
#50078=CARTESIAN_POINT('Ctrl Pts',(3.83300543380504,-4.52014550256365,104.946765184276));
#50079=CARTESIAN_POINT('Ctrl Pts',(2.33650935043775,-5.7891483733698,104.853975425699));
#50080=CARTESIAN_POINT('Ctrl Pts',(0.147203017841625,-6.2411414104402,104.761185667122));
#50081=CARTESIAN_POINT('Ctrl Pts',(-1.72949886827872,-5.6685518154594,104.668395908546));
#50082=CARTESIAN_POINT('Ctrl Pts',(-3.60620075439917,-5.09596222047856,
104.575606149969));
#50083=CARTESIAN_POINT('Ctrl Pts',(-5.1702981940439,-3.49878999344632,104.482816391392));
#50084=CARTESIAN_POINT('Ctrl Pts',(-5.7034967539857,-1.61051879753076,104.390026632815));
#50085=CARTESIAN_POINT('Ctrl Pts',(-5.85031769046941,-1.09056663308795,
104.364476152612));
#50086=CARTESIAN_POINT('Ctrl Pts',(-5.91897330666809,-0.548542619906705,
104.338925672408));
#50087=CARTESIAN_POINT('Ctrl Pts',(-5.91423563825394,-0.00534293135961927,
104.313375192205));
#50088=CARTESIAN_POINT('Ctrl Pts',(-5.9167872280184,-0.00546137831681672,
104.061624807795));
#50089=CARTESIAN_POINT('Ctrl Pts',(-5.92101779736746,-0.462707212097632,
104.083155920966));
#50090=CARTESIAN_POINT('Ctrl Pts',(-5.87250845240857,-0.919064997863135,
104.104687034137));
#50091=CARTESIAN_POINT('Ctrl Pts',(-5.76786374926362,-1.36216559570815,
104.126218147308));
#50092=CARTESIAN_POINT('Ctrl Pts',(-5.31680204951344,-3.27211137239461,
104.219026098524));
#50093=CARTESIAN_POINT('Ctrl Pts',(-3.8227653420916,-4.93574330839516,104.31183404974));
#50094=CARTESIAN_POINT('Ctrl Pts',(-1.9721197275602,-5.58878261523637,104.404642000956));
#50095=CARTESIAN_POINT('Ctrl Pts',(-0.121474113029111,-6.24182192207747,
104.497449952171));
#50096=CARTESIAN_POINT('Ctrl Pts',(2.08578040861131,-5.88426859975954,104.590257903387));
#50097=CARTESIAN_POINT('Ctrl Pts',(3.6356227818944,-4.68038399364526,104.683065854603));
#50098=CARTESIAN_POINT('Ctrl Pts',(5.18546515517775,-3.47649938753077,104.775873805818));
#50099=CARTESIAN_POINT('Ctrl Pts',(6.07789538010348,-1.42628349761935,104.868681757034));
#50100=CARTESIAN_POINT('Ctrl Pts',(5.90292764409852,0.528386760562654,104.96148970825));
#50101=CARTESIAN_POINT('Ctrl Pts',(5.72795990809357,2.48305701874455,105.054297659466));
#50102=CARTESIAN_POINT('Ctrl Pts',(4.4855942111583,4.34218164519717,105.147105610681));
#50103=CARTESIAN_POINT('Ctrl Pts',(2.74657804205345,5.25167177183706,105.239913561897));
#50104=CARTESIAN_POINT('Ctrl Pts',(1.0075618729488,6.16116189847685,105.332721513113));
#50105=CARTESIAN_POINT('Ctrl Pts',(-1.22810476832518,6.1210175253041,105.425529464328));
#50106=CARTESIAN_POINT('Ctrl Pts',(-2.93334819133995,5.14968112882371,105.518337415544));
#50107=CARTESIAN_POINT('Ctrl Pts',(-4.63859161435491,4.1783447323432,105.61114536676));
#50108=CARTESIAN_POINT('Ctrl Pts',(-5.81341181911044,2.27581631255488,105.703953317976));
#50109=CARTESIAN_POINT('Ctrl Pts',(-5.91809197081005,0.316124603968129,
105.796761269191));
#50110=CARTESIAN_POINT('Ctrl Pts',(-5.92368027603418,0.21150729844301,105.801715782059));
#50111=CARTESIAN_POINT('Ctrl Pts',(-5.92621877557426,0.106727082537521,
105.806670294927));
#50112=CARTESIAN_POINT('Ctrl Pts',(-5.9257749495935,0.00192492296004073,
105.811624807795));
#50113=CARTESIAN_POINT('Origin',(0.,0.,-10.));
#50114=CARTESIAN_POINT('',(-5.91298589814417,0.00513333739083355,107.813375192205));
#50115=CARTESIAN_POINT('',(-5.91092078228077,0.00451530674276642,107.561624807795));
#50116=CARTESIAN_POINT('',(-5.91675,-7.2459289488551E-16,-10.));
#50117=CARTESIAN_POINT('Ctrl Pts',(-5.91298589814417,0.00513333739083355,
107.813375192205));
#50118=CARTESIAN_POINT('Ctrl Pts',(-5.91783226872518,0.593051106927172,
107.785736108663));
#50119=CARTESIAN_POINT('Ctrl Pts',(-5.83726005077582,1.17967014789196,107.758097025121));
#50120=CARTESIAN_POINT('Ctrl Pts',(-5.66582521821169,1.73841037059773,107.730457941578));
#50121=CARTESIAN_POINT('Ctrl Pts',(-5.09028526946242,3.61420955522335,107.637668183002));
#50122=CARTESIAN_POINT('Ctrl Pts',(-3.49065551721405,5.17579355207652,107.544878424425));
#50123=CARTESIAN_POINT('Ctrl Pts',(-1.60154821588312,5.70602219870611,107.452088665848));
#50124=CARTESIAN_POINT('Ctrl Pts',(0.2875590854477,6.23625084533567,107.359298907272));
#50125=CARTESIAN_POINT('Ctrl Pts',(2.46614393586105,5.73512414174176,107.266509148695));
#50126=CARTESIAN_POINT('Ctrl Pts',(3.93371536164864,4.43277897863799,107.173719390118));
#50127=CARTESIAN_POINT('Ctrl Pts',(5.40128678743632,3.13043381553414,107.080929631541));
#50128=CARTESIAN_POINT('Ctrl Pts',(6.15784478859817,1.02687019292034,106.988139872964));
#50129=CARTESIAN_POINT('Ctrl Pts',(5.85594847886084,-0.91187358381125,106.895350114388));
#50130=CARTESIAN_POINT('Ctrl Pts',(5.55405216912353,-2.85061736054273,106.802560355811));
#50131=CARTESIAN_POINT('Ctrl Pts',(4.19370154848718,-4.624541291392,106.709770597234));
#50132=CARTESIAN_POINT('Ctrl Pts',(2.39962257920517,-5.41899045000949,106.616980838657));
#50133=CARTESIAN_POINT('Ctrl Pts',(0.605543609923058,-6.21343960862703,
106.524191080081));
#50134=CARTESIAN_POINT('Ctrl Pts',(-1.62226370800443,-6.02841399501274,
106.431401321504));
#50135=CARTESIAN_POINT('Ctrl Pts',(-3.26070352759948,-4.94888457382324,
106.338611562927));
#50136=CARTESIAN_POINT('Ctrl Pts',(-4.88070353805124,-3.8815047087256,106.24686610602));
#50137=CARTESIAN_POINT('Ctrl Pts',(-5.92452746328279,-1.93964210828605,
106.155120649112));
#50138=CARTESIAN_POINT('Ctrl Pts',(-5.92648446538136,0.00041551144474657,
106.063375192205));
#50139=CARTESIAN_POINT('Ctrl Pts',(-5.9257749495935,0.00192492296004073,
105.811624807795));
#50140=CARTESIAN_POINT('Ctrl Pts',(-5.9179050258539,-1.8564273127613,105.899478246143));
#50141=CARTESIAN_POINT('Ctrl Pts',(-4.9723205622003,-3.7216791642822,105.987331684491));
#50142=CARTESIAN_POINT('Ctrl Pts',(-3.46524818821572,-4.80788959256222,
106.075185122838));
#50143=CARTESIAN_POINT('Ctrl Pts',(-1.87318415527777,-5.95535708312111,
106.167993074054));
#50144=CARTESIAN_POINT('Ctrl Pts',(0.345484009241598,-6.23343706685349,
106.26080102527));
#50145=CARTESIAN_POINT('Ctrl Pts',(2.17149177927208,-5.5143785500049,106.353608976486));
#50146=CARTESIAN_POINT('Ctrl Pts',(3.99749954930236,-4.79532003315639,106.446416927701));
#50147=CARTESIAN_POINT('Ctrl Pts',(5.43084692484366,-3.07912301572704,106.539224878917));
#50148=CARTESIAN_POINT('Ctrl Pts',(5.81304871338755,-1.15421488293286,106.632032830133));
#50149=CARTESIAN_POINT('Ctrl Pts',(6.1952505019314,0.770693249861093,106.724840781348));
#50150=CARTESIAN_POINT('Ctrl Pts',(5.52630670347817,2.90431249801998,106.817648732564));
#50151=CARTESIAN_POINT('Ctrl Pts',(4.11353262303918,4.26645012854864,106.91045668378));
#50152=CARTESIAN_POINT('Ctrl Pts',(2.70075854260003,5.62858775907746,107.003264634996));
#50153=CARTESIAN_POINT('Ctrl Pts',(0.544154180174869,6.21924377197597,107.096072586211));
#50154=CARTESIAN_POINT('Ctrl Pts',(-1.36552828302161,5.76706856630545,107.188880537427));
#50155=CARTESIAN_POINT('Ctrl Pts',(-3.27521074621809,5.31489336063493,107.281688488643));
#50156=CARTESIAN_POINT('Ctrl Pts',(-4.93797131018577,3.81988693639561,107.374496439858));
#50157=CARTESIAN_POINT('Ctrl Pts',(-5.58993149805126,1.96886088571407,107.467304391074));
#50158=CARTESIAN_POINT('Ctrl Pts',(-5.81079316561159,1.3417969823343,107.498744529981));
#50159=CARTESIAN_POINT('Ctrl Pts',(-5.91565324474178,0.673875513844714,
107.530184668888));
#50160=CARTESIAN_POINT('Ctrl Pts',(-5.91092078228077,0.00451530674276642,
107.561624807795));
#50161=CARTESIAN_POINT('Origin',(0.,0.,-10.));
#50162=CARTESIAN_POINT('',(-5.90808735901173,-0.00265285794674774,109.563375192205));
#50163=CARTESIAN_POINT('',(-5.90935748219384,-0.00371301381819065,109.311624807795));
#50164=CARTESIAN_POINT('',(-5.91675,-7.2459289488551E-16,-10.));
#50165=CARTESIAN_POINT('Ctrl Pts',(-5.90808735901173,-0.00265285794674774,
109.563375192205));
#50166=CARTESIAN_POINT('Ctrl Pts',(-5.90342863114805,1.15337485265749,109.50914132679));
#50167=CARTESIAN_POINT('Ctrl Pts',(-5.57622077201164,2.31183763756103,109.454907461375));
#50168=CARTESIAN_POINT('Ctrl Pts',(-4.94375108945386,3.26848148005295,109.40067359596));
#50169=CARTESIAN_POINT('Ctrl Pts',(-3.86164660173687,4.90522174390387,109.307883837383));
#50170=CARTESIAN_POINT('Ctrl Pts',(-1.8859661764013,5.95118865564213,109.215094078807));
#50171=CARTESIAN_POINT('Ctrl Pts',(0.0759808237317083,5.92603349082254,
109.12230432023));
#50172=CARTESIAN_POINT('Ctrl Pts',(2.03792782386472,5.90087832600295,109.029514561653));
#50173=CARTESIAN_POINT('Ctrl Pts',(3.98614139879518,4.8046010846255,108.936724803076));
#50174=CARTESIAN_POINT('Ctrl Pts',(5.02592603266835,3.14065495304274,108.843935044499));
#50175=CARTESIAN_POINT('Ctrl Pts',(6.06571066654153,1.47670882145997,108.751145285923));
#50176=CARTESIAN_POINT('Ctrl Pts',(6.19706635935743,-0.754906200328122,
108.658355527346));
#50177=CARTESIAN_POINT('Ctrl Pts',(5.35966946341301,-2.52934561949991,108.565565768769));
#50178=CARTESIAN_POINT('Ctrl Pts',(4.5222725674686,-4.30378503867169,108.472776010193));
#50179=CARTESIAN_POINT('Ctrl Pts',(2.71612308276388,-5.62104885522717,108.379986251616));
#50180=CARTESIAN_POINT('Ctrl Pts',(0.770675164491407,-5.8761982446784,108.287196493039));
#50181=CARTESIAN_POINT('Ctrl Pts',(-1.17477275378118,-6.13134763412965,
108.194406734462));
#50182=CARTESIAN_POINT('Ctrl Pts',(-3.25951910562152,-5.32438259647652,
108.101616975886));
#50183=CARTESIAN_POINT('Ctrl Pts',(-4.52616720891648,-3.82589289145091,
108.008827217309));
#50184=CARTESIAN_POINT('Ctrl Pts',(-5.41552159701752,-2.77375505520261,
107.943676542274));
#50185=CARTESIAN_POINT('Ctrl Pts',(-5.90156206369103,-1.38070275561479,
107.878525867239));
#50186=CARTESIAN_POINT('Ctrl Pts',(-5.91298589814417,0.00513333739083355,
107.813375192205));
#50187=CARTESIAN_POINT('Ctrl Pts',(-5.91092078228077,0.00451530674276642,
107.561624807795));
#50188=CARTESIAN_POINT('Ctrl Pts',(-5.90168351812861,-1.30200473369831,
107.622992620104));
#50189=CARTESIAN_POINT('Ctrl Pts',(-5.4749107893125,-2.61400620915615,107.684360432413));
#50190=CARTESIAN_POINT('Ctrl Pts',(-4.67826346976177,-3.63835103414898,
107.745728244721));
#50191=CARTESIAN_POINT('Ctrl Pts',(-3.47347544184374,-5.18749122620678,
107.838536195937));
#50192=CARTESIAN_POINT('Ctrl Pts',(-1.4227395742447,-6.07872593319865,107.931344147153));
#50193=CARTESIAN_POINT('Ctrl Pts',(0.53182833779797,-5.90261856800144,108.024152098368));
#50194=CARTESIAN_POINT('Ctrl Pts',(2.48639624984053,-5.72651120280424,108.116960049584));
#50195=CARTESIAN_POINT('Ctrl Pts',(4.3447962063266,-4.48306176541808,108.2097680008));
#50196=CARTESIAN_POINT('Ctrl Pts',(5.25327225528971,-2.74351561905591,108.302575952015));
#50197=CARTESIAN_POINT('Ctrl Pts',(6.16174830425282,-1.00396947269373,108.395383903231));
#50198=CARTESIAN_POINT('Ctrl Pts',(6.12030044569285,1.23167338264468,108.488191854447));
#50199=CARTESIAN_POINT('Ctrl Pts',(5.14796998221979,2.93635018387868,108.580999805663));
#50200=CARTESIAN_POINT('Ctrl Pts',(4.17563951874667,4.64102698511278,108.673807756878));
#50201=CARTESIAN_POINT('Ctrl Pts',(2.27242645036048,5.81473773224261,108.766615708094));
#50202=CARTESIAN_POINT('Ctrl Pts',(0.312674041719707,5.91827527949106,108.85942365931));
#50203=CARTESIAN_POINT('Ctrl Pts',(-1.64707836692096,6.02181282673951,108.952231610525));
#50204=CARTESIAN_POINT('Ctrl Pts',(-3.66337011581607,5.05517717410668,109.045039561741));
#50205=CARTESIAN_POINT('Ctrl Pts',(-4.80990916782254,3.4624443876396,109.137847512957));
#50206=CARTESIAN_POINT('Ctrl Pts',(-5.52551759100319,2.4683456730104,109.195773277903));
#50207=CARTESIAN_POINT('Ctrl Pts',(-5.90230606863383,1.23034521762944,109.253699042849));
#50208=CARTESIAN_POINT('Ctrl Pts',(-5.90935748219384,-0.00371301381819065,
109.311624807795));
#50209=CARTESIAN_POINT('Origin',(0.,0.,-10.));
#50210=CARTESIAN_POINT('',(-5.92273005567057,-0.00413167202517661,111.313375192205));
#50211=CARTESIAN_POINT('',(-5.92451012806985,-0.0031152991902449,111.061624807795));
#50212=CARTESIAN_POINT('',(-5.91675,-7.2459289488551E-16,-10.));
#50213=CARTESIAN_POINT('Ctrl Pts',(-5.92273005567057,-0.00413167202517661,
111.313375192205));
#50214=CARTESIAN_POINT('Ctrl Pts',(-5.9091339542178,1.70794336761187,111.232546544917));
#50215=CARTESIAN_POINT('Ctrl Pts',(-5.12583041727858,3.43086149514118,111.151717897629));
#50216=CARTESIAN_POINT('Ctrl Pts',(-3.81877088892424,4.53217772354859,111.070889250342));
#50217=CARTESIAN_POINT('Ctrl Pts',(-2.31829126751189,5.79646792732884,110.978099491765));
#50218=CARTESIAN_POINT('Ctrl Pts',(-0.127574270496055,6.24157349064171,
110.885309733188));
#50219=CARTESIAN_POINT('Ctrl Pts',(1.7473175744012,5.66308461124448,110.792519974611));
#50220=CARTESIAN_POINT('Ctrl Pts',(3.62220941929823,5.08459573184732,110.699730216035));
#50221=CARTESIAN_POINT('Ctrl Pts',(5.18127611207678,3.48251240974035,110.606940457458));
#50222=CARTESIAN_POINT('Ctrl Pts',(5.70853353431331,1.59257367413433,110.514150698881));
#50223=CARTESIAN_POINT('Ctrl Pts',(6.23579095654991,-0.297365061471903,
110.421360940304));
#50224=CARTESIAN_POINT('Ctrl Pts',(5.73123910824425,-2.47515921057725,110.328571181728));
#50225=CARTESIAN_POINT('Ctrl Pts',(4.42658783989949,-3.94068092029528,110.235781423151));
#50226=CARTESIAN_POINT('Ctrl Pts',(3.12193657155488,-5.40620263001315,110.142991664574));
#50227=CARTESIAN_POINT('Ctrl Pts',(1.01718588317135,-6.15945190034387,110.050201905997));
#50228=CARTESIAN_POINT('Ctrl Pts',(-0.921080773046223,-5.85450734301785,
109.957412147421));
#50229=CARTESIAN_POINT('Ctrl Pts',(-2.85934742926401,-5.54956278569179,
109.864622388844));
#50230=CARTESIAN_POINT('Ctrl Pts',(-4.63113005331579,-4.18642440070869,
109.771832630267));
#50231=CARTESIAN_POINT('Ctrl Pts',(-5.42275709029251,-2.39109840023526,
109.67904287169));
#50232=CARTESIAN_POINT('Ctrl Pts',(-5.75169304109037,-1.64510661701725,
109.640486978528));
#50233=CARTESIAN_POINT('Ctrl Pts',(-5.91139933783546,-0.824495088097872,
109.601931085367));
#50234=CARTESIAN_POINT('Ctrl Pts',(-5.90808735901173,-0.00265285794674774,
109.563375192205));
#50235=CARTESIAN_POINT('Ctrl Pts',(-5.90935748219384,-0.00371301381819065,
109.311624807795));
#50236=CARTESIAN_POINT('Ctrl Pts',(-5.91360375708538,-0.746847768048513,
109.346506994065));
#50237=CARTESIAN_POINT('Ctrl Pts',(-5.78377224693165,-1.48855295325666,
109.381389180334));
#50238=CARTESIAN_POINT('Ctrl Pts',(-5.51311153728789,-2.17470653597755,
109.416271366604));
#50239=CARTESIAN_POINT('Ctrl Pts',(-4.79298849962897,-4.00029475282613,
109.50907931782));
#50240=CARTESIAN_POINT('Ctrl Pts',(-3.07595606919342,-5.4326412662218,109.601887269035));
#50241=CARTESIAN_POINT('Ctrl Pts',(-1.15082542308427,-5.81372068350237,
109.694695220251));
#50242=CARTESIAN_POINT('Ctrl Pts',(0.774305223024769,-6.19480010078292,
109.787503171467));
#50243=CARTESIAN_POINT('Ctrl Pts',(2.90753408480728,-5.52461242194847,109.880311122683));
#50244=CARTESIAN_POINT('Ctrl Pts',(4.26884777424252,-4.11104439535077,109.973119073898));
#50245=CARTESIAN_POINT('Ctrl Pts',(5.63016146367777,-2.69747636875307,110.065927025114));
#50246=CARTESIAN_POINT('Ctrl Pts',(6.21955998076569,-0.540527994391874,
110.15873497633));
#50247=CARTESIAN_POINT('Ctrl Pts',(5.76627142288757,1.36889050613647,110.251542927545));
#50248=CARTESIAN_POINT('Ctrl Pts',(5.31298286500946,3.2783090066647,110.344350878761));
#50249=CARTESIAN_POINT('Ctrl Pts',(3.81700723216561,4.94019763336027,110.437158829977));
#50250=CARTESIAN_POINT('Ctrl Pts',(1.96560137457252,5.59107848062241,110.529966781192));
#50251=CARTESIAN_POINT('Ctrl Pts',(0.114195516979119,6.24195932788466,110.622774732408));
#50252=CARTESIAN_POINT('Ctrl Pts',(-2.09264056536353,5.88183239571303,110.715582683624));
#50253=CARTESIAN_POINT('Ctrl Pts',(-3.64107804958066,4.67614135554757,110.80839063484));
#50254=CARTESIAN_POINT('Ctrl Pts',(-5.04942464256389,3.57953210530978,110.892802025825));
#50255=CARTESIAN_POINT('Ctrl Pts',(-5.91311730723571,1.78343805305531,110.97721341681));
#50256=CARTESIAN_POINT('Ctrl Pts',(-5.92451012806985,-0.0031152991902449,
111.061624807795));
#50257=CARTESIAN_POINT('Origin',(0.,0.,-10.));
#50258=CARTESIAN_POINT('',(-5.92118311221449,0.004721389953629,113.063375192205));
#50259=CARTESIAN_POINT('',(-5.91902054661466,0.0052408541572496,112.811624807795));
#50260=CARTESIAN_POINT('',(-5.91675,-7.2459289488551E-16,-10.));
#50261=CARTESIAN_POINT('Ctrl Pts',(-5.92118311221449,0.004721389953629,
113.063375192205));
#50262=CARTESIAN_POINT('Ctrl Pts',(-5.9238846454292,0.314895936846653,113.048741521621));
#50263=CARTESIAN_POINT('Ctrl Pts',(-5.901624485963,0.624681876463416,113.034107851037));
#50264=CARTESIAN_POINT('Ctrl Pts',(-5.85305173090669,0.930285684752532,
113.019474180454));
#50265=CARTESIAN_POINT('Ctrl Pts',(-5.5450596800191,2.86807042776155,112.926684421877));
#50266=CARTESIAN_POINT('Ctrl Pts',(-4.17913690128139,4.63770736398083,112.8338946633));
#50267=CARTESIAN_POINT('Ctrl Pts',(-2.38256830886638,5.42651032188376,112.741104904723));
#50268=CARTESIAN_POINT('Ctrl Pts',(-0.585999716451469,6.21531327978665,
112.648315146147));
#50269=CARTESIAN_POINT('Ctrl Pts',(1.64121468964069,6.02328225937329,112.55552538757));
#50270=CARTESIAN_POINT('Ctrl Pts',(3.27625135062814,4.9386053808168,112.462735628993));
#50271=CARTESIAN_POINT('Ctrl Pts',(4.91128801161559,3.85392850226031,112.369945870416));
#50272=CARTESIAN_POINT('Ctrl Pts',(5.95414692749833,1.87660576556068,112.27715611184));
#50273=CARTESIAN_POINT('Ctrl Pts',(5.92590668651959,-0.0852992531488124,
112.184366353263));
#50274=CARTESIAN_POINT('Ctrl Pts',(5.89766644554085,-2.04720427185831,112.091576594686));
#50275=CARTESIAN_POINT('Ctrl Pts',(4.79832704770064,-3.99369157257767,111.998786836109));
#50276=CARTESIAN_POINT('Ctrl Pts',(3.13274794080624,-5.03085841177226,111.905997077533));
#50277=CARTESIAN_POINT('Ctrl Pts',(1.46716883391174,-6.0680252509669,111.813207318956));
#50278=CARTESIAN_POINT('Ctrl Pts',(-0.764649982037001,-6.19587162863665,
111.720417560379));
#50279=CARTESIAN_POINT('Ctrl Pts',(-2.53777042400616,-5.35568551120816,
111.627627801802));
#50280=CARTESIAN_POINT('Ctrl Pts',(-4.31089086597521,-4.51549939377971,
111.534838043225));
#50281=CARTESIAN_POINT('Ctrl Pts',(-5.62531293396473,-2.70728078125311,
111.442048284649));
#50282=CARTESIAN_POINT('Ctrl Pts',(-5.87740284505506,-0.761434052866085,
111.349258526072));
#50283=CARTESIAN_POINT('Ctrl Pts',(-5.90989862398217,-0.510603685088854,
111.337297414783));
#50284=CARTESIAN_POINT('Ctrl Pts',(-5.92474202157661,-0.257486401710428,
111.325336303494));
#50285=CARTESIAN_POINT('Ctrl Pts',(-5.92273005567057,-0.00413167202517661,
111.313375192205));
#50286=CARTESIAN_POINT('Ctrl Pts',(-5.92451012806985,-0.0031152991902449,
111.061624807795));
#50287=CARTESIAN_POINT('Ctrl Pts',(-5.92564339344094,-0.180827129928352,
111.070021368026));
#50288=CARTESIAN_POINT('Ctrl Pts',(-5.91834344502106,-0.358444558721565,
111.078417928256));
#50289=CARTESIAN_POINT('Ctrl Pts',(-5.90230748536562,-0.535269734243664,
111.086814488487));
#50290=CARTESIAN_POINT('Ctrl Pts',(-5.72506055084205,-2.48973463571031,
111.179622439702));
#50291=CARTESIAN_POINT('Ctrl Pts',(-4.48052779570348,-4.34740929048461,
111.272430390918));
#50292=CARTESIAN_POINT('Ctrl Pts',(-2.74045226342587,-5.25487095294303,
111.365238342134));
#50293=CARTESIAN_POINT('Ctrl Pts',(-1.00037673114817,-6.1623326154015,111.45804629335));
#50294=CARTESIAN_POINT('Ctrl Pts',(1.23524157826863,-6.11958128554399,111.550854244565));
#50295=CARTESIAN_POINT('Ctrl Pts',(2.93935117823326,-5.14625708561272,111.643662195781));
#50296=CARTESIAN_POINT('Ctrl Pts',(4.64346077819779,-4.1729328856815,111.736470146997));
#50297=CARTESIAN_POINT('Ctrl Pts',(5.8160616687102,-2.26903581567664,111.829278098212));
#50298=CARTESIAN_POINT('Ctrl Pts',(5.918456576311,-0.309223373181075,111.922086049428));
#50299=CARTESIAN_POINT('Ctrl Pts',(6.0208514839118,1.6505890693146,112.014894000644));
#50300=CARTESIAN_POINT('Ctrl Pts',(5.05304040860088,3.66631688430099,112.10770195186));
#50301=CARTESIAN_POINT('Ctrl Pts',(3.45963941003865,4.81192710800027,112.200509903075));
#50302=CARTESIAN_POINT('Ctrl Pts',(1.86623841147642,5.95753733169955,112.293317854291));
#50303=CARTESIAN_POINT('Ctrl Pts',(-0.352752510337116,6.23302996411172,
112.386125805507));
#50304=CARTESIAN_POINT('Ctrl Pts',(-2.17792055341265,5.51184265044123,112.478933756722));
#50305=CARTESIAN_POINT('Ctrl Pts',(-4.00308859648809,4.79065533677078,112.571741707938));
#50306=CARTESIAN_POINT('Ctrl Pts',(-5.43443376082557,3.07278807701779,112.664549659154));
#50307=CARTESIAN_POINT('Ctrl Pts',(-5.81439067729846,1.14743557202359,112.75735761037));
#50308=CARTESIAN_POINT('Ctrl Pts',(-5.88844753963049,0.772167852918489,
112.775446676178));
#50309=CARTESIAN_POINT('Ctrl Pts',(-5.92256284181212,0.389017903419475,
112.793535741987));
#50310=CARTESIAN_POINT('Ctrl Pts',(-5.91902054661466,0.00524085415724961,
112.811624807795));
#50311=CARTESIAN_POINT('Origin',(0.,0.,-10.));
#50312=CARTESIAN_POINT('',(-5.90744685829511,0.00179048289942529,114.813375192205));
#50313=CARTESIAN_POINT('',(-5.90700152101349,0.000644589703395199,114.561624807795));
#50314=CARTESIAN_POINT('',(-5.91675,-7.2459289488551E-16,-10.));
#50315=CARTESIAN_POINT('Ctrl Pts',(-5.90744685829511,0.00179048289942529,
114.813375192205));
#50316=CARTESIAN_POINT('Ctrl Pts',(-5.90982243185645,0.880837885823255,
114.772146739748));
#50317=CARTESIAN_POINT('Ctrl Pts',(-5.72623916706124,1.7589420329495,114.730918287292));
#50318=CARTESIAN_POINT('Ctrl Pts',(-5.35168831615744,2.54618895344184,114.689689834835));
#50319=CARTESIAN_POINT('Ctrl Pts',(-4.50871505474855,4.31798603386546,114.596900076258));
#50320=CARTESIAN_POINT('Ctrl Pts',(-2.69843178552914,5.62956310315636,114.504110317682));
#50321=CARTESIAN_POINT('Ctrl Pts',(-0.752191058465522,5.87859291255057,
114.411320559105));
#50322=CARTESIAN_POINT('Ctrl Pts',(1.19404966859809,6.1276227219448,114.318530800528));
#50323=CARTESIAN_POINT('Ctrl Pts',(3.27624785350592,5.31410527144234,114.225741041951));
#50324=CARTESIAN_POINT('Ctrl Pts',(4.5381770315982,3.81163944383515,114.132951283375));
#50325=CARTESIAN_POINT('Ctrl Pts',(5.80010620969055,2.30917361622787,114.040161524798));
#50326=CARTESIAN_POINT('Ctrl Pts',(6.24176638096727,0.117759411515774,113.947371766221));
#50327=CARTESIAN_POINT('Ctrl Pts',(5.66033000133476,-1.75622045766327,113.854582007644));
#50328=CARTESIAN_POINT('Ctrl Pts',(5.07889362170229,-3.63020032684221,113.761792249068));
#50329=CARTESIAN_POINT('Ctrl Pts',(3.4743606911607,-5.18674586048813,113.669002490491));
#50330=CARTESIAN_POINT('Ctrl Pts',(1.58359519447514,-5.71103075459768,113.576212731914));
#50331=CARTESIAN_POINT('Ctrl Pts',(-0.307170302210411,-6.23531564870724,
113.483422973337));
#50332=CARTESIAN_POINT('Ctrl Pts',(-2.48416836503994,-5.72733990328042,
113.390633214761));
#50333=CARTESIAN_POINT('Ctrl Pts',(-3.9476367349359,-4.42038575566771,113.297843456184));
#50334=CARTESIAN_POINT('Ctrl Pts',(-5.18030469794229,-3.31954849808144,
113.219687368191));
#50335=CARTESIAN_POINT('Ctrl Pts',(-5.90675465652134,-1.65187112670505,
113.141531280198));
#50336=CARTESIAN_POINT('Ctrl Pts',(-5.92118311221449,0.004721389953629,
113.063375192205));
#50337=CARTESIAN_POINT('Ctrl Pts',(-5.91902054661466,0.00524085415724961,
112.811624807795));
#50338=CARTESIAN_POINT('Ctrl Pts',(-5.90438870483032,-1.57999266034137,
112.886343693202));
#50339=CARTESIAN_POINT('Ctrl Pts',(-5.2472450749989,-3.17592571538899,112.961062578609));
#50340=CARTESIAN_POINT('Ctrl Pts',(-4.10855477015215,-4.27124396878244,
113.035781464017));
#50341=CARTESIAN_POINT('Ctrl Pts',(-2.69419327792475,-5.63173325435863,
113.128589415232));
#50342=CARTESIAN_POINT('Ctrl Pts',(-0.536901624861667,-6.21987407527553,
113.221397366448));
#50343=CARTESIAN_POINT('Ctrl Pts',(1.37225226391009,-5.76547231928087,113.314205317664));
#50344=CARTESIAN_POINT('Ctrl Pts',(3.28140615268174,-5.31107056328625,113.40701326888));
#50345=CARTESIAN_POINT('Ctrl Pts',(4.94242227716222,-3.81412623038015,113.499821220095));
#50346=CARTESIAN_POINT('Ctrl Pts',(5.59222356256014,-1.96234119524295,113.592629171311));
#50347=CARTESIAN_POINT('Ctrl Pts',(6.2420248479581,-0.110556160105644,113.685437122527));
#50348=CARTESIAN_POINT('Ctrl Pts',(5.88061129427344,2.09606957726296,113.778245073742));
#50349=CARTESIAN_POINT('Ctrl Pts',(4.67401765172385,3.64380382726269,113.871053024958));
#50350=CARTESIAN_POINT('Ctrl Pts',(3.46742400917419,5.19153807726251,113.963860976174));
#50351=CARTESIAN_POINT('Ctrl Pts',(1.41565027775974,6.0803808398934,114.056668927389));
#50352=CARTESIAN_POINT('Ctrl Pts',(-0.538710948729533,5.90199439629684,
114.149476878605));
#50353=CARTESIAN_POINT('Ctrl Pts',(-2.49307217521848,5.72360795270031,114.242284829821));
#50354=CARTESIAN_POINT('Ctrl Pts',(-4.3500208967822,4.47799230287646,114.335092781037));
#50355=CARTESIAN_POINT('Ctrl Pts',(-5.25646786425308,2.73738797620561,114.427900732252));
#50356=CARTESIAN_POINT('Ctrl Pts',(-5.69182489694245,1.90139385637306,114.4724754241));
#50357=CARTESIAN_POINT('Ctrl Pts',(-5.90792200995091,0.951216698938335,
114.517050115948));
#50358=CARTESIAN_POINT('Ctrl Pts',(-5.90700152101349,0.000644589703395199,
114.561624807795));
#50359=CARTESIAN_POINT('Origin',(0.,0.,-10.));
#50360=CARTESIAN_POINT('',(-5.91459626807812,-0.00538349094479307,116.563375192205));
#50361=CARTESIAN_POINT('',(-5.91664694577537,-0.00546538710318724,116.311624807795));
#50362=CARTESIAN_POINT('',(-5.91675,-7.2459289488551E-16,-10.));
#50363=CARTESIAN_POINT('Ctrl Pts',(-5.91459626807812,-0.00538349094479307,
116.563375192205));
#50364=CARTESIAN_POINT('Ctrl Pts',(-5.9018638407151,1.4363059330357,116.495551957875));
#50365=CARTESIAN_POINT('Ctrl Pts',(-5.37115148883914,2.88638679209883,116.427728723546));
#50366=CARTESIAN_POINT('Ctrl Pts',(-4.41417274127812,3.95458278837131,116.359905489217));
#50367=CARTESIAN_POINT('Ctrl Pts',(-3.10491894606437,5.41599419977019,116.26711573064));
#50368=CARTESIAN_POINT('Ctrl Pts',(-0.997809742128125,6.16262042901297,
116.174325972063));
#50369=CARTESIAN_POINT('Ctrl Pts',(0.939488296168799,5.85158164612673,116.081536213487));
#50370=CARTESIAN_POINT('Ctrl Pts',(2.8767863344655,5.54054286324053,115.98874645491));
#50371=CARTESIAN_POINT('Ctrl Pts',(4.64427320712292,4.17183906822554,115.895956696333));
#50372=CARTESIAN_POINT('Ctrl Pts',(5.43025013550231,2.37403232619154,115.803166937756));
#50373=CARTESIAN_POINT('Ctrl Pts',(6.21622706388179,0.576225584157339,115.71037717918));
#50374=CARTESIAN_POINT('Ctrl Pts',(6.02069404798297,-1.650684104896,115.617587420603));
#50375=CARTESIAN_POINT('Ctrl Pts',(4.93344746063551,-3.28401312011301,115.524797662026));
#50376=CARTESIAN_POINT('Ctrl Pts',(3.84620087328818,-4.91734213532984,115.432007903449));
#50377=CARTESIAN_POINT('Ctrl Pts',(1.86724071449241,-5.95709047671048,115.339218144873));
#50378=CARTESIAN_POINT('Ctrl Pts',(-0.0946174716486306,-5.92576522940153,
115.246428386296));
#50379=CARTESIAN_POINT('Ctrl Pts',(-2.05647565779001,-5.89443998209257,
115.153638627719));
#50380=CARTESIAN_POINT('Ctrl Pts',(-4.00123187127666,-4.79204114609361,
115.060848869142));
#50381=CARTESIAN_POINT('Ctrl Pts',(-5.03577835122075,-3.12483318231579,
114.968059110565));
#50382=CARTESIAN_POINT('Ctrl Pts',(-5.61065394704331,-2.19840098219977,
114.916497804445));
#50383=CARTESIAN_POINT('Ctrl Pts',(-5.90447590817912,-1.0975675947347,114.864936498325));
#50384=CARTESIAN_POINT('Ctrl Pts',(-5.90744685829511,0.00179048289942529,
114.813375192205));
#50385=CARTESIAN_POINT('Ctrl Pts',(-5.90700152101349,0.000644589703395199,
114.561624807795));
#50386=CARTESIAN_POINT('Ctrl Pts',(-5.90600548088795,-1.02794785126051,
114.609858067163));
#50387=CARTESIAN_POINT('Ctrl Pts',(-5.65090545221675,-2.05700273779024,
114.658091326531));
#50388=CARTESIAN_POINT('Ctrl Pts',(-5.14454243958478,-2.94235117338353,
114.706324585899));
#50389=CARTESIAN_POINT('Ctrl Pts',(-4.17022483406764,-4.64589299278287,
114.799132537115));
#50390=CARTESIAN_POINT('Ctrl Pts',(-2.26564440965561,-5.81738362806337,
114.891940488331));
#50391=CARTESIAN_POINT('Ctrl Pts',(-0.305772599524579,-5.91863586120825,
114.984748439547));
#50392=CARTESIAN_POINT('Ctrl Pts',(1.65409921060645,-6.01988809435313,115.077556390762));
#50393=CARTESIAN_POINT('Ctrl Pts',(3.66926240645635,-5.05090192536239,115.170364341978));
#50394=CARTESIAN_POINT('Ctrl Pts',(4.8139434124092,-3.45683325636664,115.263172293194));
#50395=CARTESIAN_POINT('Ctrl Pts',(5.95862441836219,-1.86276458737071,115.355980244409));
#50396=CARTESIAN_POINT('Ctrl Pts',(6.23282323441778,0.356386581630305,115.448788195625));
#50397=CARTESIAN_POINT('Ctrl Pts',(5.5105718898964,2.1811338304845,115.541596146841));
#50398=CARTESIAN_POINT('Ctrl Pts',(4.78832054537515,4.00588107933838,115.634404098056));
#50399=CARTESIAN_POINT('Ctrl Pts',(3.06961904027696,5.43622440804573,115.727212049272));
#50400=CARTESIAN_POINT('Ctrl Pts',(1.14404533090283,5.81505869454813,115.820020000488));
#50401=CARTESIAN_POINT('Ctrl Pts',(-0.781528378471534,6.19389298105057,
115.912827951704));
#50402=CARTESIAN_POINT('Ctrl Pts',(-2.91397429212202,5.52121822534809,116.005635902919));
#50403=CARTESIAN_POINT('Ctrl Pts',(-4.27363871135382,4.10606374828964,116.098443854135));
#50404=CARTESIAN_POINT('Ctrl Pts',(-5.31469375657614,3.02252159827662,116.169504172022));
#50405=CARTESIAN_POINT('Ctrl Pts',(-5.90270453950121,1.50369964399586,116.240564489909));
#50406=CARTESIAN_POINT('Ctrl Pts',(-5.91664694577537,-0.00546538710318724,
116.311624807795));
#50407=CARTESIAN_POINT('Origin',(0.,0.,-10.));
#50408=CARTESIAN_POINT('',(-5.92643375485155,0.000646757142401377,118.313375192205));
#50409=CARTESIAN_POINT('',(-5.92583646225612,0.00184477398095578,118.061624807795));
#50410=CARTESIAN_POINT('',(-5.91675,-7.2459289488551E-16,-10.));
#50411=CARTESIAN_POINT('Ctrl Pts',(-5.92643375485155,0.000646757142401377,
118.313375192205));
#50412=CARTESIAN_POINT('Ctrl Pts',(-5.92648696415084,0.0350788317316276,
118.311746934579));
#50413=CARTESIAN_POINT('Ctrl Pts',(-5.92621294326389,0.0695100363376435,
118.310118676954));
#50414=CARTESIAN_POINT('Ctrl Pts',(-5.9256091198181,0.103935456191626,118.308490419329));
#50415=CARTESIAN_POINT('Ctrl Pts',(-5.89119894363559,2.06574195873543,118.215700660752));
#50416=CARTESIAN_POINT('Ctrl Pts',(-4.78574339534727,4.00876227624729,118.122910902175));
#50417=CARTESIAN_POINT('Ctrl Pts',(-3.11691069714255,5.04068583884809,118.030121143598));
#50418=CARTESIAN_POINT('Ctrl Pts',(-1.44807799893782,6.07260940144889,117.937331385022));
#50419=CARTESIAN_POINT('Ctrl Pts',(0.784131849183317,6.19343620913865,117.844541626445));
#50420=CARTESIAN_POINT('Ctrl Pts',(2.554601186991,5.3476778881445,117.751751867868));
#50421=CARTESIAN_POINT('Ctrl Pts',(4.32507052479859,4.50191956715039,117.658962109291));
#50422=CARTESIAN_POINT('Ctrl Pts',(5.63379935229277,2.68957611747247,117.566172350715));
#50423=CARTESIAN_POINT('Ctrl Pts',(5.87976844422231,0.742946204144582,117.473382592138));
#50424=CARTESIAN_POINT('Ctrl Pts',(6.12573753615187,-1.20368370918353,117.380592833561));
#50425=CARTESIAN_POINT('Ctrl Pts',(5.30894689251649,-3.28460008616166,117.287803074984));
#50426=CARTESIAN_POINT('Ctrl Pts',(3.80449857381735,-4.54416511823098,117.195013316408));
#50427=CARTESIAN_POINT('Ctrl Pts',(2.3000502551182,-5.80373015030029,117.102223557831));
#50428=CARTESIAN_POINT('Ctrl Pts',(0.107944261355265,-6.24194383746075,
117.009433799254));
#50429=CARTESIAN_POINT('Ctrl Pts',(-1.76511899837069,-5.65756139529358,
116.916644040677));
#50430=CARTESIAN_POINT('Ctrl Pts',(-3.63818225809653,-5.07317895312644,
116.823854282101));
#50431=CARTESIAN_POINT('Ctrl Pts',(-5.19220278378542,-3.46620038163178,
116.731064523524));
#50432=CARTESIAN_POINT('Ctrl Pts',(-5.71351385338424,-1.57461279910704,
116.638274764947));
#50433=CARTESIAN_POINT('Ctrl Pts',(-5.85378068519037,-1.06565181063473,
116.6133082407));
#50434=CARTESIAN_POINT('Ctrl Pts',(-5.91928322321424,-0.536086196545553,
116.588341716452));
#50435=CARTESIAN_POINT('Ctrl Pts',(-5.91459626807812,-0.00538349094479307,
116.563375192205));
#50436=CARTESIAN_POINT('Ctrl Pts',(-5.91664694577537,-0.00546538710318724,
116.311624807795));
#50437=CARTESIAN_POINT('Ctrl Pts',(-5.920913945254,-0.467337339063882,116.333372441124));
#50438=CARTESIAN_POINT('Ctrl Pts',(-5.87141177430932,-0.92830479119591,
116.355120074453));
#50439=CARTESIAN_POINT('Ctrl Pts',(-5.7646712557571,-1.37561355519936,116.376867707782));
#50440=CARTESIAN_POINT('Ctrl Pts',(-5.30915645611559,-3.28450218321582,
116.469675658998));
#50441=CARTESIAN_POINT('Ctrl Pts',(-3.8112439320195,-4.94464524083455,116.562483610214));
#50442=CARTESIAN_POINT('Ctrl Pts',(-1.9590803488349,-5.59336674347474,116.655291561429));
#50443=CARTESIAN_POINT('Ctrl Pts',(-0.106916765650188,-6.24208824611498,
116.748099512645));
#50444=CARTESIAN_POINT('Ctrl Pts',(2.09949787662346,-5.87938819377639,116.840907463861));
#50445=CARTESIAN_POINT('Ctrl Pts',(3.64652836626847,-4.67189235901254,116.933715415076));
#50446=CARTESIAN_POINT('Ctrl Pts',(5.19355885591348,-3.46439652424869,117.026523366292));
#50447=CARTESIAN_POINT('Ctrl Pts',(6.08120519293021,-1.41210490705985,117.119331317508));
#50448=CARTESIAN_POINT('Ctrl Pts',(5.90167930090155,0.542151980085433,117.212139268724));
#50449=CARTESIAN_POINT('Ctrl Pts',(5.72215340887289,2.49640886723071,117.304947219939));
#50450=CARTESIAN_POINT('Ctrl Pts',(4.47545528779867,4.35263102433215,117.397755171155));
#50451=CARTESIAN_POINT('Ctrl Pts',(2.7343227584359,5.25806298867747,117.490563122371));
#50452=CARTESIAN_POINT('Ctrl Pts',(0.993190229073134,6.16349495302279,117.583371073586));
#50453=CARTESIAN_POINT('Ctrl Pts',(-1.24237670857819,6.11813672461201,117.676179024802));
#50454=CARTESIAN_POINT('Ctrl Pts',(-2.94535016830966,5.14282604471886,117.768986976018));
#50455=CARTESIAN_POINT('Ctrl Pts',(-4.64832362804114,4.1675153648257,117.861794927234));
#50456=CARTESIAN_POINT('Ctrl Pts',(-5.81870360985277,2.26225223345017,117.954602878449));
#50457=CARTESIAN_POINT('Ctrl Pts',(-5.91881313412188,0.302321721923281,
118.047410829665));
#50458=CARTESIAN_POINT('Ctrl Pts',(-5.92392388368571,0.202264169157404,
118.052148822375));
#50459=CARTESIAN_POINT('Ctrl Pts',(-5.92624522588486,0.102064138766616,
118.056886815085));
#50460=CARTESIAN_POINT('Ctrl Pts',(-5.92583646225612,0.00184477398095578,
118.061624807795));
#50461=CARTESIAN_POINT('Origin',(0.,0.,-10.));
#50462=CARTESIAN_POINT('',(-5.91264952969134,0.00505721487104038,120.063375192205));
#50463=CARTESIAN_POINT('',(-5.91102966775968,0.00455868499465235,119.811624807795));
#50464=CARTESIAN_POINT('',(-5.91675,-7.2459289488551E-16,-10.));
#50465=CARTESIAN_POINT('Ctrl Pts',(-5.91264952969134,0.00505721487104038,
120.063375192205));
#50466=CARTESIAN_POINT('Ctrl Pts',(-5.91750501305584,0.605482795756369,
120.035152152707));
#50467=CARTESIAN_POINT('Ctrl Pts',(-5.83342087274394,1.20458030872588,120.006929113208));
#50468=CARTESIAN_POINT('Ctrl Pts',(-5.65477879996619,1.77401317452086,119.97870607371));
#50469=CARTESIAN_POINT('Ctrl Pts',(-5.06745174024911,3.6461551933258,119.885916315134));
#50470=CARTESIAN_POINT('Ctrl Pts',(-3.458031501331,5.19764686847578,119.793126556557));
#50471=CARTESIAN_POINT('Ctrl Pts',(-1.56562651024018,5.71598282453298,119.70033679798));
#50472=CARTESIAN_POINT('Ctrl Pts',(0.326778480850637,6.23431878059017,119.607547039403));
#50473=CARTESIAN_POINT('Ctrl Pts',(2.50216822411417,5.71949901755457,119.514757280827));
#50474=CARTESIAN_POINT('Ctrl Pts',(3.96151906342687,4.40794881209317,119.42196752225));
#50475=CARTESIAN_POINT('Ctrl Pts',(5.42086990273941,3.09639860663192,119.329177763673));
#50476=CARTESIAN_POINT('Ctrl Pts',(6.16418183810132,0.988117958745099,119.236388005096));
#50477=CARTESIAN_POINT('Ctrl Pts',(5.85009709231295,-0.948688584539746,
119.143598246519));
#50478=CARTESIAN_POINT('Ctrl Pts',(5.53601234652456,-2.8854951278247,119.050808487943));
#50479=CARTESIAN_POINT('Ctrl Pts',(4.16453091958576,-4.65082756650766,118.958018729366));
#50480=CARTESIAN_POINT('Ctrl Pts',(2.36549047331626,-5.43397652190135,118.865228970789));
#50481=CARTESIAN_POINT('Ctrl Pts',(0.566450027046652,-6.21712547729509,
118.772439212213));
#50482=CARTESIAN_POINT('Ctrl Pts',(-1.66014943855372,-6.01809094939945,
118.679649453636));
#50483=CARTESIAN_POINT('Ctrl Pts',(-3.29176676931556,-4.92827734166367,
118.586859695059));
#50484=CARTESIAN_POINT('Ctrl Pts',(-4.89475277910877,-3.85758758276841,
118.495698194108));
#50485=CARTESIAN_POINT('Ctrl Pts',(-5.92345471792749,-1.92710690519565,
118.404536693156));
#50486=CARTESIAN_POINT('Ctrl Pts',(-5.92643375485155,0.000646757142401377,
118.313375192205));
#50487=CARTESIAN_POINT('Ctrl Pts',(-5.92583646225612,0.00184477398095578,
118.061624807795));
#50488=CARTESIAN_POINT('Ctrl Pts',(-5.91823835098307,-1.86103595172694,
118.149694766301));
#50489=CARTESIAN_POINT('Ctrl Pts',(-4.96734794015348,-3.7305969993527,118.237764724806));
#50490=CARTESIAN_POINT('Ctrl Pts',(-3.45402592757642,-4.81595808036472,
118.325834683312));
#50491=CARTESIAN_POINT('Ctrl Pts',(-1.85929013003522,-5.95970947944757,
118.418642634528));
#50492=CARTESIAN_POINT('Ctrl Pts',(0.360020531773886,-6.23261438593508,
118.511450585744));
#50493=CARTESIAN_POINT('Ctrl Pts',(2.18434636610108,-5.50929925608524,118.604258536959));
#50494=CARTESIAN_POINT('Ctrl Pts',(4.00867220042817,-4.78598412623543,118.697066488175));
#50495=CARTESIAN_POINT('Ctrl Pts',(5.43801320727335,-3.06644896004871,118.789874439391));
#50496=CARTESIAN_POINT('Ctrl Pts',(5.81572473502421,-1.14065470087481,118.882682390606));
#50497=CARTESIAN_POINT('Ctrl Pts',(6.19343626277509,0.7851395582992,118.975490341822));
#50498=CARTESIAN_POINT('Ctrl Pts',(5.51951831143128,2.91719291046021,119.068298293038));
#50499=CARTESIAN_POINT('Ctrl Pts',(4.10357133061007,4.27603200114264,119.161106244254));
#50500=CARTESIAN_POINT('Ctrl Pts',(2.68762434978902,5.63487109182491,119.253914195469));
#50501=CARTESIAN_POINT('Ctrl Pts',(0.529648339490302,6.2204959210289,119.346722146685));
#50502=CARTESIAN_POINT('Ctrl Pts',(-1.37897437886234,5.76386823258837,119.439530097901));
#50503=CARTESIAN_POINT('Ctrl Pts',(-3.2875970972153,5.30724054414775,119.532338049116));
#50504=CARTESIAN_POINT('Ctrl Pts',(-4.94686652362224,3.80836033806268,119.625146000332));
#50505=CARTESIAN_POINT('Ctrl Pts',(-5.59450802297796,1.95581883645566,119.717953951548));
#50506=CARTESIAN_POINT('Ctrl Pts',(-5.81239572545508,1.33256351398138,119.749177570297));
#50507=CARTESIAN_POINT('Ctrl Pts',(-5.91578041622014,0.669278371866502,
119.780401189046));
#50508=CARTESIAN_POINT('Ctrl Pts',(-5.91102966775968,0.00455868499465235,
119.811624807795));
#50509=CARTESIAN_POINT('Origin',(0.,0.,-10.));
#50510=CARTESIAN_POINT('',(-5.90826032391765,-0.00283186500595667,121.813375192205));
#50511=CARTESIAN_POINT('',(-5.90927045785071,-0.00365599742955411,121.561624807795));
#50512=CARTESIAN_POINT('',(-5.91675,-7.2459289488551E-16,-10.));
#50513=CARTESIAN_POINT('Ctrl Pts',(-5.90826032391765,-0.00283186500595667,
121.813375192205));
#50514=CARTESIAN_POINT('Ctrl Pts',(-5.90322516476143,1.16555772389332,121.758557370834));
#50515=CARTESIAN_POINT('Ctrl Pts',(-5.56844404220564,2.3366080019099,121.703739549463));
#50516=CARTESIAN_POINT('Ctrl Pts',(-4.9230950366585,3.29951227908924,121.648921728092));
#50517=CARTESIAN_POINT('Ctrl Pts',(-3.83071710326124,4.92941389096632,121.556131969515));
#50518=CARTESIAN_POINT('Ctrl Pts',(-1.84849678431158,5.9629333781242,121.463342210938));
#50519=CARTESIAN_POINT('Ctrl Pts',(0.113253183721438,5.92543835814145,121.370552452362));
#50520=CARTESIAN_POINT('Ctrl Pts',(2.07500315175423,5.88794333815871,121.277762693785));
#50521=CARTESIAN_POINT('Ctrl Pts',(4.01628276887011,4.7794338110354,121.184972935208));
#50522=CARTESIAN_POINT('Ctrl Pts',(5.04558086252729,3.10898050488358,121.092183176631));
#50523=CARTESIAN_POINT('Ctrl Pts',(6.07487895618459,1.43852719873157,120.999393418055));
#50524=CARTESIAN_POINT('Ctrl Pts',(6.19219552638293,-0.793869886449118,
120.906603659478));
#50525=CARTESIAN_POINT('Ctrl Pts',(5.34365423708173,-2.56300710385687,120.813813900901));
#50526=CARTESIAN_POINT('Ctrl Pts',(4.49511294778054,-4.33214432126463,120.721024142324));
#50527=CARTESIAN_POINT('Ctrl Pts',(2.68071379897976,-5.63802167089943,120.628234383748));
#50528=CARTESIAN_POINT('Ctrl Pts',(0.733699512763562,-5.88092943716167,
120.535444625171));
#50529=CARTESIAN_POINT('Ctrl Pts',(-1.21331477345253,-6.12383720342389,
120.442654866594));
#50530=CARTESIAN_POINT('Ctrl Pts',(-3.29294419708403,-5.30377538631367,
120.349865108017));
#50531=CARTESIAN_POINT('Ctrl Pts',(-4.5501419686417,-3.79734829652869,120.257075349441));
#50532=CARTESIAN_POINT('Ctrl Pts',(-5.42494902264784,-2.74911779986066,
120.192508630362));
#50533=CARTESIAN_POINT('Ctrl Pts',(-5.90154149044533,-1.36855492960636,
120.127941911283));
#50534=CARTESIAN_POINT('Ctrl Pts',(-5.91264952969134,0.00505721487104038,
120.063375192205));
#50535=CARTESIAN_POINT('Ctrl Pts',(-5.91102966775968,0.00455868499465235,
119.811624807795));
#50536=CARTESIAN_POINT('Ctrl Pts',(-5.9016594639084,-1.30651030166878,119.873209140262));
#50537=CARTESIAN_POINT('Ctrl Pts',(-5.47161876324425,-2.62315998102597,
119.934793472728));
#50538=CARTESIAN_POINT('Ctrl Pts',(-4.66976547813631,-3.64925166567194,
119.996377805195));
#50539=CARTESIAN_POINT('Ctrl Pts',(-3.46136786163473,-5.19557786906385,
120.089185756411));
#50540=CARTESIAN_POINT('Ctrl Pts',(-1.40855905632735,-6.08202747871909,
120.181993707626));
#50541=CARTESIAN_POINT('Ctrl Pts',(0.545592827142654,-5.90136219928656,
120.274801658842));
#50542=CARTESIAN_POINT('Ctrl Pts',(2.49974471061277,-5.72069691985401,120.367609610058));
#50543=CARTESIAN_POINT('Ctrl Pts',(4.35523967224537,-4.4729167513336,120.460417561273));
#50544=CARTESIAN_POINT('Ctrl Pts',(5.25965632567281,-2.7312566111601,120.553225512489));
#50545=CARTESIAN_POINT('Ctrl Pts',(6.16407297910019,-0.989596470986702,
120.646033463705));
#50546=CARTESIAN_POINT('Ctrl Pts',(6.11741132432244,1.2459436408396,120.738841414921));
#50547=CARTESIAN_POINT('Ctrl Pts',(5.14110790159988,2.94834816199279,120.831649366136));
#50548=CARTESIAN_POINT('Ctrl Pts',(4.16480447887727,4.65075268314607,120.924457317352));
#50549=CARTESIAN_POINT('Ctrl Pts',(2.25885928820944,5.82002161362627,121.017265268568));
#50550=CARTESIAN_POINT('Ctrl Pts',(0.298870741548488,5.91898839498991,121.110073219783));
#50551=CARTESIAN_POINT('Ctrl Pts',(-1.66111780511235,6.01795517635354,121.202881170999));
#50552=CARTESIAN_POINT('Ctrl Pts',(-3.67514970776645,5.04661980860101,121.295689122215));
#50553=CARTESIAN_POINT('Ctrl Pts',(-4.81797111117614,3.45121742462712,121.388497073431));
#50554=CARTESIAN_POINT('Ctrl Pts',(-5.5285929841372,2.45917454999816,121.446206318219));
#50555=CARTESIAN_POINT('Ctrl Pts',(-5.9023594588355,1.22583483209864,121.503915563007));
#50556=CARTESIAN_POINT('Ctrl Pts',(-5.90927045785071,-0.00365599742955411,
121.561624807795));
#50557=CARTESIAN_POINT('Origin',(0.,0.,-10.));
#50558=CARTESIAN_POINT('',(-5.92304633245574,-0.00398199821673939,123.563375192205));
#50559=CARTESIAN_POINT('',(-5.92441432658438,-0.0031840572747424,123.311624807795));
#50560=CARTESIAN_POINT('',(-5.91675,-7.2459289488551E-16,-10.));
#50561=CARTESIAN_POINT('Ctrl Pts',(-5.92304633245574,-0.00398199821673939,
123.563375192205));
#50562=CARTESIAN_POINT('Ctrl Pts',(-5.90972172210851,1.72022136801727,123.481962588961));
#50563=CARTESIAN_POINT('Ctrl Pts',(-5.11364227888086,3.45513729943991,123.400549985717));
#50564=CARTESIAN_POINT('Ctrl Pts',(-3.79018862841945,4.55610756923942,123.319137382473));
#50565=CARTESIAN_POINT('Ctrl Pts',(-2.28178649139079,5.81093497267106,123.226347623897));
#50566=CARTESIAN_POINT('Ctrl Pts',(-0.0883131846642343,6.24225244714527,
123.13355786532));
#50567=CARTESIAN_POINT('Ctrl Pts',(1.78290296347007,5.65198222160363,123.040768106743));
#50568=CARTESIAN_POINT('Ctrl Pts',(3.65411911160426,5.06171199606203,122.947978348167));
#50569=CARTESIAN_POINT('Ctrl Pts',(5.20307810114624,3.4498540705047,122.85518858959));
#50570=CARTESIAN_POINT('Ctrl Pts',(5.71843766228389,1.55663635042864,122.762398831013));
#50571=CARTESIAN_POINT('Ctrl Pts',(6.23379722342157,-0.336581369647533,
122.669609072436));
#50572=CARTESIAN_POINT('Ctrl Pts',(5.71555735615491,-2.51115888424216,122.576819313859));
#50573=CARTESIAN_POINT('Ctrl Pts',(4.40171398332094,-3.96844554312672,122.484029555283));
#50574=CARTESIAN_POINT('Ctrl Pts',(3.08787061048711,-5.42573220201112,122.391239796706));
#50575=CARTESIAN_POINT('Ctrl Pts',(0.978423732085748,-6.16572800518541,
122.298450038129));
#50576=CARTESIAN_POINT('Ctrl Pts',(-0.957886527019627,-5.84859807304264,
122.205660279552));
#50577=CARTESIAN_POINT('Ctrl Pts',(-2.89419678612522,-5.53146814089984,
122.112870520976));
#50578=CARTESIAN_POINT('Ctrl Pts',(-4.65737042593512,-4.15721247343991,
122.020080762399));
#50579=CARTESIAN_POINT('Ctrl Pts',(-5.43768947191774,-2.35694277141183,
121.927291003822));
#50580=CARTESIAN_POINT('Ctrl Pts',(-5.75701593928944,-1.62022646642786,
121.889319066616));
#50581=CARTESIAN_POINT('Ctrl Pts',(-5.91174814489485,-0.812167496962084,
121.851347129411));
#50582=CARTESIAN_POINT('Ctrl Pts',(-5.90826032391765,-0.00283186500595667,
121.813375192205));
#50583=CARTESIAN_POINT('Ctrl Pts',(-5.90927045785071,-0.00365599742955411,
121.561624807795));
#50584=CARTESIAN_POINT('Ctrl Pts',(-5.91347372071519,-0.751431121489131,
121.596723514223));
#50585=CARTESIAN_POINT('Ctrl Pts',(-5.78197492207068,-1.49778251843781,
121.63182222065));
#50586=CARTESIAN_POINT('Ctrl Pts',(-5.50802474944973,-2.18755815917475,
121.666920927078));
#50587=CARTESIAN_POINT('Ctrl Pts',(-4.78364608014831,-4.01146195880812,
121.759728878293));
#50588=CARTESIAN_POINT('Ctrl Pts',(-3.06327783737993,-5.43980015787935,
121.852536829509));
#50589=CARTESIAN_POINT('Ctrl Pts',(-1.13726368307564,-5.81638879848899,
121.945344780725));
#50590=CARTESIAN_POINT('Ctrl Pts',(0.788750471228538,-6.19297743909861,
122.038152731941));
#50591=CARTESIAN_POINT('Ctrl Pts',(2.9204105370686,-5.51781652124677,122.130960683156));
#50592=CARTESIAN_POINT('Ctrl Pts',(4.27842383730411,-4.10107751798203,122.223768634372));
#50593=CARTESIAN_POINT('Ctrl Pts',(5.63643713753963,-2.68433851471728,122.316576585588));
#50594=CARTESIAN_POINT('Ctrl Pts',(6.22080367217059,-0.526021426039627,
122.409384536803));
#50595=CARTESIAN_POINT('Ctrl Pts',(5.76306325010652,1.38233473379682,122.502192488019));
#50596=CARTESIAN_POINT('Ctrl Pts',(5.30532282804248,3.29069089363317,122.595000439235));
#50597=CARTESIAN_POINT('Ctrl Pts',(3.80547544928359,4.94908612462835,122.68780839045));
#50598=CARTESIAN_POINT('Ctrl Pts',(1.95255665910373,5.59564740060542,122.780616341666));
#50599=CARTESIAN_POINT('Ctrl Pts',(0.0996378689237742,6.24220867658253,
122.873424292882));
#50600=CARTESIAN_POINT('Ctrl Pts',(-2.10635233267718,5.87693599754143,122.966232244098));
#50601=CARTESIAN_POINT('Ctrl Pts',(-3.65197372433744,4.66763700996177,123.059040195313));
#50602=CARTESIAN_POINT('Ctrl Pts',(-5.05415308196879,3.57056751626948,123.143235066141));
#50603=CARTESIAN_POINT('Ctrl Pts',(-5.91284757783128,1.77886266924099,123.227429936968));
#50604=CARTESIAN_POINT('Ctrl Pts',(-5.92441432658438,-0.0031840572747424,
123.311624807795));
#50605=CARTESIAN_POINT('Origin',(0.,0.,-10.));
#50606=CARTESIAN_POINT('',(-5.92082732894822,0.0048284439233276,125.313375192205));
#50607=CARTESIAN_POINT('',(-5.91915982610221,0.00521712502770736,125.061624807795));
#50608=CARTESIAN_POINT('',(-5.91675,-7.2459289488551E-16,-10.));
#50609=CARTESIAN_POINT('Ctrl Pts',(-5.92082732894822,0.0048284439233276,
125.313375192205));
#50610=CARTESIAN_POINT('Ctrl Pts',(-5.9236770812749,0.327430742195007,125.298157565665));
#50611=CARTESIAN_POINT('Ctrl Pts',(-5.8995936395555,0.64960709265275,125.282939939125));
#50612=CARTESIAN_POINT('Ctrl Pts',(-5.84708469732352,0.9670819991819,125.267722312585));
#50613=CARTESIAN_POINT('Ctrl Pts',(-5.52691045332391,2.90289109885381,125.174932554009));
#50614=CARTESIAN_POINT('Ctrl Pts',(-4.1498837400031,4.66390177683713,125.082142795432));
#50615=CARTESIAN_POINT('Ctrl Pts',(-2.34838918584629,5.44138903022236,124.989353036855));
#50616=CARTESIAN_POINT('Ctrl Pts',(-0.546894631689373,6.21887628360764,
124.896563278278));
#50617=CARTESIAN_POINT('Ctrl Pts',(1.67906776330359,6.01284011239471,124.803773519702));
#50618=CARTESIAN_POINT('Ctrl Pts',(3.30724960074758,4.91790052991357,124.710983761125));
#50619=CARTESIAN_POINT('Ctrl Pts',(4.93543143819138,3.82296094743256,124.618194002548));
#50620=CARTESIAN_POINT('Ctrl Pts',(5.96583271808636,1.83911795368359,124.525404243971));
#50621=CARTESIAN_POINT('Ctrl Pts',(5.92525296043562,-0.122570616094663,
124.432614485395));
#50622=CARTESIAN_POINT('Ctrl Pts',(5.88467320278487,-2.08425918587314,124.339824726818));
#50623=CARTESIAN_POINT('Ctrl Pts',(4.77311240758814,-4.02379333168089,124.247034968241));
#50624=CARTESIAN_POINT('Ctrl Pts',(3.10104261686253,-5.05046341815464,124.154245209664));
#50625=CARTESIAN_POINT('Ctrl Pts',(1.42897282613711,-6.07713350462827,124.061455451088));
#50626=CARTESIAN_POINT('Ctrl Pts',(-0.803605960117068,-6.19093953176812,
123.968665692511));
#50627=CARTESIAN_POINT('Ctrl Pts',(-2.57140667886717,-5.33961736868184,
123.875875933934));
#50628=CARTESIAN_POINT('Ctrl Pts',(-4.33920739761747,-4.48829520559547,
123.783086175357));
#50629=CARTESIAN_POINT('Ctrl Pts',(-5.64223004886356,-2.6718448522827,123.690296416781));
#50630=CARTESIAN_POINT('Ctrl Pts',(-5.88207589082117,-0.724451009431805,
123.597506658204));
#50631=CARTESIAN_POINT('Ctrl Pts',(-5.91148391431208,-0.485676789252728,
123.586129502871));
#50632=CARTESIAN_POINT('Ctrl Pts',(-5.92490840485771,-0.244933997561633,
123.574752347538));
#50633=CARTESIAN_POINT('Ctrl Pts',(-5.92304633245574,-0.00398199821673939,
123.563375192205));
#50634=CARTESIAN_POINT('Ctrl Pts',(-5.92441432658438,-0.0031840572747424,
123.311624807795));
#50635=CARTESIAN_POINT('Ctrl Pts',(-5.92559759744001,-0.185486275457294,
123.320237888184));
#50636=CARTESIAN_POINT('Ctrl Pts',(-5.91791554376533,-0.367687419896257,
123.328850968572));
#50637=CARTESIAN_POINT('Ctrl Pts',(-5.90104309195602,-0.54903348900264,
123.337464048961));
#50638=CARTESIAN_POINT('Ctrl Pts',(-5.71923848619479,-2.50307970426905,
123.430272000176));
#50639=CARTESIAN_POINT('Ctrl Pts',(-4.47037669295292,-4.35784683868379,
123.523079951392));
#50640=CARTESIAN_POINT('Ctrl Pts',(-2.7281895346718,-5.26124787418566,123.615887902608));
#50641=CARTESIAN_POINT('Ctrl Pts',(-0.986002376390676,-6.16464890968752,
123.708695853823));
#50642=CARTESIAN_POINT('Ctrl Pts',(1.24951014692971,-6.11668384627651,123.801503805039));
#50643=CARTESIAN_POINT('Ctrl Pts',(2.95134515200119,-5.13938801177825,123.894311756255));
#50644=CARTESIAN_POINT('Ctrl Pts',(4.65318015707267,-4.16209217727999,123.98711970747));
#50645=CARTESIAN_POINT('Ctrl Pts',(5.82133764389525,-2.25546557169447,124.079927658686));
#50646=CARTESIAN_POINT('Ctrl Pts',(5.91916164642105,-0.29541965774841,124.172735609902));
#50647=CARTESIAN_POINT('Ctrl Pts',(6.01698564894686,1.66462625619787,124.265543561117));
#50648=CARTESIAN_POINT('Ctrl Pts',(5.04447616717559,3.67809147850472,124.358351512333));
#50649=CARTESIAN_POINT('Ctrl Pts',(3.44840774343408,4.81998250071349,124.451159463549));
#50650=CARTESIAN_POINT('Ctrl Pts',(1.85233931969265,5.96187352292221,124.543967414765));
#50651=CARTESIAN_POINT('Ctrl Pts',(-0.367288046018615,6.23219034503295,
124.63677536598));
#50652=CARTESIAN_POINT('Ctrl Pts',(-2.19076919910286,5.50674837692975,124.729583317196));
#50653=CARTESIAN_POINT('Ctrl Pts',(-4.014250352187,4.78130640882659,124.822391268412));
#50654=CARTESIAN_POINT('Ctrl Pts',(-5.44158529264409,3.06010565050916,124.915199219628));
#50655=CARTESIAN_POINT('Ctrl Pts',(-5.81705090267984,1.13387226637038,125.008007170843));
#50656=CARTESIAN_POINT('Ctrl Pts',(-5.88935641279735,0.762926742405473,
125.025879716494));
#50657=CARTESIAN_POINT('Ctrl Pts',(-5.92265297372955,0.384377510403178,
125.043752262145));
#50658=CARTESIAN_POINT('Ctrl Pts',(-5.91915982610221,0.00521712502770735,
125.061624807795));
#50659=CARTESIAN_POINT('Origin',(0.,0.,-10.));
#50660=CARTESIAN_POINT('',(-5.90733548964813,0.0015994485885984,127.063375192205));
#50661=CARTESIAN_POINT('',(-5.90701629014678,0.000721185244744792,126.811624807795));
#50662=CARTESIAN_POINT('',(-5.91675,-7.2459289488551E-16,-10.));
#50663=CARTESIAN_POINT('Ctrl Pts',(-5.90733548964813,0.0015994485885984,
127.063375192205));
#50664=CARTESIAN_POINT('Ctrl Pts',(-5.90948223967714,0.893133898673095,
127.021562783792));
#50665=CARTESIAN_POINT('Ctrl Pts',(-5.72044046389006,1.78380468906801,126.97975037538));
#50666=CARTESIAN_POINT('Ctrl Pts',(-5.33557206520579,2.57979528293403,126.937937966967));
#50667=CARTESIAN_POINT('Ctrl Pts',(-4.4814752276016,4.346251170993,126.84514820839));
#50668=CARTESIAN_POINT('Ctrl Pts',(-2.66296894213967,5.64642482067912,126.752358449814));
#50669=CARTESIAN_POINT('Ctrl Pts',(-0.715198189598532,5.88321024295047,
126.659568691237));
#50670=CARTESIAN_POINT('Ctrl Pts',(1.23257256294227,6.11999566522179,126.56677893266));
#50671=CARTESIAN_POINT('Ctrl Pts',(3.30960778256256,5.29339286007849,126.473989174083));
#50672=CARTESIAN_POINT('Ctrl Pts',(4.56206056674281,3.78301829464937,126.381199415506));
#50673=CARTESIAN_POINT('Ctrl Pts',(5.81451335092313,2.27264372922017,126.28840965693));
#50674=CARTESIAN_POINT('Ctrl Pts',(6.24238369966374,0.0784974035052743,
126.195619898353));
#50675=CARTESIAN_POINT('Ctrl Pts',(5.64917237601244,-1.79178765869978,126.102830139776));
#50676=CARTESIAN_POINT('Ctrl Pts',(5.05596105236112,-3.66207272090495,126.0100403812));
#50677=CARTESIAN_POINT('Ctrl Pts',(3.44166805631763,-5.2084965195999,125.917250622623));
#50678=CARTESIAN_POINT('Ctrl Pts',(1.54764196647018,-5.72087872310008,125.824460864046));
#50679=CARTESIAN_POINT('Ctrl Pts',(-0.346384123377259,-6.23326092660026,
125.731671105469));
#50680=CARTESIAN_POINT('Ctrl Pts',(-2.52014330702865,-5.71160153490567,
125.638881346893));
#50681=CARTESIAN_POINT('Ctrl Pts',(-3.97536201151514,-4.39546807837805,
125.546091588316));
#50682=CARTESIAN_POINT('Ctrl Pts',(-5.19192318398324,-3.29518201411753,
125.468519456279));
#50683=CARTESIAN_POINT('Ctrl Pts',(-5.90630066388776,-1.63964272322248,
125.390947324242));
#50684=CARTESIAN_POINT('Ctrl Pts',(-5.92082732894822,0.0048284439233276,
125.313375192205));
#50685=CARTESIAN_POINT('Ctrl Pts',(-5.91915982610221,0.00521712502770735,
125.061624807795));
#50686=CARTESIAN_POINT('Ctrl Pts',(-5.90451387474925,-1.58451372852251,
125.13656021336));
#50687=CARTESIAN_POINT('Ctrl Pts',(-5.24313102181849,-3.18498822355375,
125.211495618925));
#50688=CARTESIAN_POINT('Ctrl Pts',(-4.09858227733526,-4.28081419582354,
125.28643102449));
#50689=CARTESIAN_POINT('Ctrl Pts',(-2.68105176234036,-5.63800126391799,
125.379238975706));
#50690=CARTESIAN_POINT('Ctrl Pts',(-0.522394452736071,-6.22110939014652,
125.472046926922));
#50691=CARTESIAN_POINT('Ctrl Pts',(1.38569455481539,-5.76225635239487,125.564854878137));
#50692=CARTESIAN_POINT('Ctrl Pts',(3.29378356236686,-5.30340331464321,125.657662829353));
#50693=CARTESIAN_POINT('Ctrl Pts',(4.95130426786537,-3.8025891129114,125.750470780569));
#50694=CARTESIAN_POINT('Ctrl Pts',(5.59678499689816,-1.94929373516699,125.843278731785));
#50695=CARTESIAN_POINT('Ctrl Pts',(6.24226572593094,-0.0959983574225864,
125.936086683));
#50696=CARTESIAN_POINT('Ctrl Pts',(5.87570647849779,2.10977819633463,126.028894634216));
#50697=CARTESIAN_POINT('Ctrl Pts',(4.66550672687537,3.65469438514516,126.121702585432));
#50698=CARTESIAN_POINT('Ctrl Pts',(3.45530697525289,5.19961057395578,126.214510536647));
#50699=CARTESIAN_POINT('Ctrl Pts',(1.40146671944114,6.08366639781989,126.307318487863));
#50700=CARTESIAN_POINT('Ctrl Pts',(-0.552473533347532,5.90072227394494,
126.400126439079));
#50701=CARTESIAN_POINT('Ctrl Pts',(-2.5064137861362,5.71777815007,126.492934390295));
#50702=CARTESIAN_POINT('Ctrl Pts',(-4.36045403590167,4.46783407845601,126.58574234151));
#50703=CARTESIAN_POINT('Ctrl Pts',(-5.26283844776865,2.72512097313255,126.678550292726));
#50704=CARTESIAN_POINT('Ctrl Pts',(-5.69413902220643,1.89217976368593,126.722908464416));
#50705=CARTESIAN_POINT('Ctrl Pts',(-5.90804095800662,0.946669164313941,
126.767266636106));
#50706=CARTESIAN_POINT('Ctrl Pts',(-5.90701629014678,0.000721185244744792,
126.811624807795));
#50707=CARTESIAN_POINT('Origin',(0.,0.,-10.));
#50708=CARTESIAN_POINT('',(-5.91675,7.2459289488551E-16,147.));
#50709=CARTESIAN_POINT('Origin',(0.,0.,147.));
#50710=CARTESIAN_POINT('',(-5.91675,-7.2459289488551E-16,130.));
#50711=CARTESIAN_POINT('',(-5.91675,-7.2459289488551E-16,-10.));
#50712=CARTESIAN_POINT('',(2.58391981634458,5.32271443393329,130.));
#50713=CARTESIAN_POINT('Origin',(0.,0.,130.));
#50714=CARTESIAN_POINT('',(-5.91448192755925,-0.0049507822674949,128.813375192205));
#50715=CARTESIAN_POINT('Ctrl Pts',(2.58391981634458,5.32271443393329,130.));
#50716=CARTESIAN_POINT('Ctrl Pts',(3.47055515188225,4.89229596196688,129.953605120712));
#50717=CARTESIAN_POINT('Ctrl Pts',(4.24029712840795,4.23605651223856,129.907210241423));
#50718=CARTESIAN_POINT('Ctrl Pts',(4.81442615980519,3.43370417302639,129.860815362135));
#50719=CARTESIAN_POINT('Ctrl Pts',(5.38855519120244,2.63135183381422,129.814420482847));
#50720=CARTESIAN_POINT('Ctrl Pts',(5.76707127747114,1.68288660511834,129.768025603558));
#50721=CARTESIAN_POINT('Ctrl Pts',(5.88207504663892,0.705646679344999,129.72163072427));
#50722=CARTESIAN_POINT('Ctrl Pts',(6.11208258497448,-1.2488331722018,129.628840965693));
#50723=CARTESIAN_POINT('Ctrl Pts',(5.28804085490593,-3.31841181205823,129.536051207116));
#50724=CARTESIAN_POINT('Ctrl Pts',(3.7771742476755,-4.56683408622936,129.443261448539));
#50725=CARTESIAN_POINT('Ctrl Pts',(2.26630764044515,-5.81525636040042,129.350471689963));
#50726=CARTESIAN_POINT('Ctrl Pts',(0.0686161560530948,-6.24252226888644,
129.257681931386));
#50727=CARTESIAN_POINT('Ctrl Pts',(-1.80142318997057,-5.64706513861724,
129.164892172809));
#50728=CARTESIAN_POINT('Ctrl Pts',(-3.67146253599433,-5.05160800834801,
129.072102414232));
#50729=CARTESIAN_POINT('Ctrl Pts',(-5.21384974364968,-3.43342783932321,
128.979312655656));
#50730=CARTESIAN_POINT('Ctrl Pts',(-5.72289947820789,-1.53825253979548,
128.886522897079));
#50731=CARTESIAN_POINT('Ctrl Pts',(-5.85666359298725,-1.04025317139774,
128.862140328787));
#50732=CARTESIAN_POINT('Ctrl Pts',(-5.91907655599569,-0.523127503885872,
128.837757760496));
#50733=CARTESIAN_POINT('Ctrl Pts',(-5.91448192755925,-0.0049507822674949,
128.813375192205));
#50734=CARTESIAN_POINT('',(-5.91642361182645,-0.00541095714722729,128.561624807795));
#50735=CARTESIAN_POINT('',(-5.91675,-7.2459289488551E-16,-10.));
#50736=CARTESIAN_POINT('',(-2.59168464642692,5.32810255942641,130.));
#50737=CARTESIAN_POINT('Ctrl Pts',(-5.91642361182645,-0.00541095714722729,
128.561624807795));
#50738=CARTESIAN_POINT('Ctrl Pts',(-5.92072243615008,-0.47190700523705,
128.583588961282));
#50739=CARTESIAN_POINT('Ctrl Pts',(-5.87022027230614,-0.937486925898181,
128.605553114769));
#50740=CARTESIAN_POINT('Ctrl Pts',(-5.76137787898222,-1.38900619205342,
128.627517268256));
#50741=CARTESIAN_POINT('Ctrl Pts',(-5.30147217235758,-3.29686838447854,
128.720325219472));
#50742=CARTESIAN_POINT('Ctrl Pts',(-3.79994585631488,-4.95368824049658,
128.813133170687));
#50743=CARTESIAN_POINT('Ctrl Pts',(-1.94616157152931,-5.5980107456732,128.905941121903));
#50744=CARTESIAN_POINT('Ctrl Pts',(-0.092377286743959,-6.24233325084974,
128.998749073119));
#50745=CARTESIAN_POINT('Ctrl Pts',(2.11366496678405,-5.87415840518507,129.091557024334));
#50746=CARTESIAN_POINT('Ctrl Pts',(3.65766172888916,-4.66320511213384,129.18436497555));
#50747=CARTESIAN_POINT('Ctrl Pts',(5.20165849099436,-3.45225181908255,129.277172926766));
#50748=CARTESIAN_POINT('Ctrl Pts',(6.08360976167645,-1.3985200786447,129.369980877982));
#50749=CARTESIAN_POINT('Ctrl Pts',(5.89993317977312,0.555595301027637,129.462788829197));
#50750=CARTESIAN_POINT('Ctrl Pts',(5.7162565978698,2.50971068069987,129.555596780413));
#50751=CARTESIAN_POINT('Ctrl Pts',(4.46695216338095,4.36420969960679,129.648404731629));
#50752=CARTESIAN_POINT('Ctrl Pts',(2.7229167058007,5.26500797028939,129.741212682844));
#50753=CARTESIAN_POINT('Ctrl Pts',(1.10188369738893,6.10227519691029,129.827475121896));
#50754=CARTESIAN_POINT('Ctrl Pts',(-0.946556911312304,6.11562209275089,
129.913737560948));
#50755=CARTESIAN_POINT('Ctrl Pts',(-2.59168464642692,5.32810255942641,130.));
#50756=CARTESIAN_POINT('Origin',(0.,0.,130.));
#50757=CARTESIAN_POINT('Origin',(0.,0.,-13.2351405640096));
#50758=CARTESIAN_POINT('',(-4.9163646833512,-0.00411529722797478,129.38985943599));
#50759=CARTESIAN_POINT('',(-4.92459990823896,0.000661498711628031,129.735140564009));
#50760=CARTESIAN_POINT('',(-4.91825,6.88216836313478E-12,-13.2351405640096));
#50761=CARTESIAN_POINT('',(2.86417334265864,-4.00661193697147,130.));
#50762=CARTESIAN_POINT('Ctrl Pts',(-4.9163646833512,-0.00411529722797478,
129.38985943599));
#50763=CARTESIAN_POINT('Ctrl Pts',(-4.92018393062525,-0.43484545501757,
129.414242004282));
#50764=CARTESIAN_POINT('Ctrl Pts',(-4.86830366606858,-0.864701932685717,
129.438624572573));
#50765=CARTESIAN_POINT('Ctrl Pts',(-4.75711334071876,-1.27865983079266,
129.463007140865));
#50766=CARTESIAN_POINT('Ctrl Pts',(-4.33396991620548,-2.85400878366436,
129.555796899442));
#50767=CARTESIAN_POINT('Ctrl Pts',(-3.05187317660211,-4.19910780192726,
129.648586658018));
#50768=CARTESIAN_POINT('Ctrl Pts',(-1.49741827930524,-4.69407666675153,
129.741376416595));
#50769=CARTESIAN_POINT('Ctrl Pts',(-0.0532262264089908,-5.15393568373128,
129.82758427773));
#50770=CARTESIAN_POINT('Ctrl Pts',(1.62605576293774,-4.87999239627907,129.913792138865));
#50771=CARTESIAN_POINT('Ctrl Pts',(2.86417334265864,-4.00661193697147,130.));
#50772=CARTESIAN_POINT('',(-2.85706463458608,-4.00329423553871,130.));
#50773=CARTESIAN_POINT('Origin',(0.,0.,130.));
#50774=CARTESIAN_POINT('Ctrl Pts',(-4.92459990823896,0.000661498711628031,
129.735140564009));
#50775=CARTESIAN_POINT('Ctrl Pts',(-4.92384457190956,-0.738149461065841,
129.777023067065));
#50776=CARTESIAN_POINT('Ctrl Pts',(-4.74695671268496,-1.47922316861453,
129.818905570121));
#50777=CARTESIAN_POINT('Ctrl Pts',(-4.42287481469073,-2.14486768324074,
129.860788073176));
#50778=CARTESIAN_POINT('Ctrl Pts',(-4.06380629222381,-2.88237259738225,
129.907192048784));
#50779=CARTESIAN_POINT('Ctrl Pts',(-3.52404725972277,-3.52728314116421,
129.953596024392));
#50780=CARTESIAN_POINT('Ctrl Pts',(-2.85706463458654,-4.00329423553838,
130.));
#50781=CARTESIAN_POINT('Origin',(0.,0.,-13.2351405640096));
#50782=CARTESIAN_POINT('',(-4.91042426534194,0.00132952854738158,127.63985943599));
#50783=CARTESIAN_POINT('',(-4.91797869250264,-0.00449781382338033,127.985140564009));
#50784=CARTESIAN_POINT('',(-4.91825,6.88216836313478E-12,-13.2351405640096));
#50785=CARTESIAN_POINT('Ctrl Pts',(-4.91042426534194,0.00132952854738161,
127.63985943599));
#50786=CARTESIAN_POINT('Ctrl Pts',(-4.90824865591709,-0.902190083096324,
127.690836786155));
#50787=CARTESIAN_POINT('Ctrl Pts',(-4.23589608641458,-3.4533195340969,127.834603894896));
#50788=CARTESIAN_POINT('Ctrl Pts',(-0.129499705332998,-5.81541776548578,
128.071160762213));
#50789=CARTESIAN_POINT('Ctrl Pts',(4.82184908053961,-3.25351245829232,128.349530037944));
#50790=CARTESIAN_POINT('Ctrl Pts',(5.34408280538262,2.29632880892462,128.627899313674));
#50791=CARTESIAN_POINT('Ctrl Pts',(0.958562204898396,5.73769098457033,128.906268589404));
#50792=CARTESIAN_POINT('Ctrl Pts',(-3.84727915788463,4.06816077427375,129.160255296843));
#50793=CARTESIAN_POINT('Ctrl Pts',(-4.90564948830288,1.20433163556846,129.321452245705));
#50794=CARTESIAN_POINT('Ctrl Pts',(-4.9163646833512,-0.00411529722797593,
129.38985943599));
#50795=CARTESIAN_POINT('Ctrl Pts',(-4.91797869250264,-0.00449781382338123,
127.985140564009));
#50796=CARTESIAN_POINT('Ctrl Pts',(-4.92155205503,-0.39226883482863,128.007104717496));
#50797=CARTESIAN_POINT('Ctrl Pts',(-4.70219114273014,-2.41455913631502,
128.121876822199));
#50798=CARTESIAN_POINT('Ctrl Pts',(-1.91054242683083,-5.49493073827346,
128.329456878117));
#50799=CARTESIAN_POINT('Ctrl Pts',(3.59072126358126,-4.5768037590934,128.607880731764));
#50800=CARTESIAN_POINT('Ctrl Pts',(5.79006558455199,0.54463932997096,128.886304585412));
#50801=CARTESIAN_POINT('Ctrl Pts',(2.67464333335573,5.16925071277719,129.164728439058));
#50802=CARTESIAN_POINT('Ctrl Pts',(-2.90822559480448,5.03732645866885,129.443152292706));
#50803=CARTESIAN_POINT('Ctrl Pts',(-4.88224936370592,1.79675240995502,129.633289667689));
#50804=CARTESIAN_POINT('Ctrl Pts',(-4.92468145141885,0.0804206638054886,
129.730619091457));
#50805=CARTESIAN_POINT('Ctrl Pts',(-4.92459990823896,0.000661498711627927,
129.735140564009));
#50806=CARTESIAN_POINT('Origin',(0.,0.,-13.2351405640096));
#50807=CARTESIAN_POINT('',(-4.92163924630915,0.0040136044860252,125.88985943599));
#50808=CARTESIAN_POINT('',(-4.91015893336957,0.000599479339165321,126.235140564009));
#50809=CARTESIAN_POINT('',(-4.91825,6.88216836313478E-12,-13.2351405640096));
#50810=CARTESIAN_POINT('Ctrl Pts',(-4.92163924630915,0.00401360448602523,
125.88985943599));
#50811=CARTESIAN_POINT('Ctrl Pts',(-4.90956407490104,-1.36293959073401,
125.967431568027));
#50812=CARTESIAN_POINT('Ctrl Pts',(-3.60543114971607,-4.38521193124015,
126.137793458641));
#50813=CARTESIAN_POINT('Ctrl Pts',(1.51899055903744,-5.61497221539792,126.400945107832));
#50814=CARTESIAN_POINT('Ctrl Pts',(5.54459407167148,-1.75861584681939,126.679314383562));
#50815=CARTESIAN_POINT('Ctrl Pts',(4.4776028977884,3.71298266576747,126.957683659292));
#50816=CARTESIAN_POINT('Ctrl Pts',(-0.701952670164813,5.77430311013206,
127.236052935023));
#50817=CARTESIAN_POINT('Ctrl Pts',(-4.40634675631825,3.12578018922078,127.463444860589));
#50818=CARTESIAN_POINT('Ctrl Pts',(-4.91220873372888,0.742410241629219,
127.598047027578));
#50819=CARTESIAN_POINT('Ctrl Pts',(-4.91042426534194,0.00132952854738161,
127.63985943599));
#50820=CARTESIAN_POINT('Ctrl Pts',(-4.91015893336957,0.000599479339165182,
126.235140564009));
#50821=CARTESIAN_POINT('Ctrl Pts',(-4.90922862128532,-0.858241586946162,
126.283590343535));
#50822=CARTESIAN_POINT('Ctrl Pts',(-4.28511186721648,-3.36349980276401,
126.424848074277));
#50823=CARTESIAN_POINT('Ctrl Pts',(-0.286591160200441,-5.81013496081811,
126.658913756234));
#50824=CARTESIAN_POINT('Ctrl Pts',(4.73304984475302,-3.38201813095182,126.937337609882));
#50825=CARTESIAN_POINT('Ctrl Pts',(5.40386860173048,2.15348096294236,127.215761463529));
#50826=CARTESIAN_POINT('Ctrl Pts',(1.10968603140598,5.71042388849744,127.494185317176));
#50827=CARTESIAN_POINT('Ctrl Pts',(-3.78509266885793,4.15375692724055,127.750645017336));
#50828=CARTESIAN_POINT('Ctrl Pts',(-4.90645306861513,1.24622973155316,127.91429676628));
#50829=CARTESIAN_POINT('Ctrl Pts',(-4.91797869250264,-0.00449781382338123,
127.985140564009));
#50830=CARTESIAN_POINT('Origin',(0.,0.,-13.2351405640096));
#50831=CARTESIAN_POINT('',(-4.92348377480886,-0.0033100034161842,124.13985943599));
#50832=CARTESIAN_POINT('',(-4.92025314821947,0.00433669247712778,124.485140564009));
#50833=CARTESIAN_POINT('',(-4.91825,6.88216836313478E-12,-13.2351405640096));
#50834=CARTESIAN_POINT('Ctrl Pts',(-4.92348377480886,-0.00331000341618409,
124.13985943599));
#50835=CARTESIAN_POINT('Ctrl Pts',(-4.92503160724926,-0.203599380317578,
124.151236591323));
#50836=CARTESIAN_POINT('Ctrl Pts',(-4.82286209861274,-2.03581585448879,
124.255403505233));
#50837=CARTESIAN_POINT('Ctrl Pts',(-2.52380371468285,-5.24076813201426,
124.45236017772));
#50838=CARTESIAN_POINT('Ctrl Pts',(3.04363480249081,-4.95696714685634,124.73072945345));
#50839=CARTESIAN_POINT('Ctrl Pts',(5.8155622361216,-0.120301504763635,125.00909872918));
#50840=CARTESIAN_POINT('Ctrl Pts',(3.24602435053818,4.82685823868056,125.287468004911));
#50841=CARTESIAN_POINT('Ctrl Pts',(-2.30491470342209,5.34065588049586,125.565837280641));
#50842=CARTESIAN_POINT('Ctrl Pts',(-4.78192169540783,2.17293537069928,125.766634424334));
#50843=CARTESIAN_POINT('Ctrl Pts',(-4.92400807960103,0.27217412393866,125.874641809451));
#50844=CARTESIAN_POINT('Ctrl Pts',(-4.92163924630915,0.00401360448602523,
125.88985943599));
#50845=CARTESIAN_POINT('Ctrl Pts',(-4.92025314821947,0.00433669247712733,
124.485140564009));
#50846=CARTESIAN_POINT('Ctrl Pts',(-4.90807882105857,-1.31711406519994,
124.560075969574));
#50847=CARTESIAN_POINT('Ctrl Pts',(-3.67741741891198,-4.29518066827556,
124.727819326355));
#50848=CARTESIAN_POINT('Ctrl Pts',(1.36013010449734,-5.65595010773044,124.988370634352));
#50849=CARTESIAN_POINT('Ctrl Pts',(5.49353165593364,-1.91333155142861,125.266794487999));
#50850=CARTESIAN_POINT('Ctrl Pts',(4.57943353516515,3.58726955670461,125.545218341646));
#50851=CARTESIAN_POINT('Ctrl Pts',(-0.542280161447921,5.79186205548623,
125.823642195293));
#50852=CARTESIAN_POINT('Ctrl Pts',(-4.36119727820526,3.21725084589819,126.053616269414));
#50853=CARTESIAN_POINT('Ctrl Pts',(-4.91101068013832,0.786910992930685,
126.190782392319));
#50854=CARTESIAN_POINT('Ctrl Pts',(-4.91015893336957,0.000599479339165182,
126.235140564009));
#50855=CARTESIAN_POINT('Origin',(0.,0.,-13.2351405640096));
#50856=CARTESIAN_POINT('',(-4.91119302625731,-0.00235396460084376,122.38985943599));
#50857=CARTESIAN_POINT('',(-4.92462090872917,-0.00264672153492462,122.735140564009));
#50858=CARTESIAN_POINT('',(-4.91825,6.88216836313478E-12,-13.2351405640096));
#50859=CARTESIAN_POINT('Ctrl Pts',(-4.91119302625731,-0.00235396460084351,
122.38985943599));
#50860=CARTESIAN_POINT('Ctrl Pts',(-4.91409224889185,-0.675107583035024,
122.427831373196));
#50861=CARTESIAN_POINT('Ctrl Pts',(-4.47117164087798,-2.98817465699793,
122.558593068979));
#50862=CARTESIAN_POINT('Ctrl Pts',(-0.940153731250069,-5.74032638196031,
122.782144523338));
#50863=CARTESIAN_POINT('Ctrl Pts',(4.3202276147748,-3.89498002173257,123.060513799069));
#50864=CARTESIAN_POINT('Ctrl Pts',(5.61257555605349,1.52781924872262,123.338883074799));
#50865=CARTESIAN_POINT('Ctrl Pts',(1.74989711756287,5.54735036413612,123.617252350529));
#50866=CARTESIAN_POINT('Ctrl Pts',(-3.49646344277389,4.51572304497822,123.884244470926));
#50867=CARTESIAN_POINT('Ctrl Pts',(-4.91240780153887,1.42991992956681,124.058446832747));
#50868=CARTESIAN_POINT('Ctrl Pts',(-4.92348377480886,-0.00331000341618409,
124.13985943599));
#50869=CARTESIAN_POINT('Ctrl Pts',(-4.92462090872918,-0.00264672153492481,
122.735140564009));
#50870=CARTESIAN_POINT('Ctrl Pts',(-4.92560449294135,-0.15418394798358,
122.743753644397));
#50871=CARTESIAN_POINT('Ctrl Pts',(-4.85041204194471,-1.937580837054,122.845174676002));
#50872=CARTESIAN_POINT('Ctrl Pts',(-2.67785788744019,-5.1641845055458,123.039403658822));
#50873=CARTESIAN_POINT('Ctrl Pts',(2.89689656449083,-5.04457280666451,123.317827512469));
#50874=CARTESIAN_POINT('Ctrl Pts',(5.80996060787651,-0.289969534807391,
123.596251366116));
#50875=CARTESIAN_POINT('Ctrl Pts',(3.3847889720702,4.73105991359457,123.874675219763));
#50876=CARTESIAN_POINT('Ctrl Pts',(-2.15035225820507,5.40515584988507,124.15309907341));
#50877=CARTESIAN_POINT('Ctrl Pts',(-4.75175655075456,2.26816332338643,124.356587521492));
#50878=CARTESIAN_POINT('Ctrl Pts',(-4.9231567985875,0.319510658820078,124.467268018358));
#50879=CARTESIAN_POINT('Ctrl Pts',(-4.92025314821947,0.00433669247712733,
124.485140564009));
#50880=CARTESIAN_POINT('Origin',(0.,0.,-13.2351405640096));
#50881=CARTESIAN_POINT('',(-4.91484151762446,0.00420376846348179,120.63985943599));
#50882=CARTESIAN_POINT('',(-4.91203269181966,-0.00303901792530925,120.985140564009));
#50883=CARTESIAN_POINT('',(-4.91825,6.88216836313478E-12,-13.2351405640096));
#50884=CARTESIAN_POINT('Ctrl Pts',(-4.91484151762446,0.00420376846348151,
120.63985943599));
#50885=CARTESIAN_POINT('Ctrl Pts',(-4.90560805093787,-1.13760008155203,
120.704426155069));
#50886=CARTESIAN_POINT('Ctrl Pts',(-3.94011208720615,-3.93438762851029,
120.861782632725));
#50887=CARTESIAN_POINT('Ctrl Pts',(0.720116960871199,-5.77205921455916,
121.111928868956));
#50888=CARTESIAN_POINT('Ctrl Pts',(5.24473027743382,-2.51555964562078,121.390298144687));
#50889=CARTESIAN_POINT('Ctrl Pts',(4.95217496174117,3.05142575896264,121.668667420417));
#50890=CARTESIAN_POINT('Ctrl Pts',(0.111156593441196,5.81574416777347,121.947036696148));
#50891=CARTESIAN_POINT('Ctrl Pts',(-4.15767394946337,3.58999786132769,122.187434034672));
#50892=CARTESIAN_POINT('Ctrl Pts',(-4.90700759142861,0.968860316144871,
122.335041614619));
#50893=CARTESIAN_POINT('Ctrl Pts',(-4.91119302625731,-0.00235396460084351,
122.38985943599));
#50894=CARTESIAN_POINT('Ctrl Pts',(-4.91203269181966,-0.00303901792530974,
120.985140564009));
#50895=CARTESIAN_POINT('Ctrl Pts',(-4.91552661966674,-0.624620968137917,
121.020239270437));
#50896=CARTESIAN_POINT('Ctrl Pts',(-4.51718910800845,-2.88547628658539,
121.14814592808));
#50897=CARTESIAN_POINT('Ctrl Pts',(-1.11628260678685,-5.7090837831698,121.368860536939));
#50898=CARTESIAN_POINT('Ctrl Pts',(4.19949232986848,-4.02541782590159,121.647284390586));
#50899=CARTESIAN_POINT('Ctrl Pts',(5.65674202384814,1.35683240677064,121.925708244233));
#50900=CARTESIAN_POINT('Ctrl Pts',(1.9165344585906,5.49241478468641,122.20413209788));
#50901=CARTESIAN_POINT('Ctrl Pts',(-3.41442109159254,4.60970351323632,122.473942871139));
#50902=CARTESIAN_POINT('Ctrl Pts',(-4.91500614351677,1.47866503114549,122.650945693182));
#50903=CARTESIAN_POINT('Ctrl Pts',(-4.92462090872918,-0.00264672153492481,
122.735140564009));
#50904=CARTESIAN_POINT('Origin',(0.,0.,-13.2351405640096));
#50905=CARTESIAN_POINT('',(-4.92629954194425,0.000537611582497406,118.88985943599));
#50906=CARTESIAN_POINT('',(-4.91349502065481,0.00378936958999432,119.235140564009));
#50907=CARTESIAN_POINT('',(-4.91825,6.88216836313478E-12,-13.2351405640096));
#50908=CARTESIAN_POINT('Ctrl Pts',(-4.92629954194425,0.000537611582497478,
118.88985943599));
#50909=CARTESIAN_POINT('Ctrl Pts',(-4.92382324188989,-1.6018918386726,118.981020936942));
#50910=CARTESIAN_POINT('Ctrl Pts',(-3.19834996239224,-4.83994622551109,
119.16497219647));
#50911=CARTESIAN_POINT('Ctrl Pts',(2.32169952544947,-5.33338047839311,119.441713214575));
#50912=CARTESIAN_POINT('Ctrl Pts',(5.74179765096292,-0.931126065133631,
119.720082490305));
#50913=CARTESIAN_POINT('Ctrl Pts',(3.88818176753445,4.3263470221884,119.998451766036));
#50914=CARTESIAN_POINT('Ctrl Pts',(-1.53664297821521,5.61016616253672,120.276821041766));
#50915=CARTESIAN_POINT('Ctrl Pts',(-4.6191898500751,2.63857074308124,120.490623598417));
#50916=CARTESIAN_POINT('Ctrl Pts',(-4.91887759842147,0.503302617187181,
120.611636396492));
#50917=CARTESIAN_POINT('Ctrl Pts',(-4.91484151762446,0.00420376846348151,
120.63985943599));
#50918=CARTESIAN_POINT('Ctrl Pts',(-4.91349502065481,0.00378936958999446,
119.235140564009));
#50919=CARTESIAN_POINT('Ctrl Pts',(-4.90570611541432,-1.08602599250415,
119.296724896476));
#50920=CARTESIAN_POINT('Ctrl Pts',(-4.00953220865736,-3.8298292770796,119.451117180158));
#50921=CARTESIAN_POINT('Ctrl Pts',(0.535527329685027,-5.79248953224288,
119.698317415056));
#50922=CARTESIAN_POINT('Ctrl Pts',(5.16262232020387,-2.68086838186981,119.976741268703));
#50923=CARTESIAN_POINT('Ctrl Pts',(5.04626096459074,2.89395486822036,120.25516512235));
#50924=CARTESIAN_POINT('Ctrl Pts',(0.29335695445051,5.80979054693031,120.533588975998));
#50925=CARTESIAN_POINT('Ctrl Pts',(-4.09594578481282,3.69290005239632,120.776914123217));
#50926=CARTESIAN_POINT('Ctrl Pts',(-4.90628798046357,1.01896516888556,120.927431319221));
#50927=CARTESIAN_POINT('Ctrl Pts',(-4.91203269181966,-0.00303901792530974,
120.985140564009));
#50928=CARTESIAN_POINT('Origin',(0.,0.,-13.2351405640096));
#50929=CARTESIAN_POINT('',(-4.91645972797145,-0.00447498277304698,117.13985943599));
#50930=CARTESIAN_POINT('',(-4.92580304736406,0.00153345327726321,117.485140564009));
#50931=CARTESIAN_POINT('',(-4.91825,6.88216836313478E-12,-13.2351405640096));
#50932=CARTESIAN_POINT('Ctrl Pts',(-4.91645972797146,-0.00447498277304677,
117.13985943599));
#50933=CARTESIAN_POINT('Ctrl Pts',(-4.92035572105884,-0.445617262204197,
117.164825960238));
#50934=CARTESIAN_POINT('Ctrl Pts',(-4.66354596905633,-2.52183626266821,
117.282582243062));
#50935=CARTESIAN_POINT('Ctrl Pts',(-1.73244237806593,-5.5528262552018,117.493128284463));
#50936=CARTESIAN_POINT('Ctrl Pts',(3.7340681068242,-4.46004163516174,117.771497560194));
#50937=CARTESIAN_POINT('Ctrl Pts',(5.77091971441071,0.72919247363337,118.049866835924));
#50938=CARTESIAN_POINT('Ctrl Pts',(2.50730934259094,5.24867944099596,118.328236111654));
#50939=CARTESIAN_POINT('Ctrl Pts',(-3.05920914417388,4.94737055676852,118.606605387384));
#50940=CARTESIAN_POINT('Ctrl Pts',(-4.91313559719146,1.68878926784965,118.793813162163));
#50941=CARTESIAN_POINT('Ctrl Pts',(-4.92634377173867,0.0291589917059973,
118.888231178365));
#50942=CARTESIAN_POINT('Ctrl Pts',(-4.92629954194425,0.000537611582497478,
118.88985943599));
#50943=CARTESIAN_POINT('Ctrl Pts',(-4.92580304736406,0.00153345327726352,
117.485140564009));
#50944=CARTESIAN_POINT('Ctrl Pts',(-4.91948717957292,-1.54697089948827,
117.573210522515));
#50945=CARTESIAN_POINT('Ctrl Pts',(-3.2961243867519,-4.73869079598163,117.754088432236));
#50946=CARTESIAN_POINT('Ctrl Pts',(2.14404793895791,-5.40765965436446,118.027774293173));
#50947=CARTESIAN_POINT('Ctrl Pts',(5.70843197086043,-1.11961106463314,118.306198146821));
#50948=CARTESIAN_POINT('Ctrl Pts',(4.02786563079502,4.19714462012598,118.584622000468));
#50949=CARTESIAN_POINT('Ctrl Pts',(-1.35353404604633,5.65753215529382,118.863045854115));
#50950=CARTESIAN_POINT('Ctrl Pts',(-4.57606832878287,2.74649626627515,119.079885375295));
#50951=CARTESIAN_POINT('Ctrl Pts',(-4.91744404141966,0.556332167569323,
119.20391694526));
#50952=CARTESIAN_POINT('Ctrl Pts',(-4.91349502065481,0.00378936958999446,
119.235140564009));
#50953=CARTESIAN_POINT('Origin',(0.,0.,-13.2351405640096));
#50954=CARTESIAN_POINT('',(-4.91051683961802,0.0014883242551948,115.38985943599));
#50955=CARTESIAN_POINT('',(-4.91816433701936,-0.0045430582786804,115.735140564009));
#50956=CARTESIAN_POINT('',(-4.91825,6.88216836313478E-12,-13.2351405640096));
#50957=CARTESIAN_POINT('Ctrl Pts',(-4.91051683961802,0.00148832425519413,
115.38985943599));
#50958=CARTESIAN_POINT('Ctrl Pts',(-4.90804726165632,-0.912344077878977,
115.441420742111));
#50959=CARTESIAN_POINT('Ctrl Pts',(-4.22428092503253,-3.47414309954378,
115.585771806808));
#50960=CARTESIAN_POINT('Ctrl Pts',(-0.0928658734872262,-5.81606498788651,
115.822912630082));
#50961=CARTESIAN_POINT('Ctrl Pts',(4.84211742021259,-3.22321809728275,116.101281905812));
#50962=CARTESIAN_POINT('Ctrl Pts',(5.329723076416,2.33008324797548,116.379651181542));
#50963=CARTESIAN_POINT('Ctrl Pts',(0.922096096344309,5.74325472209657,116.658020457272));
#50964=CARTESIAN_POINT('Ctrl Pts',(-3.86118283221186,4.04836320761304,116.911423208755));
#50965=CARTESIAN_POINT('Ctrl Pts',(-4.90587600195934,1.19391754851335,117.072036201661));
#50966=CARTESIAN_POINT('Ctrl Pts',(-4.91645972797146,-0.00447498277304677,
117.13985943599));
#50967=CARTESIAN_POINT('Ctrl Pts',(-4.91816433701936,-0.00454305827868106,
115.735140564009));
#50968=CARTESIAN_POINT('Ctrl Pts',(-4.92171124540485,-0.388470337231666,
115.756888197338));
#50969=CARTESIAN_POINT('Ctrl Pts',(-4.70496285032225,-2.40684556258418,
115.871443781883));
#50970=CARTESIAN_POINT('Ctrl Pts',(-1.92293779473958,-5.49017620296048,
116.078807317644));
#50971=CARTESIAN_POINT('Ctrl Pts',(3.57925453095985,-4.58570185517924,116.35723117129));
#50972=CARTESIAN_POINT('Ctrl Pts',(5.79280078373477,0.532149961902354,116.635655024938));
#50973=CARTESIAN_POINT('Ctrl Pts',(2.68387796260612,5.16105837826204,116.914078878585));
#50974=CARTESIAN_POINT('Ctrl Pts',(-2.89101218372597,5.04794741013998,117.192502732232));
#50975=CARTESIAN_POINT('Ctrl Pts',(-4.88641623084225,1.79962650389789,117.382856627373));
#50976=CARTESIAN_POINT('Ctrl Pts',(-4.92614282878396,0.0848399798069363,
117.480402571299));
#50977=CARTESIAN_POINT('Ctrl Pts',(-4.92580304736406,0.00153345327726352,
117.485140564009));
#50978=CARTESIAN_POINT('Origin',(0.,0.,-13.2351405640096));
#50979=CARTESIAN_POINT('',(-4.92193498823661,0.0039246167501111,113.63985943599));
#50980=CARTESIAN_POINT('',(-4.91014665664844,0.000535809922468655,113.985140564009));
#50981=CARTESIAN_POINT('',(-4.91825,6.88216836313478E-12,-13.2351405640096));
#50982=CARTESIAN_POINT('Ctrl Pts',(-4.92193498823661,0.00392461675011099,
113.63985943599));
#50983=CARTESIAN_POINT('Ctrl Pts',(-4.9099414525611,-1.37310435102102,113.718015523984));
#50984=CARTESIAN_POINT('Ctrl Pts',(-3.58916649890494,-4.40514596226126,
113.888961370553));
#50985=CARTESIAN_POINT('Ctrl Pts',(1.55427901866009,-5.60530576738952,114.1526969757));
#50986=CARTESIAN_POINT('Ctrl Pts',(5.55554360765141,-1.72370857086153,114.43106625143));
#50987=CARTESIAN_POINT('Ctrl Pts',(4.45416440249025,3.74107678207312,114.70943552716));
#50988=CARTESIAN_POINT('Ctrl Pts',(-0.738266183349346,5.76976594467228,
114.987804802891));
#50989=CARTESIAN_POINT('Ctrl Pts',(-4.41643946083194,3.10487486952994,115.214612772501));
#50990=CARTESIAN_POINT('Ctrl Pts',(-4.91249151569284,0.73218928160962,115.348630983534));
#50991=CARTESIAN_POINT('Ctrl Pts',(-4.91051683961802,0.00148832425519413,
115.38985943599));
#50992=CARTESIAN_POINT('Ctrl Pts',(-4.91014665664844,0.0005358099224681,
113.985140564009));
#50993=CARTESIAN_POINT('Ctrl Pts',(-4.90931870644957,-0.854473236054642,
114.033373823377));
#50994=CARTESIAN_POINT('Ctrl Pts',(-4.28925358204272,-3.35577066657218,
114.174415033961));
#50995=CARTESIAN_POINT('Ctrl Pts',(-0.300131481883046,-5.80944451695458,
114.408264195761));
#50996=CARTESIAN_POINT('Ctrl Pts',(4.72513224634132,-3.39305905586345,114.686688049408));
#50997=CARTESIAN_POINT('Ctrl Pts',(5.40890880969165,2.14089467055971,114.965111903055));
#50998=CARTESIAN_POINT('Ctrl Pts',(1.12293914182643,5.70777821798859,115.243535756702));
#50999=CARTESIAN_POINT('Ctrl Pts',(-3.77942826098378,4.1613386229973,115.50021197702));
#51000=CARTESIAN_POINT('Ctrl Pts',(-4.90657482594142,1.2499380190338,115.664080246122));
#51001=CARTESIAN_POINT('Ctrl Pts',(-4.91816433701936,-0.00454305827868106,
115.735140564009));
#51002=CARTESIAN_POINT('Origin',(0.,0.,-13.2351405640096));
#51003=CARTESIAN_POINT('',(-4.92322087232039,-0.0034344185441411,111.88985943599));
#51004=CARTESIAN_POINT('',(-4.92013737328565,0.00435641712180093,112.235140564009));
#51005=CARTESIAN_POINT('',(-4.91825,6.88216836313478E-12,-13.2351405640096));
#51006=CARTESIAN_POINT('Ctrl Pts',(-4.92322087232039,-0.0034344185441413,
111.88985943599));
#51007=CARTESIAN_POINT('Ctrl Pts',(-4.92489330250895,-0.214033463505952,
111.90182054728));
#51008=CARTESIAN_POINT('Ctrl Pts',(-4.81683781957552,-2.05665137631426,
112.006571417145));
#51009=CARTESIAN_POINT('Ctrl Pts',(-2.49079015772174,-5.25653882359623,
112.204112045588));
#51010=CARTESIAN_POINT('Ctrl Pts',(3.07475320216653,-4.9377250591284,112.482481321318));
#51011=CARTESIAN_POINT('Ctrl Pts',(5.81620382629126,-0.0837201577406925,
112.760850597049));
#51012=CARTESIAN_POINT('Ctrl Pts',(3.21560001691721,4.84717985482067,113.039219872779));
#51013=CARTESIAN_POINT('Ctrl Pts',(-2.3384612089734,5.3260524957894,113.317589148509));
#51014=CARTESIAN_POINT('Ctrl Pts',(-4.78834883631155,2.15207245650155,113.517802336246));
#51015=CARTESIAN_POINT('Ctrl Pts',(-4.92418061560507,0.261754669609081,
113.625225765407));
#51016=CARTESIAN_POINT('Ctrl Pts',(-4.92193498823661,0.00392461675011099,
113.63985943599));
#51017=CARTESIAN_POINT('Ctrl Pts',(-4.92013737328565,0.00435641712180083,
112.235140564009));
#51018=CARTESIAN_POINT('Ctrl Pts',(-4.90797477458816,-1.31335596428614,
112.309859449416));
#51019=CARTESIAN_POINT('Ctrl Pts',(-3.68324102270088,-4.28773323820959,
112.477386286039));
#51020=CARTESIAN_POINT('Ctrl Pts',(1.34693594561081,-5.65910664861623,112.737721073878));
#51021=CARTESIAN_POINT('Ctrl Pts',(5.48905411228744,-1.92613848265676,113.016144927525));
#51022=CARTESIAN_POINT('Ctrl Pts',(4.58778793892862,3.57658025625215,113.294568781172));
#51023=CARTESIAN_POINT('Ctrl Pts',(-0.528772413221697,5.79311006601865,
113.572992634819));
#51024=CARTESIAN_POINT('Ctrl Pts',(-4.35728148891868,3.22499886036145,113.803183229098));
#51025=CARTESIAN_POINT('Ctrl Pts',(-4.91091180554078,0.79069109385873,113.940565872161));
#51026=CARTESIAN_POINT('Ctrl Pts',(-4.91014665664844,0.0005358099224681,
113.985140564009));
#51027=CARTESIAN_POINT('Origin',(0.,0.,-13.2351405640096));
#51028=CARTESIAN_POINT('',(-4.91104925059525,-0.00220516644860025,110.13985943599));
#51029=CARTESIAN_POINT('',(-4.92470054292969,-0.00258956693979628,110.485140564009));
#51030=CARTESIAN_POINT('',(-4.91825,6.88216836313478E-12,-13.2351405640096));
#51031=CARTESIAN_POINT('Ctrl Pts',(-4.91104925059525,-0.00220516644859954,
110.13985943599));
#51032=CARTESIAN_POINT('Ctrl Pts',(-4.91380230587921,-0.685354792246956,
110.178415329152));
#51033=CARTESIAN_POINT('Ctrl Pts',(-4.4615567037503,-3.00910759707894,110.309760980891));
#51034=CARTESIAN_POINT('Ctrl Pts',(-0.904029340980253,-5.74612625726445,
110.533896391206));
#51035=CARTESIAN_POINT('Ctrl Pts',(4.34464099652475,-3.86772938881385,110.812265666937));
#51036=CARTESIAN_POINT('Ctrl Pts',(5.60285477669039,1.56309128495284,111.090634942667));
#51037=CARTESIAN_POINT('Ctrl Pts',(1.71497050149349,5.55824722307171,111.369004218397));
#51038=CARTESIAN_POINT('Ctrl Pts',(-3.51333726348395,4.49596995217328,111.635412382838));
#51039=CARTESIAN_POINT('Ctrl Pts',(-4.91191922429149,1.41971394224373,111.809030788703));
#51040=CARTESIAN_POINT('Ctrl Pts',(-4.92322087232039,-0.0034344185441413,
111.88985943599));
#51041=CARTESIAN_POINT('Ctrl Pts',(-4.92470054292969,-0.00258956693979698,
110.485140564009));
#51042=CARTESIAN_POINT('Ctrl Pts',(-4.92564256049222,-0.150311071404671,
110.49353712424));
#51043=CARTESIAN_POINT('Ctrl Pts',(-4.85250412977593,-1.92986611247264,
110.594741635686));
#51044=CARTESIAN_POINT('Ctrl Pts',(-2.68989438598306,-5.1579252315488,110.788754098348));
#51045=CARTESIAN_POINT('Ctrl Pts',(2.88512386742743,-5.05131515266979,111.067177951995));
#51046=CARTESIAN_POINT('Ctrl Pts',(5.80926853963687,-0.303518593130995,
111.345601805642));
#51047=CARTESIAN_POINT('Ctrl Pts',(3.39581343955041,4.72315314019781,111.62402565929));
#51048=CARTESIAN_POINT('Ctrl Pts',(-2.13774067438488,5.41015612631201,111.902449512937));
#51049=CARTESIAN_POINT('Ctrl Pts',(-4.7492296217318,2.27590767693226,112.106154481176));
#51050=CARTESIAN_POINT('Ctrl Pts',(-4.923081877169,0.323367947526276,112.217051498201));
#51051=CARTESIAN_POINT('Ctrl Pts',(-4.92013737328565,0.00435641712180083,
112.235140564009));
#51052=CARTESIAN_POINT('Origin',(0.,0.,-13.2351405640096));
#51053=CARTESIAN_POINT('',(-4.91512112114719,0.00426704468460083,108.38985943599));
#51054=CARTESIAN_POINT('',(-4.91210503009247,-0.00308641233103812,108.735140564009));
#51055=CARTESIAN_POINT('',(-4.91825,6.88216836313478E-12,-13.2351405640096));
#51056=CARTESIAN_POINT('Ctrl Pts',(-4.91512112114719,0.00426704468460083,
108.38985943599));
#51057=CARTESIAN_POINT('Ctrl Pts',(-4.90562515227987,-1.14769786247349,
108.455010111025));
#51058=CARTESIAN_POINT('Ctrl Pts',(-3.92619331620162,-3.95487106119495,
108.612950544637));
#51059=CARTESIAN_POINT('Ctrl Pts',(0.756408103882341,-5.76741560789225,
108.863680736825));
#51060=CARTESIAN_POINT('Ctrl Pts',(5.26044902321342,-2.48252131671617,109.142050012555));
#51061=CARTESIAN_POINT('Ctrl Pts',(4.93288399028696,3.08251383648926,109.420419288285));
#51062=CARTESIAN_POINT('Ctrl Pts',(0.0745742349817975,5.81632828314004,
109.698788564016));
#51063=CARTESIAN_POINT('Ctrl Pts',(-4.16983692941391,3.56924743907384,109.938601946584));
#51064=CARTESIAN_POINT('Ctrl Pts',(-4.90717672119688,0.958733404164842,
110.085625570576));
#51065=CARTESIAN_POINT('Ctrl Pts',(-4.91104925059525,-0.00220516644859954,
110.13985943599));
#51066=CARTESIAN_POINT('Ctrl Pts',(-4.91210503009247,-0.00308641233103826,
108.735140564009));
#51067=CARTESIAN_POINT('Ctrl Pts',(-4.91563471133498,-0.620811093111574,
108.770022750279));
#51068=CARTESIAN_POINT('Ctrl Pts',(-4.52057645045832,-2.87771128788229,
108.897712887764));
#51069=CARTESIAN_POINT('Ctrl Pts',(-1.1295941498845,-5.70646489155393,109.118210976465));
#51070=CARTESIAN_POINT('Ctrl Pts',(4.19009293312384,-4.03520082694487,109.396634830112));
#51071=CARTESIAN_POINT('Ctrl Pts',(5.65989100977229,1.34363620801531,109.675058683759));
#51072=CARTESIAN_POINT('Ctrl Pts',(1.92933851580168,5.48793015566298,109.953482537407));
#51073=CARTESIAN_POINT('Ctrl Pts',(-3.40794084750014,4.61695561495044,110.223509830823));
#51074=CARTESIAN_POINT('Ctrl Pts',(-4.91523035387596,1.48246828148492,110.400729173024));
#51075=CARTESIAN_POINT('Ctrl Pts',(-4.92470054292969,-0.00258956693979698,
110.485140564009));
#51076=CARTESIAN_POINT('Origin',(0.,0.,-13.2351405640096));
#51077=CARTESIAN_POINT('',(-4.92634169465701,0.000345390489136179,106.639859435991));
#51078=CARTESIAN_POINT('',(-4.91340451049185,0.00375331177323163,106.985140564009));
#51079=CARTESIAN_POINT('',(-4.91825,6.88216836313478E-12,-13.2351405640096));
#51080=CARTESIAN_POINT('Ctrl Pts',(-4.92634169465701,0.000345390489136449,
106.639859435991));
#51081=CARTESIAN_POINT('Ctrl Pts',(-4.92471495268435,-1.61231162362228,
106.731604892898));
#51082=CARTESIAN_POINT('Ctrl Pts',(-3.17949842752432,-4.85899970765747,
106.916140108382));
#51083=CARTESIAN_POINT('Ctrl Pts',(2.35519976353486,-5.31867183492482,107.193465082443));
#51084=CARTESIAN_POINT('Ctrl Pts',(5.74754071419879,-0.894992599078435,
107.471834358174));
#51085=CARTESIAN_POINT('Ctrl Pts',(3.860892779499,4.35071752231632,107.750203633904));
#51086=CARTESIAN_POINT('Ctrl Pts',(-1.57189968623559,5.60038993197703,108.028572909634));
#51087=CARTESIAN_POINT('Ctrl Pts',(-4.62732659044495,2.61763360948482,108.24179151033));
#51088=CARTESIAN_POINT('Ctrl Pts',(-4.91914962701757,0.492968877619891,
108.362220352448));
#51089=CARTESIAN_POINT('Ctrl Pts',(-4.91512112114719,0.00426704468460083,
108.38985943599));
#51090=CARTESIAN_POINT('Ctrl Pts',(-4.91340451049185,0.00375331177323107,
106.985140564009));
#51091=CARTESIAN_POINT('Ctrl Pts',(-4.90572611028794,-1.08228077601355,
107.046508376318));
#51092=CARTESIAN_POINT('Ctrl Pts',(-4.0144761831106,-3.82219628726396,107.200684139842));
#51093=CARTESIAN_POINT('Ctrl Pts',(0.522016777754955,-5.79372272254491,
107.447667854582));
#51094=CARTESIAN_POINT('Ctrl Pts',(5.15635602784475,-2.69290122657703,107.72609170823));
#51095=CARTESIAN_POINT('Ctrl Pts',(5.05299644850137,2.88217823762239,108.004515561877));
#51096=CARTESIAN_POINT('Ctrl Pts',(0.306905601200556,5.8090905875139,108.282939415524));
#51097=CARTESIAN_POINT('Ctrl Pts',(-4.09123231337672,3.7005678919498,108.526481082901));
#51098=CARTESIAN_POINT('Ctrl Pts',(-4.9062436002954,1.02271438993413,108.677214799063));
#51099=CARTESIAN_POINT('Ctrl Pts',(-4.91210503009247,-0.00308641233103826,
108.735140564009));
#51100=CARTESIAN_POINT('Origin',(0.,0.,-13.2351405640096));
#51101=CARTESIAN_POINT('',(-4.9161599573824,-0.00444126794963291,104.88985943599));
#51102=CARTESIAN_POINT('',(-4.92575191546683,0.00160007646054477,105.235140564009));
#51103=CARTESIAN_POINT('',(-4.91825,6.88216836313478E-12,-13.2351405640096));
#51104=CARTESIAN_POINT('Ctrl Pts',(-4.9161599573824,-0.00444126794963244,
104.88985943599));
#51105=CARTESIAN_POINT('Ctrl Pts',(-4.92009810546701,-0.455971562148408,
104.915409916194));
#51106=CARTESIAN_POINT('Ctrl Pts',(-4.65577396722329,-2.5427641382639,105.033750154974));
#51107=CARTESIAN_POINT('Ctrl Pts',(-1.69748166270338,-5.56361321611808,
105.244880152331));
#51108=CARTESIAN_POINT('Ctrl Pts',(3.76204723591069,-4.43646668065416,105.523249428062));
#51109=CARTESIAN_POINT('Ctrl Pts',(5.76621904666208,0.765476269840323,105.801618703792));
#51110=CARTESIAN_POINT('Ctrl Pts',(2.47424633725344,5.26434621547303,106.079987979522));
#51111=CARTESIAN_POINT('Ctrl Pts',(-3.0902668487708,4.92803072404851,106.358357255252));
#51112=CARTESIAN_POINT('Ctrl Pts',(-4.91794174754249,1.66805361794024,106.544981074075));
#51113=CARTESIAN_POINT('Ctrl Pts',(-4.9263602112072,0.0187016172552051,
106.638815134321));
#51114=CARTESIAN_POINT('Ctrl Pts',(-4.92634169465701,0.000345390489136449,
106.639859435991));
#51115=CARTESIAN_POINT('Ctrl Pts',(-4.92575191546683,0.00160007646054441,
105.235140564009));
#51116=CARTESIAN_POINT('Ctrl Pts',(-4.91921010578824,-1.54314000607646,
105.322994002357));
#51117=CARTESIAN_POINT('Ctrl Pts',(-3.30286425710867,-4.73153004719997,
105.50365539192));
#51118=CARTESIAN_POINT('Ctrl Pts',(2.13143050299427,-5.4126452417369,105.7771247327));
#51119=CARTESIAN_POINT('Ctrl Pts',(5.70580531843759,-1.13292107848706,106.055548586347));
#51120=CARTESIAN_POINT('Ctrl Pts',(4.03764314998017,4.18773952095986,106.333972439994));
#51121=CARTESIAN_POINT('Ctrl Pts',(-1.34033601366353,5.66067344690254,106.612396293641));
#51122=CARTESIAN_POINT('Ctrl Pts',(-4.57287513429699,2.75426175018904,106.829452334979));
#51123=CARTESIAN_POINT('Ctrl Pts',(-4.91733833116936,0.560153504204194,
106.953700425102));
#51124=CARTESIAN_POINT('Ctrl Pts',(-4.91340451049185,0.00375331177323107,
106.985140564009));
#51125=CARTESIAN_POINT('Origin',(0.,0.,-13.2351405640096));
#51126=CARTESIAN_POINT('',(-4.9106152160553,0.00164937912531336,103.13985943599));
#51127=CARTESIAN_POINT('',(-4.91828094548546,-0.00453972600810759,103.485140564009));
#51128=CARTESIAN_POINT('',(-4.91825,6.88216836313478E-12,-13.2351405640096));
#51129=CARTESIAN_POINT('Ctrl Pts',(-4.9106152160553,0.00164937912531374,
103.13985943599));
#51130=CARTESIAN_POINT('Ctrl Pts',(-4.90784427716826,-0.92248639834868,
103.192004698067));
#51131=CARTESIAN_POINT('Ctrl Pts',(-4.21255514724753,-3.49494162507719,
103.33693971872));
#51132=CARTESIAN_POINT('Ctrl Pts',(-0.0562818588867149,-5.81653405097377,
103.57466449795));
#51133=CARTESIAN_POINT('Ctrl Pts',(4.86229519584828,-3.19269814454921,103.85303377368));
#51134=CARTESIAN_POINT('Ctrl Pts',(5.31496177293694,2.36356031570952,104.13140304941));
#51135=CARTESIAN_POINT('Ctrl Pts',(0.885953644154715,5.74894095935824,104.409772325141));
#51136=CARTESIAN_POINT('Ctrl Pts',(-3.87557197153686,4.02797192499425,104.662591120667));
#51137=CARTESIAN_POINT('Ctrl Pts',(-4.90579622906001,1.18381707019861,104.822620157617));
#51138=CARTESIAN_POINT('Ctrl Pts',(-4.9161599573824,-0.00444126794963244,
104.88985943599));
#51139=CARTESIAN_POINT('Ctrl Pts',(-4.91828094548546,-0.0045397260081078,
103.485140564009));
#51140=CARTESIAN_POINT('Ctrl Pts',(-4.92179757162394,-0.3846215820958,103.50667167718));
#51141=CARTESIAN_POINT('Ctrl Pts',(-4.70766588298512,-2.39909247163602,
103.621010741567));
#51142=CARTESIAN_POINT('Ctrl Pts',(-1.93573661342329,-5.48567664608875,
103.82815775717));
#51143=CARTESIAN_POINT('Ctrl Pts',(3.56855014082175,-4.59403682989503,104.106581610817));
#51144=CARTESIAN_POINT('Ctrl Pts',(5.79402609657907,0.518638693265626,104.385005464464));
#51145=CARTESIAN_POINT('Ctrl Pts',(2.69590715174485,5.15478507128686,104.663429318111));
#51146=CARTESIAN_POINT('Ctrl Pts',(-2.87923162804837,5.05467602661504,104.941853171758));
#51147=CARTESIAN_POINT('Ctrl Pts',(-4.88448420473077,1.80732804898653,105.132423587058));
#51148=CARTESIAN_POINT('Ctrl Pts',(-4.92612084217979,0.0887160136435684,
105.230186051141));
#51149=CARTESIAN_POINT('Ctrl Pts',(-4.92575191546683,0.00160007646054441,
105.235140564009));
#51150=CARTESIAN_POINT('Origin',(0.,0.,-13.2351405640096));
#51151=CARTESIAN_POINT('',(-4.92222608014563,0.00382897363343741,101.389859435991));
#51152=CARTESIAN_POINT('',(-4.91013498857969,0.0004726267068067,101.735140564009));
#51153=CARTESIAN_POINT('',(-4.91825,6.88216836313478E-12,-13.2351405640096));
#51154=CARTESIAN_POINT('Ctrl Pts',(-4.92222608014563,0.0038289736334372,
101.389859435991));
#51155=CARTESIAN_POINT('Ctrl Pts',(-4.91033810900471,-1.38327561748898,
101.46859947994));
#51156=CARTESIAN_POINT('Ctrl Pts',(-3.57279275371078,-4.42504846667363,
101.640129282465));
#51157=CARTESIAN_POINT('Ctrl Pts',(1.58950480666019,-5.5954187049212,101.904448843568));
#51158=CARTESIAN_POINT('Ctrl Pts',(5.56627558047574,-1.68873093652502,102.182818119298));
#51159=CARTESIAN_POINT('Ctrl Pts',(4.43054548072448,3.76901880560565,102.461187395029));
#51160=CARTESIAN_POINT('Ctrl Pts',(-0.774542543027661,5.76500822747185,
102.739556670759));
#51161=CARTESIAN_POINT('Ctrl Pts',(-4.42645455217522,3.08395535649196,102.965780684413));
#51162=CARTESIAN_POINT('Ctrl Pts',(-4.91277501756771,0.72196474197561,103.09921493949));
#51163=CARTESIAN_POINT('Ctrl Pts',(-4.9106152160553,0.00164937912531374,
103.13985943599));
#51164=CARTESIAN_POINT('Ctrl Pts',(-4.91013498857969,0.000472626706806561,
101.735140564009));
#51165=CARTESIAN_POINT('Ctrl Pts',(-4.90940804483265,-0.85070330671101,
101.783157303219));
#51166=CARTESIAN_POINT('Ctrl Pts',(-4.29337995317973,-3.34803870942995,
101.923981993645));
#51167=CARTESIAN_POINT('Ctrl Pts',(-0.313679303199746,-5.8087287590948,
102.157614635287));
#51168=CARTESIAN_POINT('Ctrl Pts',(4.71720619091674,-3.40406966062208,102.436038488934));
#51169=CARTESIAN_POINT('Ctrl Pts',(5.41388703969527,2.12827432992347,102.714462342581));
#51170=CARTESIAN_POINT('Ctrl Pts',(1.13624762196393,5.70514380568731,102.992886196228));
#51171=CARTESIAN_POINT('Ctrl Pts',(-3.77385145643153,4.16884673512571,103.249778936704));
#51172=CARTESIAN_POINT('Ctrl Pts',(-4.90663946695428,1.25368750472487,103.413863725964));
#51173=CARTESIAN_POINT('Ctrl Pts',(-4.91828094548546,-0.0045397260081078,
103.485140564009));
#51174=CARTESIAN_POINT('Origin',(0.,0.,-13.2351405640096));
#51175=CARTESIAN_POINT('',(-4.92295084975763,-0.00355279698548788,99.6398594359904));
#51176=CARTESIAN_POINT('',(-4.92002136431585,0.00437517423019299,99.9851405640091));
#51177=CARTESIAN_POINT('',(-4.91825,6.88216836313478E-12,-13.2351405640096));
#51178=CARTESIAN_POINT('Ctrl Pts',(-4.92295084975763,-0.0035527969854883,
99.6398594359904));
#51179=CARTESIAN_POINT('Ctrl Pts',(-4.92474865037419,-0.224465174800093,
99.6524045032355));
#51180=CARTESIAN_POINT('Ctrl Pts',(-4.81074196999753,-2.07749203204646,
99.7577393290575));
#51181=CARTESIAN_POINT('Ctrl Pts',(-2.4576780448157,-5.27210153940609,99.9558639134564));
#51182=CARTESIAN_POINT('Ctrl Pts',(3.10574993054631,-4.91828764741234,100.234233189186));
#51183=CARTESIAN_POINT('Ctrl Pts',(5.81661536145012,-0.0471354507815979,
100.512602464917));
#51184=CARTESIAN_POINT('Ctrl Pts',(3.18504837292365,4.8673096137306,100.790971740647));
#51185=CARTESIAN_POINT('Ctrl Pts',(-2.3719150235782,5.3112385687993,101.069341016377));
#51186=CARTESIAN_POINT('Ctrl Pts',(-4.79470318360075,2.13121410472449,101.268970248158));
#51187=CARTESIAN_POINT('Ctrl Pts',(-4.92434727024986,0.251332311027171,
101.375809721363));
#51188=CARTESIAN_POINT('Ctrl Pts',(-4.92222608014563,0.0038289736334372,
101.389859435991));
#51189=CARTESIAN_POINT('Ctrl Pts',(-4.92002136431585,0.00437517423019302,
99.9851405640091));
#51190=CARTESIAN_POINT('Ctrl Pts',(-4.90787315670411,-1.30959848678255,
100.059642929258));
#51191=CARTESIAN_POINT('Ctrl Pts',(-3.68904982626242,-4.28028194088868,
100.226953245723));
#51192=CARTESIAN_POINT('Ctrl Pts',(1.33373425917899,-5.66223254802231,100.487071513404));
#51193=CARTESIAN_POINT('Ctrl Pts',(5.48454709390498,-1.93893467572513,100.765495367051));
#51194=CARTESIAN_POINT('Ctrl Pts',(4.59611667109638,3.56587100827567,101.043919220699));
#51195=CARTESIAN_POINT('Ctrl Pts',(-0.515260432469941,5.79432750098943,
101.322343074346));
#51196=CARTESIAN_POINT('Ctrl Pts',(-4.353355146971,3.23274483753813,101.552750188783));
#51197=CARTESIAN_POINT('Ctrl Pts',(-4.91081309983891,0.794470768077152,
101.690349352004));
#51198=CARTESIAN_POINT('Ctrl Pts',(-4.91013498857969,0.000472626706806561,
101.735140564009));
#51199=CARTESIAN_POINT('Origin',(0.,0.,-13.2351405640096));
#51200=CARTESIAN_POINT('',(-4.91091515388363,-0.00205329971730024,97.8898594359905));
#51201=CARTESIAN_POINT('',(-4.92477872676417,-0.00253174555402969,98.235140564009));
#51202=CARTESIAN_POINT('',(-4.91825,6.88216836313478E-12,-13.2351405640096));
#51203=CARTESIAN_POINT('Ctrl Pts',(-4.91091515388363,-0.00205329971729964,
97.8898594359905));
#51204=CARTESIAN_POINT('Ctrl Pts',(-4.91351335274079,-0.695597017619058,
97.9289992851084));
#51205=CARTESIAN_POINT('Ctrl Pts',(-4.45185496108958,-3.03003808629795,
98.0609288928032));
#51206=CARTESIAN_POINT('Ctrl Pts',(-0.867869184648594,-5.75169880053843,
98.2856482590747));
#51207=CARTESIAN_POINT('Ctrl Pts',(4.36888249237581,-3.84032573899534,98.5640175348048));
#51208=CARTESIAN_POINT('Ctrl Pts',(5.59291233487078,1.5983014822703,98.8423868105353));
#51209=CARTESIAN_POINT('Ctrl Pts',(1.67997603467162,5.56892418126753,99.1207560862653));
#51210=CARTESIAN_POINT('Ctrl Pts',(-3.53010137522744,4.47618315698173,99.3865802947507));
#51211=CARTESIAN_POINT('Ctrl Pts',(-4.91145119393814,1.4095161983887,99.5596147446588));
#51212=CARTESIAN_POINT('Ctrl Pts',(-4.92295084975763,-0.0035527969854883,
99.6398594359904));
#51213=CARTESIAN_POINT('Ctrl Pts',(-4.92477872676416,-0.00253174555403059,
98.235140564009));
#51214=CARTESIAN_POINT('Ctrl Pts',(-4.92567969671966,-0.146437961420724,
98.2433206040817));
#51215=CARTESIAN_POINT('Ctrl Pts',(-4.85458662833453,-1.9221521487663,98.3443085953702));
#51216=CARTESIAN_POINT('Ctrl Pts',(-2.70191625171569,-5.15163790174596,
98.5381045378744));
#51217=CARTESIAN_POINT('Ctrl Pts',(2.87333547360048,-5.05803002740593,98.8165283915213));
#51218=CARTESIAN_POINT('Ctrl Pts',(5.80854488292173,-0.31706599482648,99.0949522451687));
#51219=CARTESIAN_POINT('Ctrl Pts',(3.40681942119772,4.71522066645252,99.3733760988158));
#51220=CARTESIAN_POINT('Ctrl Pts',(-2.12511743336623,5.41512699725444,99.6517999524627));
#51221=CARTESIAN_POINT('Ctrl Pts',(-4.74669243361833,2.28365257603715,99.8557214408607));
#51222=CARTESIAN_POINT('Ctrl Pts',(-4.92300623678305,0.327224760665144,
99.9668349780427));
#51223=CARTESIAN_POINT('Ctrl Pts',(-4.92002136431585,0.00437517423019302,
99.9851405640091));
#51224=CARTESIAN_POINT('Origin',(0.,0.,-13.2351405640096));
#51225=CARTESIAN_POINT('',(-4.91540576548025,0.004324049150998,96.1398594359904));
#51226=CARTESIAN_POINT('',(-4.91217854052457,-0.00313320867413813,96.485140564009));
#51227=CARTESIAN_POINT('',(-4.91825,6.88216836313478E-12,-13.2351405640096));
#51228=CARTESIAN_POINT('Ctrl Pts',(-4.91540576548025,0.00432404915099827,
96.1398594359904));
#51229=CARTESIAN_POINT('Ctrl Pts',(-4.90565543805024,-1.1577958144934,96.2055940669812));
#51230=CARTESIAN_POINT('Ctrl Pts',(-3.91217231939379,-3.97533522155579,
96.3641184565489));
#51231=CARTESIAN_POINT('Ctrl Pts',(0.792669321423524,-5.76254382722172,
96.6154326046929));
#51232=CARTESIAN_POINT('Ctrl Pts',(5.27595965190304,-2.44938477280896,96.8938018804233));
#51233=CARTESIAN_POINT('Ctrl Pts',(4.91339786110621,3.11347996175579,97.1721711561536));
#51234=CARTESIAN_POINT('Ctrl Pts',(0.0379889261259919,5.81668228935273,
97.4505404318838));
#51235=CARTESIAN_POINT('Ctrl Pts',(-4.18190377251469,3.5484858234407,97.6897698584961));
#51236=CARTESIAN_POINT('Ctrl Pts',(-4.90735374175294,0.948603345866484,
97.8362095265317));
#51237=CARTESIAN_POINT('Ctrl Pts',(-4.91091515388363,-0.00205329971729964,
97.8898594359905));
#51238=CARTESIAN_POINT('Ctrl Pts',(-4.91217854052457,-0.00313320867413834,
96.485140564009));
#51239=CARTESIAN_POINT('Ctrl Pts',(-4.91574274650194,-0.617000532358035,
96.5198062301208));
#51240=CARTESIAN_POINT('Ctrl Pts',(-4.52395216156159,-2.86994616856643,
96.6472798474483));
#51241=CARTESIAN_POINT('Ctrl Pts',(-1.14289954901735,-5.70381496218517,
96.8675614159915));
#51242=CARTESIAN_POINT('Ctrl Pts',(4.18067074617859,-4.04496188041834,97.1459852696388));
#51243=CARTESIAN_POINT('Ctrl Pts',(5.66300921148187,1.33043270129022,97.4244091232857));
#51244=CARTESIAN_POINT('Ctrl Pts',(1.94213207890468,5.4834156773019,97.702832976933));
#51245=CARTESIAN_POINT('Ctrl Pts',(-3.40144532435673,4.62420256715795,97.9730767905073));
#51246=CARTESIAN_POINT('Ctrl Pts',(-4.91545759818065,1.4862729963575,98.150512652866));
#51247=CARTESIAN_POINT('Ctrl Pts',(-4.92477872676416,-0.00253174555403059,
98.235140564009));
#51248=CARTESIAN_POINT('Origin',(0.,0.,-13.2351405640096));
#51249=CARTESIAN_POINT('',(-4.92636580856042,0.000152401533172132,94.3898594359904));
#51250=CARTESIAN_POINT('',(-4.91331497134253,0.00371651414183716,94.7351405640091));
#51251=CARTESIAN_POINT('',(-4.91825,6.88216836313478E-12,-13.2351405640096));
#51252=CARTESIAN_POINT('Ctrl Pts',(-4.92636580856042,0.000152401533172267,
94.3898594359904));
#51253=CARTESIAN_POINT('Ctrl Pts',(-4.9256315120383,-1.6227476720123,94.482188848854));
#51254=CARTESIAN_POINT('Ctrl Pts',(-3.16053327954862,-4.87800756232656,
94.6673080202944));
#51255=CARTESIAN_POINT('Ctrl Pts',(2.38860682377799,-5.30375277093297,94.9452169503114));
#51256=CARTESIAN_POINT('Ctrl Pts',(5.75305638973991,-0.858823724782912,
95.2235862260417));
#51257=CARTESIAN_POINT('Ctrl Pts',(3.83345104448049,4.37491589671717,95.5019555017719));
#51258=CARTESIAN_POINT('Ctrl Pts',(-1.60709420580738,5.59039213539071,95.7803247775023));
#51259=CARTESIAN_POINT('Ctrl Pts',(-4.63538302620171,2.59669818368088,95.9929594222416));
#51260=CARTESIAN_POINT('Ctrl Pts',(-4.91941881535439,0.482630547677397,
96.1128043084044));
#51261=CARTESIAN_POINT('Ctrl Pts',(-4.91540576548025,0.00432404915099827,
96.1398594359904));
#51262=CARTESIAN_POINT('Ctrl Pts',(-4.91331497134253,0.00371651414183681,
94.7351405640091));
#51263=CARTESIAN_POINT('Ctrl Pts',(-4.9057476635683,-1.07853539604368,94.7962918561599));
#51264=CARTESIAN_POINT('Ctrl Pts',(-4.0194063842934,-3.81456105823947,94.9502510995264));
#51265=CARTESIAN_POINT('Ctrl Pts',(0.508503386553553,-5.7949244005297,95.1970182941089));
#51266=CARTESIAN_POINT('Ctrl Pts',(5.15006168983296,-2.70491942447578,95.4754421477558));
#51267=CARTESIAN_POINT('Ctrl Pts',(5.05970444894282,2.87038593073113,95.7538660014031));
#51268=CARTESIAN_POINT('Ctrl Pts',(0.320452578669648,5.80835903218928,96.0322898550501));
#51269=CARTESIAN_POINT('Ctrl Pts',(-4.08650533321589,3.7082338422809,96.2760480425855));
#51270=CARTESIAN_POINT('Ctrl Pts',(-4.90620054836839,1.02646330432835,96.4269982789051));
#51271=CARTESIAN_POINT('Ctrl Pts',(-4.91217854052457,-0.00313320867413834,
96.485140564009));
#51272=CARTESIAN_POINT('Origin',(0.,0.,-13.2351405640096));
#51273=CARTESIAN_POINT('',(-4.91586394481066,-0.0044009184501047,92.6398594359905));
#51274=CARTESIAN_POINT('',(-4.92569885802918,0.00166625634000921,92.985140564009));
#51275=CARTESIAN_POINT('',(-4.91825,6.88216836313478E-12,-13.2351405640096));
#51276=CARTESIAN_POINT('Ctrl Pts',(-4.91586394481065,-0.00440091845010419,
92.6398594359905));
#51277=CARTESIAN_POINT('Ctrl Pts',(-4.91983703663366,-0.466321471806239,
92.66599387215));
#51278=CARTESIAN_POINT('Ctrl Pts',(-4.64792287731085,-2.56369434537738,
92.7849180668864));
#51279=CARTESIAN_POINT('Ctrl Pts',(-1.66245379054078,-5.57418006599121,
92.9966320201996));
#51280=CARTESIAN_POINT('Ctrl Pts',(3.78987752860088,-4.41271620795891,93.2750012959297));
#51281=CARTESIAN_POINT('Ctrl Pts',(5.76129025225566,0.801729781810469,93.5533705716601));
#51282=CARTESIAN_POINT('Ctrl Pts',(2.44108544428034,5.27980471868994,93.8317398473903));
#51283=CARTESIAN_POINT('Ctrl Pts',(-3.12120229435501,4.90849592558558,94.1101091231206));
#51284=CARTESIAN_POINT('Ctrl Pts',(-4.92268165233641,1.64732391744147,94.2961489859873));
#51285=CARTESIAN_POINT('Ctrl Pts',(-4.92636946969337,0.00824402768593246,
94.3893990902772));
#51286=CARTESIAN_POINT('Ctrl Pts',(-4.92636580856042,0.000152401533172267,
94.3898594359904));
#51287=CARTESIAN_POINT('Ctrl Pts',(-4.92569885802918,0.00166625634000918,
92.985140564009));
#51288=CARTESIAN_POINT('Ctrl Pts',(-4.918936253497,-1.5393109239517,93.0727774821989));
#51289=CARTESIAN_POINT('Ctrl Pts',(-3.30958867840564,-4.72436363233033,
93.2532223516047));
#51290=CARTESIAN_POINT('Ctrl Pts',(2.11880147408499,-5.4176013894902,93.526475172226));
#51291=CARTESIAN_POINT('Ctrl Pts',(5.70314763188498,-1.14622493033275,93.8048990258731));
#51292=CARTESIAN_POINT('Ctrl Pts',(4.04739870824418,4.17831164449162,94.0833228795204));
#51293=CARTESIAN_POINT('Ctrl Pts',(-1.32713069113358,5.66378394985563,94.3617467331672));
#51294=CARTESIAN_POINT('Ctrl Pts',(-4.56967059078738,2.76202729401532,94.5790192946638));
#51295=CARTESIAN_POINT('Ctrl Pts',(-4.91723239767682,0.563974172450816,
94.7034839049442));
#51296=CARTESIAN_POINT('Ctrl Pts',(-4.91331497134253,0.00371651414183681,
94.7351405640091));
#51297=CARTESIAN_POINT('Origin',(0.,0.,-13.2351405640096));
#51298=CARTESIAN_POINT('',(-4.9107237361743,0.00180815062061624,90.8898594359904));
#51299=CARTESIAN_POINT('',(-4.9183976868952,-0.00453542631586867,91.235140564009));
#51300=CARTESIAN_POINT('',(-4.91825,6.88216836313478E-12,-13.2351405640096));
#51301=CARTESIAN_POINT('Ctrl Pts',(-4.9107237361743,0.00180815062061683,
90.8898594359904));
#51302=CARTESIAN_POINT('Ctrl Pts',(-4.90764819817127,-0.932625139035979,
90.9425886540228));
#51303=CARTESIAN_POINT('Ctrl Pts',(-4.20073444988904,-3.51573031561613,
91.088107630632));
#51304=CARTESIAN_POINT('Ctrl Pts',(-0.0196956176291403,-5.81677299681053,
91.3264163658181));
#51305=CARTESIAN_POINT('Ctrl Pts',(4.88228060641031,-3.16205188035358,91.6047856415481));
#51306=CARTESIAN_POINT('Ctrl Pts',(5.29999019571399,2.3969438748358,91.8831549172785));
#51307=CARTESIAN_POINT('Ctrl Pts',(0.849776141329328,5.75439975352813,92.1615241930086));
#51308=CARTESIAN_POINT('Ctrl Pts',(-3.88985778820703,4.00755963785217,92.4137590325795));
#51309=CARTESIAN_POINT('Ctrl Pts',(-4.90573065879529,1.17371760789,92.5732041135733));
#51310=CARTESIAN_POINT('Ctrl Pts',(-4.91586394481065,-0.00440091845010419,
92.6398594359905));
#51311=CARTESIAN_POINT('Ctrl Pts',(-4.9183976868952,-0.0045354263158684,
91.235140564009));
#51312=CARTESIAN_POINT('Ctrl Pts',(-4.92188327701382,-0.38077228891719,
91.2564551570223));
#51313=CARTESIAN_POINT('Ctrl Pts',(-4.7103583587901,-2.39133984619341,91.3705777012513));
#51314=CARTESIAN_POINT('Ctrl Pts',(-1.94852490354921,-5.48114725237695,
91.5775081966962));
#51315=CARTESIAN_POINT('Ctrl Pts',(3.55782634118013,-4.60234681743952,91.8559320503431));
#51316=CARTESIAN_POINT('Ctrl Pts',(5.79521989545676,0.505124603729757,92.1343559039904));
#51317=CARTESIAN_POINT('Ctrl Pts',(2.70792167772444,5.14848372720567,92.4127797576374));
#51318=CARTESIAN_POINT('Ctrl Pts',(-2.86743541210141,5.06137715048165,92.6912036112847));
#51319=CARTESIAN_POINT('Ctrl Pts',(-4.88254282097151,1.81503039074797,92.8819905467418));
#51320=CARTESIAN_POINT('Ctrl Pts',(-4.92609788679581,0.0925919079470681,
92.9799695309832));
#51321=CARTESIAN_POINT('Ctrl Pts',(-4.92569885802918,0.00166625634000918,
92.985140564009));
#51322=CARTESIAN_POINT('Origin',(0.,0.,-13.2351405640096));
#51323=CARTESIAN_POINT('',(-4.92251196586327,0.00372681388479887,89.1398594359905));
#51324=CARTESIAN_POINT('',(-4.91012478479042,0.000409354062299583,89.485140564009));
#51325=CARTESIAN_POINT('',(-4.91825,6.88216836313478E-12,-13.2351405640096));
#51326=CARTESIAN_POINT('Ctrl Pts',(-4.92251196586327,0.0037268138847989,
89.1398594359905));
#51327=CARTESIAN_POINT('Ctrl Pts',(-4.91075438653713,-1.39345382076143,
89.2191834358957));
#51328=CARTESIAN_POINT('Ctrl Pts',(-3.55631018654717,-4.44491937563105,
89.3912971943777));
#51329=CARTESIAN_POINT('Ctrl Pts',(1.62466770970617,-5.58531027310169,89.6562007114362));
#51330=CARTESIAN_POINT('Ctrl Pts',(5.57678733692693,-1.65368649159043,89.9345699871666));
#51331=CARTESIAN_POINT('Ctrl Pts',(4.40675127502924,3.79681171692856,90.2129392628969));
#51332=CARTESIAN_POINT('Ctrl Pts',(-0.810788259783799,5.76002243151662,
90.4913085386271));
#51333=CARTESIAN_POINT('Ctrl Pts',(-4.43638158111647,3.06303241975059,90.716948596325));
#51334=CARTESIAN_POINT('Ctrl Pts',(-4.91306034800856,0.711735285578314,
90.8497988954461));
#51335=CARTESIAN_POINT('Ctrl Pts',(-4.9107237361743,0.00180815062061683,
90.8898594359904));
#51336=CARTESIAN_POINT('Ctrl Pts',(-4.91012478479042,0.000409354062299305,
89.485140564009));
#51337=CARTESIAN_POINT('Ctrl Pts',(-4.90949807124995,-0.846932791369525,
89.5329407830614));
#51338=CARTESIAN_POINT('Ctrl Pts',(-4.29749360927449,-3.3403057452366,89.6735489533296));
#51339=CARTESIAN_POINT('Ctrl Pts',(-0.327225418400649,-5.80798140730008,
89.9069650748132));
#51340=CARTESIAN_POINT('Ctrl Pts',(4.70925447839735,-3.41506175049384,90.1853889284604));
#51341=CARTESIAN_POINT('Ctrl Pts',(5.41883582332552,2.11564241350824,90.4638127821077));
#51342=CARTESIAN_POINT('Ctrl Pts',(1.14954992199983,5.70247836285427,90.7422366357546));
#51343=CARTESIAN_POINT('Ctrl Pts',(-3.76826016539578,4.17635147584231,90.9993458963886));
#51344=CARTESIAN_POINT('Ctrl Pts',(-4.90670632864398,1.25743738123968,91.1636472058066));
#51345=CARTESIAN_POINT('Ctrl Pts',(-4.9183976868952,-0.0045354263158684,
91.235140564009));
#51346=CARTESIAN_POINT('Origin',(0.,0.,-13.2351405640096));
#51347=CARTESIAN_POINT('',(-4.92267424784073,-0.00366498708994259,87.3898594359905));
#51348=CARTESIAN_POINT('',(-4.91990514195361,0.00439296476756349,87.735140564009));
#51349=CARTESIAN_POINT('',(-4.91825,6.88216836313478E-12,-13.2351405640096));
#51350=CARTESIAN_POINT('Ctrl Pts',(-4.92267424784073,-0.0036649870899429,
87.3898594359905));
#51351=CARTESIAN_POINT('Ctrl Pts',(-4.92459773178982,-0.234894405579778,
87.4029884591917));
#51352=CARTESIAN_POINT('Ctrl Pts',(-4.80457424349024,-2.09833774282285,
87.5089072409697));
#51353=CARTESIAN_POINT('Ctrl Pts',(-2.42446869975928,-5.28745567713485,
87.7076157813245));
#51354=CARTESIAN_POINT('Ctrl Pts',(3.1366237873624,-4.89865565541509,87.9859850570546));
#51355=CARTESIAN_POINT('Ctrl Pts',(5.81679677614137,-0.0105488790210397,
88.2643543327851));
#51356=CARTESIAN_POINT('Ctrl Pts',(3.15437072011317,4.88724680918305,88.5427236085151));
#51357=CARTESIAN_POINT('Ctrl Pts',(-2.40527499904105,5.29621451536529,88.8210928842456));
#51358=CARTESIAN_POINT('Ctrl Pts',(-4.80098485902228,2.11036059073919,89.0201381600706));
#51359=CARTESIAN_POINT('Ctrl Pts',(-4.92450789050092,0.240907204047213,
89.1263936773189));
#51360=CARTESIAN_POINT('Ctrl Pts',(-4.92251196586327,0.0037268138847989,
89.1398594359905));
#51361=CARTESIAN_POINT('Ctrl Pts',(-4.91990514195361,0.00439296476756341,
87.735140564009));
#51362=CARTESIAN_POINT('Ctrl Pts',(-4.90777396943026,-1.30584162754635,
87.8094264091005));
#51363=CARTESIAN_POINT('Ctrl Pts',(-3.69484393042714,-4.27282686419821,
87.9765202054077));
#51364=CARTESIAN_POINT('Ctrl Pts',(1.32052531850694,-5.66532765029288,88.2364219529305));
#51365=CARTESIAN_POINT('Ctrl Pts',(5.48001024482615,-1.95172032284121,88.5148458065777));
#51366=CARTESIAN_POINT('Ctrl Pts',(4.60442040478046,3.5551423653677,88.7932696602248));
#51367=CARTESIAN_POINT('Ctrl Pts',(-0.501745649193681,5.79551342035425,
89.071693513872));
#51368=CARTESIAN_POINT('Ctrl Pts',(-4.34941635491549,3.24049005489256,89.3023171484666));
#51369=CARTESIAN_POINT('Ctrl Pts',(-4.91071488575088,0.798249805180592,
89.4401328318457));
#51370=CARTESIAN_POINT('Ctrl Pts',(-4.91012478479042,0.000409354062299305,
89.485140564009));
#51371=CARTESIAN_POINT('Origin',(0.,0.,-13.2351405640096));
#51372=CARTESIAN_POINT('',(-4.91079088019924,-0.00189858029133678,85.6398594359905));
#51373=CARTESIAN_POINT('',(-4.92485543050125,-0.00247326924054714,85.9851405640091));
#51374=CARTESIAN_POINT('',(-4.91825,6.88216836313478E-12,-13.2351405640096));
#51375=CARTESIAN_POINT('Ctrl Pts',(-4.91079088019924,-0.00189858029133678,
85.6398594359905));
#51376=CARTESIAN_POINT('Ctrl Pts',(-4.91322562087344,-0.705834272848961,
85.6795832410645));
#51377=CARTESIAN_POINT('Ctrl Pts',(-4.7719853585205,-1.40883815722723,85.7193070461385));
#51378=CARTESIAN_POINT('Ctrl Pts',(-4.48226309624073,-2.04412712243916,
85.7590308512125));
#51379=CARTESIAN_POINT('Ctrl Pts',(-3.80550872386488,-3.52808138106679,
85.8518206097893));
#51380=CARTESIAN_POINT('Ctrl Pts',(-2.31859170850729,-4.64256258633989,
85.944610368366));
#51381=CARTESIAN_POINT('Ctrl Pts',(-0.704362227995952,-4.87575758302086,
86.0374001269428));
#51382=CARTESIAN_POINT('Ctrl Pts',(0.909867252515474,-5.10895257970185,
86.1301898855195));
#51383=CARTESIAN_POINT('Ctrl Pts',(2.65140919818075,-4.46086136779037,86.2229796440963));
#51384=CARTESIAN_POINT('Ctrl Pts',(3.72047975084877,-3.2291126614191,86.3157694026731));
#51385=CARTESIAN_POINT('Ctrl Pts',(4.78955030351679,-1.99736395504783,86.4085591612498));
#51386=CARTESIAN_POINT('Ctrl Pts',(5.18614946318774,-0.181957754216804,
86.5013489198265));
#51387=CARTESIAN_POINT('Ctrl Pts',(4.72814345648312,1.38340074148049,86.5941386784033));
#51388=CARTESIAN_POINT('Ctrl Pts',(4.27013744977847,2.94875923717787,86.6869284369801));
#51389=CARTESIAN_POINT('Ctrl Pts',(2.95752627669819,4.26407002774135,86.7797181955569));
#51390=CARTESIAN_POINT('Ctrl Pts',(1.39311208672304,4.72529119424815,86.8725079541337));
#51391=CARTESIAN_POINT('Ctrl Pts',(-0.17130210325193,5.18651236075489,86.9652977127104));
#51392=CARTESIAN_POINT('Ctrl Pts',(-1.98751931012186,4.793643903205,87.0580874712871));
#51393=CARTESIAN_POINT('Ctrl Pts',(-3.22146188874805,3.72710631133011,87.1508772298639));
#51394=CARTESIAN_POINT('Ctrl Pts',(-4.2808112688118,2.81147542514635,87.2305379652394));
#51395=CARTESIAN_POINT('Ctrl Pts',(-4.91100345226673,1.39932632727122,87.3101987006149));
#51396=CARTESIAN_POINT('Ctrl Pts',(-4.92267424784073,-0.00366498708994259,
87.3898594359905));
#51397=CARTESIAN_POINT('Ctrl Pts',(-4.92485543050125,-0.00247326924054743,
85.9851405640091));
#51398=CARTESIAN_POINT('Ctrl Pts',(-4.92571589835969,-0.142564623586291,
85.9931040839239));
#51399=CARTESIAN_POINT('Ctrl Pts',(-4.85665955234442,-1.91443894856322,
86.0938755550544));
#51400=CARTESIAN_POINT('Ctrl Pts',(-2.71392342160519,-5.14532255195471,
86.2874549774007));
#51401=CARTESIAN_POINT('Ctrl Pts',(2.86153145157372,-5.06471739129104,86.5658788310476));
#51402=CARTESIAN_POINT('Ctrl Pts',(5.80778963327165,-0.330611671985869,
86.844302684695));
#51403=CARTESIAN_POINT('Ctrl Pts',(3.4178068730022,4.70726254641164,87.1227265383419));
#51404=CARTESIAN_POINT('Ctrl Pts',(-2.11248263373895,5.42006841507948,87.4011503919893));
#51405=CARTESIAN_POINT('Ctrl Pts',(-4.74414493672689,2.29139803765962,87.6052884005448));
#51406=CARTESIAN_POINT('Ctrl Pts',(-4.92292987519333,0.331081099453985,
87.7166184578847));
#51407=CARTESIAN_POINT('Ctrl Pts',(-4.91990514195361,0.00439296476756341,
87.735140564009));
#51408=CARTESIAN_POINT('Origin',(0.,0.,-13.2351405640096));
#51409=CARTESIAN_POINT('',(-4.91569510392104,0.00437467045132868,83.8898594359905));
#51410=CARTESIAN_POINT('',(-4.91225321192224,-0.00317939731315275,84.235140564009));
#51411=CARTESIAN_POINT('',(-4.91825,6.88216836313478E-12,-13.2351405640096));
#51412=CARTESIAN_POINT('Ctrl Pts',(-4.91569510392104,0.00437467045132868,
83.8898594359905));
#51413=CARTESIAN_POINT('Ctrl Pts',(-4.90569919331825,-1.16789416685134,
83.9561780229373));
#51414=CARTESIAN_POINT('Ctrl Pts',(-4.48569639064107,-2.34659643687551,
84.0224966098841));
#51415=CARTESIAN_POINT('Ctrl Pts',(-3.72203604387737,-3.22731867727539,
84.0888151968309));
#51416=CARTESIAN_POINT('Ctrl Pts',(-2.65355943010873,-4.45958262954313,
84.1816049554077));
#51417=CARTESIAN_POINT('Ctrl Pts',(-0.912330125604573,-5.10851334741882,
84.2743947139844));
#51418=CARTESIAN_POINT('Ctrl Pts',(0.702011588476717,-4.87609658295006,
84.3671844725612));
#51419=CARTESIAN_POINT('Ctrl Pts',(2.3163533025581,-4.64367981848129,84.459974231138));
#51420=CARTESIAN_POINT('Ctrl Pts',(3.80380742621645,-3.5299155716678,84.5527639897147));
#51421=CARTESIAN_POINT('Ctrl Pts',(4.48127712058259,-2.04628774251226,84.6455537482915));
#51422=CARTESIAN_POINT('Ctrl Pts',(5.15874681494869,-0.562659913356806,
84.7383435068682));
#51423=CARTESIAN_POINT('Ctrl Pts',(5.02623208002272,1.29083149814077,84.8311332654449));
#51424=CARTESIAN_POINT('Ctrl Pts',(4.14458884076517,2.66299108102481,84.9239230240217));
#51425=CARTESIAN_POINT('Ctrl Pts',(3.26294560150757,4.03515066390892,85.0167127825985));
#51426=CARTESIAN_POINT('Ctrl Pts',(1.6321738579185,4.92597841817944,85.1095025411753));
#51427=CARTESIAN_POINT('Ctrl Pts',(0.00118747916824744,4.92637155993192,
85.202292299752));
#51428=CARTESIAN_POINT('Ctrl Pts',(-1.62979889958191,4.92676470168441,85.2950820583288));
#51429=CARTESIAN_POINT('Ctrl Pts',(-3.2609999134932,4.03672323091877,85.3878718169055));
#51430=CARTESIAN_POINT('Ctrl Pts',(-4.14330455575185,2.6649888395449,85.4806615754822));
#51431=CARTESIAN_POINT('Ctrl Pts',(-4.64788973669743,1.88050147211048,85.533727528985));
#51432=CARTESIAN_POINT('Ctrl Pts',(-4.90753837618641,0.938470013819249,
85.5867934824877));
#51433=CARTESIAN_POINT('Ctrl Pts',(-4.91079088019924,-0.00189858029133678,
85.6398594359905));
#51434=CARTESIAN_POINT('Ctrl Pts',(-4.91225321192224,-0.00317939731315296,
84.235140564009));
#51435=CARTESIAN_POINT('Ctrl Pts',(-4.9158507142751,-0.613189286481138,
84.2695897099629));
#51436=CARTESIAN_POINT('Ctrl Pts',(-4.5273162591334,-2.86218094060655,84.3968468071324));
#51437=CARTESIAN_POINT('Ctrl Pts',(-1.15619873186854,-5.70113400951219,
84.6169118555179));
#51438=CARTESIAN_POINT('Ctrl Pts',(4.1712258203786,-4.05470093316368,84.8953357091649));
#51439=CARTESIAN_POINT('Ctrl Pts',(5.66609661183164,1.31722195828223,85.1737595628121));
#51440=CARTESIAN_POINT('Ctrl Pts',(1.95491507866457,5.47887137439827,85.4521834164592));
#51441=CARTESIAN_POINT('Ctrl Pts',(-3.39493451155719,4.63144433755238,85.7226437501916));
#51442=CARTESIAN_POINT('Ctrl Pts',(-4.91568788814768,1.49007919710422,85.9002961327082));
#51443=CARTESIAN_POINT('Ctrl Pts',(-4.92485543050125,-0.00247326924054743,
85.9851405640091));
#51444=CARTESIAN_POINT('Origin',(0.,0.,-13.2351405640096));
#51445=CARTESIAN_POINT('',(-4.92637127541955,-4.0931223634067E-5,82.1398594359905));
#51446=CARTESIAN_POINT('',(-4.91322641730633,0.00367898483844581,82.4851405640091));
#51447=CARTESIAN_POINT('',(-4.91825,6.88216836313478E-12,-13.2351405640096));
#51448=CARTESIAN_POINT('Ctrl Pts',(-4.92637127541955,-4.09312236341073E-5,
82.1398594359905));
#51449=CARTESIAN_POINT('Ctrl Pts',(-4.92637154201875,-0.00221365673367821,
82.1399830462334));
#51450=CARTESIAN_POINT('Ctrl Pts',(-4.92538488475959,-1.63537294175407,
82.232896415053));
#51451=CARTESIAN_POINT('Ctrl Pts',(-3.13898501948552,-4.89714294882462,
82.4185995424493));
#51452=CARTESIAN_POINT('Ctrl Pts',(2.42191938450794,-5.28862387665468,82.6969688181796));
#51453=CARTESIAN_POINT('Ctrl Pts',(5.75834445937218,-0.822620873182145,
82.9753380939098));
#51454=CARTESIAN_POINT('Ctrl Pts',(3.805857648145,4.39894118803992,83.2537073696402));
#51455=CARTESIAN_POINT('Ctrl Pts',(-1.64222514454274,5.5801731683174,83.5320766453704));
#51456=CARTESIAN_POINT('Ctrl Pts',(-4.64335949870137,2.57576464547258,83.7441273341538));
#51457=CARTESIAN_POINT('Ctrl Pts',(-4.91968498786378,0.472287679719399,
83.8633882643606));
#51458=CARTESIAN_POINT('Ctrl Pts',(-4.91569510392104,0.00437467045132874,
83.8898594359905));
#51459=CARTESIAN_POINT('Ctrl Pts',(-4.91322641730633,0.00367898483844553,
82.4851405640091));
#51460=CARTESIAN_POINT('Ctrl Pts',(-4.90577076072416,-1.07478984285633,
82.546075336002));
#51461=CARTESIAN_POINT('Ctrl Pts',(-4.02432282862942,-3.80692361268266,
82.6998180592107));
#51462=CARTESIAN_POINT('Ctrl Pts',(0.494987229579467,-5.79609455966206,
82.946368733635));
#51463=CARTESIAN_POINT('Ctrl Pts',(5.14373934040566,-2.71692291019715,83.2247925872822));
#51464=CARTESIAN_POINT('Ctrl Pts',(5.06638492942612,2.85857801168262,83.5032164409293));
#51465=CARTESIAN_POINT('Ctrl Pts',(0.333997813182944,5.80759588494068,83.7816402945764));
#51466=CARTESIAN_POINT('Ctrl Pts',(-4.08176482749318,3.71589788202843,84.0256150022698));
#51467=CARTESIAN_POINT('Ctrl Pts',(-4.90615883908873,1.03021192035268,84.1767817587472));
#51468=CARTESIAN_POINT('Ctrl Pts',(-4.91225321192224,-0.00317939731315296,
84.235140564009));
#51469=CARTESIAN_POINT('Origin',(0.,0.,-13.2351405640096));
#51470=CARTESIAN_POINT('',(-4.91557206079122,-0.00435402565801867,80.3898594359905));
#51471=CARTESIAN_POINT('',(-4.92564390538527,0.00173197686021732,80.7351405640091));
#51472=CARTESIAN_POINT('',(-4.91825,6.88216836313478E-12,-13.2351405640096));
#51473=CARTESIAN_POINT('Ctrl Pts',(-4.91557206079122,-0.00435402565801879,
80.3898594359905));
#51474=CARTESIAN_POINT('Ctrl Pts',(-4.91957268173767,-0.476666931688224,
80.4165778281061));
#51475=CARTESIAN_POINT('Ctrl Pts',(-4.63999236043617,-2.5846267150224,80.5360859787985));
#51476=CARTESIAN_POINT('Ctrl Pts',(-1.62736014737243,-5.58452638676924,
80.7483838880677));
#51477=CARTESIAN_POINT('Ctrl Pts',(3.81755788385611,-4.3887911567066,81.0267531637979));
#51478=CARTESIAN_POINT('Ctrl Pts',(5.75613352618714,0.837951575260477,81.3051224395282));
#51479=CARTESIAN_POINT('Ctrl Pts',(2.40782797560329,5.29505433906766,81.5834917152585));
#51480=CARTESIAN_POINT('Ctrl Pts',(-3.14954540178693,4.8889473466839,81.8617373807459));
#51481=CARTESIAN_POINT('Ctrl Pts',(-4.92617141560022,1.62877315225414,82.0471932876566));
#51482=CARTESIAN_POINT('Ctrl Pts',(-4.92637127541955,-4.09312236341073E-5,
82.1398594359905));
#51483=CARTESIAN_POINT('Ctrl Pts',(-4.92564390538527,0.0017319768602176,
80.7351405640091));
#51484=CARTESIAN_POINT('Ctrl Pts',(-4.91866561127433,-1.53548363053209,
80.8225609620411));
#51485=CARTESIAN_POINT('Ctrl Pts',(-3.316297660866,-4.71719158443029,81.0027893112887));
#51486=CARTESIAN_POINT('Ctrl Pts',(2.10616092092011,-5.42252807066782,81.2758256117524));
#51487=CARTESIAN_POINT('Ctrl Pts',(5.7004589256578,-1.15952254780973,81.5542494653993));
#51488=CARTESIAN_POINT('Ctrl Pts',(4.05713225252595,4.16886104199992,81.8326733190467));
#51489=CARTESIAN_POINT('Ctrl Pts',(-1.31391815028062,5.6668636472351,82.1110971726936));
#51490=CARTESIAN_POINT('Ctrl Pts',(-4.56645468057018,2.76979288701375,82.3285862543479));
#51491=CARTESIAN_POINT('Ctrl Pts',(-4.91712625102515,0.567794170749911,
82.4532673847863));
#51492=CARTESIAN_POINT('Ctrl Pts',(-4.91322641730633,0.00367898483844553,
82.4851405640091));
#51493=CARTESIAN_POINT('Origin',(0.,0.,-13.2351405640096));
#51494=CARTESIAN_POINT('',(-4.91084228422721,0.00196441572767522,78.6398594359905));
#51495=CARTESIAN_POINT('',(-4.91851453902819,-0.00453015795356559,78.9851405640091));
#51496=CARTESIAN_POINT('',(-4.91825,6.88216836313478E-12,-13.2351405640096));
#51497=CARTESIAN_POINT('Ctrl Pts',(-4.91084228422721,0.00196441572767485,
78.6398594359905));
#51498=CARTESIAN_POINT('Ctrl Pts',(-4.90745929868568,-0.942760414910041,
78.6931726099789));
#51499=CARTESIAN_POINT('Ctrl Pts',(-4.18881849136433,-3.53650879740012,
78.8392755425441));
#51500=CARTESIAN_POINT('Ctrl Pts',(0.0168914028385561,-5.81678181594319,
79.0781682336861));
#51501=CARTESIAN_POINT('Ctrl Pts',(4.90207286122337,-3.13128051714223,79.3565375094163));
#51502=CARTESIAN_POINT('Ctrl Pts',(5.28480893706208,2.43023260461352,79.6349067851467));
#51503=CARTESIAN_POINT('Ctrl Pts',(0.813565019144324,5.75963088864231,79.9132760608768));
#51504=CARTESIAN_POINT('Ctrl Pts',(-3.9040405862657,3.98712683648866,80.1649269444916));
#51505=CARTESIAN_POINT('Ctrl Pts',(-4.90567900691728,1.16361891835689,80.3237880695294));
#51506=CARTESIAN_POINT('Ctrl Pts',(-4.91557206079122,-0.00435402565801879,
80.3898594359905));
#51507=CARTESIAN_POINT('Ctrl Pts',(-4.91851453902819,-0.00453015795356587,
78.9851405640091));
#51508=CARTESIAN_POINT('Ctrl Pts',(-4.92196835436792,-0.376922461688771,
79.0062386368645));
#51509=CARTESIAN_POINT('Ctrl Pts',(-4.71304029456911,-2.38358769329157,
79.1201446609356));
#51510=CARTESIAN_POINT('Ctrl Pts',(-1.96130259556129,-5.47658804646063,
79.3268586362224));
#51511=CARTESIAN_POINT('Ctrl Pts',(3.54708319036234,-4.61063177261423,79.6052824898694));
#51512=CARTESIAN_POINT('Ctrl Pts',(5.79638217387485,0.491607766798655,79.8837063435167));
#51513=CARTESIAN_POINT('Ctrl Pts',(2.71992147519714,5.14215438029163,80.1621301971638));
#51514=CARTESIAN_POINT('Ctrl Pts',(-2.85562360004527,5.06805074529212,80.4405540508108));
#51515=CARTESIAN_POINT('Ctrl Pts',(-4.88059206529341,1.82273352739509,80.631557506426));
#51516=CARTESIAN_POINT('Ctrl Pts',(-4.92607396440468,0.0964676567022224,
80.7297530108254));
#51517=CARTESIAN_POINT('Ctrl Pts',(-4.92564390538527,0.0017319768602176,
80.7351405640091));
#51518=CARTESIAN_POINT('Origin',(0.,0.,-13.2351405640096));
#51519=CARTESIAN_POINT('',(-4.92279211704217,0.0036182553321711,76.8898594359905));
#51520=CARTESIAN_POINT('',(-4.91011604675776,0.000346003969231568,77.2351405640091));
#51521=CARTESIAN_POINT('',(-4.91825,6.88216836313478E-12,-13.2351405640096));
#51522=CARTESIAN_POINT('Ctrl Pts',(-4.92279211704217,0.00361825533217116,
76.8898594359905));
#51523=CARTESIAN_POINT('Ctrl Pts',(-4.91119054578483,-1.40363931961367,
76.9697673918518));
#51524=CARTESIAN_POINT('Ctrl Pts',(-3.539718546453,-4.46475810474062,77.1424651062897));
#51525=CARTESIAN_POINT('Ctrl Pts',(1.65976633666211,-5.5749808718471,77.4079525793045));
#51526=CARTESIAN_POINT('Ctrl Pts',(5.58707846113262,-1.61857662250689,77.6863218550347));
#51527=CARTESIAN_POINT('Ctrl Pts',(4.38278272676508,3.82445441648177,77.964691130765));
#51528=CARTESIAN_POINT('Ctrl Pts',(-0.847001899642621,5.75480875405768,
78.2430604064953));
#51529=CARTESIAN_POINT('Ctrl Pts',(-4.44622089908048,3.0421063371335,78.4681165082371));
#51530=CARTESIAN_POINT('Ctrl Pts',(-4.91334726948508,0.701500888597644,
78.6003828514022));
#51531=CARTESIAN_POINT('Ctrl Pts',(-4.91084228422721,0.00196441572767485,
78.6398594359905));
#51532=CARTESIAN_POINT('Ctrl Pts',(-4.91011604675776,0.000346003969231637,
77.2351405640091));
#51533=CARTESIAN_POINT('Ctrl Pts',(-4.90958877228912,-0.843161686015328,
77.2827242629036));
#51534=CARTESIAN_POINT('Ctrl Pts',(-4.30159456804404,-3.33257179119856,
77.4231159130138));
#51535=CARTESIAN_POINT('Ctrl Pts',(-0.340769753807865,-5.80720246563535,
77.6563155143396));
#51536=CARTESIAN_POINT('Ctrl Pts',(4.70127715203259,-3.42603526569229,77.9347393679867));
#51537=CARTESIAN_POINT('Ctrl Pts',(5.42375513366596,2.1029989900195,78.2131632216339));
#51538=CARTESIAN_POINT('Ctrl Pts',(1.16284596958247,5.69978190398691,78.4915870752809));
#51539=CARTESIAN_POINT('Ctrl Pts',(-3.76265437325353,4.18385281836137,78.7489128560728));
#51540=CARTESIAN_POINT('Ctrl Pts',(-4.90677542524329,1.26118766311134,78.9134306856488));
#51541=CARTESIAN_POINT('Ctrl Pts',(-4.91851453902819,-0.00453015795356587,
78.9851405640091));
#51542=CARTESIAN_POINT('Origin',(0.,0.,-13.2351405640096));
#51543=CARTESIAN_POINT('',(-4.92239160404736,-0.00377085183543027,75.1398594359906));
#51544=CARTESIAN_POINT('',(-4.91978873044366,0.00440978733039096,75.4851405640091));
#51545=CARTESIAN_POINT('',(-4.91825,6.88216836313478E-12,-13.2351405640096));
#51546=CARTESIAN_POINT('Ctrl Pts',(-4.92239160404736,-0.00377085183543145,
75.1398594359906));
#51547=CARTESIAN_POINT('Ctrl Pts',(-4.92444063379938,-0.245321050757574,
75.1535724151478));
#51548=CARTESIAN_POINT('Ctrl Pts',(-4.79833433295751,-2.11918842723071,
75.2600751528818));
#51549=CARTESIAN_POINT('Ctrl Pts',(-2.39116343640037,-5.30260062933267,
75.4593676491925));
#51550=CARTESIAN_POINT('Ctrl Pts',(3.16737355116417,-4.87882985982939,75.7377369249229));
#51551=CARTESIAN_POINT('Ctrl Pts',(5.81674806318794,0.0260381100804274,
76.016106200653));
#51552=CARTESIAN_POINT('Ctrl Pts',(3.12356827217368,4.90699065241089,76.2944754763835));
#51553=CARTESIAN_POINT('Ctrl Pts',(-2.43853981555445,5.28098092987785,76.5728447521136));
#51554=CARTESIAN_POINT('Ctrl Pts',(-4.80719417250829,2.08951200176882,76.7713060719827));
#51555=CARTESIAN_POINT('Ctrl Pts',(-4.92466238328182,0.23047945150494,76.876977633275));
#51556=CARTESIAN_POINT('Ctrl Pts',(-4.92279211704217,0.00361825533217116,
76.8898594359905));
#51557=CARTESIAN_POINT('Ctrl Pts',(-4.91978873044366,0.00440978733039082,
75.4851405640091));
#51558=CARTESIAN_POINT('Ctrl Pts',(-4.90767719882995,-1.30208537057339,
75.5592098889426));
#51559=CARTESIAN_POINT('Ctrl Pts',(-3.70062334914684,-4.26536803612013,
75.7260871650919));
#51560=CARTESIAN_POINT('Ctrl Pts',(1.30730919543873,-5.66839193859359,75.9857723924568));
#51561=CARTESIAN_POINT('Ctrl Pts',(5.475443589727,-1.96449535446343,76.264196246104));
#51562=CARTESIAN_POINT('Ctrl Pts',(4.61269909481645,3.54439438588181,76.542620099751));
#51563=CARTESIAN_POINT('Ctrl Pts',(-0.488228136900599,5.79666781766301,
76.8210439533983));
#51564=CARTESIAN_POINT('Ctrl Pts',(-4.3454650949107,3.24823449643751,77.0518841081509));
#51565=CARTESIAN_POINT('Ctrl Pts',(-4.91061717622366,0.802028208023915,
77.1899163116879));
#51566=CARTESIAN_POINT('Ctrl Pts',(-4.91011604675776,0.000346003969231637,
77.2351405640091));
#51567=CARTESIAN_POINT('Origin',(0.,0.,-13.2351405640096));
#51568=CARTESIAN_POINT('',(-4.91067656268135,-0.00174122703138476,73.3898594359905));
#51569=CARTESIAN_POINT('',(-4.92493062471777,-0.00241415038567228,73.7351405640091));
#51570=CARTESIAN_POINT('',(-4.91825,6.88216836313478E-12,-13.2351405640096));
#51571=CARTESIAN_POINT('Ctrl Pts',(-4.91067656268135,-0.0017412270313847,
73.3898594359905));
#51572=CARTESIAN_POINT('Ctrl Pts',(-4.91293934412357,-0.716066575557565,
73.4301671970206));
#51573=CARTESIAN_POINT('Ctrl Pts',(-4.43218965357877,-3.07189064286557,
73.5632647166273));
#51574=CARTESIAN_POINT('Ctrl Pts',(-0.795447298431173,-5.7621610190272,
73.7891519948111));
#51575=CARTESIAN_POINT('Ctrl Pts',(4.41684599871641,-3.78506372963529,74.0675212705412));
#51576=CARTESIAN_POINT('Ctrl Pts',(5.57236404275686,1.66853078747969,74.3458905462716));
#51577=CARTESIAN_POINT('Ctrl Pts',(1.60978909543459,5.58961672049141,74.6242598220017));
#51578=CARTESIAN_POINT('Ctrl Pts',(-3.56330145772682,4.43651082739373,74.8889161185748));
#51579=CARTESIAN_POINT('Ctrl Pts',(-4.91057574172695,1.38914396119285,75.0607826565711));
#51580=CARTESIAN_POINT('Ctrl Pts',(-4.92239160404736,-0.00377085183543145,
75.1398594359906));
#51581=CARTESIAN_POINT('Ctrl Pts',(-4.92493062471777,-0.00241415038567332,
73.7351405640091));
#51582=CARTESIAN_POINT('Ctrl Pts',(-4.92575116259624,-0.138691063730488,
73.742887563766));
#51583=CARTESIAN_POINT('Ctrl Pts',(-4.85872291664768,-1.90672651453574,
73.8434425147386));
#51584=CARTESIAN_POINT('Ctrl Pts',(-2.72591583034415,-5.13897921652443,
74.0368054169269));
#51585=CARTESIAN_POINT('Ctrl Pts',(2.84971186554951,-5.07137720795222,74.315229270574));
#51586=CARTESIAN_POINT('Ctrl Pts',(5.80700279479466,-0.344155550933751,
74.5936531242212));
#51587=CARTESIAN_POINT('Ctrl Pts',(3.42877573520264,4.69927882335965,74.8720769778683));
#51588=CARTESIAN_POINT('Ctrl Pts',(-2.09983634422443,5.42498035291051,75.1505008315154));
#51589=CARTESIAN_POINT('Ctrl Pts',(-4.7415871145915,2.29914405580575,75.354855360229));
#51590=CARTESIAN_POINT('Ctrl Pts',(-4.92285279866377,0.334936959346778,
75.4664019377269));
#51591=CARTESIAN_POINT('Ctrl Pts',(-4.91978873044366,0.00440978733039082,
75.4851405640091));
#51592=CARTESIAN_POINT('Origin',(0.,0.,-13.2351405640096));
#51593=CARTESIAN_POINT('',(-4.9159887804262,0.00441880477913321,71.6398594359906));
#51594=CARTESIAN_POINT('',(-4.91232903289984,-0.00322496870272804,71.9851405640091));
#51595=CARTESIAN_POINT('',(-4.91825,6.88216836313478E-12,-13.2351405640096));
#51596=CARTESIAN_POINT('Ctrl Pts',(-4.9159887804262,0.00441880477913298,
71.6398594359906));
#51597=CARTESIAN_POINT('Ctrl Pts',(-4.90575670288894,-1.17799315420249,
71.7067619788934));
#51598=CARTESIAN_POINT('Ctrl Pts',(-3.88382241329164,-4.01620380740258,
71.8664542803729));
#51599=CARTESIAN_POINT('Ctrl Pts',(0.865096242963933,-5.75211652387075,
72.1189363404294));
#51600=CARTESIAN_POINT('Ctrl Pts',(5.30635411174501,-2.38282228765471,72.3973056161595));
#51601=CARTESIAN_POINT('Ctrl Pts',(4.87384322087152,3.17504145990924,72.67567489189));
#51602=CARTESIAN_POINT('Ctrl Pts',(-0.0351847529388852,5.81669992753095,
72.95404416762));
#51603=CARTESIAN_POINT('Ctrl Pts',(-4.20575040548237,3.50693055059452,73.1921056823205));
#51604=CARTESIAN_POINT('Ctrl Pts',(-4.9077303486753,0.92833328544159,73.3373774384439));
#51605=CARTESIAN_POINT('Ctrl Pts',(-4.91067656268135,-0.0017412270313847,
73.3898594359905));
#51606=CARTESIAN_POINT('Ctrl Pts',(-4.91232903289984,-0.00322496870272818,
71.9851405640091));
#51607=CARTESIAN_POINT('Ctrl Pts',(-4.91595860382257,-0.609377356158057,
72.0193731898051));
#51608=CARTESIAN_POINT('Ctrl Pts',(-4.53066876099212,-2.85441561589539,
72.1464137668167));
#51609=CARTESIAN_POINT('Ctrl Pts',(-1.16949162610311,-5.69842204811702,
72.3662622950442));
#51610=CARTESIAN_POINT('Ctrl Pts',(4.16175820709524,-4.06441793220953,72.6446861486912));
#51611=CARTESIAN_POINT('Ctrl Pts',(5.66915319402907,1.30400405084528,72.9231100023384));
#51612=CARTESIAN_POINT('Ctrl Pts',(1.96768744555408,5.47429727166879,73.2015338559855));
#51613=CARTESIAN_POINT('Ctrl Pts',(-3.38840839793359,4.63868089417945,73.4722107098757));
#51614=CARTESIAN_POINT('Ctrl Pts',(-4.91592123594264,1.49388690482925,73.6500796125503));
#51615=CARTESIAN_POINT('Ctrl Pts',(-4.92493062471777,-0.00241415038567332,
73.7351405640091));
#51616=CARTESIAN_POINT('Origin',(0.,0.,-13.2351405640096));
#51617=CARTESIAN_POINT('',(-4.92635784080807,-0.000234171170717763,69.8898594359906));
#51618=CARTESIAN_POINT('',(-4.91313886229116,0.00364073211770066,70.2351405640091));
#51619=CARTESIAN_POINT('',(-4.91825,6.88216836313478E-12,-13.2351405640096));
#51620=CARTESIAN_POINT('Ctrl Pts',(-4.92635784080807,-0.000234171170717511,
69.8898594359906));
#51621=CARTESIAN_POINT('Ctrl Pts',(-4.92636642702435,-0.0126713156829149,
69.8905670021894));
#51622=CARTESIAN_POINT('Ctrl Pts',(-4.9206830606955,-1.65609920609382,69.9840643269651));
#51623=CARTESIAN_POINT('Ctrl Pts',(-3.10812063065928,-4.91678982254146,
70.1703514103174));
#51624=CARTESIAN_POINT('Ctrl Pts',(2.45513612779318,-5.2732857506286,70.4487206860478));
#51625=CARTESIAN_POINT('Ctrl Pts',(5.76340471388584,-0.786385476554853,
70.7270899617779));
#51626=CARTESIAN_POINT('Ctrl Pts',(3.77811368215897,4.42279244578133,71.0054592375083));
#51627=CARTESIAN_POINT('Ctrl Pts',(-1.67729111257008,5.56973343504611,71.2838285132385));
#51628=CARTESIAN_POINT('Ctrl Pts',(-4.65125634837052,2.5548331704508,71.495295246066));
#51629=CARTESIAN_POINT('Ctrl Pts',(-4.91994797220735,0.461940328916346,
71.6139722203167));
#51630=CARTESIAN_POINT('Ctrl Pts',(-4.9159887804262,0.00441880477913298,
71.6398594359906));
#51631=CARTESIAN_POINT('Ctrl Pts',(-4.91313886229116,0.00364073211770066,
70.2351405640091));
#51632=CARTESIAN_POINT('Ctrl Pts',(-4.90579538722953,-1.07104410681227,
70.2958588158442));
#51633=CARTESIAN_POINT('Ctrl Pts',(-4.02922553257357,-3.79928397318142,
70.4493850188949));
#51634=CARTESIAN_POINT('Ctrl Pts',(0.481468380347833,-5.79723319357744,
70.6957191731614));
#51635=CARTESIAN_POINT('Ctrl Pts',(5.13738901395058,-2.72891161845354,70.9741430268085));
#51636=CARTESIAN_POINT('Ctrl Pts',(5.07303785361562,2.84675454470068,71.2525668804556));
#51637=CARTESIAN_POINT('Ctrl Pts',(0.347541231067252,5.80680114991893,71.5309907341027));
#51638=CARTESIAN_POINT('Ctrl Pts',(-4.07701077938671,3.72355998975012,71.7751819619539));
#51639=CARTESIAN_POINT('Ctrl Pts',(-4.90611848687863,1.03396024638341,71.9265652385894));
#51640=CARTESIAN_POINT('Ctrl Pts',(-4.91232903289984,-0.00322496870272818,
71.9851405640091));
#51641=CARTESIAN_POINT('Origin',(0.,0.,-13.2351405640096));
#51642=CARTESIAN_POINT('',(-4.91528466670162,-0.00430068889825521,68.1398594359906));
#51643=CARTESIAN_POINT('',(-4.92558708781353,0.00179722223583485,68.4851405640091));
#51644=CARTESIAN_POINT('',(-4.91825,6.88216836313478E-12,-13.2351405640096));
#51645=CARTESIAN_POINT('Ctrl Pts',(-4.91528466670162,-0.00430068889825559,
68.1398594359906));
#51646=CARTESIAN_POINT('Ctrl Pts',(-4.91930521123973,-0.487007885028925,
68.1671617840622));
#51647=CARTESIAN_POINT('Ctrl Pts',(-4.63198207672563,-2.60556107402994,
68.2872538907107));
#51648=CARTESIAN_POINT('Ctrl Pts',(-1.59220212159397,-5.59465176912459,
68.5001357559359));
#51649=CARTESIAN_POINT('Ctrl Pts',(3.84508720656895,-4.36469247343464,68.7785050316661));
#51650=CARTESIAN_POINT('Ctrl Pts',(5.75074907247032,0.874140217161407,69.0568743073964));
#51651=CARTESIAN_POINT('Ctrl Pts',(2.37447524697441,5.31009447329176,69.3352435831267));
#51652=CARTESIAN_POINT('Ctrl Pts',(-3.16857614270845,4.86996611098083,69.6129052926581));
#51653=CARTESIAN_POINT('Ctrl Pts',(-4.92524043635853,1.61832750604788,69.7977772436127));
#51654=CARTESIAN_POINT('Ctrl Pts',(-4.92635784080807,-0.000234171170717511,
69.8898594359906));
#51655=CARTESIAN_POINT('Ctrl Pts',(-4.92558708781353,0.00179722223583461,
68.4851405640091));
#51656=CARTESIAN_POINT('Ctrl Pts',(-4.91839816763849,-1.53165810334221,
68.5723444418832));
#51657=CARTESIAN_POINT('Ctrl Pts',(-3.32299121478259,-4.71001393647895,
68.7523562709731));
#51658=CARTESIAN_POINT('Ctrl Pts',(2.09350891225194,-5.42742525847318,69.0251760512785));
#51659=CARTESIAN_POINT('Ctrl Pts',(5.69773921438019,-1.17281385859187,69.3035999049257));
#51660=CARTESIAN_POINT('Ctrl Pts',(4.06684372988438,4.15938776488691,69.5820237585728));
#51661=CARTESIAN_POINT('Ctrl Pts',(-1.30069846296805,5.66991252229023,69.8604476122199));
#51662=CARTESIAN_POINT('Ctrl Pts',(-4.56322738594952,2.77755851836255,70.0781532140321));
#51663=CARTESIAN_POINT('Ctrl Pts',(-4.91701990135298,0.571613497603942,
70.2030508646285));
#51664=CARTESIAN_POINT('Ctrl Pts',(-4.91313886229116,0.00364073211770066,
70.2351405640091));
#51665=CARTESIAN_POINT('Origin',(0.,0.,-13.2351405640096));
#51666=CARTESIAN_POINT('',(-4.91097073342421,0.00211795400143013,66.3898594359906));
#51667=CARTESIAN_POINT('',(-4.91863147951157,-0.0045239198518876,66.7351405640092));
#51668=CARTESIAN_POINT('',(-4.91825,6.88216836313478E-12,-13.2351405640096));
#51669=CARTESIAN_POINT('Ctrl Pts',(-4.91097073342421,0.00211795400142982,
66.3898594359906));
#51670=CARTESIAN_POINT('Ctrl Pts',(-4.90727785389205,-0.952892345756783,
66.443756565935));
#51671=CARTESIAN_POINT('Ctrl Pts',(-4.17680693104425,-3.55727669197261,
66.5904434544562));
#51672=CARTESIAN_POINT('Ctrl Pts',(0.0534777550381669,-5.8165605080231,
66.8299201015543));
#51673=CARTESIAN_POINT('Ctrl Pts',(4.92167117725461,-3.10038527231038,67.1082893772844));
#51674=CARTESIAN_POINT('Ctrl Pts',(5.26941859759108,2.46342518805391,67.3866586530149));
#51675=CARTESIAN_POINT('Ctrl Pts',(0.777321710206332,5.76463415774316,67.665027928745));
#51676=CARTESIAN_POINT('Ctrl Pts',(-3.91812067181916,3.9666740065567,67.9160948564037));
#51677=CARTESIAN_POINT('Ctrl Pts',(-4.90564098880511,1.15352076381265,68.0743720254855));
#51678=CARTESIAN_POINT('Ctrl Pts',(-4.91528466670162,-0.00430068889825559,
68.1398594359906));
#51679=CARTESIAN_POINT('Ctrl Pts',(-4.91863147951157,-0.00452391985188844,
66.7351405640092));
#51680=CARTESIAN_POINT('Ctrl Pts',(-4.92205279654655,-0.373072104444159,
66.7560221167066));
#51681=CARTESIAN_POINT('Ctrl Pts',(-4.71571170713008,-2.37583601988883,
66.8697116206198));
#51682=CARTESIAN_POINT('Ctrl Pts',(-1.97406961996107,-5.47199905313755,
67.0762090757487));
#51683=CARTESIAN_POINT('Ctrl Pts',(3.53632074680071,-4.61889165035702,67.3546329293958));
#51684=CARTESIAN_POINT('Ctrl Pts',(5.79751292551162,0.478088255991047,67.633056783043));
#51685=CARTESIAN_POINT('Ctrl Pts',(2.73190647889548,5.13579706497058,67.91148063669));
#51686=CARTESIAN_POINT('Ctrl Pts',(-2.843796256125,5.07469677474826,68.1899044903372));
#51687=CARTESIAN_POINT('Ctrl Pts',(-4.87863192338278,1.83043745707829,68.3811244661102));
#51688=CARTESIAN_POINT('Ctrl Pts',(-4.9260490768545,0.100343253904555,68.4795364906675));
#51689=CARTESIAN_POINT('Ctrl Pts',(-4.92558708781353,0.00179722223583461,
68.4851405640091));
#51690=CARTESIAN_POINT('Origin',(0.,0.,-13.2351405640096));
#51691=CARTESIAN_POINT('',(-4.92306599949043,0.00350342792735477,64.6398594359906));
#51692=CARTESIAN_POINT('',(-4.91010877574632,0.000282588420590091,64.9851405640092));
#51693=CARTESIAN_POINT('',(-4.91825,6.88216836313478E-12,-13.2351405640096));
#51694=CARTESIAN_POINT('Ctrl Pts',(-4.92306599949043,0.00350342792735464,
64.6398594359906));
#51695=CARTESIAN_POINT('Ctrl Pts',(-4.91164684544424,-1.41383247848128,
64.7203513478078));
#51696=CARTESIAN_POINT('Ctrl Pts',(-3.52301758553069,-4.48456406519882,
64.8936330182019));
#51697=CARTESIAN_POINT('Ctrl Pts',(1.69479929893489,-5.56443090981521,65.1597044471726));
#51698=CARTESIAN_POINT('Ctrl Pts',(5.59714854594884,-1.58340271831267,65.4380737229028));
#51699=CARTESIAN_POINT('Ctrl Pts',(4.3586407841906,3.85194581064795,65.7164429986333));
#51700=CARTESIAN_POINT('Ctrl Pts',(-0.883182029898331,5.74936740136187,
65.9948122743633));
#51701=CARTESIAN_POINT('Ctrl Pts',(-4.45597285748787,3.02117738192304,66.2192844201493));
#51702=CARTESIAN_POINT('Ctrl Pts',(-4.91363554678953,0.691261531159927,
66.3509668073583));
#51703=CARTESIAN_POINT('Ctrl Pts',(-4.91097073342421,0.00211795400142982,
66.3898594359906));
#51704=CARTESIAN_POINT('Ctrl Pts',(-4.91010877574632,0.00028258842059023,
64.9851405640092));
#51705=CARTESIAN_POINT('Ctrl Pts',(-4.90968013456912,-0.839389986717853,
65.0325077427457));
#51706=CARTESIAN_POINT('Ctrl Pts',(-4.30568284721683,-3.32483686443376,
65.172682872698));
#51707=CARTESIAN_POINT('Ctrl Pts',(-0.354312235753313,-5.80639193833713,
65.4056659538659));
#51708=CARTESIAN_POINT('Ctrl Pts',(4.69327425521161,-3.4369901465322,65.684089807513));
#51709=CARTESIAN_POINT('Ctrl Pts',(5.42864494396021,2.09034412822534,65.9625136611601));
#51710=CARTESIAN_POINT('Ctrl Pts',(1.1761356923939,5.69705444375144,66.2409375148073));
#51711=CARTESIAN_POINT('Ctrl Pts',(-3.75703406542712,4.19135073581093,66.498479815757));
#51712=CARTESIAN_POINT('Ctrl Pts',(-4.90684677096616,1.26493836497993,66.6632141654909));
#51713=CARTESIAN_POINT('Ctrl Pts',(-4.91863147951157,-0.00452391985188844,
66.7351405640092));
#51714=CARTESIAN_POINT('Origin',(0.,0.,-13.2351405640096));
#51715=CARTESIAN_POINT('',(-4.92210345011766,-0.00387026642323893,62.8898594359906));
#51716=CARTESIAN_POINT('',(-4.91967215389204,0.00442564071372511,63.2351405640092));
#51717=CARTESIAN_POINT('',(-4.91825,6.88216836313478E-12,-13.2351405640096));
#51718=CARTESIAN_POINT('Ctrl Pts',(-4.92210345011766,-0.00387026642323842,
62.8898594359906));
#51719=CARTESIAN_POINT('Ctrl Pts',(-4.92427744727768,-0.255745006656511,
62.9041563711039));
#51720=CARTESIAN_POINT('Ctrl Pts',(-4.79202192949461,-2.14004400017903,
63.011243064794));
#51721=CARTESIAN_POINT('Ctrl Pts',(-2.35776357238246,-5.31753579682578,
63.2111195170607));
#51722=CARTESIAN_POINT('Ctrl Pts',(3.19799800541104,-4.85881104501553,63.489488792791));
#51723=CARTESIAN_POINT('Ctrl Pts',(5.81646922451705,0.0626240690466223,
63.7678580685212));
#51724=CARTESIAN_POINT('Ctrl Pts',(3.09264224773008,4.92654036229607,64.0462273442516));
#51725=CARTESIAN_POINT('Ctrl Pts',(-2.47170815707546,5.26553841501739,64.3245966199818));
#51726=CARTESIAN_POINT('Ctrl Pts',(-4.8133314322023,2.06866842134372,64.5224739838948));
#51727=CARTESIAN_POINT('Ctrl Pts',(-4.92481065933777,0.220049157681148,
64.6275615892311));
#51728=CARTESIAN_POINT('Ctrl Pts',(-4.92306599949043,0.00350342792735464,
64.6398594359906));
#51729=CARTESIAN_POINT('Ctrl Pts',(-4.91967215389204,0.00442564071372501,
63.2351405640092));
#51730=CARTESIAN_POINT('Ctrl Pts',(-4.90758283094165,-1.29832969996648,
63.3089933687848));
#51731=CARTESIAN_POINT('Ctrl Pts',(-3.70638809642316,-4.25790548455125,
63.4756541247759));
#51732=CARTESIAN_POINT('Ctrl Pts',(1.29408596185757,-5.67142539625746,63.7351228319832));
#51733=CARTESIAN_POINT('Ctrl Pts',(5.47084715344585,-1.97725970110767,64.0135466856302));
#51734=CARTESIAN_POINT('Ctrl Pts',(4.62095269617623,3.53362712827672,64.2919705392774));
#51735=CARTESIAN_POINT('Ctrl Pts',(-0.474707969112876,5.79779068663673,
64.5703943929245));
#51736=CARTESIAN_POINT('Ctrl Pts',(-4.34150134912124,3.25597814609928,64.8014510678351));
#51737=CARTESIAN_POINT('Ctrl Pts',(-4.91051998423979,0.805805979545269,
64.93969979153));
#51738=CARTESIAN_POINT('Ctrl Pts',(-4.91010877574632,0.00028258842059023,
64.9851405640092));
#51739=CARTESIAN_POINT('Origin',(0.,0.,-13.2351405640096));
#51740=CARTESIAN_POINT('',(-4.91057232344976,-0.0015814614971166,61.1398594359906));
#51741=CARTESIAN_POINT('',(-4.92500427991532,-0.00235440163140754,61.4851405640091));
#51742=CARTESIAN_POINT('',(-4.91825,6.88216836313478E-12,-13.2351405640096));
#51743=CARTESIAN_POINT('Ctrl Pts',(-4.91057232344976,-0.00158146149711672,
61.1398594359906));
#51744=CARTESIAN_POINT('Ctrl Pts',(-4.91265475868819,-0.726293947282865,
61.1807511529767));
#51745=CARTESIAN_POINT('Ctrl Pts',(-4.4222253859021,-3.09281216434233,61.3144326285396));
#51746=CARTESIAN_POINT('Ctrl Pts',(-0.75918843374404,-5.76705028032932,
61.5409038626791));
#51747=CARTESIAN_POINT('Ctrl Pts',(4.4405661116445,-3.75720755640298,61.8192731384095));
#51748=CARTESIAN_POINT('Ctrl Pts',(5.56175900540656,1.703547116917,62.0976424141395));
#51749=CARTESIAN_POINT('Ctrl Pts',(1.57459939979797,5.59963148286865,62.3760116898701));
#51750=CARTESIAN_POINT('Ctrl Pts',(-3.57973792379162,4.41662647127613,62.6400840304868));
#51751=CARTESIAN_POINT('Ctrl Pts',(-4.9101678027961,1.37896873811473,62.8113666125271));
#51752=CARTESIAN_POINT('Ctrl Pts',(-4.92210345011766,-0.00387026642323842,
62.8898594359906));
#51753=CARTESIAN_POINT('Ctrl Pts',(-4.92500427991532,-0.00235440163140841,
61.4851405640091));
#51754=CARTESIAN_POINT('Ctrl Pts',(-4.92578548668796,-0.134817287697758,
61.4926710436081));
#51755=CARTESIAN_POINT('Ctrl Pts',(-4.86077673604698,-1.89901484929061,
61.5930094744228));
#51756=CARTESIAN_POINT('Ctrl Pts',(-2.73789341270518,-5.13260792995689,
61.7861558564532));
#51757=CARTESIAN_POINT('Ctrl Pts',(2.83787677981535,-5.07800944116647,62.0645797101003));
#51758=CARTESIAN_POINT('Ctrl Pts',(5.80618437177022,-0.357697558004235,
62.3430035637474));
#51759=CARTESIAN_POINT('Ctrl Pts',(3.4397259481389,4.69126954072045,62.6214274173947));
#51760=CARTESIAN_POINT('Ctrl Pts',(-2.08717863360625,5.42986278403133,62.8998512710416));
#51761=CARTESIAN_POINT('Ctrl Pts',(-4.73901895071827,2.30689062440745,63.1044223199133));
#51762=CARTESIAN_POINT('Ctrl Pts',(-4.92277501352727,0.338792335834338,
63.2161854175691));
#51763=CARTESIAN_POINT('Ctrl Pts',(-4.91967215389204,0.00442564071372501,
63.2351405640092));
#51764=CARTESIAN_POINT('Origin',(0.,0.,-13.2351405640096));
#51765=CARTESIAN_POINT('',(-4.91628642972681,0.00445635614462418,59.3898594359906));
#51766=CARTESIAN_POINT('',(-4.91240599187292,-0.00326991338738425,59.7351405640091));
#51767=CARTESIAN_POINT('',(-4.91825,6.88216836313478E-12,-13.2351405640096));
#51768=CARTESIAN_POINT('Ctrl Pts',(-4.91628642972681,0.00445635614462425,
59.3898594359906));
#51769=CARTESIAN_POINT('Ctrl Pts',(-4.9058282512334,-1.18809301663682,59.4573459348495));
#51770=CARTESIAN_POINT('Ctrl Pts',(-3.86949289148344,-4.03660726229823,
59.6176221922852));
#51771=CARTESIAN_POINT('Ctrl Pts',(0.901259081565336,-5.74656141372159,
59.8706882082974));
#51772=CARTESIAN_POINT('Ctrl Pts',(5.32123674041329,-2.34939897979313,60.1490574840279));
#51773=CARTESIAN_POINT('Ctrl Pts',(4.85377627470227,3.20563439726283,60.4274267597579));
#51774=CARTESIAN_POINT('Ctrl Pts',(-0.0717702282064447,5.81636355879867,
60.7057960354884));
#51775=CARTESIAN_POINT('Ctrl Pts',(-4.21753087644577,3.4861376510141,60.9432735942325));
#51776=CARTESIAN_POINT('Ctrl Pts',(-4.90792938452277,0.918193042991883,
61.0879613943999));
#51777=CARTESIAN_POINT('Ctrl Pts',(-4.91057232344976,-0.00158146149711672,
61.1398594359906));
#51778=CARTESIAN_POINT('Ctrl Pts',(-4.91240599187292,-0.00326991338738404,
59.7351405640092));
#51779=CARTESIAN_POINT('Ctrl Pts',(-4.91606640436456,-0.605564742131566,
59.7691566696472));
#51780=CARTESIAN_POINT('Ctrl Pts',(-4.53400968494839,-2.84665020624194,
59.8959807265009));
#51781=CARTESIAN_POINT('Ctrl Pts',(-1.18277815942064,-5.69567909274991,
60.1156127345705));
#51782=CARTESIAN_POINT('Ctrl Pts',(4.15226795782324,-4.07411282470503,60.3940365882174));
#51783=CARTESIAN_POINT('Ctrl Pts',(5.67217894144929,1.29077905087206,60.6724604418648));
#51784=CARTESIAN_POINT('Ctrl Pts',(1.98044911010386,5.469693393992,60.9508842955118));
#51785=CARTESIAN_POINT('Ctrl Pts',(-3.38186697238311,4.64591220500507,61.22177766956));
#51786=CARTESIAN_POINT('Ctrl Pts',(-4.91615765368059,1.4976961407447,61.3998630923924));
#51787=CARTESIAN_POINT('Ctrl Pts',(-4.92500427991532,-0.00235440163140841,
61.4851405640091));
#51788=CARTESIAN_POINT('Origin',(0.,0.,-13.2351405640096));
#51789=CARTESIAN_POINT('',(-4.9263260156827,-0.000426885928948556,57.6398594359905));
#51790=CARTESIAN_POINT('',(-4.91305232001281,0.00360176434312187,57.9851405640092));
#51791=CARTESIAN_POINT('',(-4.91825,6.88216836313478E-12,-13.2351405640096));
#51792=CARTESIAN_POINT('Ctrl Pts',(-4.9263260156827,-0.000426885928949852,
57.6398594359905));
#51793=CARTESIAN_POINT('Ctrl Pts',(-4.92635412757088,-0.0231288288560638,
57.6411509581455));
#51794=CARTESIAN_POINT('Ctrl Pts',(-4.9159151427125,-1.67683142689444,57.7352322388772));
#51795=CARTESIAN_POINT('Ctrl Pts',(-3.0771332764778,-4.93624217523513,57.9221032781857));
#51796=CARTESIAN_POINT('Ctrl Pts',(2.4882557394928,-5.25773899967072,58.2004725539159));
#51797=CARTESIAN_POINT('Ctrl Pts',(5.76823695308387,-0.750118968468039,
58.4788418296462));
#51798=CARTESIAN_POINT('Ctrl Pts',(3.7502202441463,4.44646872632352,58.7572111053764));
#51799=CARTESIAN_POINT('Ctrl Pts',(-1.7122907225886,5.55907334859995,59.0355803811067));
#51800=CARTESIAN_POINT('Ctrl Pts',(-4.65907391466842,2.53390393001092,59.2464631579781));
#51801=CARTESIAN_POINT('Ctrl Pts',(-4.9202075993099,0.451588553192956,59.3645561762727));
#51802=CARTESIAN_POINT('Ctrl Pts',(-4.91628642972681,0.00445635614462425,
59.3898594359906));
#51803=CARTESIAN_POINT('Ctrl Pts',(-4.91305232001281,0.00360176434312139,
57.9851405640092));
#51804=CARTESIAN_POINT('Ctrl Pts',(-4.90582152856365,-1.06729817837134,
58.0456422956863));
#51805=CARTESIAN_POINT('Ctrl Pts',(-4.0341145126111,-3.79164216223504,58.1989519785791));
#51806=CARTESIAN_POINT('Ctrl Pts',(0.467946912388112,-5.79834029608278,
58.4450696126877));
#51807=CARTESIAN_POINT('Ctrl Pts',(5.13101074500744,-2.7408854840378,58.7234934663347));
#51808=CARTESIAN_POINT('Ctrl Pts',(5.07966318532585,2.83491559409379,59.001917319982));
#51809=CARTESIAN_POINT('Ctrl Pts',(0.361082758659297,5.80597483144648,59.2803411736289));
#51810=CARTESIAN_POINT('Ctrl Pts',(-4.07224317210069,3.73122014391495,59.5247489216382));
#51811=CARTESIAN_POINT('Ctrl Pts',(-4.90607950617085,1.03770829089449,59.6763487184315));
#51812=CARTESIAN_POINT('Ctrl Pts',(-4.91240599187292,-0.00326991338738404,
59.7351405640092));
#51813=CARTESIAN_POINT('Origin',(0.,0.,-13.2351405640096));
#51814=CARTESIAN_POINT('',(-4.91500211464461,-0.00424101522293115,55.8898594359906));
#51815=CARTESIAN_POINT('',(-4.92552843553515,0.00186197695103037,56.2351405640092));
#51816=CARTESIAN_POINT('',(-4.91825,6.88216836313478E-12,-13.2351405640096));
#51817=CARTESIAN_POINT('Ctrl Pts',(-4.91500211464461,-0.00424101522293059,
55.8898594359906));
#51818=CARTESIAN_POINT('Ctrl Pts',(-4.91903479884973,-0.497344277840858,
55.9177457400183));
#51819=CARTESIAN_POINT('Ctrl Pts',(-4.62389168535497,-2.62649724502737,
56.0384218026228));
#51820=CARTESIAN_POINT('Ctrl Pts',(-1.55698110414879,-5.60455581247088,
56.2518876238041));
#51821=CARTESIAN_POINT('Ctrl Pts',(3.87246440760804,-4.34042111154972,56.5302568995343));
#51822=CARTESIAN_POINT('Ctrl Pts',(5.74513710412806,0.910294275796876,56.8086261752646));
#51823=CARTESIAN_POINT('Ctrl Pts',(2.34102857791428,5.3249245263352,57.0869954509948));
#51824=CARTESIAN_POINT('Ctrl Pts',(-3.18749317080709,4.85093885713963,57.3640732045702));
#51825=CARTESIAN_POINT('Ctrl Pts',(-4.92433442136023,1.60789840159787,57.5483611995687));
#51826=CARTESIAN_POINT('Ctrl Pts',(-4.9263260156827,-0.000426885928949852,
57.6398594359905));
#51827=CARTESIAN_POINT('Ctrl Pts',(-4.92552843553515,0.00186197695103052,
56.2351405640092));
#51828=CARTESIAN_POINT('Ctrl Pts',(-4.9181339110517,-1.52783432001219,56.3221279217254));
#51829=CARTESIAN_POINT('Ctrl Pts',(-3.32966935051829,-4.70283072137663,
56.5019232306572));
#51830=CARTESIAN_POINT('Ctrl Pts',(2.08084551689526,-5.43229292627044,56.7745264908049));
#51831=CARTESIAN_POINT('Ctrl Pts',(5.69498851284468,-1.18609879038724,57.052950344452));
#51832=CARTESIAN_POINT('Ctrl Pts',(4.07653308749828,4.14989186467828,57.3313741980992));
#51833=CARTESIAN_POINT('Ctrl Pts',(-1.2874717010986,5.67293055843817,57.6097980517462));
#51834=CARTESIAN_POINT('Ctrl Pts',(-4.55998868921863,2.78532417715685,57.8277201737163));
#51835=CARTESIAN_POINT('Ctrl Pts',(-4.91691335885449,0.57543215157618,57.9528343444706));
#51836=CARTESIAN_POINT('Ctrl Pts',(-4.91305232001281,0.00360176434312139,
57.9851405640092));
#51837=CARTESIAN_POINT('Origin',(0.,0.,-13.2351405640096));
#51838=CARTESIAN_POINT('',(-4.91110894597329,0.00226854779708756,54.1398594359906));
#51839=CARTESIAN_POINT('',(-4.91874848582105,-0.00451671112762952,54.4851405640092));
#51840=CARTESIAN_POINT('',(-4.91825,6.88216836313478E-12,-13.2351405640096));
#51841=CARTESIAN_POINT('Ctrl Pts',(-4.91110894597329,0.00226854779708741,
54.1398594359906));
#51842=CARTESIAN_POINT('Ctrl Pts',(-4.9071041400712,-0.963021056215211,
54.1943405218911));
#51843=CARTESIAN_POINT('Ctrl Pts',(-4.16469942930719,-3.57803361618035,
54.3416113663684));
#51844=CARTESIAN_POINT('Ctrl Pts',(0.0900619915185718,-5.81610908180557,
54.5816719694224));
#51845=CARTESIAN_POINT('Ctrl Pts',(4.94107477914329,-3.06936736815449,54.8600412451526));
#51846=CARTESIAN_POINT('Ctrl Pts',(5.25381978618318,2.49652031197179,55.138410520883));
#51847=CARTESIAN_POINT('Ctrl Pts',(0.741047648394848,5.76940936288854,55.4167797966132));
#51848=CARTESIAN_POINT('Ctrl Pts',(-3.93209835299061,3.94620162905268,55.6672627683158));
#51849=CARTESIAN_POINT('Ctrl Pts',(-4.90561631953321,1.14342291189664,55.8249559814415));
#51850=CARTESIAN_POINT('Ctrl Pts',(-4.91500211464461,-0.00424101522293059,
55.8898594359906));
#51851=CARTESIAN_POINT('Ctrl Pts',(-4.91874848582105,-0.00451671112763018,
54.4851405640092));
#51852=CARTESIAN_POINT('Ctrl Pts',(-4.92213659647667,-0.36922122126081,
54.5058055965487));
#51853=CARTESIAN_POINT('Ctrl Pts',(-4.7183726132553,-2.36808483286878,54.619278580304));
#51854=CARTESIAN_POINT('Ctrl Pts',(-1.98682590730801,-5.46738029736734,
54.8255595152749));
#51855=CARTESIAN_POINT('Ctrl Pts',(3.52553906903275,-4.627126405742,55.1039833689222));
#51856=CARTESIAN_POINT('Ctrl Pts',(5.7986121442169,0.464566144840059,55.3824072225692));
#51857=CARTESIAN_POINT('Ctrl Pts',(2.74387662363257,5.12941181581999,55.6608310762164));
#51858=CARTESIAN_POINT('Ctrl Pts',(-2.83195344466994,5.08131520270228,55.9392549298634));
#51859=CARTESIAN_POINT('Ctrl Pts',(-4.87666238088383,1.83814217788545,56.1306914257944));
#51860=CARTESIAN_POINT('Ctrl Pts',(-4.92602322606875,0.104218693560284,
56.2293199705097));
#51861=CARTESIAN_POINT('Ctrl Pts',(-4.92552843553515,0.00186197695103052,
56.2351405640092));
#51862=CARTESIAN_POINT('Origin',(0.,0.,-13.2351405640096));
#51863=CARTESIAN_POINT('',(-4.92333307335781,0.0033824739169612,52.3898594359906));
#51864=CARTESIAN_POINT('',(-4.91010297280824,0.000219119417446956,52.7351405640092));
#51865=CARTESIAN_POINT('',(-4.91825,6.88216836313478E-12,-13.2351405640096));
#51866=CARTESIAN_POINT('Ctrl Pts',(-4.92333307335781,0.00338247391696123,
52.3898594359906));
#51867=CARTESIAN_POINT('Ctrl Pts',(-4.9121235422079,-1.4240336674598,52.4709353037639));
#51868=CARTESIAN_POINT('Ctrl Pts',(-3.50620705899313,-4.50433666380612,
52.6448009301139));
#51869=CARTESIAN_POINT('Ctrl Pts',(1.72976521052916,-5.55366080439025,52.9114563150408));
#51870=CARTESIAN_POINT('Ctrl Pts',(5.6069971929771,-1.54816617057876,53.1898255907711));
#51871=CARTESIAN_POINT('Ctrl Pts',(4.33432640242356,3.87928481179605,53.4681948665013));
#51872=CARTESIAN_POINT('Ctrl Pts',(-0.919327219170563,5.74369858870307,
53.7465641422317));
#51873=CARTESIAN_POINT('Ctrl Pts',(-4.4656378077124,3.0002458228677,53.9704523320613));
#51874=CARTESIAN_POINT('Ctrl Pts',(-4.91392494708448,0.68101719729,54.1015507633143));
#51875=CARTESIAN_POINT('Ctrl Pts',(-4.91110894597329,0.00226854779708741,
54.1398594359906));
#51876=CARTESIAN_POINT('Ctrl Pts',(-4.91010297280824,0.000219119417446609,
52.7351405640092));
#51877=CARTESIAN_POINT('Ctrl Pts',(-4.90977214474024,-0.835617689631801,
52.7822912225878));
#51878=CARTESIAN_POINT('Ctrl Pts',(-4.30975846453187,-3.3171009819724,52.9222498323822));
#51879=CARTESIAN_POINT('Ctrl Pts',(-0.367852790578618,-5.80554982981413,
53.1550163933922));
#51880=CARTESIAN_POINT('Ctrl Pts',(4.68524583146246,-3.4479263334292,53.4334402470393));
#51881=CARTESIAN_POINT('Ctrl Pts',(5.43350522761236,2.0776778969562,53.7118641006865));
#51882=CARTESIAN_POINT('Ctrl Pts',(1.18941901815086,5.69429599698262,53.9902879543335));
#51883=CARTESIAN_POINT('Ctrl Pts',(-3.75139922738628,4.19884520123217,54.2480467754412));
#51884=CARTESIAN_POINT('Ctrl Pts',(-4.90692038000867,1.26868950158949,54.412997645333));
#51885=CARTESIAN_POINT('Ctrl Pts',(-4.91874848582105,-0.00451671112763018,
54.4851405640092));
#51886=CARTESIAN_POINT('Origin',(0.,0.,-13.2351405640096));
#51887=CARTESIAN_POINT('',(-4.92181031186921,-0.00396311810717911,50.6398594359906));
#51888=CARTESIAN_POINT('',(-4.91955543626503,0.00444052391018634,50.9851405640092));
#51889=CARTESIAN_POINT('',(-4.91825,6.88216836313478E-12,-13.2351405640096));
#51890=CARTESIAN_POINT('Ctrl Pts',(-4.92181031186921,-0.00396311810717906,
50.6398594359906));
#51891=CARTESIAN_POINT('Ctrl Pts',(-4.92410826691375,-0.266166171072131,
50.6547403270599));
#51892=CARTESIAN_POINT('Ctrl Pts',(-4.78563672242207,-2.16090437287408,
50.762410976706));
#51893=CARTESIAN_POINT('Ctrl Pts',(-2.32427042909063,-5.33226058874023,
50.962871384929));
#51894=CARTESIAN_POINT('Ctrl Pts',(3.22849593851986,-4.8386000029697,51.2412406606591));
#51895=CARTESIAN_POINT('Ctrl Pts',(5.81596027116012,0.0992075504414687,
51.5196099363895));
#51896=CARTESIAN_POINT('Ctrl Pts',(3.06159387029672,4.94589516540121,51.7979792121197));
#51897=CARTESIAN_POINT('Ctrl Pts',(-2.50477871137838,5.24988758173003,52.07634848785));
#51898=CARTESIAN_POINT('Ctrl Pts',(-4.81939694442464,2.04782992932728,52.273641895807));
#51899=CARTESIAN_POINT('Ctrl Pts',(-4.9249526332522,0.209616428241301,52.3781455451872));
#51900=CARTESIAN_POINT('Ctrl Pts',(-4.92333307335781,0.00338247391696123,
52.3898594359906));
#51901=CARTESIAN_POINT('Ctrl Pts',(-4.91955543626503,0.00444052391018648,
50.9851405640092));
#51902=CARTESIAN_POINT('Ctrl Pts',(-4.90749085177966,-1.29457459993488,
51.0587768486269));
#51903=CARTESIAN_POINT('Ctrl Pts',(-3.71213818630798,-4.25043923730225,
51.2252210844603));
#51904=CARTESIAN_POINT('Ctrl Pts',(1.28085568968505,-5.67442800678559,51.4844732715094));
#51905=CARTESIAN_POINT('Ctrl Pts',(5.4662209609829,-1.99001329334819,51.7628971251566));
#51906=CARTESIAN_POINT('Ctrl Pts',(4.62918116396803,3.52284065111588,52.0413209788037));
#51907=CARTESIAN_POINT('Ctrl Pts',(-0.461185219367196,5.79888202116823,
52.3197448324508));
#51908=CARTESIAN_POINT('Ctrl Pts',(-4.33752509971949,3.26372098771621,52.5510180275193));
#51909=CARTESIAN_POINT('Ctrl Pts',(-4.91042332281752,0.809583122763727,
52.6894832713721));
#51910=CARTESIAN_POINT('Ctrl Pts',(-4.91010297280824,0.000219119417446609,
52.7351405640092));
#51911=CARTESIAN_POINT('Origin',(0.,0.,-13.2351405640096));
#51912=CARTESIAN_POINT('',(-4.91047827356641,-0.00141950771611534,48.8898594359906));
#51913=CARTESIAN_POINT('',(-4.92507636652171,-0.00229403587955257,49.2351405640092));
#51914=CARTESIAN_POINT('',(-4.91825,6.88216836313478E-12,-13.2351405640096));
#51915=CARTESIAN_POINT('Ctrl Pts',(-4.91047827356641,-0.00141950771611582,
48.8898594359906));
#51916=CARTESIAN_POINT('Ctrl Pts',(-4.91237210306681,-0.736516413527698,
48.9313351089327));
#51917=CARTESIAN_POINT('Ctrl Pts',(-4.41217290705613,-3.11373014312353,
49.0656005404517));
#51918=CARTESIAN_POINT('Ctrl Pts',(-0.722899533583313,-5.77171138208786,
49.2926557305472));
#51919=CARTESIAN_POINT('Ctrl Pts',(4.46411054420093,-3.72920273824468,49.5710250062776));
#51920=CARTESIAN_POINT('Ctrl Pts',(5.55093393037054,1.73849604958962,49.8493942820078));
#51921=CARTESIAN_POINT('Ctrl Pts',(1.53934740890388,5.60942470922629,50.1277635577381));
#51922=CARTESIAN_POINT('Ctrl Pts',(-3.59606567504477,4.39671076577627,50.391251942399));
#51923=CARTESIAN_POINT('Ctrl Pts',(-4.90977937405317,1.36880030165654,50.5619505684832));
#51924=CARTESIAN_POINT('Ctrl Pts',(-4.92181031186921,-0.00396311810717906,
50.6398594359906));
#51925=CARTESIAN_POINT('Ctrl Pts',(-4.92507636652171,-0.00229403587955276,
49.2351405640092));
#51926=CARTESIAN_POINT('Ctrl Pts',(-4.92581886796819,-0.130943301348753,
49.2424545234503));
#51927=CARTESIAN_POINT('Ctrl Pts',(-4.86282102530499,-1.89130395537016,
49.342576434107));
#51928=CARTESIAN_POINT('Ctrl Pts',(-2.7498561035418,-5.1262087269058,49.5355062959795));
#51929=CARTESIAN_POINT('Ctrl Pts',(2.82602625874287,-5.08461405486067,49.8139301496266));
#51930=CARTESIAN_POINT('Ctrl Pts',(5.80533436864992,-0.371237619541609,
50.0923540032738));
#51931=CARTESIAN_POINT('Ctrl Pts',(3.4506574522521,4.68323474205681,50.3707778569208));
#51932=CARTESIAN_POINT('Ctrl Pts',(-2.07450957073036,5.43471568188616,50.649201710568));
#51933=CARTESIAN_POINT('Ctrl Pts',(-4.73644042858587,2.31463773732241,50.8539892795975));
#51934=CARTESIAN_POINT('Ctrl Pts',(-4.92269652618555,0.342647224444224,
50.9659688974112));
#51935=CARTESIAN_POINT('Ctrl Pts',(-4.91955543626503,0.00444052391018648,
50.9851405640092));
#51936=CARTESIAN_POINT('Origin',(0.,0.,-13.2351405640096));
#51937=CARTESIAN_POINT('',(-4.91658767744717,0.00448723658957973,47.1398594359906));
#51938=CARTESIAN_POINT('',(-4.9124840770588,-0.00331422200313403,47.4851405640092));
#51939=CARTESIAN_POINT('',(-4.91825,6.88216836313478E-12,-13.2351405640096));
#51940=CARTESIAN_POINT('Ctrl Pts',(-4.91658767744717,0.00448723658958032,
47.1398594359906));
#51941=CARTESIAN_POINT('Ctrl Pts',(-4.9059141224208,-1.19819399969518,47.2079298908056));
#51942=CARTESIAN_POINT('Ctrl Pts',(-3.85505991893494,-4.05698950369964,
47.3687901041973));
#51943=CARTESIAN_POINT('Ctrl Pts',(0.937386264007801,-5.74077895462167,
47.6224400761656));
#51944=CARTESIAN_POINT('Ctrl Pts',(5.33590884708369,-2.31588272358329,47.900809351896));
#51945=CARTESIAN_POINT('Ctrl Pts',(4.83351730048996,3.23610051136267,48.1791786276262));
#51946=CARTESIAN_POINT('Ctrl Pts',(-0.108352864056654,5.81579707956082,
48.4575479033566));
#51947=CARTESIAN_POINT('Ctrl Pts',(-4.22921657272871,3.4653350732591,48.6944415061446));
#51948=CARTESIAN_POINT('Ctrl Pts',(-4.90813521021704,0.908049173531873,
48.838545350356));
#51949=CARTESIAN_POINT('Ctrl Pts',(-4.91047827356641,-0.00141950771611582,
48.8898594359906));
#51950=CARTESIAN_POINT('Ctrl Pts',(-4.9124840770588,-0.00331422200313375,
47.4851405640092));
#51951=CARTESIAN_POINT('Ctrl Pts',(-4.91617410517375,-0.601751445209023,
47.5189401494893));
#51952=CARTESIAN_POINT('Ctrl Pts',(-4.53733904880512,-2.83888472337153,
47.6455476861851));
#51953=CARTESIAN_POINT('Ctrl Pts',(-1.19605825955486,-5.69290515833011,
47.8649631740968));
#51954=CARTESIAN_POINT('Ctrl Pts',(4.14275512418048,-4.08378555791893,48.1433870277438));
#51955=CARTESIAN_POINT('Ctrl Pts',(5.67517383763514,1.27754703029398,48.421810881391));
#51956=CARTESIAN_POINT('Ctrl Pts',(1.99320000290249,5.46505976640885,48.7002347350381));
#51957=CARTESIAN_POINT('Ctrl Pts',(-3.37531022387012,4.65313823791433,48.9713446292442));
#51958=CARTESIAN_POINT('Ctrl Pts',(-4.91639715342663,1.50150692616823,49.1496465722345));
#51959=CARTESIAN_POINT('Ctrl Pts',(-4.92507636652171,-0.00229403587955276,
49.2351405640092));
#51960=CARTESIAN_POINT('Origin',(0.,0.,-13.2351405640096));
#51961=CARTESIAN_POINT('',(-4.92627640968079,-0.00061865787654027,45.3898594359906));
#51962=CARTESIAN_POINT('',(-4.91296680399423,0.00356208998599034,45.7351405640092));
#51963=CARTESIAN_POINT('',(-4.91825,6.88216836313478E-12,-13.2351405640096));
#51964=CARTESIAN_POINT('Ctrl Pts',(-4.92627640968079,-0.000618657876541137,
45.3898594359906));
#51965=CARTESIAN_POINT('Ctrl Pts',(-4.92633465053822,-0.033586076024589,
45.3917349141016));
#51966=CARTESIAN_POINT('Ctrl Pts',(-4.91108086732445,-1.69756959127752,
45.4864001507893));
#51967=CARTESIAN_POINT('Ctrl Pts',(-3.046024182882,-4.95549923731964,45.6738551460538));
#51968=CARTESIAN_POINT('Ctrl Pts',(2.52127690930862,-5.24198423885123,45.9522244217841));
#51969=CARTESIAN_POINT('Ctrl Pts',(5.77284098579036,-0.713822783719208,
46.2305936975144));
#51970=CARTESIAN_POINT('Ctrl Pts',(3.72217843764396,4.46996909297098,46.5089629732446));
#51971=CARTESIAN_POINT('Ctrl Pts',(-1.74722258992204,5.54819333071977,46.7873322489749));
#51972=CARTESIAN_POINT('Ctrl Pts',(-4.66681253604691,2.51297709137372,46.9976310698902));
#51973=CARTESIAN_POINT('Ctrl Pts',(-4.92046370339166,0.441232413174631,
47.1151401322288));
#51974=CARTESIAN_POINT('Ctrl Pts',(-4.91658767744717,0.00448723658958032,
47.1398594359906));
#51975=CARTESIAN_POINT('Ctrl Pts',(-4.91296680399423,0.00356208998598999,
45.7351405640092));
#51976=CARTESIAN_POINT('Ctrl Pts',(-4.90584917021152,-1.0635520480926,45.7954257755284));
#51977=CARTESIAN_POINT('Ctrl Pts',(-4.03898978525713,-3.78399820225403,
45.9485189382633));
#51978=CARTESIAN_POINT('Ctrl Pts',(0.454422899244266,-5.79941586115651,
46.1944200522139));
#51979=CARTESIAN_POINT('Ctrl Pts',(5.12460456826788,-2.75284444182363,46.4728439058611));
#51980=CARTESIAN_POINT('Ctrl Pts',(5.08626088852126,2.82306122425459,46.7512677595082));
#51981=CARTESIAN_POINT('Ctrl Pts',(0.374622322305924,5.8051169340179,47.0296916131553));
#51982=CARTESIAN_POINT('Ctrl Pts',(-4.06746198886625,3.7388783229028,47.2743158813224));
#51983=CARTESIAN_POINT('Ctrl Pts',(-4.9060419114083,1.04145606245698,47.4261321982736));
#51984=CARTESIAN_POINT('Ctrl Pts',(-4.9124840770588,-0.00331422200313375,
47.4851405640092));
#51985=CARTESIAN_POINT('Origin',(0.,0.,-13.2351405640096));
#51986=CARTESIAN_POINT('',(-4.91472474733406,-0.00417511919816473,43.6398594359906));
#51987=CARTESIAN_POINT('',(-4.92546797871252,0.00192622575846596,43.9851405640092));
#51988=CARTESIAN_POINT('',(-4.91825,6.88216836313478E-12,-13.2351405640096));
#51989=CARTESIAN_POINT('Ctrl Pts',(-4.91472474733406,-0.00417511919816496,
43.6398594359906));
#51990=CARTESIAN_POINT('Ctrl Pts',(-4.91876162149318,-0.507676058970831,
43.6683296959744));
#51991=CARTESIAN_POINT('Ctrl Pts',(-4.61572084458829,-2.6474350464209,43.789589714535));
#51992=CARTESIAN_POINT('Ctrl Pts',(-1.52169848847216,-5.61423812497824,
44.0036394916721));
#51993=CARTESIAN_POINT('Ctrl Pts',(3.89968840385962,-4.31597803129028,44.2820087674025));
#51994=CARTESIAN_POINT('Ctrl Pts',(5.73929784318452,0.946412320817448,44.5603780431327));
#51995=CARTESIAN_POINT('Ctrl Pts',(2.30748929166079,5.33954391148237,44.838747318863));
#51996=CARTESIAN_POINT('Ctrl Pts',(-3.20629665985511,4.83186626178632,45.1152411164823));
#51997=CARTESIAN_POINT('Ctrl Pts',(-4.92345316924109,1.59748535742421,45.2989451555248));
#51998=CARTESIAN_POINT('Ctrl Pts',(-4.92627640968079,-0.000618657876541137,
45.3898594359906));
#51999=CARTESIAN_POINT('Ctrl Pts',(-4.92546797871252,0.00192622575846612,
43.9851405640092));
#52000=CARTESIAN_POINT('Ctrl Pts',(-4.91787282992045,-1.52401225827842,
44.0719114015675));
#52001=CARTESIAN_POINT('Ctrl Pts',(-3.33633207850513,-4.6956419719452,44.2514901903414));
#52002=CARTESIAN_POINT('Ctrl Pts',(2.06817080372702,-5.43713104758401,44.5238769303312));
#52003=CARTESIAN_POINT('Ctrl Pts',(5.69220683601255,-1.19937727093821,44.8023007839783));
#52004=CARTESIAN_POINT('Ctrl Pts',(4.08620027266672,4.14037339302263,45.0807246376255));
#52005=CARTESIAN_POINT('Ctrl Pts',(-1.27423793661312,5.67591773926357,45.3591484912725));
#52006=CARTESIAN_POINT('Ctrl Pts',(-4.55673857265977,2.7930898524097,45.5772871334005));
#52007=CARTESIAN_POINT('Ctrl Pts',(-4.91680663377896,0.579250131291795,
45.7026178243127));
#52008=CARTESIAN_POINT('Ctrl Pts',(-4.91296680399423,0.00356208998598999,
45.7351405640092));
#52009=CARTESIAN_POINT('Origin',(0.,0.,-13.2351405640096));
#52010=CARTESIAN_POINT('',(-4.91125677312356,0.00241598250425361,41.8898594359907));
#52011=CARTESIAN_POINT('',(-4.91886553528195,-0.00450853108237725,42.2351405640092));
#52012=CARTESIAN_POINT('',(-4.91825,6.88216836313478E-12,-13.2351405640096));
#52013=CARTESIAN_POINT('Ctrl Pts',(-4.91125677312356,0.0024159825042535,
41.8898594359907));
#52014=CARTESIAN_POINT('Ctrl Pts',(-4.90693843454433,-0.973146675809823,
41.9449244778472));
#52015=CARTESIAN_POINT('Ctrl Pts',(-4.15249564758543,-3.59877918216972,
42.0927792782805));
#52016=CARTESIAN_POINT('Ctrl Pts',(0.126642664911688,-5.81542755515032,
42.3334238372905));
#52017=CARTESIAN_POINT('Ctrl Pts',(4.96028289923243,-3.03822803182378,42.6117931130208));
#52018=CARTESIAN_POINT('Ctrl Pts',(5.23801311996793,2.52951666703768,42.8901623887511));
#52019=CARTESIAN_POINT('Ctrl Pts',(0.704744268806608,5.77395631515876,43.1685316644814));
#52020=CARTESIAN_POINT('Ctrl Pts',(-3.94597393987301,3.92571018031166,43.4184306802278));
#52021=CARTESIAN_POINT('Ctrl Pts',(-4.90560471393971,1.13332513565534,43.5755399373976));
#52022=CARTESIAN_POINT('Ctrl Pts',(-4.91472474733406,-0.00417511919816496,
43.6398594359906));
#52023=CARTESIAN_POINT('Ctrl Pts',(-4.91886553528195,-0.00450853108237819,
42.2351405640092));
#52024=CARTESIAN_POINT('Ctrl Pts',(-4.92221974715232,-0.365369816257576,
42.2555890763908));
#52025=CARTESIAN_POINT('Ctrl Pts',(-4.72102302970205,-2.36033413903901,
42.3688455399882));
#52026=CARTESIAN_POINT('Ctrl Pts',(-1.99957138822013,-5.46273180427181,
42.5749099548013));
#52027=CARTESIAN_POINT('Ctrl Pts',(3.51473821570051,-4.6353359939799,42.8533338084484));
#52028=CARTESIAN_POINT('Ctrl Pts',(5.79967982401188,0.45104150689311,43.1317576620956));
#52029=CARTESIAN_POINT('Ctrl Pts',(2.75583184430228,5.12299866756965,43.4101815157427));
#52030=CARTESIAN_POINT('Ctrl Pts',(-2.82009523009366,5.08790599315611,43.6886053693897));
#52031=CARTESIAN_POINT('Ctrl Pts',(-4.87468342339853,1.84584768784173,43.8802583854787));
#52032=CARTESIAN_POINT('Ctrl Pts',(-4.92599641404625,0.108093969687443,
43.9791034503518));
#52033=CARTESIAN_POINT('Ctrl Pts',(-4.92546797871252,0.00192622575846612,
43.9851405640092));
#52034=CARTESIAN_POINT('Origin',(0.,0.,-13.2351405640096));
#52035=CARTESIAN_POINT('',(-4.92359279332473,0.00325554800820353,40.1398594359906));
#52036=CARTESIAN_POINT('',(-4.91009863878307,0.000155608968132326,40.4851405640092));
#52037=CARTESIAN_POINT('',(-4.91825,6.88216836313478E-12,-13.2351405640096));
#52038=CARTESIAN_POINT('Ctrl Pts',(-4.92359279332473,0.0032555480082035,
40.1398594359906));
#52039=CARTESIAN_POINT('Ctrl Pts',(-4.91262089068949,-1.43424326230662,
40.22151925972));
#52040=CARTESIAN_POINT('Ctrl Pts',(-3.489286725208,-4.52407530298379,40.3959688420261));
#52041=CARTESIAN_POINT('Ctrl Pts',(1.76466268810206,-5.5426709816656,40.663208182909));
#52042=CARTESIAN_POINT('Ctrl Pts',(5.61662401257895,-1.5128683733554,40.9415774586392));
#52043=CARTESIAN_POINT('Ctrl Pts',(4.30984054340475,3.90647033832362,41.2199467343696));
#52044=CARTESIAN_POINT('Ctrl Pts',(-0.955436037461097,5.73780254035447,
41.4983160100997));
#52045=CARTESIAN_POINT('Ctrl Pts',(-4.4752161010382,2.97931192419287,41.7216202439735));
#52046=CARTESIAN_POINT('Ctrl Pts',(-4.91421523994953,0.670767874864228,
41.8521347192705));
#52047=CARTESIAN_POINT('Ctrl Pts',(-4.91125677312356,0.0024159825042535,
41.8898594359907));
#52048=CARTESIAN_POINT('Ctrl Pts',(-4.91009863878307,0.000155608968132256,
40.4851405640092));
#52049=CARTESIAN_POINT('Ctrl Pts',(-4.9098647894845,-0.831844790997033,
40.53207470243));
#52050=CARTESIAN_POINT('Ctrl Pts',(-4.31382143773829,-3.30936416075672,
40.6718167920664));
#52051=CARTESIAN_POINT('Ctrl Pts',(-0.381391344636143,-5.80467614464644,
40.9043668329184));
#52052=CARTESIAN_POINT('Ctrl Pts',(4.67719192445218,-3.45884376690104,41.1827906865657));
#52053=CARTESIAN_POINT('Ctrl Pts',(5.43833595818706,2.06500036510422,41.4612145402126));
#52054=CARTESIAN_POINT('Ctrl Pts',(1.20269587460476,5.69150657868371,41.7396383938599));
#52055=CARTESIAN_POINT('Ctrl Pts',(-3.74574984464755,4.20633618758006,41.9976137351253));
#52056=CARTESIAN_POINT('Ctrl Pts',(-4.90699626654784,1.27244108778943,42.1627811251751));
#52057=CARTESIAN_POINT('Ctrl Pts',(-4.91886553528195,-0.00450853108237819,
42.2351405640092));
#52058=CARTESIAN_POINT('Origin',(0.,0.,-13.2351405640096));
#52059=CARTESIAN_POINT('',(-4.92151270901473,-0.00404930601734944,38.3898594359906));
#52060=CARTESIAN_POINT('',(-4.91943860138798,0.00445443611122698,38.7351405640092));
#52061=CARTESIAN_POINT('',(-4.91825,6.88216836313478E-12,-13.2351405640096));
#52062=CARTESIAN_POINT('Ctrl Pts',(-4.92151270901473,-0.00404930601735014,
38.3898594359906));
#52063=CARTESIAN_POINT('Ctrl Pts',(-4.92393319119315,-0.276584443330804,
38.405324283016));
#52064=CARTESIAN_POINT('Ctrl Pts',(-4.77917839932122,-2.18176945279143,
38.5135788886182));
#52065=CARTESIAN_POINT('Ctrl Pts',(-2.29068533160149,-5.3467744225246,38.7146232527971));
#52066=CARTESIAN_POINT('Ctrl Pts',(3.25886614391259,-4.81819753329374,38.9929925285273));
#52067=CARTESIAN_POINT('Ctrl Pts',(5.81522122325282,0.135787106926827,39.2713618042576));
#52068=CARTESIAN_POINT('Ctrl Pts',(3.03042436822842,4.96505429599969,39.5497310799879));
#52069=CARTESIAN_POINT('Ctrl Pts',(-2.53775017010531,5.23402904920365,39.8281003557182));
#52070=CARTESIAN_POINT('Ctrl Pts',(-4.82539101363885,2.02699660194297,40.0248098077191));
#52071=CARTESIAN_POINT('Ctrl Pts',(-4.9250882234629,0.199181370173329,40.1287295011432));
#52072=CARTESIAN_POINT('Ctrl Pts',(-4.92359279332473,0.0032555480082035,
40.1398594359906));
#52073=CARTESIAN_POINT('Ctrl Pts',(-4.91943860138798,0.00445443611122684,
38.7351405640092));
#52074=CARTESIAN_POINT('Ctrl Pts',(-4.90740124733523,-1.29082005479286,
38.808560328469));
#52075=CARTESIAN_POINT('Ctrl Pts',(-3.7178736329033,-4.24296932209831,38.9747880441445));
#52076=CARTESIAN_POINT('Ctrl Pts',(1.26761845088123,-5.6773997538465,39.2338237110357));
#52077=CARTESIAN_POINT('Ctrl Pts',(5.46156503750013,-2.00275606181767,39.5122475646828));
#52078=CARTESIAN_POINT('Ctrl Pts',(4.63738445343698,3.51203501306753,39.79067141833));
#52079=CARTESIAN_POINT('Ctrl Pts',(-0.447659961214595,5.79994181532161,
40.0690952719771));
#52080=CARTESIAN_POINT('Ctrl Pts',(-4.33353632888539,3.27146300503898,40.3005849872035));
#52081=CARTESIAN_POINT('Ctrl Pts',(-4.91032720501026,0.813359640780624,
40.4392667512142));
#52082=CARTESIAN_POINT('Ctrl Pts',(-4.91009863878307,0.000155608968132256,
40.4851405640092));
#52083=CARTESIAN_POINT('Origin',(0.,0.,-13.2351405640096));
#52084=CARTESIAN_POINT('',(-4.91039451300053,-0.00125559194926212,36.6398594359907));
#52085=CARTESIAN_POINT('',(-4.92514685489251,-0.00223306629119513,36.9851405640092));
#52086=CARTESIAN_POINT('',(-4.91825,6.88216836313478E-12,-13.2351405640096));
#52087=CARTESIAN_POINT('Ctrl Pts',(-4.91039451300053,-0.00125559194926225,
36.6398594359907));
#52088=CARTESIAN_POINT('Ctrl Pts',(-4.91209161801324,-0.746734003806369,
36.6819190648888));
#52089=CARTESIAN_POINT('Ctrl Pts',(-4.40203186568558,-3.13464429489364,
36.8167684523638));
#52090=CARTESIAN_POINT('Ctrl Pts',(-0.6865820336325,-5.77614413989737,37.0444075984155));
#52091=CARTESIAN_POINT('Ctrl Pts',(4.48747836490629,-3.70105038310417,37.3227768741457));
#52092=CARTESIAN_POINT('Ctrl Pts',(5.53988924591708,1.77337620282608,37.601146149876));
#52093=CARTESIAN_POINT('Ctrl Pts',(1.50403451741344,5.61899601211875,37.8795154256062));
#52094=CARTESIAN_POINT('Ctrl Pts',(-3.61228496672945,4.376764288983,38.1424198543112));
#52095=CARTESIAN_POINT('Ctrl Pts',(-4.90941019225197,1.35863830109606,38.3125345244393));
#52096=CARTESIAN_POINT('Ctrl Pts',(-4.92151270901473,-0.00404930601735014,
38.3898594359906));
#52097=CARTESIAN_POINT('Ctrl Pts',(-4.92514685489251,-0.00223306629119565,
36.9851405640092));
#52098=CARTESIAN_POINT('Ctrl Pts',(-4.92585130384514,-0.127069110559573,
36.9922380032924));
#52099=CARTESIAN_POINT('Ctrl Pts',(-4.8648557991442,-1.883593835252,37.0921433937912));
#52100=CARTESIAN_POINT('Ctrl Pts',(-2.76180383778841,-5.11978164217659,
37.2848567355058));
#52101=CARTESIAN_POINT('Ctrl Pts',(2.81416036678732,-5.09119101311223,37.5632805891529));
#52102=CARTESIAN_POINT('Ctrl Pts',(5.80445279005691,-0.384775661901064,
37.8417044428));
#52103=CARTESIAN_POINT('Ctrl Pts',(3.46157018808544,4.67517447107051,38.1201282964472));
#52104=CARTESIAN_POINT('Ctrl Pts',(-2.06182922450441,5.4395390200798,38.3985521500943));
#52105=CARTESIAN_POINT('Ctrl Pts',(-4.73385153164491,2.3223853883346,38.6035562392816));
#52106=CARTESIAN_POINT('Ctrl Pts',(-4.92261734310881,0.346501620743559,
38.7157523772533));
#52107=CARTESIAN_POINT('Ctrl Pts',(-4.91943860138798,0.00445443611122684,
38.7351405640092));
#52108=CARTESIAN_POINT('Origin',(0.,0.,-13.2351405640096));
#52109=CARTESIAN_POINT('',(-4.9168921402267,0.00451136639437725,34.8898594359907));
#52110=CARTESIAN_POINT('',(-4.91256327647705,-0.0033578852818672,35.2351405640092));
#52111=CARTESIAN_POINT('',(-4.91825,6.88216836313478E-12,-13.2351405640096));
#52112=CARTESIAN_POINT('Ctrl Pts',(-4.9168921402267,0.00451136639437716,
34.8898594359907));
#52113=CARTESIAN_POINT('Ctrl Pts',(-4.90601460004845,-1.20829635438866,
34.9585138467616));
#52114=CARTESIAN_POINT('Ctrl Pts',(-3.84052319461895,-4.07735003469892,
35.1199580161093));
#52115=CARTESIAN_POINT('Ctrl Pts',(0.973476361005944,-5.73476937534023,
35.3741919440339));
#52116=CARTESIAN_POINT('Ctrl Pts',(5.3503698512895,-2.28227484501538,35.6525612197641));
#52117=CARTESIAN_POINT('Ctrl Pts',(4.81306709973239,3.26643859688978,35.9309304954944));
#52118=CARTESIAN_POINT('Ctrl Pts',(-0.144931213185082,5.81500051222889,
36.2092997712246));
#52119=CARTESIAN_POINT('Ctrl Pts',(-4.24080783721543,3.44452318441275,36.4456094180567));
#52120=CARTESIAN_POINT('Ctrl Pts',(-4.90834755349023,0.897901568891311,
36.5891293063121));
#52121=CARTESIAN_POINT('Ctrl Pts',(-4.91039451300053,-0.00125559194926225,
36.6398594359907));
#52122=CARTESIAN_POINT('Ctrl Pts',(-4.91256327647705,-0.00335788528186755,
35.2351405640092));
#52123=CARTESIAN_POINT('Ctrl Pts',(-4.91628169557517,-0.597937466264363,
35.2687236293315));
#52124=CARTESIAN_POINT('Ctrl Pts',(-4.54065687035625,-2.83111917892638,
35.3951146458694));
#52125=CARTESIAN_POINT('Ctrl Pts',(-1.20933185427489,-5.69010025994507,
35.614313613623));
#52126=CARTESIAN_POINT('Ctrl Pts',(4.13321975790782,-4.09343607924097,35.8927374672701));
#52127=CARTESIAN_POINT('Ctrl Pts',(5.67813786629717,1.26430806108067,36.1711613209173));
#52128=CARTESIAN_POINT('Ctrl Pts',(2.00594005459731,5.46039641412169,36.4495851745644));
#52129=CARTESIAN_POINT('Ctrl Pts',(-3.3687381414251,4.66035896071285,36.7209115889284));
#52130=CARTESIAN_POINT('Ctrl Pts',(-4.91663974719475,1.50531928252447,36.8994300520767));
#52131=CARTESIAN_POINT('Ctrl Pts',(-4.92514685489251,-0.00223306629119565,
36.9851405640092));
#52132=CARTESIAN_POINT('Origin',(0.,0.,-13.2351405640096));
#52133=CARTESIAN_POINT('',(-4.92620963101609,-0.000809084526366828,33.1398594359907));
#52134=CARTESIAN_POINT('',(-4.91288232756503,0.00352171762486198,33.4851405640093));
#52135=CARTESIAN_POINT('',(-4.91825,6.88216836313478E-12,-13.2351405640096));
#52136=CARTESIAN_POINT('Ctrl Pts',(-4.92620963101609,-0.00080908452636648,
33.1398594359907));
#52137=CARTESIAN_POINT('Ctrl Pts',(-4.92630800682412,-0.0440429370985507,
33.1423188700577));
#52138=CARTESIAN_POINT('Ctrl Pts',(-4.90617996860179,-1.7183136832693,33.2375680627015));
#52139=CARTESIAN_POINT('Ctrl Pts',(-3.01479458062872,-4.97456024693533,
33.425607013922));
#52140=CARTESIAN_POINT('Ctrl Pts',(2.55419833083681,-5.22602209146957,33.7039762896522));
#52141=CARTESIAN_POINT('Ctrl Pts',(5.77721662985775,-0.677498358280351,
33.9823455653825));
#52142=CARTESIAN_POINT('Ctrl Pts',(3.69398937205911,4.49329261598795,34.2607148411128));
#52143=CARTESIAN_POINT('Ctrl Pts',(-1.78208533257483,5.53709381184744,34.539084116843));
#52144=CARTESIAN_POINT('Ctrl Pts',(-4.67447254991247,2.4920528176031,34.7487989818024));
#52145=CARTESIAN_POINT('Ctrl Pts',(-4.92071612200041,0.43087197212862,34.8657240881849));
#52146=CARTESIAN_POINT('Ctrl Pts',(-4.9168921402267,0.00451136639437716,
34.8898594359907));
#52147=CARTESIAN_POINT('Ctrl Pts',(-4.91288232756503,0.0035217176248617,
33.4851405640092));
#52148=CARTESIAN_POINT('Ctrl Pts',(-4.90587829766462,-1.059805706633,33.5452092553706));
#52149=CARTESIAN_POINT('Ctrl Pts',(-4.04385136705686,-3.77635211556013,
33.6980858979476));
#52150=CARTESIAN_POINT('Ctrl Pts',(0.440896414474084,-5.80045988294852,
33.9437704917402));
#52151=CARTESIAN_POINT('Ctrl Pts',(5.11817051857534,-2.76478842676563,34.2221943453874));
#52152=CARTESIAN_POINT('Ctrl Pts',(5.09283092731677,2.81119149965931,34.5006181990345));
#52153=CARTESIAN_POINT('Ctrl Pts',(0.388159848365178,5.80422746229918,34.7790420526816));
#52154=CARTESIAN_POINT('Ctrl Pts',(-4.06266721294199,3.74653450500493,35.0238828410066));
#52155=CARTESIAN_POINT('Ctrl Pts',(-4.90600571704411,1.04520356973813,35.1759156781158));
#52156=CARTESIAN_POINT('Ctrl Pts',(-4.91256327647705,-0.00335788528186755,
35.2351405640092));
#52157=CARTESIAN_POINT('Origin',(0.,0.,-13.2351405640096));
#52158=CARTESIAN_POINT('',(-4.91445289798421,-0.00410312268860868,31.3898594359907));
#52159=CARTESIAN_POINT('',(-4.92540574744767,0.00198995367837004,31.7351405640093));
#52160=CARTESIAN_POINT('',(-4.91825,6.88216836313478E-12,-13.2351405640096));
#52161=CARTESIAN_POINT('Ctrl Pts',(-4.91445289798421,-0.00410312268860874,
31.3898594359907));
#52162=CARTESIAN_POINT('Ctrl Pts',(-4.9184858592771,-0.518003180154603,
31.4189136519305));
#52163=CARTESIAN_POINT('Ctrl Pts',(-4.60746921181795,-2.66837429237667,
31.540757626447));
#52164=CARTESIAN_POINT('Ctrl Pts',(-1.48635567043628,-5.62369832358916,
31.7553913595403));
#52165=CARTESIAN_POINT('Ctrl Pts',(3.92675811827154,-4.29136419968826,32.0337606352706));
#52166=CARTESIAN_POINT('Ctrl Pts',(5.73323152065607,0.982492923299337,32.3121299110009));
#52167=CARTESIAN_POINT('Ctrl Pts',(2.27385871511533,5.35395205035231,32.5904991867312));
#52168=CARTESIAN_POINT('Ctrl Pts',(-3.22498678761868,4.8127489975417,32.8664090283944));
#52169=CARTESIAN_POINT('Ctrl Pts',(-4.92259647513489,1.58708789756534,33.0495291114809));
#52170=CARTESIAN_POINT('Ctrl Pts',(-4.92620963101609,-0.00080908452636648,
33.1398594359907));
#52171=CARTESIAN_POINT('Ctrl Pts',(-4.92540574744767,0.0019899536783699,
31.7351405640093));
#52172=CARTESIAN_POINT('Ctrl Pts',(-4.91761491259624,-1.52019189598326,
31.8216948814096));
#52173=CARTESIAN_POINT('Ctrl Pts',(-3.34297940924432,-4.68844772092739,
32.0010571500257));
#52174=CARTESIAN_POINT('Ctrl Pts',(2.05548484168548,-5.44193959609919,32.2732273698575));
#52175=CARTESIAN_POINT('Ctrl Pts',(5.68939419901335,-1.21264922802275,32.5516512235046));
#52176=CARTESIAN_POINT('Ctrl Pts',(4.09584523280961,4.13083240169122,32.8300750771517));
#52177=CARTESIAN_POINT('Ctrl Pts',(-1.26099724149055,5.67887404851917,33.1084989307988));
#52178=CARTESIAN_POINT('Ctrl Pts',(-4.55347701854424,2.80085553305158,33.3268540930847));
#52179=CARTESIAN_POINT('Ctrl Pts',(-4.91669973643047,0.583067435438709,
33.4524013041548));
#52180=CARTESIAN_POINT('Ctrl Pts',(-4.91288232756503,0.0035217176248617,
33.4851405640092));
#52181=CARTESIAN_POINT('Origin',(0.,0.,-13.2351405640096));
#52182=CARTESIAN_POINT('',(-4.91141405521213,0.00256004678308836,29.6398594359907));
#52183=CARTESIAN_POINT('',(-4.91898260507021,-0.0044993792021053,29.9851405640093));
#52184=CARTESIAN_POINT('',(-4.91825,6.88216836313478E-12,-13.2351405640096));
#52185=CARTESIAN_POINT('Ctrl Pts',(-4.91141405521213,0.00256004678308774,
29.6398594359907));
#52186=CARTESIAN_POINT('Ctrl Pts',(-4.90678101561315,-0.983269338981918,
29.6955084338033));
#52187=CARTESIAN_POINT('Ctrl Pts',(-4.1401952484112,-3.6195129973856,29.8439471901927));
#52188=CARTESIAN_POINT('Ctrl Pts',(0.163218327990816,-5.81451595502028,
30.0851757051587));
#52189=CARTESIAN_POINT('Ctrl Pts',(4.97929477759872,-3.00696849527155,30.363544980889));
#52190=CARTESIAN_POINT('Ctrl Pts',(5.22199922429825,2.56241294782984,30.6419142566192));
#52191=CARTESIAN_POINT('Ctrl Pts',(0.668413007697845,5.77827483466457,30.9202835323496));
#52192=CARTESIAN_POINT('Ctrl Pts',(-3.95974774448338,3.90520013200073,31.16959859214));
#52193=CARTESIAN_POINT('Ctrl Pts',(-4.9056058866944,1.12322721352206,31.3261238933537));
#52194=CARTESIAN_POINT('Ctrl Pts',(-4.91445289798421,-0.00410312268860874,
31.3898594359907));
#52195=CARTESIAN_POINT('Ctrl Pts',(-4.91898260507021,-0.00449937920210593,
29.9851405640093));
#52196=CARTESIAN_POINT('Ctrl Pts',(-4.92230224163488,-0.361517893593529,
30.005372556233));
#52197=CARTESIAN_POINT('Ctrl Pts',(-4.72366297320252,-2.35258394513135,
30.1184124996724));
#52198=CARTESIAN_POINT('Ctrl Pts',(-2.01230599337432,-5.4580535991341,30.3242603943276));
#52199=CARTESIAN_POINT('Ctrl Pts',(3.50391824555016,-4.64352037041854,30.6026842479747));
#52200=CARTESIAN_POINT('Ctrl Pts',(5.80071595908955,0.437514415711182,30.8811081016218));
#52201=CARTESIAN_POINT('Ctrl Pts',(2.76777207587959,5.11655765510094,31.1595319552689));
#52202=CARTESIAN_POINT('Ctrl Pts',(-2.80822167689368,5.0944691102622,31.4379558089161));
#52203=CARTESIAN_POINT('Ctrl Pts',(-4.87269503648718,1.85355398490913,31.6298253451628));
#52204=CARTESIAN_POINT('Ctrl Pts',(-4.9259686428611,0.111969076315626,31.7288869301939));
#52205=CARTESIAN_POINT('Ctrl Pts',(-4.92540574744767,0.0019899536783699,
31.7351405640093));
#52206=CARTESIAN_POINT('Origin',(0.,0.,-13.2351405640096));
#52207=CARTESIAN_POINT('',(-4.92384460879403,0.00312281753491277,27.8898594359907));
#52208=CARTESIAN_POINT('',(-4.9100957742978,9.20690869954388E-5,28.2351405640093));
#52209=CARTESIAN_POINT('',(-4.91825,6.88216836313478E-12,-13.2351405640096));
#52210=CARTESIAN_POINT('Ctrl Pts',(-4.92384460879403,0.00312281753491236,
27.8898594359907));
#52211=CARTESIAN_POINT('Ctrl Pts',(-4.91313914334963,-1.44446164443976,
27.9721032156761));
#52212=CARTESIAN_POINT('Ctrl Pts',(-3.47225634574353,-4.54377938079009,
28.1471367539382));
#52213=CARTESIAN_POINT('Ctrl Pts',(1.79949035101865,-5.53146187642727,28.4149600507771));
#52214=CARTESIAN_POINT('Ctrl Pts',(5.62602862389248,-1.47751072311508,28.6933293265074));
#52215=CARTESIAN_POINT('Ctrl Pts',(4.28518417585832,3.93350131470056,28.9716986022376));
#52216=CARTESIAN_POINT('Ctrl Pts',(-0.991507056211286,5.73167948957902,
29.250067877968));
#52217=CARTESIAN_POINT('Ctrl Pts',(-4.48470808861617,2.95837594561327,29.4727881558856));
#52218=CARTESIAN_POINT('Ctrl Pts',(-4.9145061974271,0.660513555564752,29.6027186752265));
#52219=CARTESIAN_POINT('Ctrl Pts',(-4.91141405521213,0.00256004678308774,
29.6398594359907));
#52220=CARTESIAN_POINT('Ctrl Pts',(-4.9100957742978,9.20690869953694E-5,
28.2351405640093));
#52221=CARTESIAN_POINT('Ctrl Pts',(-4.9099580555162,-0.828071287137276,
28.2818581822721));
#52222=CARTESIAN_POINT('Ctrl Pts',(-4.31787178459561,-3.3016264176408,28.4213837517506));
#52223=CARTESIAN_POINT('Ctrl Pts',(-0.394927824289227,-5.80377088758623,
28.6537172724448));
#52224=CARTESIAN_POINT('Ctrl Pts',(4.6691125779863,-3.46974238756726,28.9321411260919));
#52225=CARTESIAN_POINT('Ctrl Pts',(5.4431371094098,2.0523116016232,29.210564979739));
#52226=CARTESIAN_POINT('Ctrl Pts',(1.215966189542,5.68868620402655,29.4889888333862));
#52227=CARTESIAN_POINT('Ctrl Pts',(-3.74008590277417,4.21382366772307,29.7471806948096));
#52228=CARTESIAN_POINT('Ctrl Pts',(-4.90707444474069,1.27619313853601,29.9125646050173));
#52229=CARTESIAN_POINT('Ctrl Pts',(-4.91898260507021,-0.00449937920210593,
29.9851405640093));
#52230=CARTESIAN_POINT('Origin',(0.,0.,-13.2351405640096));
#52231=CARTESIAN_POINT('',(-4.92121115498267,-0.00412874098909444,26.1398594359907));
#52232=CARTESIAN_POINT('',(-4.91932167294426,0.00446737670234801,26.4851405640093));
#52233=CARTESIAN_POINT('',(-4.91825,6.88216836313478E-12,-13.2351405640096));
#52234=CARTESIAN_POINT('Ctrl Pts',(-4.92121115498267,-0.00412874098909458,
26.1398594359907));
#52235=CARTESIAN_POINT('Ctrl Pts',(-4.92375232237933,-0.286999724354,26.1559082389721));
#52236=CARTESIAN_POINT('Ctrl Pts',(-4.77264664606773,-2.20263914365286,
26.2647468005303));
#52237=CARTESIAN_POINT('Ctrl Pts',(-2.25700960862895,-5.36107672397384,
26.4663751206653));
#52238=CARTESIAN_POINT('Ctrl Pts',(3.28910742006482,-4.79760444316246,26.7447443963955));
#52239=CARTESIAN_POINT('Ctrl Pts',(5.81425211003376,0.17236129132015,27.0231136721258));
#52240=CARTESIAN_POINT('Ctrl Pts',(2.99913497467191,4.98401699610638,27.3014829478561));
#52241=CARTESIAN_POINT('Ctrl Pts',(-2.57062122881967,5.21796344484313,27.5798522235863));
#52242=CARTESIAN_POINT('Ctrl Pts',(-4.83131394241821,2.00616851179972,27.7759777196312));
#52243=CARTESIAN_POINT('Ctrl Pts',(-4.92521735227726,0.188744091725602,
27.8793134570993));
#52244=CARTESIAN_POINT('Ctrl Pts',(-4.92384460879403,0.00312281753491236,
27.8898594359907));
#52245=CARTESIAN_POINT('Ctrl Pts',(-4.91932167294426,0.00446737670234811,
26.4851405640093));
#52246=CARTESIAN_POINT('Ctrl Pts',(-4.90731400357618,-1.28706604896177,
26.5583438083111));
#52247=CARTESIAN_POINT('Ctrl Pts',(-3.72359445036012,-4.23549576657875,
26.7243550038287));
#52248=CARTESIAN_POINT('Ctrl Pts',(1.2543743174442,-5.68034062127683,26.983174150562));
#52249=CARTESIAN_POINT('Ctrl Pts',(5.45687940832144,-2.01548793720741,27.2615980042091));
#52250=CARTESIAN_POINT('Ctrl Pts',(4.64556251996484,3.50121027290405,27.5400218578563));
#52251=CARTESIAN_POINT('Ctrl Pts',(-0.434132268219488,5.80097006333265,
27.8184457115034));
#52252=CARTESIAN_POINT('Ctrl Pts',(-4.32953501880666,3.27920418173089,28.0501519468877));
#52253=CARTESIAN_POINT('Ctrl Pts',(-4.91023164390618,0.817135536779907,
28.1890502310564));
#52254=CARTESIAN_POINT('Ctrl Pts',(-4.9100957742978,9.20690869953694E-5,
28.2351405640093));
#52255=CARTESIAN_POINT('Origin',(0.,0.,-13.2351405640096));
#52256=CARTESIAN_POINT('',(-4.91032113059727,-0.00108994245123004,24.3898594359907));
#52257=CARTESIAN_POINT('',(-4.92521571531249,-0.00217150628855023,24.7351405640093));
#52258=CARTESIAN_POINT('',(-4.91825,6.88216836313478E-12,-13.2351405640096));
#52259=CARTESIAN_POINT('Ctrl Pts',(-4.91032113059727,-0.00108994245122979,
24.3898594359907));
#52260=CARTESIAN_POINT('Ctrl Pts',(-4.91181354648729,-0.756946751686931,
24.4325030208449));
#52261=CARTESIAN_POINT('Ctrl Pts',(-4.39180191053746,-3.15555433076574,
24.5679363642759));
#52262=CARTESIAN_POINT('Ctrl Pts',(-0.650237370706631,-5.78034837838638,
24.7961594662836));
#52263=CARTESIAN_POINT('Ctrl Pts',(4.51066864926873,-3.67275160476199,25.0745287420139));
#52264=CARTESIAN_POINT('Ctrl Pts',(5.52862538900271,1.8081861966767,25.3528980177442));
#52265=CARTESIAN_POINT('Ctrl Pts',(1.46866212239656,5.62834501288036,25.6312672934744));
#52266=CARTESIAN_POINT('Ctrl Pts',(-3.62839605704299,4.35678761453777,25.8935877662233));
#52267=CARTESIAN_POINT('Ctrl Pts',(-4.90905999239607,1.34848239136343,26.0631184803953));
#52268=CARTESIAN_POINT('Ctrl Pts',(-4.92121115498267,-0.00412874098909458,
26.1398594359907));
#52269=CARTESIAN_POINT('Ctrl Pts',(-4.92521571531249,-0.00217150628855014,
24.7351405640093));
#52270=CARTESIAN_POINT('Ctrl Pts',(-4.92588279180187,-0.123194721221349,
24.7420214831345));
#52271=CARTESIAN_POINT('Ctrl Pts',(-4.86688107224675,-1.8758844913496,24.8417103534754));
#52272=CARTESIAN_POINT('Ctrl Pts',(-2.77373655046063,-5.11332671072659,
25.0342071750321));
#52273=CARTESIAN_POINT('Ctrl Pts',(2.80227916848797,-5.09774028014861,25.3126310286793));
#52274=CARTESIAN_POINT('Ctrl Pts',(5.80353964078615,-0.39831161144852,25.5910548823263));
#52275=CARTESIAN_POINT('Ctrl Pts',(3.47246409628408,4.66708877160151,25.8694787359735));
#52276=CARTESIAN_POINT('Ctrl Pts',(-2.04913766389717,5.44433277237802,26.1479025896206));
#52277=CARTESIAN_POINT('Ctrl Pts',(-4.73125224331919,2.33013357115337,26.3531231989659));
#52278=CARTESIAN_POINT('Ctrl Pts',(-4.9225374708358,0.350355520336658,26.4655358570954));
#52279=CARTESIAN_POINT('Ctrl Pts',(-4.91932167294426,0.00446737670234811,
26.4851405640093));
#52280=CARTESIAN_POINT('Origin',(0.,0.,-13.2351405640096));
#52281=CARTESIAN_POINT('',(-4.91719942584508,0.00452867428901858,22.6398594359907));
#52282=CARTESIAN_POINT('',(-4.91264357795,-0.00340089404915922,22.9851405640093));
#52283=CARTESIAN_POINT('',(-4.91825,6.88216836313478E-12,-13.2351405640096));
#52284=CARTESIAN_POINT('Ctrl Pts',(-4.91719942584508,0.0045286742890192,
22.6398594359907));
#52285=CARTESIAN_POINT('Ctrl Pts',(-4.90612996717293,-1.21840033721416,
22.7090978027177));
#52286=CARTESIAN_POINT('Ctrl Pts',(-3.82588241968382,-4.09768835375591,
22.8711259280215));
#52287=CARTESIAN_POINT('Ctrl Pts',(1.00952794474132,-5.72853291363189,23.1259438119021));
#52288=CARTESIAN_POINT('Ctrl Pts',(5.36461918091565,-2.24857667370483,23.4043130876322));
#52289=CARTESIAN_POINT('Ctrl Pts',(4.79242648149282,3.29664745359036,23.6826823633626));
#52290=CARTESIAN_POINT('Ctrl Pts',(-0.181503828456812,5.8139738883171,23.9610516390928));
#52291=CARTESIAN_POINT('Ctrl Pts',(-4.25230501364173,3.42370234687152,24.1967773299688));
#52292=CARTESIAN_POINT('Ctrl Pts',(-4.90856614337602,0.887750125635713,
24.3397132622682));
#52293=CARTESIAN_POINT('Ctrl Pts',(-4.91032113059727,-0.00108994245122979,
24.3898594359907));
#52294=CARTESIAN_POINT('Ctrl Pts',(-4.91264357795,-0.00340089404915991,
22.9851405640093));
#52295=CARTESIAN_POINT('Ctrl Pts',(-4.916389164947,-0.594122806234998,23.0185071091736));
#52296=CARTESIAN_POINT('Ctrl Pts',(-4.54396316738755,-2.82335358446512,
23.1446816055536));
#52297=CARTESIAN_POINT('Ctrl Pts',(-1.222598871385,-5.68726441285079,23.3636640531493));
#52298=CARTESIAN_POINT('Ctrl Pts',(4.12366191086833,-4.10306433618151,23.6420879067964));
#52299=CARTESIAN_POINT('Ctrl Pts',(5.68107101131397,1.25106221523925,23.9205117604436));
#52300=CARTESIAN_POINT('Ctrl Pts',(2.01866919589476,5.45570336249478,24.1989356140907));
#52301=CARTESIAN_POINT('Ctrl Pts',(-3.36215071414575,4.66757434112606,24.4704785486126));
#52302=CARTESIAN_POINT('Ctrl Pts',(-4.91688544694772,1.50913323134417,24.6492135319188));
#52303=CARTESIAN_POINT('Ctrl Pts',(-4.92521571531249,-0.00217150628855014,
24.7351405640093));
#52304=CARTESIAN_POINT('Origin',(0.,0.,-13.2351405640096));
#52305=CARTESIAN_POINT('',(-4.92612628624265,-0.000997778412739117,20.8898594359907));
#52306=CARTESIAN_POINT('',(-4.91279890386086,0.00348065594282992,21.2351405640093));
#52307=CARTESIAN_POINT('',(-4.91825,6.88216836313478E-12,-13.2351405640096));
#52308=CARTESIAN_POINT('Ctrl Pts',(-4.92612628624265,-0.000997778412738558,
20.8898594359907));
#52309=CARTESIAN_POINT('Ctrl Pts',(-4.9262742113422,-0.0544992921925554,
20.8929028260137));
#52310=CARTESIAN_POINT('Ctrl Pts',(-4.90121217819937,-1.73906368377049,
20.9887359746135));
#52311=CARTESIAN_POINT('Ctrl Pts',(-2.98344570524222,-4.99342444997913,
21.1773588817902));
#52312=CARTESIAN_POINT('Ctrl Pts',(2.58701870162035,-5.20985318902981,21.4557281575204));
#52313=CARTESIAN_POINT('Ctrl Pts',(5.7813637121742,-0.641147129240114,21.7340974332507));
#52314=CARTESIAN_POINT('Ctrl Pts',(3.66565416262452,4.51643837263511,22.0124667089809));
#52315=CARTESIAN_POINT('Ctrl Pts',(-1.81687757128598,5.5257752311088,22.2908359847112));
#52316=CARTESIAN_POINT('Ctrl Pts',(-4.68205429258674,2.47113126762697,22.4999668937145));
#52317=CARTESIAN_POINT('Ctrl Pts',(-4.92096469604245,0.420507295909191,
22.616308044141));
#52318=CARTESIAN_POINT('Ctrl Pts',(-4.91719942584508,0.0045286742890192,
22.6398594359907));
#52319=CARTESIAN_POINT('Ctrl Pts',(-4.91279890386086,0.00348065594282986,
21.2351405640093));
#52320=CARTESIAN_POINT('Ctrl Pts',(-4.90590889642109,-1.05605914474809,
21.2949927352127));
#52321=CARTESIAN_POINT('Ctrl Pts',(-4.04869927458494,-3.76870392438603,
21.4476528576317));
#52322=CARTESIAN_POINT('Ctrl Pts',(0.427367531648445,-5.80147235578038,
21.6931209312665));
#52323=CARTESIAN_POINT('Ctrl Pts',(5.1117086309249,-2.77671737390015,21.9715447849137));
#52324=CARTESIAN_POINT('Ctrl Pts',(5.09937326597762,2.79930648486794,22.2499686385608));
#52325=CARTESIAN_POINT('Ctrl Pts',(0.401695263205706,5.80330642112832,22.5283924922079));
#52326=CARTESIAN_POINT('Ctrl Pts',(-4.05785882761375,3.75418866842352,22.7734498006908));
#52327=CARTESIAN_POINT('Ctrl Pts',(-4.90597093754048,1.04895082150337,22.9256991579579));
#52328=CARTESIAN_POINT('Ctrl Pts',(-4.91264357795,-0.00340089404915991,
22.9851405640093));
#52329=CARTESIAN_POINT('Origin',(0.,0.,-13.2351405640096));
#52330=CARTESIAN_POINT('',(-4.91418689020212,-0.00402515463966349,19.1398594359907));
#52331=CARTESIAN_POINT('',(-4.92534177178078,0.00205314599783006,19.4851405640093));
#52332=CARTESIAN_POINT('',(-4.91825,6.88216836313478E-12,-13.2351405640096));
#52333=CARTESIAN_POINT('Ctrl Pts',(-4.91418689020212,-0.00402515463966295,
19.1398594359907));
#52334=CARTESIAN_POINT('Ctrl Pts',(-4.91820769545533,-0.528325596070794,
19.1694976078865));
#52335=CARTESIAN_POINT('Ctrl Pts',(-4.59913644360476,-2.68931479280248,
19.2919255383591));
#52336=CARTESIAN_POINT('Ctrl Pts',(-1.45095404829527,-5.63293603403351,
19.5071432274085));
#52337=CARTESIAN_POINT('Ctrl Pts',(3.95367247989527,-4.26658059053105,19.7855125031388));
#52338=CARTESIAN_POINT('Ctrl Pts',(5.72693837654226,1.01853465579974,20.063881778869));
#52339=CARTESIAN_POINT('Ctrl Pts',(2.24013817879126,5.36814837292146,20.3422510545993));
#52340=CARTESIAN_POINT('Ctrl Pts',(-3.24356373581575,4.79358773299822,20.6175769403066));
#52341=CARTESIAN_POINT('Ctrl Pts',(-4.92176413075087,1.57670555159041,20.800113067437));
#52342=CARTESIAN_POINT('Ctrl Pts',(-4.92612628624265,-0.000997778412738558,
20.8898594359907));
#52343=CARTESIAN_POINT('Ctrl Pts',(-4.92534177178078,0.00205314599783015,
19.4851405640093));
#52344=CARTESIAN_POINT('Ctrl Pts',(-4.91736014737601,-1.516373211075,19.5714783612517));
#52345=CARTESIAN_POINT('Ctrl Pts',(-3.34961135330605,-4.68124800098687,
19.7506241097099));
#52346=CARTESIAN_POINT('Ctrl Pts',(2.04278769977008,-5.44671854566206,20.0225778093838));
#52347=CARTESIAN_POINT('Ctrl Pts',(5.68655061714523,-1.22591458945406,20.3010016630309));
#52348=CARTESIAN_POINT('Ctrl Pts',(4.10546791546748,4.12126894257805,20.579425516678));
#52349=CARTESIAN_POINT('Ctrl Pts',(-1.2477496877477,5.68179947012534,20.8578493703251));
#52350=CARTESIAN_POINT('Ctrl Pts',(-4.55020400913313,2.80862120793031,21.0764210527689));
#52351=CARTESIAN_POINT('Ctrl Pts',(-4.91659267716771,0.586884062767262,
21.202184783997));
#52352=CARTESIAN_POINT('Ctrl Pts',(-4.91279890386086,0.00348065594282986,
21.2351405640093));
#52353=CARTESIAN_POINT('Origin',(0.,0.,-13.2351405640096));
#52354=CARTESIAN_POINT('',(-4.91158062171437,0.00270053279499022,17.3898594359907));
#52355=CARTESIAN_POINT('',(-4.91909967221345,-0.00448925516201348,17.7351405640093));
#52356=CARTESIAN_POINT('',(-4.91825,6.88216836313478E-12,-13.2351405640096));
#52357=CARTESIAN_POINT('Ctrl Pts',(-4.91158062171437,0.00270053279499041,
17.3898594359907));
#52358=CARTESIAN_POINT('Ctrl Pts',(-4.90663216249858,-0.993389185122712,
17.4460923897593));
#52359=CARTESIAN_POINT('Ctrl Pts',(-4.127797895462,-3.64023466456982,17.5951151021047));
#52360=CARTESIAN_POINT('Ctrl Pts',(0.199787533727289,-5.81337431748075,
17.8369275730269));
#52361=CARTESIAN_POINT('Ctrl Pts',(4.99810966208265,-2.97558999520659,18.1152968487571));
#52362=CARTESIAN_POINT('Ctrl Pts',(5.20577873272567,2.59520785288553,18.3936661244875));
#52363=CARTESIAN_POINT('Ctrl Pts',(0.632055302428017,5.78236475055406,18.6720354002177));
#52364=CARTESIAN_POINT('Ctrl Pts',(-3.97342008071557,3.88467195111445,18.9207665040521));
#52365=CARTESIAN_POINT('Ctrl Pts',(-4.90561955236608,1.11312892929739,19.0767078493098));
#52366=CARTESIAN_POINT('Ctrl Pts',(-4.91418689020212,-0.00402515463966295,
19.1398594359907));
#52367=CARTESIAN_POINT('Ctrl Pts',(-4.91909967221345,-0.00448925516201404,
17.7351405640093));
#52368=CARTESIAN_POINT('Ctrl Pts',(-4.92238407305303,-0.357665457469601,
17.7551560360751));
#52369=CARTESIAN_POINT('Ctrl Pts',(-4.72629246046279,-2.34483425780271,
17.8679794593566));
#52370=CARTESIAN_POINT('Ctrl Pts',(-2.02502965350643,-5.45334570739934,
18.0736108338538));
#52371=CARTESIAN_POINT('Ctrl Pts',(3.49307921743211,-4.65167949054264,18.352034687501));
#52372=CARTESIAN_POINT('Ctrl Pts',(5.80172054381419,0.4239849448688,18.6304585411481));
#52373=CARTESIAN_POINT('Ctrl Pts',(2.77969725342115,5.11008881344677,18.9088823947953));
#52374=CARTESIAN_POINT('Ctrl Pts',(-2.79633284965052,5.10100451832347,19.1873062484423));
#52375=CARTESIAN_POINT('Ctrl Pts',(-4.8706972056682,1.86126106698695,19.379392304847));
#52376=CARTESIAN_POINT('Ctrl Pts',(-4.92593991466264,0.115844007487335,
19.478670410036));
#52377=CARTESIAN_POINT('Ctrl Pts',(-4.92534177178078,0.00205314599783015,
19.4851405640093));
#52378=CARTESIAN_POINT('Origin',(0.,0.,-13.2351405640096));
#52379=CARTESIAN_POINT('',(-4.92408796408552,0.00298446262078338,15.6398594359907));
#52380=CARTESIAN_POINT('',(-4.9100940628477,2.85129012446328E-5,15.9851405640093));
#52381=CARTESIAN_POINT('',(-4.91825,6.88216836313478E-12,-13.2351405640096));
#52382=CARTESIAN_POINT('Ctrl Pts',(-4.92408796408553,0.00298446262078356,
15.6398594359907));
#52383=CARTESIAN_POINT('Ctrl Pts',(-4.91367855042134,-1.45468920093622,
15.7226871716321));
#52384=CARTESIAN_POINT('Ctrl Pts',(-3.45511568541442,-4.56344829093663,
15.8983046658504));
#52385=CARTESIAN_POINT('Ctrl Pts',(1.83424682140562,-5.52003393213674,16.1667119186453));
#52386=CARTESIAN_POINT('Ctrl Pts',(5.63521065484668,-1.44209461869877,16.4450811943755));
#52387=CARTESIAN_POINT('Ctrl Pts',(4.26035827525457,3.96037667151086,16.7234504701058));
#52388=CARTESIAN_POINT('Ctrl Pts',(-1.02753884835743,5.7253296786206,17.0018197458361));
#52389=CARTESIAN_POINT('Ctrl Pts',(-4.49411412142162,2.93743814234507,17.2239560677977));
#52390=CARTESIAN_POINT('Ctrl Pts',(-4.91479759406829,0.65025423483065,17.3533026311826));
#52391=CARTESIAN_POINT('Ctrl Pts',(-4.91158062171437,0.00270053279499041,
17.3898594359907));
#52392=CARTESIAN_POINT('Ctrl Pts',(-4.91009437976676,2.85117933054163E-5,
15.9851405640093));
#52393=CARTESIAN_POINT('Ctrl Pts',(-4.91005192958233,-0.824297174460165,
16.0316416621142));
#52394=CARTESIAN_POINT('Ctrl Pts',(-4.32190952287306,-3.29388776939099,
16.1709507114348));
#52395=CARTESIAN_POINT('Ctrl Pts',(-0.408462155912262,-5.8028340635571,
16.4030677119711));
#52396=CARTESIAN_POINT('Ctrl Pts',(4.66100783600869,-3.48062213614987,16.6814915656182));
#52397=CARTESIAN_POINT('Ctrl Pts',(5.4479086551669,2.03961167552763,16.9599154192653));
#52398=CARTESIAN_POINT('Ctrl Pts',(1.22922989078505,5.68583488835121,17.2383392729125));
#52399=CARTESIAN_POINT('Ctrl Pts',(-3.73440738737732,4.22130761444361,17.4967476544938));
#52400=CARTESIAN_POINT('Ctrl Pts',(-4.90715492872457,1.27994566889007,17.6623480848594));
#52401=CARTESIAN_POINT('Ctrl Pts',(-4.91909967221345,-0.00448925516201404,
17.7351405640093));
#52402=CARTESIAN_POINT('Origin',(0.,0.,-13.2351405640096));
#52403=CARTESIAN_POINT('',(-4.92090615674067,-0.00420134538231084,13.8898594359907));
#52404=CARTESIAN_POINT('',(-4.91920467447417,0.00447934526514732,14.2351405640093));
#52405=CARTESIAN_POINT('',(-4.91825,6.88216836313478E-12,-13.2351405640096));
#52406=CARTESIAN_POINT('Ctrl Pts',(-4.92090615674067,-0.00420134538231042,
13.8898594359907));
#52407=CARTESIAN_POINT('Ctrl Pts',(-4.92356576649449,-0.297411916716882,
13.9064921949282));
#52408=CARTESIAN_POINT('Ctrl Pts',(-4.76604114686728,-2.22351334540009,
14.0159147124424));
#52409=CARTESIAN_POINT('Ctrl Pts',(-2.22324459247222,-5.3751669272517,14.2181269885334));
#52410=CARTESIAN_POINT('Ctrl Pts',(3.31921857055293,-4.77682154729211,14.4964962642637));
#52411=CARTESIAN_POINT('Ctrl Pts',(5.81305296984359,0.208928656651545,14.774865539994));
#52412=CARTESIAN_POINT('Ctrl Pts',(2.96772692751709,5.00278251550746,15.0532348157242));
#52413=CARTESIAN_POINT('Ctrl Pts',(-2.60339058705663,5.2016914042456,15.3316040914545));
#52414=CARTESIAN_POINT('Ctrl Pts',(-4.83716603141205,1.98534572792005,15.5271456315433));
#52415=CARTESIAN_POINT('Ctrl Pts',(-4.92533994588682,0.178304702346117,
15.6298974130554));
#52416=CARTESIAN_POINT('Ctrl Pts',(-4.92408796408553,0.00298446262078356,
15.6398594359907));
#52417=CARTESIAN_POINT('Ctrl Pts',(-4.91920467447417,0.00447934526514739,
14.2351405640093));
#52418=CARTESIAN_POINT('Ctrl Pts',(-4.90722910644829,-1.28331256696772,
14.3081272881532));
#52419=CARTESIAN_POINT('Ctrl Pts',(-3.72930065287923,-4.22801859829677,
14.4739219635129));
#52420=CARTESIAN_POINT('Ctrl Pts',(1.2411233614091,-5.68325059308101,14.7325245900883));
#52421=CARTESIAN_POINT('Ctrl Pts',(5.45216409893207,-2.0282088502685,15.0109484437354));
#52422=CARTESIAN_POINT('Ctrl Pts',(4.65371531907096,3.49036648950155,15.2893722973825));
#52423=CARTESIAN_POINT('Ctrl Pts',(-0.420602213959508,5.80196675960862,
15.5677961510297));
#52424=CARTESIAN_POINT('Ctrl Pts',(-4.32552115167899,3.2869445013678,15.7997189065719));
#52425=CARTESIAN_POINT('Ctrl Pts',(-4.91013665262773,0.820910814028876,
15.9388337108985));
#52426=CARTESIAN_POINT('Ctrl Pts',(-4.91009437976676,2.85117933054163E-5,
15.9851405640093));
#52427=CARTESIAN_POINT('Origin',(0.,0.,-13.2351405640096));
#52428=CARTESIAN_POINT('',(-4.91025820404979,-0.000922789237043502,12.1398594359907));
#52429=CARTESIAN_POINT('',(-4.92528291799711,-0.00210936955439167,12.4851405640093));
#52430=CARTESIAN_POINT('',(-4.91825,6.88216836313478E-12,-13.2351405640096));
#52431=CARTESIAN_POINT('Ctrl Pts',(-4.91025820404979,-0.000922789237043017,
12.1398594359907));
#52432=CARTESIAN_POINT('Ctrl Pts',(-4.91153813360514,-0.767154694837722,
12.183086976801));
#52433=CARTESIAN_POINT('Ctrl Pts',(-4.38148269050377,-3.17645995727246,
12.319104276188));
#52434=CARTESIAN_POINT('Ctrl Pts',(-0.613866982695112,-5.78432393122432,
12.5479113341518));
#52435=CARTESIAN_POINT('Ctrl Pts',(4.53368047982022,-3.64430752279149,12.8262806098821));
#52436=CARTESIAN_POINT('Ctrl Pts',(5.51714280525491,1.84292465396758,13.1046498856123));
#52437=CARTESIAN_POINT('Ctrl Pts',(1.43323162327729,5.63747134164028,13.3830191613426));
#52438=CARTESIAN_POINT('Ctrl Pts',(-3.64439920708976,4.33678131162103,13.6447556781354));
#52439=CARTESIAN_POINT('Ctrl Pts',(-4.90872850781162,1.33833223303946,13.8137024363514));
#52440=CARTESIAN_POINT('Ctrl Pts',(-4.92090615674067,-0.00420134538231042,
13.8898594359907));
#52441=CARTESIAN_POINT('Ctrl Pts',(-4.92528291799711,-0.0021093695543929,
12.4851405640093));
#52442=CARTESIAN_POINT('Ctrl Pts',(-4.92591332939639,-0.119320139238976,
12.4918049629766));
#52443=CARTESIAN_POINT('Ctrl Pts',(-4.86889685925445,-1.86817592601175,
12.5912773131596));
#52444=CARTESIAN_POINT('Ctrl Pts',(-2.78565417665601,-5.10684396766439,
12.7835576145584));
#52445=CARTESIAN_POINT('Ctrl Pts',(2.79038272846711,-5.10426182034811,13.0619814682055));
#52446=CARTESIAN_POINT('Ctrl Pts',(5.80259492580427,-0.411845394561442,
13.3404053218526));
#52447=CARTESIAN_POINT('Ctrl Pts',(3.48333911759557,4.65897768762844,13.6188291754998));
#52448=CARTESIAN_POINT('Ctrl Pts',(-2.03643495793874,5.4490969127073,13.8972530291469));
#52449=CARTESIAN_POINT('Ctrl Pts',(-4.72864254700507,2.33788227941386,14.1026901586501));
#52450=CARTESIAN_POINT('Ctrl Pts',(-4.9224569159734,0.354208918867955,14.2153193369375));
#52451=CARTESIAN_POINT('Ctrl Pts',(-4.91920467447417,0.00447934526514739,
14.2351405640093));
#52452=CARTESIAN_POINT('Origin',(0.,0.,-13.2351405640096));
#52453=CARTESIAN_POINT('',(-4.91750913335068,0.00453909766118435,10.3898594359907));
#52454=CARTESIAN_POINT('',(-4.91272496910331,-0.00344323922728262,10.7351405640093));
#52455=CARTESIAN_POINT('',(-4.91825,6.88216836313478E-12,-13.2351405640096));
#52456=CARTESIAN_POINT('Ctrl Pts',(-4.91750913335068,0.00453909766118428,
10.3898594359907));
#52457=CARTESIAN_POINT('Ctrl Pts',(-4.90626050624057,-1.22850621016978,
10.4596817586738));
#52458=CARTESIAN_POINT('Ctrl Pts',(-3.81113729750009,-4.11800395470607,
10.6222938399336));
#52459=CARTESIAN_POINT('Ctrl Pts',(1.04553958891947,-5.72206981622731,10.8776956797702));
#52460=CARTESIAN_POINT('Ctrl Pts',(5.37865627222158,-2.214789542839,11.1560649555005));
#52461=CARTESIAN_POINT('Ctrl Pts',(4.77159626236785,3.32672588632348,11.4344342312307));
#52462=CARTESIAN_POINT('Ctrl Pts',(-0.218069262963983,5.81271724844138,
11.712803506961));
#52463=CARTESIAN_POINT('Ctrl Pts',(-4.2637084465507,3.40287291834831,11.947945241881));
#52464=CARTESIAN_POINT('Ctrl Pts',(-4.90879071026785,0.877594745028542,
12.0902972182242));
#52465=CARTESIAN_POINT('Ctrl Pts',(-4.91025820404979,-0.000922789237043017,
12.1398594359907));
#52466=CARTESIAN_POINT('Ctrl Pts',(-4.91272496910331,-0.00344323922728276,
10.7351405640093));
#52467=CARTESIAN_POINT('Ctrl Pts',(-4.91649650272064,-0.590307466122425,
10.7682905890157));
#52468=CARTESIAN_POINT('Ctrl Pts',(-4.54725795767594,-2.81558795146297,
10.8942485652378));
#52469=CARTESIAN_POINT('Ctrl Pts',(-1.23585923872538,-5.68439763247154,
11.1130144926756));
#52470=CARTESIAN_POINT('Ctrl Pts',(4.11408163504771,-4.11267027637206,11.3914383463227));
#52471=CARTESIAN_POINT('Ctrl Pts',(5.683973256732,1.23780956481465,11.6698621999699));
#52472=CARTESIAN_POINT('Ctrl Pts',(2.03138735756037,5.45098063705376,11.948286053617));
#52473=CARTESIAN_POINT('Ctrl Pts',(-3.35554793119657,4.67478434679984,12.2200455082968));
#52474=CARTESIAN_POINT('Ctrl Pts',(-4.91713426459589,1.51294879426531,12.3989970117609));
#52475=CARTESIAN_POINT('Ctrl Pts',(-4.92528291799711,-0.0021093695543929,
12.4851405640093));
#52476=CARTESIAN_POINT('Origin',(0.,0.,-13.2351405640096));
#52477=CARTESIAN_POINT('',(-4.92602698002101,-0.00118436696873579,8.63985943599069));
#52478=CARTESIAN_POINT('',(-4.91271654582281,0.00343891372668881,8.98514056400927));
#52479=CARTESIAN_POINT('',(-4.91825,6.88216836313478E-12,-13.2351405640096));
#52480=CARTESIAN_POINT('Ctrl Pts',(-4.92602698002101,-0.00118436696873587,
8.6398594359907));
#52481=CARTESIAN_POINT('Ctrl Pts',(-4.92623328301914,-0.0649550216871807,
8.64348678196981));
#52482=CARTESIAN_POINT('Ctrl Pts',(-4.89617722538597,-1.75981957052431,
8.73990388652567));
#52483=CARTESIAN_POINT('Ctrl Pts',(-2.9519787969659,-5.01209110013389,8.92911074965828));
#52484=CARTESIAN_POINT('Ctrl Pts',(2.61973672319965,-5.19347817121596,9.20748002538857));
#52485=CARTESIAN_POINT('Ctrl Pts',(5.7852820686703,-0.60477053474805,9.48584930111882));
#52486=CARTESIAN_POINT('Ctrl Pts',(3.63717393035499,4.53940544720601,9.7642185768491));
#52487=CARTESIAN_POINT('Ctrl Pts',(-1.8515979295839,5.51423803629642,10.0425878525794));
#52488=CARTESIAN_POINT('Ctrl Pts',(-4.68955809926782,2.45021259625737,10.2511348056266));
#52489=CARTESIAN_POINT('Ctrl Pts',(-4.921209269813,0.410138452901258,10.366892000097));
#52490=CARTESIAN_POINT('Ctrl Pts',(-4.91750913335068,0.00453909766118428,
10.3898594359907));
#52491=CARTESIAN_POINT('Ctrl Pts',(-4.91271654582281,0.00343891372668881,
8.98514056400927));
#52492=CARTESIAN_POINT('Ctrl Pts',(-4.90594095198635,-1.05231235329147,
9.04477621505475));
#52493=CARTESIAN_POINT('Ctrl Pts',(-4.05353352444506,-3.76105365087587,
9.19721981731594));
#52494=CARTESIAN_POINT('Ctrl Pts',(0.413836324351832,-5.80245327414518,
9.44247137079281));
#52495=CARTESIAN_POINT('Ctrl Pts',(5.10521894046314,-2.78863121834486,9.72089522443996));
#52496=CARTESIAN_POINT('Ctrl Pts',(5.10588786891966,2.78740624452375,9.99931907808708));
#52497=CARTESIAN_POINT('Ctrl Pts',(0.415228493207719,5.80235381551483,10.2777429317342));
#52498=CARTESIAN_POINT('Ctrl Pts',(-4.05303681619496,3.7618407912721,10.5230167603749));
#52499=CARTESIAN_POINT('Ctrl Pts',(-4.90593758736845,1.05269782661613,10.6754826378));
#52500=CARTESIAN_POINT('Ctrl Pts',(-4.91272496910331,-0.00344323922728276,
10.7351405640093));
#52501=CARTESIAN_POINT('Origin',(0.,0.,-13.2351405640096));
#52502=CARTESIAN_POINT('',(-4.9139270378835,-0.00394135086111479,6.88985943599069));
#52503=CARTESIAN_POINT('',(-4.92527608168861,0.00211578826967762,7.23514056400927));
#52504=CARTESIAN_POINT('',(-4.91825,6.88216836313478E-12,-13.2351405640096));
#52505=CARTESIAN_POINT('Ctrl Pts',(-4.9139270378835,-0.00394135086111511,
6.88985943599069));
#52506=CARTESIAN_POINT('Ctrl Pts',(-4.9179273163929,-0.538643264396417,
6.9200815638426));
#52507=CARTESIAN_POINT('Ctrl Pts',(-4.59072219571754,-2.71025635333059,
7.04309345027126));
#52508=CARTESIAN_POINT('Ctrl Pts',(-1.41549502262945,-5.64195089084342,
7.25889509527668));
#52509=CARTESIAN_POINT('Ctrl Pts',(3.98043042392857,-4.24162818432278,7.53726437100694));
#52510=CARTESIAN_POINT('Ctrl Pts',(5.72041865981625,1.05453609241393,7.81563364673722));
#52511=CARTESIAN_POINT('Ctrl Pts',(2.20632901676084,5.38213231754632,8.09400292246748));
#52512=CARTESIAN_POINT('Ctrl Pts',(-3.2620276900715,4.77438313269691,8.36874485221864));
#52513=CARTESIAN_POINT('Ctrl Pts',(-4.92095592444886,1.56633785461507,8.55069702339305));
#52514=CARTESIAN_POINT('Ctrl Pts',(-4.92602698002101,-0.00118436696873587,
8.6398594359907));
#52515=CARTESIAN_POINT('Ctrl Pts',(-4.92527608168861,0.00211578826967746,
7.23514056400927));
#52516=CARTESIAN_POINT('Ctrl Pts',(-4.91710852250278,-1.5125561816081,7.32126184109382));
#52517=CARTESIAN_POINT('Ctrl Pts',(-3.35622792132889,-4.67404284470821,
7.50019106939408));
#52518=CARTESIAN_POINT('Ctrl Pts',(2.03007944704129,-5.45146787027966,7.77192824891004));
#52519=CARTESIAN_POINT('Ctrl Pts',(5.68367610587452,-1.23917328308113,8.05035210255719));
#52520=CARTESIAN_POINT('Ctrl Pts',(4.11506826830211,4.1116830676992,8.32877595620429));
#52521=CARTESIAN_POINT('Ctrl Pts',(-1.23449534743867,5.68469398817063,8.60719980985145));
#52522=CARTESIAN_POINT('Ctrl Pts',(-4.54691952667732,2.81638686581082,8.82598801245309));
#52523=CARTESIAN_POINT('Ctrl Pts',(-4.9164854664036,0.590700012090972,8.95196826383904));
#52524=CARTESIAN_POINT('Ctrl Pts',(-4.91271654582281,0.00343891372668881,
8.98514056400927));
#52525=CARTESIAN_POINT('Origin',(0.,0.,-13.2351405640096));
#52526=CARTESIAN_POINT('',(-4.91175629129765,0.0028372364354037,5.13985943599068));
#52527=CARTESIAN_POINT('',(-4.91921671359201,-0.00447815882576141,5.48514056400926));
#52528=CARTESIAN_POINT('',(-4.91825,6.88216836313478E-12,-13.2351405640096));
#52529=CARTESIAN_POINT('Ctrl Pts',(-4.91175629129765,0.00283723643540366,
5.13985943599068));
#52530=CARTESIAN_POINT('Ctrl Pts',(-4.90649215527958,-1.00350635860451,
5.19667634571539));
#52531=CARTESIAN_POINT('Ctrl Pts',(-4.11530325360641,-3.66094378176031,
5.34628301401685));
#52532=CARTESIAN_POINT('Ctrl Pts',(0.236348835348182,-5.81200268769786,
5.58867944089506));
#52533=CARTESIAN_POINT('Ctrl Pts',(5.01672680831839,-2.94409377304407,5.86704871662534));
#52534=CARTESIAN_POINT('Ctrl Pts',(5.18935228697503,2.62790008475296,6.1454179923556));
#52535=CARTESIAN_POINT('Ctrl Pts',(0.59567259140266,5.78622590101952,6.42378726808587));
#52536=CARTESIAN_POINT('Ctrl Pts',(-3.98699126429463,3.86412609996948,6.67193441596424));
#52537=CARTESIAN_POINT('Ctrl Pts',(-4.90564542549013,1.10303007212689,6.82729180526584));
#52538=CARTESIAN_POINT('Ctrl Pts',(-4.9139270378835,-0.00394135086111511,
6.88985943599069));
#52539=CARTESIAN_POINT('Ctrl Pts',(-4.91921671359201,-0.00447815882576173,
5.48514056400926));
#52540=CARTESIAN_POINT('Ctrl Pts',(-4.92246523460304,-0.35381251212689,
5.50493951591718));
#52541=CARTESIAN_POINT('Ctrl Pts',(-4.72891150816308,-2.33708508363489,
5.6175464190408));
#52542=CARTESIAN_POINT('Ctrl Pts',(-2.03774229941179,-5.44860815467391,
5.82296127338016));
#52543=CARTESIAN_POINT('Ctrl Pts',(3.48222119030037,-4.65981330997436,6.10138512702726));
#52544=CARTESIAN_POINT('Ctrl Pts',(5.8026935727219,0.410453167953449,6.37980898067441));
#52545=CARTESIAN_POINT('Ctrl Pts',(2.79160731206521,5.10359217779156,6.65823283432152));
#52546=CARTESIAN_POINT('Ctrl Pts',(-2.78442881302834,5.10751218179347,6.93665668796867));
#52547=CARTESIAN_POINT('Ctrl Pts',(-4.86868991641874,1.86896893191072,7.12895926453124));
#52548=CARTESIAN_POINT('Ctrl Pts',(-4.92591023167537,0.119718757257634,
7.22845388987811));
#52549=CARTESIAN_POINT('Ctrl Pts',(-4.92527608168861,0.00211578826967746,
7.23514056400927));
#52550=CARTESIAN_POINT('Origin',(0.,0.,-13.2351405640096));
#52551=CARTESIAN_POINT('',(-4.92432229863308,0.00284067633764219,3.38985943599068));
#52552=CARTESIAN_POINT('',(-4.91009411058386,-3.50523742971845E-5,3.73514056400927));
#52553=CARTESIAN_POINT('',(-4.91825,6.88216836313478E-12,-13.2351405640096));
#52554=CARTESIAN_POINT('Ctrl Pts',(-4.92432229863308,0.00284067633764233,
3.38985943599068));
#52555=CARTESIAN_POINT('Ctrl Pts',(-4.91423935983455,-1.46492632453142,
3.47327112758818));
#52556=CARTESIAN_POINT('Ctrl Pts',(-3.43786451232597,-4.58308142280596,
3.64947257776244));
#52557=CARTESIAN_POINT('Ctrl Pts',(1.86893072420659,-5.50838760091319,3.91846378651344));
#52558=CARTESIAN_POINT('Ctrl Pts',(5.64416974217652,-1.40662146125979,4.19683306224373));
#52559=CARTESIAN_POINT('Ctrl Pts',(4.23536382377072,3.98709534549548,4.47520233797398));
#52560=CARTESIAN_POINT('Ctrl Pts',(-1.06352998838801,5.71875335869428,4.75357161370427));
#52561=CARTESIAN_POINT('Ctrl Pts',(-4.50343455021169,2.91649876511814,4.97512397970982));
#52562=CARTESIAN_POINT('Ctrl Pts',(-4.91508920697772,0.639989911809819,
5.10388658713863));
#52563=CARTESIAN_POINT('Ctrl Pts',(-4.91175629129765,0.00283723643540366,
5.13985943599068));
#52564=CARTESIAN_POINT('Ctrl Pts',(-4.91009445539168,-3.50508923821491E-5,
3.73514056400927));
#52565=CARTESIAN_POINT('Ctrl Pts',(-4.91014639846267,-0.820522449457762,
3.78142514195625));
#52566=CARTESIAN_POINT('Ctrl Pts',(-4.32593467034914,-3.28614823268589,
3.92051767111895));
#52567=CARTESIAN_POINT('Ctrl Pts',(-0.421994265891336,-5.80186567765455,
4.15241815149737));
#52568=CARTESIAN_POINT('Ctrl Pts',(4.65287774260152,-3.49148295347327,4.43084200514448));
#52569=CARTESIAN_POINT('Ctrl Pts',(5.45265056950567,2.02690065589327,4.70926585879163));
#52570=CARTESIAN_POINT('Ctrl Pts',(1.24248690619172,5.68295264716619,4.98768971243874));
#52571=CARTESIAN_POINT('Ctrl Pts',(-3.72871428411602,4.22878800043754,5.24631461417798));
#52572=CARTESIAN_POINT('Ctrl Pts',(-4.9072377326162,1.28369869401846,5.41213156470147));
#52573=CARTESIAN_POINT('Ctrl Pts',(-4.91921671359201,-0.00447815882576173,
5.48514056400926));
#52574=CARTESIAN_POINT('Origin',(0.,0.,-13.2351405640096));
#52575=CARTESIAN_POINT('',(-4.92059821462187,-0.00426705290350537,1.63985943599068));
#52576=CARTESIAN_POINT('',(-4.91908762937381,0.00449034157284686,1.98514056400927));
#52577=CARTESIAN_POINT('',(-4.91825,6.88216836313478E-12,-13.2351405640096));
#52578=CARTESIAN_POINT('Ctrl Pts',(-4.92059821462188,-0.00426705290350625,
1.63985943599068));
#52579=CARTESIAN_POINT('Ctrl Pts',(-4.92337363329955,-0.307820924709806,
1.65707615088422));
#52580=CARTESIAN_POINT('Ctrl Pts',(-4.75936158429057,-2.24439195417028,
1.76708262435452));
#52581=CARTESIAN_POINT('Ctrl Pts',(-2.18939161896353,-5.38904447491294,
1.96987885640157));
#52582=CARTESIAN_POINT('Ctrl Pts',(3.34919840410121,-4.75584966790831,2.24824813213183));
#52583=CARTESIAN_POINT('Ctrl Pts',(5.81162385012341,0.245487756220548,2.5266174078621));
#52584=CARTESIAN_POINT('Ctrl Pts',(2.93620146934825,5.02135011179013,2.80498668359237));
#52585=CARTESIAN_POINT('Ctrl Pts',(-2.63605694837504,5.18521357117537,3.08335595932264));
#52586=CARTESIAN_POINT('Ctrl Pts',(-4.84294757931317,1.96452831576599,3.27831354345541));
#52587=CARTESIAN_POINT('Ctrl Pts',(-4.92545593438113,0.167863312618859,
3.38048136901143));
#52588=CARTESIAN_POINT('Ctrl Pts',(-4.92432229863308,0.00284067633764233,
3.38985943599068));
#52589=CARTESIAN_POINT('Ctrl Pts',(-4.91908762937381,0.00449034157284679,
1.98514056400927));
#52590=CARTESIAN_POINT('Ctrl Pts',(-4.90714654187502,-1.27955959344367,
2.05791076799533));
#52591=CARTESIAN_POINT('Ctrl Pts',(-3.73499225470963,-4.22053784471989,
2.2234889231971));
#52592=CARTESIAN_POINT('Ctrl Pts',(1.22786565484881,-5.68612965343156,2.48187502961459));
#52593=CARTESIAN_POINT('Ctrl Pts',(5.44741913497888,-2.040918731811,2.76029888326171));
#52594=CARTESIAN_POINT('Ctrl Pts',(4.6618428064117,3.47950372184003,3.03872273690884));
#52595=CARTESIAN_POINT('Ctrl Pts',(-0.407069872025434,5.80293189872846,
3.31714659055597));
#52596=CARTESIAN_POINT('Ctrl Pts',(-4.32149470970697,3.29468394743748,3.54928586625612));
#52597=CARTESIAN_POINT('Ctrl Pts',(-4.91004224433159,0.82468547587703,3.68861719074055));
#52598=CARTESIAN_POINT('Ctrl Pts',(-4.91009445539168,-3.50508923821491E-5,
3.73514056400927));
#52599=CARTESIAN_POINT('Origin',(0.,0.,-13.2351405640096));
#52600=CARTESIAN_POINT('',(-4.91020579987568,-0.000754363845140739,-0.110140564009323));
#52601=CARTESIAN_POINT('',(-4.92534843309394,-0.00204667003549375,0.235140564009264));
#52602=CARTESIAN_POINT('',(-4.91825,6.88216836313478E-12,-13.2351405640096));
#52603=CARTESIAN_POINT('Ctrl Pts',(-4.91020579987568,-0.00075436384514127,
-0.110140564009323));
#52604=CARTESIAN_POINT('Ctrl Pts',(-4.91126562658971,-0.777357875070976,
-0.0663290672429879));
#52605=CARTESIAN_POINT('Ctrl Pts',(-4.37107385466396,-3.19736087635733,
0.070272188100103));
#52606=CARTESIAN_POINT('Ctrl Pts',(-0.577472308506603,-5.78807064112712,
0.299663202019953));
#52607=CARTESIAN_POINT('Ctrl Pts',(4.5565129461533,-3.61571926251521,0.578032477750221));
#52608=CARTESIAN_POINT('Ctrl Pts',(5.50544194895434,1.87759020035487,0.856401753480491));
#52609=CARTESIAN_POINT('Ctrl Pts',(1.3977444217788,5.64637463733703,1.13477102921076));
#52610=CARTESIAN_POINT('Ctrl Pts',(-3.66029468083591,4.31674594493847,1.39592359004749));
#52611=CARTESIAN_POINT('Ctrl Pts',(-4.90841547022119,1.32818749234986,1.56428639230746));
#52612=CARTESIAN_POINT('Ctrl Pts',(-4.92059821462188,-0.00426705290350625,
1.63985943599068));
#52613=CARTESIAN_POINT('Ctrl Pts',(-4.92534843309394,-0.0020466700354939,
0.235140564009264));
#52614=CARTESIAN_POINT('Ctrl Pts',(-4.92594291426159,-0.115445370532234,
0.241588442818691));
#52615=CARTESIAN_POINT('Ctrl Pts',(-4.87090317476765,-1.86046814152323,
0.340844272843828));
#52616=CARTESIAN_POINT('Ctrl Pts',(-2.79755665155426,-5.10033344825063,
0.532908054084678));
#52617=CARTESIAN_POINT('Ctrl Pts',(2.7784711114303,-5.11075559823943,0.811331907731805));
#52618=CARTESIAN_POINT('Ctrl Pts',(5.80161865024956,-0.425376937628951,
1.08975576137894));
#52619=CARTESIAN_POINT('Ctrl Pts',(3.49419519287011,4.65084126326794,1.36817961502607));
#52620=CARTESIAN_POINT('Ctrl Pts',(-2.02372117571978,5.45383141515521,1.64660346867319));
#52621=CARTESIAN_POINT('Ctrl Pts',(-4.72602242607254,2.34563150667623,1.85225711833426));
#52622=CARTESIAN_POINT('Ctrl Pts',(-4.92237568519668,0.358061812020196,
1.96510281677962));
#52623=CARTESIAN_POINT('Ctrl Pts',(-4.91908762937381,0.00449034157284679,
1.98514056400927));
#52624=CARTESIAN_POINT('Origin',(0.,0.,-13.2351405640096));
#52625=CARTESIAN_POINT('',(-4.91782085325031,0.00454258279844846,-1.86014056400932));
#52626=CARTESIAN_POINT('',(-4.9128074373708,-0.00348491184884558,-1.51485943599074));
#52627=CARTESIAN_POINT('',(-4.91825,6.88216836313478E-12,-13.2351405640096));
#52628=CARTESIAN_POINT('Ctrl Pts',(-4.91782085325031,0.0045425827984481,
-1.86014056400932));
#52629=CARTESIAN_POINT('Ctrl Pts',(-4.9064064990659,-1.23861424073828,-1.78973428537019));
#52630=CARTESIAN_POINT('Ctrl Pts',(-3.79628753361988,-4.13829632682806,
-1.62653824815431));
#52631=CARTESIAN_POINT('Ctrl Pts',(1.08150986877385,-5.71538033878776,-1.37055245236166));
#52632=CARTESIAN_POINT('Ctrl Pts',(5.39248056989081,-2.18091478914392,-1.0921831766314));
#52633=CARTESIAN_POINT('Ctrl Pts',(4.75057726644074,3.35667270511782,-0.813813900901123));
#52634=CARTESIAN_POINT('Ctrl Pts',(-0.254626070074851,5.81123064231236,
-0.535444625170857));
#52635=CARTESIAN_POINT('Ctrl Pts',(-4.27501848124952,3.38203525187861,-0.30088684620692));
#52636=CARTESIAN_POINT('Ctrl Pts',(-4.90902098597739,0.867435332995769,
-0.159118825819744));
#52637=CARTESIAN_POINT('Ctrl Pts',(-4.91020579987568,-0.00075436384514127,
-0.110140564009323));
#52638=CARTESIAN_POINT('Ctrl Pts',(-4.9128074373708,-0.00348491184884551,
-1.51485943599074));
#52639=CARTESIAN_POINT('Ctrl Pts',(-4.91660369838043,-0.586491446993301,
-1.48192593114224));
#52640=CARTESIAN_POINT('Ctrl Pts',(-4.55054125897033,-2.80782229127452,
-1.35618447507802));
#52641=CARTESIAN_POINT('Ctrl Pts',(-1.24911288418635,-5.68149993443013,
-1.1376350677981));
#52642=CARTESIAN_POINT('Ctrl Pts',(4.10447898256108,-4.12225384754937,-0.859211214150975));
#52643=CARTESIAN_POINT('Ctrl Pts',(5.68684458676181,1.22455018188017,-0.580787360503842));
#52644=CARTESIAN_POINT('Ctrl Pts',(2.04409447042155,5.44622826349031,-0.302363506856717));
#52645=CARTESIAN_POINT('Ctrl Pts',(-3.34892978181137,4.68198894529797,-0.0303875320190087));
#52646=CARTESIAN_POINT('Ctrl Pts',(-4.9173862119977,1.516765993031,0.148780491602981));
#52647=CARTESIAN_POINT('Ctrl Pts',(-4.92534843309394,-0.0020466700354939,
0.235140564009264));
#52648=CARTESIAN_POINT('Origin',(0.,0.,-13.2351405640096));
#52649=CARTESIAN_POINT('',(-4.92591231680323,-0.0013684910865338,-3.61014056400932));
#52650=CARTESIAN_POINT('',(-4.91263526682963,0.00339649852347107,-3.26485943599074));
#52651=CARTESIAN_POINT('',(-4.91825,6.88216836313478E-12,-13.2351405640096));
#52652=CARTESIAN_POINT('Ctrl Pts',(-4.92591231680324,-0.00136849108653464,
-3.61014056400932));
#52653=CARTESIAN_POINT('Ctrl Pts',(-4.92618524681776,-0.0754100048993439,
-3.60592926207415));
#52654=CARTESIAN_POINT('Ctrl Pts',(-4.89107484137784,-1.78058131512418,
-3.50892820156222));
#52655=CARTESIAN_POINT('Ctrl Pts',(-2.92039509627066,-5.03055946195533,
-3.31913738247355));
#52656=CARTESIAN_POINT('Ctrl Pts',(2.65235109881223,-5.17689768424732,-3.04076810674327));
#52657=CARTESIAN_POINT('Ctrl Pts',(5.78897154557153,-0.568370014814376,
-2.76239883101301));
#52658=CARTESIAN_POINT('Ctrl Pts',(3.60854980134286,4.56219293151739,-2.48402955528274));
#52659=CARTESIAN_POINT('Ctrl Pts',(-1.8862450334912,5.50248268361132,-2.20566027955247));
#52660=CARTESIAN_POINT('Ctrl Pts',(-4.69698430404261,2.42929695424461,-1.99769728246133));
#52661=CARTESIAN_POINT('Ctrl Pts',(-4.9214496910873,0.399765514002954,-1.88252404394695));
#52662=CARTESIAN_POINT('Ctrl Pts',(-4.91782085325031,0.0045425827984481,
-1.86014056400932));
#52663=CARTESIAN_POINT('Ctrl Pts',(-4.91263526682963,0.003396498523471,
-3.26485943599074));
#52664=CARTESIAN_POINT('Ctrl Pts',(-4.90597445027353,-1.0485653240634,-3.20544030510316));
#52665=CARTESIAN_POINT('Ctrl Pts',(-4.05835413227311,-3.75340131497428,
-3.05321322299988));
#52666=CARTESIAN_POINT('Ctrl Pts',(0.400302865534793,-5.80340263407658,
-2.80817818968088));
#52667=CARTESIAN_POINT('Ctrl Pts',(5.09870148282997,-2.80052989457494,-2.52975433603375));
#52668=CARTESIAN_POINT('Ctrl Pts',(5.11237470052847,2.77549084296867,-2.25133048238662));
#52669=CARTESIAN_POINT('Ctrl Pts',(0.42875946485938,5.80136965084335,-1.97290662873949));
#52670=CARTESIAN_POINT('Ctrl Pts',(-4.04820116206155,3.76949085150405,-1.72741627994086));
#52671=CARTESIAN_POINT('Ctrl Pts',(-4.90590568102076,1.05644459400893,-1.57473388235795));
#52672=CARTESIAN_POINT('Ctrl Pts',(-4.9128074373708,-0.00348491184884551,
-1.51485943599074));
#52673=CARTESIAN_POINT('Origin',(0.,0.,-13.2351405640096));
#52674=CARTESIAN_POINT('',(-4.91367359665507,-0.00385188715628437,-5.36014056400933));
#52675=CARTESIAN_POINT('',(-4.92520873866597,0.00217779940761373,-5.01485943599074));
#52676=CARTESIAN_POINT('',(-4.91825,6.88216836313478E-12,-13.2351405640096));
#52677=CARTESIAN_POINT('Ctrl Pts',(-4.91367359665507,-0.0038518871562844,
-5.36014056400933));
#52678=CARTESIAN_POINT('Ctrl Pts',(-4.91764492376584,-0.548956137439361,
-5.32933448020136));
#52679=CARTESIAN_POINT('Ctrl Pts',(-4.58222637382267,-2.73119860279941,
-5.20573863781664));
#52680=CARTESIAN_POINT('Ctrl Pts',(-1.37997979498124,-5.65074267591175,
-4.98935303685515));
#52681=CARTESIAN_POINT('Ctrl Pts',(4.00703078514331,-4.21650789487217,-4.7109837611249));
#52682=CARTESIAN_POINT('Ctrl Pts',(5.71367268487829,1.09049576997227,-4.43261448539462));
#52683=CARTESIAN_POINT('Ctrl Pts',(2.17243253669944,5.39590335156548,-4.15424520966435));
#52684=CARTESIAN_POINT('Ctrl Pts',(-3.28037882473082,4.75513584668186,-3.88008723586925));
#52685=CARTESIAN_POINT('Ctrl Pts',(-4.92017164091969,1.5559843470402,-3.69871902065091));
#52686=CARTESIAN_POINT('Ctrl Pts',(-4.92591231680324,-0.00136849108653464,
-3.61014056400932));
#52687=CARTESIAN_POINT('Ctrl Pts',(-4.92520873866597,0.00217779940761347,
-5.01485943599074));
#52688=CARTESIAN_POINT('Ctrl Pts',(-4.91686006964921,-1.50874087785573,
-4.92895467906409));
#52689=CARTESIAN_POINT('Ctrl Pts',(-3.36282907081669,-4.6668321718968,-4.75024197092173));
#52690=CARTESIAN_POINT('Ctrl Pts',(2.01736012333282,-5.4561876061593,-4.47872131156366));
#52691=CARTESIAN_POINT('Ctrl Pts',(5.68077069634635,-1.25242520393326,-4.20029745791653));
#52692=CARTESIAN_POINT('Ctrl Pts',(4.12464623088233,4.10207481179193,-3.9218736042694));
#52693=CARTESIAN_POINT('Ctrl Pts',(-1.22123428830395,5.68755759612714,-3.64344975062227));
#52694=CARTESIAN_POINT('Ctrl Pts',(-4.54362355430201,2.82415249350275,-3.42444502786272));
#52695=CARTESIAN_POINT('Ctrl Pts',(-4.91637811536861,0.594515280668979,
-3.29824825631887));
#52696=CARTESIAN_POINT('Ctrl Pts',(-4.91263526682963,0.003396498523471,
-3.26485943599074));
#52697=CARTESIAN_POINT('Origin',(0.,0.,-13.2351405640096));
#52698=CARTESIAN_POINT('',(-4.91193228603272,0.00296404864912429,-7.11014056400932));
#52699=CARTESIAN_POINT('',(-4.91933390470069,-0.00446651128636566,-6.76485943599074));
#52700=CARTESIAN_POINT('',(-4.91825,6.88216836313478E-12,-13.2351405640096));
#52701=CARTESIAN_POINT('Ctrl Pts',(-4.91193228603272,0.00296404864912413,
-7.11014056400932));
#52702=CARTESIAN_POINT('Ctrl Pts',(-4.9063561374784,-1.01362454442101,-7.05273969832856));
#52703=CARTESIAN_POINT('Ctrl Pts',(-4.10272486587694,-3.68163039196913,
-6.90254907407105));
#52704=CARTESIAN_POINT('Ctrl Pts',(0.272909909778823,-5.81040739879541,
-6.65956869123677));
#52705=CARTESIAN_POINT('Ctrl Pts',(5.03514064798181,-2.9124777495484,-6.38119941550651));
#52706=CARTESIAN_POINT('Ctrl Pts',(5.17272309584991,2.66048658894571,-6.10283013977622));
#52707=CARTESIAN_POINT('Ctrl Pts',(0.559264958796863,5.78985906598745,-5.82446086404598));
#52708=CARTESIAN_POINT('Ctrl Pts',(-4.00046112440602,3.84356270012795,-5.57689767212365));
#52709=CARTESIAN_POINT('Ctrl Pts',(-4.90568305006145,1.09293031908751,-5.42212423877812));
#52710=CARTESIAN_POINT('Ctrl Pts',(-4.91367359665507,-0.0038518871562844,
-5.36014056400933));
#52711=CARTESIAN_POINT('Ctrl Pts',(-4.91933390470069,-0.00446651128636628,
-6.76485943599074));
#52712=CARTESIAN_POINT('Ctrl Pts',(-4.92254636011847,-0.349960418775078,
-6.74527700424072));
#52713=CARTESIAN_POINT('Ctrl Pts',(-4.73152296147135,-2.32934242081634,
-6.632886621275));
#52714=CARTESIAN_POINT('Ctrl Pts',(-2.05044135574297,-5.44383565780062,
-6.42768828709357));
#52715=CARTESIAN_POINT('Ctrl Pts',(3.47134289591715,-4.66792459610127,-6.14926443344644));
#52716=CARTESIAN_POINT('Ctrl Pts',(5.803635743461,0.3969206476142,-5.8708405797993));
#52717=CARTESIAN_POINT('Ctrl Pts',(2.80350181475234,5.09706699486434,-5.59241672615218));
#52718=CARTESIAN_POINT('Ctrl Pts',(-2.77250943461248,5.11399248292585,-5.31399287250505));
#52719=CARTESIAN_POINT('Ctrl Pts',(-4.86667316554333,1.87667755337039,-5.12147377578457));
#52720=CARTESIAN_POINT('Ctrl Pts',(-4.92587962682559,0.123593254817412,
-5.0217626302798));
#52721=CARTESIAN_POINT('Ctrl Pts',(-4.92520873866597,0.00217779940761347,
-5.01485943599074));
#52722=CARTESIAN_POINT('Origin',(0.,0.,-13.2351405640096));
#52723=CARTESIAN_POINT('',(-4.9240923050422,0.00237935796991909,-8.86014056400933));
#52724=CARTESIAN_POINT('',(-4.91001919821333,6.39834157820096E-5,-8.51485943599074));
#52725=CARTESIAN_POINT('',(-4.91825,6.88216836313478E-12,-13.2351405640096));
#52726=CARTESIAN_POINT('Ctrl Pts',(-4.9240923050422,0.00237935796991912,
-8.86014056400933));
#52727=CARTESIAN_POINT('Ctrl Pts',(-4.91423502458648,-1.47557821261336,
-8.77614491645577));
#52728=CARTESIAN_POINT('Ctrl Pts',(-3.42124592657607,-4.6021663877554,-8.59935951032545));
#52729=CARTESIAN_POINT('Ctrl Pts',(1.90395420368265,-5.4968079578387,-8.32978434561839));
#52730=CARTESIAN_POINT('Ctrl Pts',(5.65268654860171,-1.37094194360677,-8.05141506988812));
#52731=CARTESIAN_POINT('Ctrl Pts',(4.21031778233782,4.01357646538516,-7.77304579415784));
#52732=CARTESIAN_POINT('Ctrl Pts',(-1.09954047142025,5.71199305956496,-7.49467651842759));
#52733=CARTESIAN_POINT('Ctrl Pts',(-4.51265656995462,2.89554900635168,-7.27370810837807));
#52734=CARTESIAN_POINT('Ctrl Pts',(-4.91537010394053,0.629713217198827,
-7.14552945690532));
#52735=CARTESIAN_POINT('Ctrl Pts',(-4.91193228603272,0.00296404864912413,
-7.11014056400932));
#52736=CARTESIAN_POINT('Ctrl Pts',(-4.91001919821333,6.39834157814545E-5,
-8.51485943599074));
#52737=CARTESIAN_POINT('Ctrl Pts',(-4.9102107675652,-0.816682238869538,
-8.46879137820165));
#52738=CARTESIAN_POINT('Ctrl Pts',(-4.33010667838534,-3.27874551411531,
-8.32991536919685));
#52739=CARTESIAN_POINT('Ctrl Pts',(-0.435410493021885,-5.80062512701066,
-8.09823140897635));
#52740=CARTESIAN_POINT('Ctrl Pts',(4.64466218789312,-3.50245220498147,-7.81980755532921));
#52741=CARTESIAN_POINT('Ctrl Pts',(5.45739468419239,2.01424609607877,-7.54138370168209));
#52742=CARTESIAN_POINT('Ctrl Pts',(1.25572029180289,5.68000375627327,-7.26295984803495));
#52743=CARTESIAN_POINT('Ctrl Pts',(-3.72299945840702,4.23627988132658,-7.00411842613784));
#52744=CARTESIAN_POINT('Ctrl Pts',(-4.90732141719504,1.28745530777343,-6.83808495545644));
#52745=CARTESIAN_POINT('Ctrl Pts',(-4.91933390470069,-0.00446651128636628,
-6.76485943599074));
#52746=CARTESIAN_POINT('Origin',(0.,0.,-9.5));
#52747=CARTESIAN_POINT('',(-3.54932990775846,-3.52168385944726,-10.));
#52748=CARTESIAN_POINT('Ctrl Pts',(3.34446487542469,-4.86859341898352,-9.08325));
#52749=CARTESIAN_POINT('Ctrl Pts',(3.19879863164306,-4.94736391093165,-9.10154508180626));
#52750=CARTESIAN_POINT('Ctrl Pts',(3.05033436817195,-5.02004566253132,-9.11988472965185));
#52751=CARTESIAN_POINT('Ctrl Pts',(2.89941768276307,-5.08638119286217,-9.13828856187511));
#52752=CARTESIAN_POINT('Ctrl Pts',(2.75120930712827,-5.15152628381466,-9.15636212393271));
#52753=CARTESIAN_POINT('Ctrl Pts',(2.60063505538134,-5.21055103333368,-9.17449758736774));
#52754=CARTESIAN_POINT('Ctrl Pts',(2.44801186022486,-5.26316298026786,-9.19271353316328));
#52755=CARTESIAN_POINT('Ctrl Pts',(2.29775466947289,-5.31495932313839,-9.21064709063678));
#52756=CARTESIAN_POINT('Ctrl Pts',(2.14551098203089,-5.36054028317659,-9.2286586544954));
#52757=CARTESIAN_POINT('Ctrl Pts',(1.99158237653721,-5.39957715606078,-9.24676595490747));
#52758=CARTESIAN_POINT('Ctrl Pts',(1.85900718724118,-5.43319872234177,-9.26236135884212));
#52759=CARTESIAN_POINT('Ctrl Pts',(1.72518191031146,-5.46196520161207,-9.2780277799907));
#52760=CARTESIAN_POINT('Ctrl Pts',(1.59030358846426,-5.48563510874125,-9.29377654605015));
#52761=CARTESIAN_POINT('Ctrl Pts',(1.53227521801134,-5.49581855498129,-9.30055209914541));
#52762=CARTESIAN_POINT('Ctrl Pts',(1.47405201016708,-5.50505826954835,-9.30734289393353));
#52763=CARTESIAN_POINT('Ctrl Pts',(1.41565008458091,-5.51333327452099,-9.31414983247631));
#52764=CARTESIAN_POINT('Ctrl Pts',(1.39022440435432,-5.5169358548845,-9.31711328001633));
#52765=CARTESIAN_POINT('Ctrl Pts',(1.36476184378213,-5.52035588011081,-9.32008013785663));
#52766=CARTESIAN_POINT('Ctrl Pts',(1.33928832028401,-5.52358866726458,-9.32304761925695));
#52767=CARTESIAN_POINT('Ctrl Pts',(1.28727163537636,-5.53018998689608,-9.32910718714441));
#52768=CARTESIAN_POINT('Ctrl Pts',(1.23518854185695,-5.53601374978223,-9.33517176846418));
#52769=CARTESIAN_POINT('Ctrl Pts',(1.18304992365009,-5.54105054431051,-9.34124208925133));
#52770=CARTESIAN_POINT('Ctrl Pts',(1.02673277346924,-5.55615139266026,-9.35944155979285));
#52771=CARTESIAN_POINT('Ctrl Pts',(0.869916237775008,-5.56418242497692,
-9.37769262036853));
#52772=CARTESIAN_POINT('Ctrl Pts',(0.713056273219087,-5.56532307499083,
-9.39601483683802));
#52773=CARTESIAN_POINT('Ctrl Pts',(0.554631282752025,-5.5664751055175,-9.41451985803785));
#52774=CARTESIAN_POINT('Ctrl Pts',(0.396161147779864,-5.56059828159109,
-9.43309746209029));
#52775=CARTESIAN_POINT('Ctrl Pts',(0.238126550129667,-5.54782555539949,
-9.45176780635592));
#52776=CARTESIAN_POINT('Ctrl Pts',(0.0814929446544512,-5.53516606067564,
-9.47027263619237));
#52777=CARTESIAN_POINT('Ctrl Pts',(-0.0747135674656943,-5.5157319593914,
-9.48886856922834));
#52778=CARTESIAN_POINT('Ctrl Pts',(-0.230002369134159,-5.48960759431231,
-9.50757523147196));
#52779=CARTESIAN_POINT('Ctrl Pts',(-0.341080017822252,-5.47092090850318,
-9.52095605503746));
#52780=CARTESIAN_POINT('Ctrl Pts',(-0.451687676746772,-5.4488102013679,
-9.53439353321513));
#52781=CARTESIAN_POINT('Ctrl Pts',(-0.561635393178398,-5.42329377189995,
-9.54789484876889));
#52782=CARTESIAN_POINT('Ctrl Pts',(-0.603914210286864,-5.41348179499175,
-9.55308658598315));
#52783=CARTESIAN_POINT('Ctrl Pts',(-0.64609533818728,-5.40316611823237,
-9.55828776268145));
#52784=CARTESIAN_POINT('Ctrl Pts',(-0.688167556291023,-5.39234740569837,
-9.56349878727855));
#52785=CARTESIAN_POINT('Ctrl Pts',(-0.712858909949692,-5.38599811703834,
-9.5665570346696));
#52786=CARTESIAN_POINT('Ctrl Pts',(-0.737512747340636,-5.37947556474227,
-9.56961867395688));
#52787=CARTESIAN_POINT('Ctrl Pts',(-0.762126759085168,-5.37277985131085,
-9.57268378769665));
#52788=CARTESIAN_POINT('Ctrl Pts',(-0.781035172201083,-5.36763622348695,
-9.57503839926669));
#52789=CARTESIAN_POINT('Ctrl Pts',(-0.799910762238151,-5.36239293904086,
-9.57739390086569));
#52790=CARTESIAN_POINT('Ctrl Pts',(-0.818751399856817,-5.35705067432398,
-9.57975018027239));
#52791=CARTESIAN_POINT('Ctrl Pts',(-0.966624994112708,-5.31512110160247,
-9.59824379561558));
#52792=CARTESIAN_POINT('Ctrl Pts',(-1.11237269054818,-5.26709116156679,
-9.61678848533419));
#52793=CARTESIAN_POINT('Ctrl Pts',(-1.2555573640261,-5.21309665032415,-9.635405210757));
#52794=CARTESIAN_POINT('Ctrl Pts',(-1.34560868000601,-5.17913856895281,
-9.64711359115024));
#52795=CARTESIAN_POINT('Ctrl Pts',(-1.43464583115756,-5.14282031676834,
-9.65885046432624));
#52796=CARTESIAN_POINT('Ctrl Pts',(-1.5225544255541,-5.10416673508712,-9.67062104462566));
#52797=CARTESIAN_POINT('Ctrl Pts',(-1.66238523492523,-5.04268285346346,
-9.68934378477791));
#52798=CARTESIAN_POINT('Ctrl Pts',(-1.79936268643465,-4.97529188425519,
-9.70815180838046));
#52799=CARTESIAN_POINT('Ctrl Pts',(-1.93314075803419,-4.90216296398429,
-9.72706610067654));
#52800=CARTESIAN_POINT('Ctrl Pts',(-2.06568174395399,-4.82971028862378,
-9.74580548687731));
#52801=CARTESIAN_POINT('Ctrl Pts',(-2.19508269636191,-4.75162475819703,
-9.76464918546239));
#52802=CARTESIAN_POINT('Ctrl Pts',(-2.32096600124785,-4.66804080983962,
-9.78361760487156));
#52803=CARTESIAN_POINT('Ctrl Pts',(-2.37965096368007,-4.62907519105692,
-9.79246040560224));
#52804=CARTESIAN_POINT('Ctrl Pts',(-2.4375708125932,-4.58891422837344,-9.80133031176665));
#52805=CARTESIAN_POINT('Ctrl Pts',(-2.49468378132543,-4.547569770274,-9.810229391057));
#52806=CARTESIAN_POINT('Ctrl Pts',(-2.52796808704415,-4.52347503988782,
-9.81541559801297));
#52807=CARTESIAN_POINT('Ctrl Pts',(-2.56097830625555,-4.49897833648104,
-9.8206117131173));
#52808=CARTESIAN_POINT('Ctrl Pts',(-2.59370579156265,-4.47408185876841,
-9.82581814563082));
#52809=CARTESIAN_POINT('Ctrl Pts',(-2.60830979622556,-4.4629722891454,-9.82814141501712));
#52810=CARTESIAN_POINT('Ctrl Pts',(-2.62285735082004,-4.45178316892005,
-9.83046672058383));
#52811=CARTESIAN_POINT('Ctrl Pts',(-2.63733749771883,-4.44052277762685,
-9.83279244866301));
#52812=CARTESIAN_POINT('Ctrl Pts',(-2.75344399409984,-4.35023332199701,
-9.85144088784646));
#52813=CARTESIAN_POINT('Ctrl Pts',(-2.86539772416489,-4.25522984404488,
-9.87014472889391));
#52814=CARTESIAN_POINT('Ctrl Pts',(-2.97290571973465,-4.15568845804594,
-9.88892585516935));
#52815=CARTESIAN_POINT('Ctrl Pts',(-3.07913398797304,-4.05733196840369,
-9.9074834192764));
#52816=CARTESIAN_POINT('Ctrl Pts',(-3.18102210231045,-3.95454441586392,
-9.92611643962443));
#52817=CARTESIAN_POINT('Ctrl Pts',(-3.2782462026002,-3.84746691787586,-9.94484602737331));
#52818=CARTESIAN_POINT('Ctrl Pts',(-3.37316798191902,-3.74292507481694,
-9.96313208802836));
#52819=CARTESIAN_POINT('Ctrl Pts',(-3.46364424021495,-3.63429354697869,
-9.98151019669632));
#52820=CARTESIAN_POINT('Ctrl Pts',(-3.54932990775845,-3.52168385944727,
-10.));
#52821=CARTESIAN_POINT('',(3.54932990775696,-3.52168385944877,-10.));
#52822=CARTESIAN_POINT('Ctrl Pts',(3.54751238410166,-3.52143928316711,-10.));
#52823=CARTESIAN_POINT('Ctrl Pts',(3.65508312862553,-3.41996290417742,-9.99476917353171));
#52824=CARTESIAN_POINT('Ctrl Pts',(3.75814035868601,-3.31372395112702,-9.98954665627179));
#52825=CARTESIAN_POINT('Ctrl Pts',(3.85646778381177,-3.20303931222073,-9.98432713957975));
#52826=CARTESIAN_POINT('Ctrl Pts',(3.923641246713,-3.12742388269231,-9.98076136929311));
#52827=CARTESIAN_POINT('Ctrl Pts',(3.98860659175575,-3.04973273944966,-9.97719699939839));
#52828=CARTESIAN_POINT('Ctrl Pts',(4.05128444657531,-2.97005757844254,-9.97363233730264));
#52829=CARTESIAN_POINT('Ctrl Pts',(4.07561399842648,-2.93913021236477,-9.97224864873289));
#52830=CARTESIAN_POINT('Ctrl Pts',(4.099598786423,-2.90790383263907,-9.97086491613587));
#52831=CARTESIAN_POINT('Ctrl Pts',(4.12323378449639,-2.8763835412882,-9.96948104051677));
#52832=CARTESIAN_POINT('Ctrl Pts',(4.13398915280514,-2.86203988271776,-9.96885129255018));
#52833=CARTESIAN_POINT('Ctrl Pts',(4.14467115873595,-2.84763653652582,-9.96822156758605));
#52834=CARTESIAN_POINT('Ctrl Pts',(4.15527382809579,-2.83318170099535,-9.96759218868572));
#52835=CARTESIAN_POINT('Ctrl Pts',(4.24378373503389,-2.71251433844854,-9.96233820348577));
#52836=CARTESIAN_POINT('Ctrl Pts',(4.32687797709647,-2.58811568558574,-9.95710189140309));
#52837=CARTESIAN_POINT('Ctrl Pts',(4.4043694477894,-2.46033758996999,-9.95187801813126));
#52838=CARTESIAN_POINT('Ctrl Pts',(4.45485165672787,-2.37709590591168,-9.94847489957359));
#52839=CARTESIAN_POINT('Ctrl Pts',(4.50295544391612,-2.29241912223262,-9.94507705996846));
#52840=CARTESIAN_POINT('Ctrl Pts',(4.54862070762841,-2.20639609047384,-9.94168305216942));
#52841=CARTESIAN_POINT('Ctrl Pts',(4.61880161012226,-2.07419113832192,-9.9364669533003));
#52842=CARTESIAN_POINT('Ctrl Pts',(4.6832252135784,-1.93880757714367,-9.93125990486675));
#52843=CARTESIAN_POINT('Ctrl Pts',(4.74171890553884,-1.80071137001634,-9.92605665382018));
#52844=CARTESIAN_POINT('Ctrl Pts',(4.77596862098491,-1.71985212451872,-9.92301000277514));
#52845=CARTESIAN_POINT('Ctrl Pts',(4.80818447948761,-1.63806232182356,-9.91996465363939));
#52846=CARTESIAN_POINT('Ctrl Pts',(4.83832430884422,-1.55543201942794,-9.91691955189195));
#52847=CARTESIAN_POINT('Ctrl Pts',(4.8532086808827,-1.51462554544438,-9.91541574685153));
#52848=CARTESIAN_POINT('Ctrl Pts',(4.86758665820026,-1.4736140570085,-9.91391200214463));
#52849=CARTESIAN_POINT('Ctrl Pts',(4.88145262570607,-1.43240824637402,-9.91240819076519));
#52850=CARTESIAN_POINT('Ctrl Pts',(4.89270606139725,-1.39896615588277,-9.9111877173548));
#52851=CARTESIAN_POINT('Ctrl Pts',(4.9036222434836,-1.36539606845859,-9.90996720002901));
#52852=CARTESIAN_POINT('Ctrl Pts',(4.91419799178983,-1.33170366495726,-9.90874657089416));
#52853=CARTESIAN_POINT('Ctrl Pts',(4.92037675597896,-1.31201925018379,-9.90803343179815));
#52854=CARTESIAN_POINT('Ctrl Pts',(4.92643945384592,-1.29229242931547,-9.90732023154963));
#52855=CARTESIAN_POINT('Ctrl Pts',(4.93238098424579,-1.27253967687844,-9.90660750838836));
#52856=CARTESIAN_POINT('Ctrl Pts',(4.97609052146227,-1.12722633003541,-9.90136428022223));
#52857=CARTESIAN_POINT('Ctrl Pts',(5.01330854498342,-0.980316288849063,
-9.89613976777481));
#52858=CARTESIAN_POINT('Ctrl Pts',(5.04390188651618,-0.832299452109599,
-9.8909287871518));
#52859=CARTESIAN_POINT('Ctrl Pts',(5.07450394234213,-0.684240453839277,
-9.88571632221846));
#52860=CARTESIAN_POINT('Ctrl Pts',(5.09847787962514,-0.535073232147375,
-9.88051739681951));
#52861=CARTESIAN_POINT('Ctrl Pts',(5.11564390371681,-0.385264822007308,
-9.8753268226296));
#52862=CARTESIAN_POINT('Ctrl Pts',(5.13254133760872,-0.237800406643843,
-9.87021746336465));
#52863=CARTESIAN_POINT('Ctrl Pts',(5.14284243623783,-0.089713929354489,
-9.86511619601691));
#52864=CARTESIAN_POINT('Ctrl Pts',(5.14632684128669,0.0585599414038308,
-9.86001807200956));
#52865=CARTESIAN_POINT('Ctrl Pts',(5.14782497925894,0.122311059015022,-9.85782610722489));
#52866=CARTESIAN_POINT('Ctrl Pts',(5.1480623354105,0.186096887079666,-9.85563472352268));
#52867=CARTESIAN_POINT('Ctrl Pts',(5.14701840430152,0.249882961654822,-9.85344352757947));
#52868=CARTESIAN_POINT('Ctrl Pts',(5.14523776540626,0.358683211391727,-9.84970599289919));
#52869=CARTESIAN_POINT('Ctrl Pts',(5.13973005118594,0.467484324210803,-9.84596900449073));
#52870=CARTESIAN_POINT('Ctrl Pts',(5.13058176480017,0.576148493099822,-9.84223061043461));
#52871=CARTESIAN_POINT('Ctrl Pts',(5.12862737772094,0.599362878690334,-9.84143196151477));
#52872=CARTESIAN_POINT('Ctrl Pts',(5.12650678498253,0.622571005372613,-9.84063324844177));
#52873=CARTESIAN_POINT('Ctrl Pts',(5.12422074716705,0.645771512820038,-9.83983445218403));
#52874=CARTESIAN_POINT('Ctrl Pts',(5.12234618145826,0.664796078115013,-9.83917943411612));
#52875=CARTESIAN_POINT('Ctrl Pts',(5.12036039172749,0.683814766160387,-9.83852438594634));
#52876=CARTESIAN_POINT('Ctrl Pts',(5.11826539452591,0.702813831563803,-9.83786974525181));
#52877=CARTESIAN_POINT('Ctrl Pts',(5.10210352212495,0.849382271156973,-9.83281951446132));
#52878=CARTESIAN_POINT('Ctrl Pts',(5.07942731567127,0.994985322764188,-9.82778654540807));
#52879=CARTESIAN_POINT('Ctrl Pts',(5.05055882614455,1.13928743301165,-9.82276620697614));
#52880=CARTESIAN_POINT('Ctrl Pts',(5.02102945684531,1.28689301868713,-9.81763093907698));
#52881=CARTESIAN_POINT('Ctrl Pts',(4.98502090518309,1.43313803605949,-9.81250888671849));
#52882=CARTESIAN_POINT('Ctrl Pts',(4.94282336643821,1.57766552599623,-9.80739509339072));
#52883=CARTESIAN_POINT('Ctrl Pts',(4.89995783591708,1.72448090232613,-9.80220034814039));
#52884=CARTESIAN_POINT('Ctrl Pts',(4.85070560322117,1.86952465184268,-9.7970141254732));
#52885=CARTESIAN_POINT('Ctrl Pts',(4.79531809543285,2.01241464363871,-9.79183122974702));
#52886=CARTESIAN_POINT('Ctrl Pts',(4.74368240911756,2.14562559839358,-9.78699941137121));
#52887=CARTESIAN_POINT('Ctrl Pts',(4.68671374369661,2.27696508058455,-9.78217048448318));
#52888=CARTESIAN_POINT('Ctrl Pts',(4.62457829497681,2.4061090829116,-9.77734023935897));
#52889=CARTESIAN_POINT('Ctrl Pts',(4.60514189625996,2.4465062213058,-9.77582930522928));
#52890=CARTESIAN_POINT('Ctrl Pts',(4.58519968636458,2.48668840236422,-9.77431824211259));
#52891=CARTESIAN_POINT('Ctrl Pts',(4.56475608548958,2.52664530516031,-9.77280692115941));
#52892=CARTESIAN_POINT('Ctrl Pts',(4.55525175077551,2.54522147384181,-9.77210430031061));
#52893=CARTESIAN_POINT('Ctrl Pts',(4.5456390427194,2.56374894853136,-9.77140162373386));
#52894=CARTESIAN_POINT('Ctrl Pts',(4.53591838330546,2.58222667542352,-9.77069887848196));
#52895=CARTESIAN_POINT('Ctrl Pts',(4.52641793441604,2.6002858103501,-9.77001205312747));
#52896=CARTESIAN_POINT('Ctrl Pts',(4.51681805327452,2.6182903808933,-9.76932542975162));
#52897=CARTESIAN_POINT('Ctrl Pts',(4.50712198593273,2.63623477492454,-9.76863917841065));
#52898=CARTESIAN_POINT('Ctrl Pts',(4.43327641607358,2.77289987390772,-9.76341266547974));
#52899=CARTESIAN_POINT('Ctrl Pts',(4.35380963597557,2.90616348574592,-9.75820438137484));
#52900=CARTESIAN_POINT('Ctrl Pts',(4.2690165533173,3.03565215533473,-9.75300919073388));
#52901=CARTESIAN_POINT('Ctrl Pts',(4.18369488725524,3.16594803182743,-9.74778161429604));
#52902=CARTESIAN_POINT('Ctrl Pts',(4.09297996159635,3.29242249771891,-9.74256729507512));
#52903=CARTESIAN_POINT('Ctrl Pts',(3.99712250040057,3.41467782938133,-9.73736100107061));
#52904=CARTESIAN_POINT('Ctrl Pts',(3.90251511176284,3.53533883512192,-9.73222260209674));
#52905=CARTESIAN_POINT('Ctrl Pts',(3.80289797907067,3.65189067996929,-9.72709202039119));
#52906=CARTESIAN_POINT('Ctrl Pts',(3.69847007959931,3.76392400377687,-9.7219642259865));
#52907=CARTESIAN_POINT('Ctrl Pts',(3.62190098220249,3.84606958484991,-9.71820440134969));
#52908=CARTESIAN_POINT('Ctrl Pts',(3.54274464208819,3.92578541816275,-9.71444607521657));
#52909=CARTESIAN_POINT('Ctrl Pts',(3.46106691159086,4.0028976587042,-9.71068726479984));
#52910=CARTESIAN_POINT('Ctrl Pts',(3.42356702701269,4.03830143525703,-9.70896151953342));
#52911=CARTESIAN_POINT('Ctrl Pts',(3.38553551647611,4.07315623363686,-9.70723567218425));
#52912=CARTESIAN_POINT('Ctrl Pts',(3.3469780762519,4.10744433178595,-9.7055095308612));
#52913=CARTESIAN_POINT('Ctrl Pts',(3.32402527509264,4.12785564266054,-9.70448197876411));
#52914=CARTESIAN_POINT('Ctrl Pts',(3.30088609320679,4.14806612156554,-9.70345432249197));
#52915=CARTESIAN_POINT('Ctrl Pts',(3.27756166527489,4.168071925129,-9.70242652156505));
#52916=CARTESIAN_POINT('Ctrl Pts',(3.26270593229633,4.18081396864784,-9.70177189731574));
#52917=CARTESIAN_POINT('Ctrl Pts',(3.24777526204805,4.19347273003535,-9.70111722521979));
#52918=CARTESIAN_POINT('Ctrl Pts',(3.23278066815151,4.20603842872606,-9.70046295819114));
#52919=CARTESIAN_POINT('Ctrl Pts',(3.11335631773141,4.30611785829023,-9.69525205248491));
#52920=CARTESIAN_POINT('Ctrl Pts',(2.98971082178213,4.40044304867354,-9.69005933831205));
#52921=CARTESIAN_POINT('Ctrl Pts',(2.86208820640147,4.48862411075741,-9.68487973117774));
#52922=CARTESIAN_POINT('Ctrl Pts',(2.7970006164004,4.53359649122191,-9.68223812926009));
#52923=CARTESIAN_POINT('Ctrl Pts',(2.73087789159375,4.57697031785747,-9.67959993648905));
#52924=CARTESIAN_POINT('Ctrl Pts',(2.66374840647643,4.61869047738687,-9.67696447839955));
#52925=CARTESIAN_POINT('Ctrl Pts',(2.53534702353607,4.69849037709868,-9.67192352712782));
#52926=CARTESIAN_POINT('Ctrl Pts',(2.40326422843609,4.77224301178556,-9.66689258091221));
#52927=CARTESIAN_POINT('Ctrl Pts',(2.26796505031953,4.84000307398862,-9.66186691989815));
#52928=CARTESIAN_POINT('Ctrl Pts',(2.13014247260833,4.90902689637023,-9.65674752770892));
#52929=CARTESIAN_POINT('Ctrl Pts',(1.98898175619273,4.97183275027531,-9.65163361970313));
#52930=CARTESIAN_POINT('Ctrl Pts',(1.84494702971633,5.0284315690857,-9.64652020698713));
#52931=CARTESIAN_POINT('Ctrl Pts',(1.7580990880663,5.06255869268814,-9.64343699656937));
#52932=CARTESIAN_POINT('Ctrl Pts',(1.67020576767861,5.09442822583008,-9.6403539662227));
#52933=CARTESIAN_POINT('Ctrl Pts',(1.58136572634967,5.12403406159239,-9.63727002228997));
#52934=CARTESIAN_POINT('Ctrl Pts',(1.55287794159396,5.13352758122716,-9.63628111312648));
#52935=CARTESIAN_POINT('Ctrl Pts',(1.52429279737253,5.14278828576354,-9.63529211002327));
#52936=CARTESIAN_POINT('Ctrl Pts',(1.49561351608857,5.15181583211708,-9.63430297691988));
#52937=CARTESIAN_POINT('Ctrl Pts',(1.47064629134486,5.1596749125613,-9.63344187066519));
#52938=CARTESIAN_POINT('Ctrl Pts',(1.44560369716888,5.16735840950949,-9.63258052873048));
#52939=CARTESIAN_POINT('Ctrl Pts',(1.42051478324143,5.17485823755497,-9.63171984848409));
#52940=CARTESIAN_POINT('Ctrl Pts',(1.27281033665945,5.21901152191478,-9.62665281768929));
#52941=CARTESIAN_POINT('Ctrl Pts',(1.12333461568641,5.25685764911356,-9.62160289217849));
#52942=CARTESIAN_POINT('Ctrl Pts',(0.972565836059491,5.28847001595391,-9.61656539809095));
#52943=CARTESIAN_POINT('Ctrl Pts',(0.817722274810746,5.32093676054902,-9.61139175719385));
#52944=CARTESIAN_POINT('Ctrl Pts',(0.661514135419789,5.34682850300569,-9.60623122876099));
#52945=CARTESIAN_POINT('Ctrl Pts',(0.504434245978927,5.366176087194,-9.60107874964041));
#52946=CARTESIAN_POINT('Ctrl Pts',(0.346736308694608,5.38559979654847,-9.5959059975325));
#52947=CARTESIAN_POINT('Ctrl Pts',(0.188158926194008,5.39842785415446,-9.59074135820327));
#52948=CARTESIAN_POINT('Ctrl Pts',(0.0291872541970131,5.40464051199876,
-9.58557970850075));
#52949=CARTESIAN_POINT('Ctrl Pts',(-0.0807427828887296,5.40893660889857,
-9.58201039117462));
#52950=CARTESIAN_POINT('Ctrl Pts',(-0.190861650141258,5.41006828149116,
-9.57844250343431));
#52951=CARTESIAN_POINT('Ctrl Pts',(-0.30100952587624,5.40801441897329,-9.57487435122625));
#52952=CARTESIAN_POINT('Ctrl Pts',(-0.397441723071222,5.40621630462915,
-9.57175050743849));
#52953=CARTESIAN_POINT('Ctrl Pts',(-0.493896213953238,5.40197642027737,
-9.56862646094568));
#52954=CARTESIAN_POINT('Ctrl Pts',(-0.590264680648783,5.39527294553146,
-9.56550107499785));
#52955=CARTESIAN_POINT('Ctrl Pts',(-0.615978987046301,5.39348423591041,
-9.56466711826253));
#52956=CARTESIAN_POINT('Ctrl Pts',(-0.641690795569914,5.39151970479417,
-9.56383294798454));
#52957=CARTESIAN_POINT('Ctrl Pts',(-0.667371531977541,5.3893812707165,-9.56299940297276));
#52958=CARTESIAN_POINT('Ctrl Pts',(-0.829270594756447,5.37589994107338,
-9.5577444852769));
#52959=CARTESIAN_POINT('Ctrl Pts',(-0.990135744404899,5.35549932104634,
-9.55250787197851));
#52960=CARTESIAN_POINT('Ctrl Pts',(-1.14945847310104,5.32820571619838,-9.54728435100756));
#52961=CARTESIAN_POINT('Ctrl Pts',(-1.30657774605491,5.30128958574357,-9.54213307206618));
#52962=CARTESIAN_POINT('Ctrl Pts',(-1.46219782294251,5.26766974957298,-9.536994525819));
#52963=CARTESIAN_POINT('Ctrl Pts',(-1.61583449285355,5.22731999533615,-9.53186371346998));
#52964=CARTESIAN_POINT('Ctrl Pts',(-1.77270308583972,5.1861214378685,-9.52662496861479));
#52965=CARTESIAN_POINT('Ctrl Pts',(-1.92750487728277,5.13790710889339,-9.52139428646294));
#52966=CARTESIAN_POINT('Ctrl Pts',(-2.07971463146265,5.08259314212322,-9.51616634606952));
#52967=CARTESIAN_POINT('Ctrl Pts',(-2.22307874051765,5.03049373754149,-9.51124222658235));
#52968=CARTESIAN_POINT('Ctrl Pts',(-2.36414389577942,4.97209550169895,-9.50632053943975));
#52969=CARTESIAN_POINT('Ctrl Pts',(-2.50245210566454,4.90728144565132,-9.50139683850687));
#52970=CARTESIAN_POINT('Ctrl Pts',(-2.51098579900357,4.90328238240823,-9.50109304342566));
#52971=CARTESIAN_POINT('Ctrl Pts',(-2.5195089888609,4.89925887980383,-9.50078924067803));
#52972=CARTESIAN_POINT('Ctrl Pts',(-2.52802156438008,4.89521090457976,-9.50048542921963));
#52973=CARTESIAN_POINT('Ctrl Pts',(-2.57132234240826,4.87462013551746,-9.49894003646592));
#52974=CARTESIAN_POINT('Ctrl Pts',(-2.61434850193029,4.85339618259019,-9.49739441832657));
#52975=CARTESIAN_POINT('Ctrl Pts',(-2.65709309431552,4.83154930784417,-9.49584843734864));
#52976=CARTESIAN_POINT('Ctrl Pts',(-2.6760615610272,4.82185447410616,-9.49516238825845));
#52977=CARTESIAN_POINT('Ctrl Pts',(-2.69496807459095,4.81204025654554,-9.4944765024017));
#52978=CARTESIAN_POINT('Ctrl Pts',(-2.71380592953414,4.80211114530722,-9.49379099483116));
#52979=CARTESIAN_POINT('Ctrl Pts',(-2.84926842013991,4.73071118273708,-9.48886152897028));
#52980=CARTESIAN_POINT('Ctrl Pts',(-2.98128317523458,4.65332256785403,-9.48394795579456));
#52981=CARTESIAN_POINT('Ctrl Pts',(-3.10968019447802,4.57039549293769,-9.47904597111631));
#52982=CARTESIAN_POINT('Ctrl Pts',(-3.24115785230975,4.48547874296108,-9.47402637277968));
#52983=CARTESIAN_POINT('Ctrl Pts',(-3.36884257048857,4.39475421907267,-9.4690189256989));
#52984=CARTESIAN_POINT('Ctrl Pts',(-3.49253305551556,4.2986536163194,-9.46401900838148));
#52985=CARTESIAN_POINT('Ctrl Pts',(-3.61846974796904,4.20080783577377,-9.45892829304183));
#52986=CARTESIAN_POINT('Ctrl Pts',(-3.74026635650893,4.09738848130592,-9.45384538342829));
#52987=CARTESIAN_POINT('Ctrl Pts',(-3.85768343310466,3.98880461048543,-9.44876540167088));
#52988=CARTESIAN_POINT('Ctrl Pts',(-3.97901726934032,3.87659863515419,-9.44351596357802));
#52989=CARTESIAN_POINT('Ctrl Pts',(-4.09567526725608,3.7588773848341,-9.43826965193208));
#52990=CARTESIAN_POINT('Ctrl Pts',(-4.20735462904591,3.63604990000422,-9.43302108425564));
#52991=CARTESIAN_POINT('Ctrl Pts',(-4.23973848882022,3.600433399503,-9.43149914791103));
#52992=CARTESIAN_POINT('Ctrl Pts',(-4.27170344532821,3.56438730989727,-9.42997702187123));
#52993=CARTESIAN_POINT('Ctrl Pts',(-4.30324139350661,3.52792105998702,-9.42845457490134));
#52994=CARTESIAN_POINT('Ctrl Pts',(-4.31633871211275,3.51277707881412,-9.42782232156284));
#52995=CARTESIAN_POINT('Ctrl Pts',(-4.32936416131798,3.49755852787676,-9.42718992591442));
#52996=CARTESIAN_POINT('Ctrl Pts',(-4.34231115280572,3.48227315974663,-9.42655767144258));
#52997=CARTESIAN_POINT('Ctrl Pts',(-4.44720672844005,3.35843222802825,-9.42143519207479));
#52998=CARTESIAN_POINT('Ctrl Pts',(-4.54678702961592,3.23041013060237,-9.4163302350616));
#52999=CARTESIAN_POINT('Ctrl Pts',(-4.64084015186826,3.09865692394184,-9.41123798111106));
#53000=CARTESIAN_POINT('Ctrl Pts',(-4.7358219581732,2.96560278118293,-9.40609544605424));
#53001=CARTESIAN_POINT('Ctrl Pts',(-4.82516742957498,2.82874288782327,-9.4009658661596));
#53002=CARTESIAN_POINT('Ctrl Pts',(-4.90862468068945,2.6884992822051,-9.39584427796333));
#53003=CARTESIAN_POINT('Ctrl Pts',(-4.99196861908384,2.54844609005268,-9.39072964351981));
#53004=CARTESIAN_POINT('Ctrl Pts',(-5.06944080169255,2.4050177011056,-9.3856229790882));
#53005=CARTESIAN_POINT('Ctrl Pts',(-5.14074940665675,2.25860287614353,-9.38051934139442));
#53006=CARTESIAN_POINT('Ctrl Pts',(-5.20678494943055,2.12301499805566,-9.37579310273924));
#53007=CARTESIAN_POINT('Ctrl Pts',(-5.26753466845846,1.98486530433382,-9.37106945973583));
#53008=CARTESIAN_POINT('Ctrl Pts',(-5.32272986425895,1.84444578167446,-9.36634448663887));
#53009=CARTESIAN_POINT('Ctrl Pts',(-5.34342806268413,1.7917884606772,-9.36457262172751));
#53010=CARTESIAN_POINT('Ctrl Pts',(-5.3633447702337,1.73881181882729,-9.36280056977174));
#53011=CARTESIAN_POINT('Ctrl Pts',(-5.38246436805708,1.68553087368646,-9.36102812374983));
#53012=CARTESIAN_POINT('Ctrl Pts',(-5.39270432228341,1.6569949994271,-9.36007884823156));
#53013=CARTESIAN_POINT('Ctrl Pts',(-5.40271562012224,1.62837183624343,-9.35912945967968));
#53014=CARTESIAN_POINT('Ctrl Pts',(-5.41249576240362,1.59966367478316,-9.35817992629075));
#53015=CARTESIAN_POINT('Ctrl Pts',(-5.41876862300425,1.58125062006888,-9.35757090748377));
#53016=CARTESIAN_POINT('Ctrl Pts',(-5.42494329014966,1.56281169347572,-9.35696212990386));
#53017=CARTESIAN_POINT('Ctrl Pts',(-5.43101927383042,1.54434791027037,-9.35635359557542));
#53018=CARTESIAN_POINT('Ctrl Pts',(-5.4823982305406,1.38821682634118,-9.35120778535601));
#53019=CARTESIAN_POINT('Ctrl Pts',(-5.52672684681361,1.23030346915463,-9.34607912837171));
#53020=CARTESIAN_POINT('Ctrl Pts',(-5.56374821171423,1.0710197864802,-9.3409627306753));
#53021=CARTESIAN_POINT('Ctrl Pts',(-5.60035869324713,0.913503921284557,
-9.33590311756048));
#53022=CARTESIAN_POINT('Ctrl Pts',(-5.62982360628131,0.754647288089156,
-9.33085549312306));
#53023=CARTESIAN_POINT('Ctrl Pts',(-5.65184871534535,0.594826257001726,
-9.32581512456111));
#53024=CARTESIAN_POINT('Ctrl Pts',(-5.65448373952039,0.575705703302327,
-9.32521210856818));
#53025=CARTESIAN_POINT('Ctrl Pts',(-5.65701221878381,0.55657132707348,-9.32460919642916));
#53026=CARTESIAN_POINT('Ctrl Pts',(-5.65943360070479,0.537423758590119,
-9.32400638003972));
#53027=CARTESIAN_POINT('Ctrl Pts',(-5.67950244104725,0.378725334558598,
-9.31901013150466));
#53028=CARTESIAN_POINT('Ctrl Pts',(-5.69221872259358,0.219121256265095,
-9.31402046037817));
#53029=CARTESIAN_POINT('Ctrl Pts',(-5.69781027578945,0.0590179871714817,
-9.3090327524765));
#53030=CARTESIAN_POINT('Ctrl Pts',(-5.70163108079481,-0.0503833456066027,
-9.30562456540425));
#53031=CARTESIAN_POINT('Ctrl Pts',(-5.7021240585946,-0.160017990101504,
-9.3022172950059));
#53032=CARTESIAN_POINT('Ctrl Pts',(-5.69934808129051,-0.26975677675946,
-9.29880946909734));
#53033=CARTESIAN_POINT('Ctrl Pts',(-5.69780356414277,-0.330813989840834,
-9.29691339972224));
#53034=CARTESIAN_POINT('Ctrl Pts',(-5.69524689311437,-0.391903436918231,
-9.29501715837992));
#53035=CARTESIAN_POINT('Ctrl Pts',(-5.69168677241887,-0.453002721037327,
-9.29312049150345));
#53036=CARTESIAN_POINT('Ctrl Pts',(-5.68974201274654,-0.486378955700753,
-9.29208441391825));
#53037=CARTESIAN_POINT('Ctrl Pts',(-5.68749780355416,-0.519758123083858,
-9.29104820935261));
#53038=CARTESIAN_POINT('Ctrl Pts',(-5.68495543794551,-0.553136547526968,
-9.29001183647358));
#53039=CARTESIAN_POINT('Ctrl Pts',(-5.68342487061243,-0.573231189268683,
-9.28938791422254));
#53040=CARTESIAN_POINT('Ctrl Pts',(-5.68178623914004,-0.593324946043118,
-9.28876395002797));
#53041=CARTESIAN_POINT('Ctrl Pts',(-5.68004112120349,-0.613403791375216,
-9.28814034562909));
#53042=CARTESIAN_POINT('Ctrl Pts',(-5.66613823063394,-0.773366613123692,
-9.28317225520109));
#53043=CARTESIAN_POINT('Ctrl Pts',(-5.6454650766378,-0.932600507598867,
-9.27822022219613));
#53044=CARTESIAN_POINT('Ctrl Pts',(-5.61829635714927,-1.09070410950735,
-9.27327984623788));
#53045=CARTESIAN_POINT('Ctrl Pts',(-5.58917703401029,-1.26015890752813,
-9.26798477136262));
#53046=CARTESIAN_POINT('Ctrl Pts',(-5.55259634674091,-1.4283160454691,-9.26270308747931));
#53047=CARTESIAN_POINT('Ctrl Pts',(-5.5088289095376,-1.59468685397629,-9.25742937674837));
#53048=CARTESIAN_POINT('Ctrl Pts',(-5.46655380827193,-1.75538492602971,
-9.25233548344682));
#53049=CARTESIAN_POINT('Ctrl Pts',(-5.41757308364143,-1.91441717627524,
-9.24724902884695));
#53050=CARTESIAN_POINT('Ctrl Pts',(-5.36208030098775,-2.07133656286447,
-9.24216513062297));
#53051=CARTESIAN_POINT('Ctrl Pts',(-5.31874665211625,-2.19387303111163,
-9.23819517543237));
#53052=CARTESIAN_POINT('Ctrl Pts',(-5.27144095230737,-2.31512109201928,
-9.23422677908423));
#53053=CARTESIAN_POINT('Ctrl Pts',(-5.22023454988606,-2.43486046781029,
-9.23025761673876));
#53054=CARTESIAN_POINT('Ctrl Pts',(-5.19766184574894,-2.48764374051623,
-9.22850793851377));
#53055=CARTESIAN_POINT('Ctrl Pts',(-5.17433092507079,-2.54013373595243,
-9.2267581114398));
#53056=CARTESIAN_POINT('Ctrl Pts',(-5.15024683751494,-2.59231099174797,
-9.22500793637109));
#53057=CARTESIAN_POINT('Ctrl Pts',(-5.13639526128057,-2.62231990259733,
-9.22400135128326));
#53058=CARTESIAN_POINT('Ctrl Pts',(-5.12229454146471,-2.65222535832149,
-9.22299465108607));
#53059=CARTESIAN_POINT('Ctrl Pts',(-5.10794554487069,-2.68202359114896,
-9.22198779789358));
#53060=CARTESIAN_POINT('Ctrl Pts',(-5.095685933705,-2.70748284507627,-9.22112755456158));
#53061=CARTESIAN_POINT('Ctrl Pts',(-5.0832428176014,-2.73286821067675,-9.22026704943273));
#53062=CARTESIAN_POINT('Ctrl Pts',(-5.07063039957229,-2.75815032754945,
-9.21940717965711));
#53063=CARTESIAN_POINT('Ctrl Pts',(-4.99566720805045,-2.90841716494984,
-9.21429645604136));
#53064=CARTESIAN_POINT('Ctrl Pts',(-4.91465075447715,-3.05520204842461,
-9.20920264493437));
#53065=CARTESIAN_POINT('Ctrl Pts',(-4.82781920673447,-3.19807080861358,
-9.20412095685482));
#53066=CARTESIAN_POINT('Ctrl Pts',(-4.74101616741469,-3.34089266231361,
-9.19904093718862));
#53067=CARTESIAN_POINT('Ctrl Pts',(-4.64840155481371,-3.47980172218689,
-9.19397303259074));
#53068=CARTESIAN_POINT('Ctrl Pts',(-4.55016419752807,-3.61434871789838,
-9.18891245829572));
#53069=CARTESIAN_POINT('Ctrl Pts',(-4.45302663040113,-3.74738942856866,
-9.18390853831187));
#53070=CARTESIAN_POINT('Ctrl Pts',(-4.35039115846723,-3.87616588444105,
-9.17891178542071));
#53071=CARTESIAN_POINT('Ctrl Pts',(-4.24239726756525,-4.00021786115194,
-9.17391757376416));
#53072=CARTESIAN_POINT('Ctrl Pts',(-4.14727373351209,-4.10948573114406,
-9.16951855583255));
#53073=CARTESIAN_POINT('Ctrl Pts',(-4.04799214062475,-4.21508806575459,
-9.16512150951696));
#53074=CARTESIAN_POINT('Ctrl Pts',(-3.94462271981528,-4.3166870024335,-9.16072327356863));
#53075=CARTESIAN_POINT('Ctrl Pts',(-3.89293800941055,-4.36748647077295,
-9.15852415559446));
#53076=CARTESIAN_POINT('Ctrl Pts',(-3.84023098885666,-4.41728470755125,
-9.1563247402121));
#53077=CARTESIAN_POINT('Ctrl Pts',(-3.78650840229268,-4.46603693343018,
-9.15412463226547));
#53078=CARTESIAN_POINT('Ctrl Pts',(-3.76979768336693,-4.48120159313429,
-9.15344027605975));
#53079=CARTESIAN_POINT('Ctrl Pts',(-3.75298869317158,-4.49626503182372,
-9.1527558528445));
#53080=CARTESIAN_POINT('Ctrl Pts',(-3.73608160926019,-4.51122586421657,
-9.15207135072695));
#53081=CARTESIAN_POINT('Ctrl Pts',(-3.72066822985047,-4.52486493924364,
-9.15144732289933));
#53082=CARTESIAN_POINT('Ctrl Pts',(-3.70517980652966,-4.53841298498712,
-9.15082349226079));
#53083=CARTESIAN_POINT('Ctrl Pts',(-3.68961891476628,-4.55186726085941,
-9.1501999389971));
#53084=CARTESIAN_POINT('Ctrl Pts',(-3.6673746372544,-4.57110013329215,-9.14930857029843));
#53085=CARTESIAN_POINT('Ctrl Pts',(-3.64498081745003,-4.59014268141462,
-9.14841770939315));
#53086=CARTESIAN_POINT('Ctrl Pts',(-3.62243853028556,-4.60899255635498,
-9.1475273308598));
#53087=CARTESIAN_POINT('Ctrl Pts',(-3.50034074186636,-4.71109080509985,
-9.14270469467454));
#53088=CARTESIAN_POINT('Ctrl Pts',(-3.373890663402,-4.80753926503602,-9.137896209963));
#53089=CARTESIAN_POINT('Ctrl Pts',(-3.24356761447411,-4.89836659707662,
-9.1330978372056));
#53090=CARTESIAN_POINT('Ctrl Pts',(-3.10895860137107,-4.99218098853959,
-9.12814165925635));
#53091=CARTESIAN_POINT('Ctrl Pts',(-2.97021723316815,-5.07999878946387,
-9.12319626930637));
#53092=CARTESIAN_POINT('Ctrl Pts',(-2.82783156379497,-5.16181301723526,
-9.11825721603946));
#53093=CARTESIAN_POINT('Ctrl Pts',(-2.68343867607943,-5.24478058452017,
-9.11324853667636));
#53094=CARTESIAN_POINT('Ctrl Pts',(-2.53529736368481,-5.32157438622776,
-9.10824637391274));
#53095=CARTESIAN_POINT('Ctrl Pts',(-2.38388466705377,-5.39214360897498,
-9.10324608551482));
#53096=CARTESIAN_POINT('Ctrl Pts',(-2.23107388974751,-5.4633644380193,-9.09819962657284));
#53097=CARTESIAN_POINT('Ctrl Pts',(-2.07493030423668,-5.5282454698157,-9.09315507677058));
#53098=CARTESIAN_POINT('Ctrl Pts',(-1.91592251661704,-5.58668647934873,
-9.08810766408999));
#53099=CARTESIAN_POINT('Ctrl Pts',(-1.86492339105374,-5.6054304693623,-9.08648878971332));
#53100=CARTESIAN_POINT('Ctrl Pts',(-1.81362950493446,-5.6235115915611,-9.08486962083241));
#53101=CARTESIAN_POINT('Ctrl Pts',(-1.76205604469197,-5.64092543727167,
-9.08325));
#53102=CARTESIAN_POINT('Origin',(0.,0.,-10.));
#53103=CARTESIAN_POINT('Origin',(0.,0.,-10.));
#53104=CARTESIAN_POINT('',(2.85706463458463,-4.00329423553975,-10.));
#53105=CARTESIAN_POINT('Ctrl Pts',(3.54751238410106,-3.52143928316762,-10.));
#53106=CARTESIAN_POINT('Ctrl Pts',(3.43727113798793,-3.61340023595403,-10.));
#53107=CARTESIAN_POINT('Ctrl Pts',(3.32309228486466,-3.70055940759421,-10.));
#53108=CARTESIAN_POINT('Ctrl Pts',(3.20515669348447,-3.78259068630623,-10.));
#53109=CARTESIAN_POINT('Ctrl Pts',(3.09250600088469,-3.86094600087759,-10.));
#53110=CARTESIAN_POINT('Ctrl Pts',(2.97642721282368,-3.93462271815296,-10.));
#53111=CARTESIAN_POINT('Ctrl Pts',(2.85706463458369,-4.00329423554042,-10.));
#53112=CARTESIAN_POINT('',(-2.85706463458558,-4.00329423553907,-10.));
#53113=CARTESIAN_POINT('Origin',(0.,0.,-10.));
#53114=CARTESIAN_POINT('Ctrl Pts',(-2.85711522928017,-4.00149011032074,
-10.));
#53115=CARTESIAN_POINT('Ctrl Pts',(-2.98510663627035,-3.92827452489103,
-10.));
#53116=CARTESIAN_POINT('Ctrl Pts',(-3.10954218075165,-3.84942396520819,
-10.));
#53117=CARTESIAN_POINT('Ctrl Pts',(-3.2300790650384,-3.76515943171096,-10.));
#53118=CARTESIAN_POINT('Ctrl Pts',(-3.33981495603391,-3.68844562151621,
-10.));
#53119=CARTESIAN_POINT('Ctrl Pts',(-3.4463200216345,-3.60724388606328,-10.));
#53120=CARTESIAN_POINT('Ctrl Pts',(-3.54932990765358,-3.52168385953437,
-10.));
#53121=CARTESIAN_POINT('Origin',(0.,0.,147.5));
#53122=CARTESIAN_POINT('',(-5.,-6.12323399573677E-16,147.));
#53123=CARTESIAN_POINT('Origin',(0.,0.,147.));
#53124=CARTESIAN_POINT('',(-5.,-6.12323399573677E-16,148.));
#53125=CARTESIAN_POINT('',(-5.,-6.12323399573677E-16,147.5));
#53126=CARTESIAN_POINT('Origin',(0.,0.,148.));
#53127=CARTESIAN_POINT('Origin',(9.,0.,147.));
#53128=CARTESIAN_POINT('Origin',(5.,0.,148.));
#53129=CARTESIAN_POINT('',(-5.91675,-7.2459289488551E-16,148.));
#53130=CARTESIAN_POINT('Origin',(0.,0.,148.));
#53131=CARTESIAN_POINT('Origin',(0.,0.,-10.));
#53132=CARTESIAN_POINT('',(-5.91675,7.2459289488551E-16,162.));
#53133=CARTESIAN_POINT('Origin',(0.,0.,162.));
#53134=CARTESIAN_POINT('',(-5.91675,-7.2459289488551E-16,-10.));
#53135=CARTESIAN_POINT('Origin',(7.01450167938425E-16,2.84304068604708E-16,
130.));
#53136=CARTESIAN_POINT('Ctrl Pts',(2.86417334265909,-4.00661193697115,130.));
#53137=CARTESIAN_POINT('Ctrl Pts',(2.96578276202768,-3.94896682571219,130.));
#53138=CARTESIAN_POINT('Ctrl Pts',(3.06499684984438,-3.88759437514104,130.));
#53139=CARTESIAN_POINT('Ctrl Pts',(3.16157834138731,-3.82254108203266,130.));
#53140=CARTESIAN_POINT('Ctrl Pts',(3.2788139169888,-3.74357605322128,130.));
#53141=CARTESIAN_POINT('Ctrl Pts',(3.39217184567194,-3.65918923033172,130.));
#53142=CARTESIAN_POINT('Ctrl Pts',(3.50155723888932,-3.56980772067352,130.));
#53143=CARTESIAN_POINT('Ctrl Pts',(3.57830130427611,-3.50709824713396,130.));
#53144=CARTESIAN_POINT('Ctrl Pts',(3.65308960208866,-3.44192910170494,130.));
#53145=CARTESIAN_POINT('Ctrl Pts',(3.72588284987221,-3.37443414400712,130.));
#53146=CARTESIAN_POINT('Ctrl Pts',(3.76351932356994,-3.33953705839175,130.));
#53147=CARTESIAN_POINT('Ctrl Pts',(3.80062238017016,-3.30401805771336,130.));
#53148=CARTESIAN_POINT('Ctrl Pts',(3.83718593267987,-3.26789459823601,130.));
#53149=CARTESIAN_POINT('Ctrl Pts',(3.8553536472403,-3.24994555730117,130.));
#53150=CARTESIAN_POINT('Ctrl Pts',(3.87338815622643,-3.23184727089816,130.));
#53151=CARTESIAN_POINT('Ctrl Pts',(3.89128866818473,-3.21360182011092,130.));
#53152=CARTESIAN_POINT('Ctrl Pts',(3.90755204940963,-3.19702504719714,130.));
#53153=CARTESIAN_POINT('Ctrl Pts',(3.92369773306074,-3.18033401739892,130.));
#53154=CARTESIAN_POINT('Ctrl Pts',(3.93972478721132,-3.16353123186673,130.));
#53155=CARTESIAN_POINT('Ctrl Pts',(4.04018601889038,-3.05820753891966,130.));
#53156=CARTESIAN_POINT('Ctrl Pts',(4.13599554083928,-2.94848917560709,130.));
#53157=CARTESIAN_POINT('Ctrl Pts',(4.22705195107335,-2.83481997013712,130.));
#53158=CARTESIAN_POINT('Ctrl Pts',(4.32452800844826,-2.7131368731902,130.));
#53159=CARTESIAN_POINT('Ctrl Pts',(4.41655796319061,-2.58692609159507,130.));
#53160=CARTESIAN_POINT('Ctrl Pts',(4.50298379913026,-2.45667794374954,130.));
#53161=CARTESIAN_POINT('Ctrl Pts',(4.54079510235386,-2.39969437906712,130.));
#53162=CARTESIAN_POINT('Ctrl Pts',(4.57753324901869,-2.34193738296473,130.));
#53163=CARTESIAN_POINT('Ctrl Pts',(4.61318252808862,-2.2834452270631,130.));
#53164=CARTESIAN_POINT('Ctrl Pts',(4.6392253424799,-2.24071504010746,130.));
#53165=CARTESIAN_POINT('Ctrl Pts',(4.66468702707171,-2.19759248458433,130.));
#53166=CARTESIAN_POINT('Ctrl Pts',(4.68956089066644,-2.15409199395247,130.));
#53167=CARTESIAN_POINT('Ctrl Pts',(4.69918353646736,-2.13726349395196,130.));
#53168=CARTESIAN_POINT('Ctrl Pts',(4.70871686517466,-2.12038070842633,130.));
#53169=CARTESIAN_POINT('Ctrl Pts',(4.71815642930611,-2.1034520684253,130.));
#53170=CARTESIAN_POINT('Ctrl Pts',(4.79232967335433,-1.97043192801249,130.));
#53171=CARTESIAN_POINT('Ctrl Pts',(4.86079223538357,-1.83445140446128,130.));
#53172=CARTESIAN_POINT('Ctrl Pts',(4.9234351422813,-1.69597533119363,130.));
#53173=CARTESIAN_POINT('Ctrl Pts',(4.98692662668076,-1.5556234241545,130.));
#53174=CARTESIAN_POINT('Ctrl Pts',(5.04444021787131,-1.41270730386396,130.));
#53175=CARTESIAN_POINT('Ctrl Pts',(5.09582801483642,-1.26766968144916,130.));
#53176=CARTESIAN_POINT('Ctrl Pts',(5.14739091908899,-1.12213783382644,130.));
#53177=CARTESIAN_POINT('Ctrl Pts',(5.19278668030377,-0.974469303347938,
130.));
#53178=CARTESIAN_POINT('Ctrl Pts',(5.23182419840718,-0.825079944137655,
130.));
#53179=CARTESIAN_POINT('Ctrl Pts',(5.26318419108894,-0.705071054249778,
130.));
#53180=CARTESIAN_POINT('Ctrl Pts',(5.29044026624906,-0.583950896370881,
130.));
#53181=CARTESIAN_POINT('Ctrl Pts',(5.31347082763723,-0.461925133621565,
130.));
#53182=CARTESIAN_POINT('Ctrl Pts',(5.32241008870535,-0.414561105803583,
130.));
#53183=CARTESIAN_POINT('Ctrl Pts',(5.33071251100927,-0.367060569029899,
130.));
#53184=CARTESIAN_POINT('Ctrl Pts',(5.33837008369061,-0.319435324949108,
130.));
#53185=CARTESIAN_POINT('Ctrl Pts',(5.34328214856315,-0.288885397677037,
130.));
#53186=CARTESIAN_POINT('Ctrl Pts',(5.34792886200234,-0.258284154039901,
130.));
#53187=CARTESIAN_POINT('Ctrl Pts',(5.35230799414418,-0.227634691612514,
130.));
#53188=CARTESIAN_POINT('Ctrl Pts',(5.35503902012298,-0.208520292819688,
130.));
#53189=CARTESIAN_POINT('Ctrl Pts',(5.3576652805494,-0.189391776026415,130.));
#53190=CARTESIAN_POINT('Ctrl Pts',(5.36018540154735,-0.170257938742505,
130.));
#53191=CARTESIAN_POINT('Ctrl Pts',(5.38088704007115,-0.0130822383109732,
130.));
#53192=CARTESIAN_POINT('Ctrl Pts',(5.39445343673034,0.144612493973096,130.));
#53193=CARTESIAN_POINT('Ctrl Pts',(5.40073333988398,0.302371939349598,130.));
#53194=CARTESIAN_POINT('Ctrl Pts',(5.40532221026111,0.417650412263869,130.));
#53195=CARTESIAN_POINT('Ctrl Pts',(5.40601960721486,0.532964206250372,130.));
#53196=CARTESIAN_POINT('Ctrl Pts',(5.40275094325442,0.648144274292171,130.));
#53197=CARTESIAN_POINT('Ctrl Pts',(5.39842112123799,0.800717068711322,130.));
#53198=CARTESIAN_POINT('Ctrl Pts',(5.38713445618709,0.953055205515926,130.));
#53199=CARTESIAN_POINT('Ctrl Pts',(5.36917158042469,1.10477541171324,130.));
#53200=CARTESIAN_POINT('Ctrl Pts',(5.35092698461533,1.25887511572479,130.));
#53201=CARTESIAN_POINT('Ctrl Pts',(5.32579502801831,1.4123380456589,130.));
#53202=CARTESIAN_POINT('Ctrl Pts',(5.29401591504677,1.56476615531412,130.));
#53203=CARTESIAN_POINT('Ctrl Pts',(5.27817026521515,1.64076961243561,130.));
#53204=CARTESIAN_POINT('Ctrl Pts',(5.26067117500297,1.71651578167034,130.));
#53205=CARTESIAN_POINT('Ctrl Pts',(5.24154366365584,1.79195479764749,130.));
#53206=CARTESIAN_POINT('Ctrl Pts',(5.2352532364493,1.81676427912813,130.));
#53207=CARTESIAN_POINT('Ctrl Pts',(5.22878666396949,1.8415405356193,130.));
#53208=CARTESIAN_POINT('Ctrl Pts',(5.22214476416494,1.86628177640074,130.));
#53209=CARTESIAN_POINT('Ctrl Pts',(5.21735806229335,1.88411235907121,130.));
#53210=CARTESIAN_POINT('Ctrl Pts',(5.2124811310063,1.90192154477755,130.));
#53211=CARTESIAN_POINT('Ctrl Pts',(5.20751665209725,1.91970078810442,130.));
#53212=CARTESIAN_POINT('Ctrl Pts',(5.16515981846288,2.0713929325444,130.));
#53213=CARTESIAN_POINT('Ctrl Pts',(5.11638897344517,2.22107460978644,130.));
#53214=CARTESIAN_POINT('Ctrl Pts',(5.0615294421976,2.3683471330429,130.));
#53215=CARTESIAN_POINT('Ctrl Pts',(5.00580294678831,2.51794705496218,130.));
#53216=CARTESIAN_POINT('Ctrl Pts',(4.94379366704092,2.66506178406266,130.));
#53217=CARTESIAN_POINT('Ctrl Pts',(4.87578870350513,2.80927707437429,130.));
#53218=CARTESIAN_POINT('Ctrl Pts',(4.80697460991496,2.9552082530509,130.));
#53219=CARTESIAN_POINT('Ctrl Pts',(4.7320211223972,3.09817137776604,130.));
#53220=CARTESIAN_POINT('Ctrl Pts',(4.65117345482382,3.23772952533661,130.));
#53221=CARTESIAN_POINT('Ctrl Pts',(4.64031025008783,3.25648144206022,130.));
#53222=CARTESIAN_POINT('Ctrl Pts',(4.62934055615847,3.27517186246557,130.));
#53223=CARTESIAN_POINT('Ctrl Pts',(4.61826490004014,3.29379970385774,130.));
#53224=CARTESIAN_POINT('Ctrl Pts',(4.55640877022608,3.3978338272541,130.));
#53225=CARTESIAN_POINT('Ctrl Pts',(4.49124877272854,3.499916689806,130.));
#53226=CARTESIAN_POINT('Ctrl Pts',(4.42288946352048,3.5999300492289,130.));
#53227=CARTESIAN_POINT('Ctrl Pts',(4.39298226574196,3.64368589397642,130.));
#53228=CARTESIAN_POINT('Ctrl Pts',(4.3624625121461,3.68704552115934,130.));
#53229=CARTESIAN_POINT('Ctrl Pts',(4.3313381114467,3.72999850731393,130.));
#53230=CARTESIAN_POINT('Ctrl Pts',(4.31168386061072,3.75712220271259,130.));
#53231=CARTESIAN_POINT('Ctrl Pts',(4.29178849095401,3.78408373943631,130.));
#53232=CARTESIAN_POINT('Ctrl Pts',(4.27165389347949,3.81088041853506,130.));
#53233=CARTESIAN_POINT('Ctrl Pts',(4.25892564129572,3.82782016067234,130.));
#53234=CARTESIAN_POINT('Ctrl Pts',(4.24610132908206,3.84469453115168,130.));
#53235=CARTESIAN_POINT('Ctrl Pts',(4.23319137984965,3.8614901296792,130.));
#53236=CARTESIAN_POINT('Ctrl Pts',(4.1334204286307,3.99129024052502,130.));
#53237=CARTESIAN_POINT('Ctrl Pts',(4.02840245584316,4.11657006442815,130.));
#53238=CARTESIAN_POINT('Ctrl Pts',(3.91847912791786,4.2370855331423,130.));
#53239=CARTESIAN_POINT('Ctrl Pts',(3.80717191983546,4.3591182318105,130.));
#53240=CARTESIAN_POINT('Ctrl Pts',(3.69083477586065,4.47626647053335,130.));
#53241=CARTESIAN_POINT('Ctrl Pts',(3.56977267870164,4.58825804551576,130.));
#53242=CARTESIAN_POINT('Ctrl Pts',(3.4488161551608,4.70015195693499,130.));
#53243=CARTESIAN_POINT('Ctrl Pts',(3.32314251076017,4.80689878301852,130.));
#53244=CARTESIAN_POINT('Ctrl Pts',(3.19301198855863,4.908199402403,130.));
#53245=CARTESIAN_POINT('Ctrl Pts',(3.06455341841885,5.00819848409614,130.));
#53246=CARTESIAN_POINT('Ctrl Pts',(2.93175130061798,5.1028909152538,130.));
#53247=CARTESIAN_POINT('Ctrl Pts',(2.79481968753776,5.19195398985847,130.));
#53248=CARTESIAN_POINT('Ctrl Pts',(2.72556825359359,5.236996515022,130.));
#53249=CARTESIAN_POINT('Ctrl Pts',(2.65526008082166,5.28059861334327,130.));
#53250=CARTESIAN_POINT('Ctrl Pts',(2.58391981634458,5.32271443393329,130.));
#53251=CARTESIAN_POINT('Ctrl Pts',(-2.59168464642813,5.32810255942583,130.));
#53252=CARTESIAN_POINT('Ctrl Pts',(-2.71132798771431,5.25826632968106,130.));
#53253=CARTESIAN_POINT('Ctrl Pts',(-2.82813785948501,5.18406707412924,130.));
#53254=CARTESIAN_POINT('Ctrl Pts',(-2.94183908547589,5.10549286651818,130.));
#53255=CARTESIAN_POINT('Ctrl Pts',(-3.07753195615672,5.01172114418801,130.));
#53256=CARTESIAN_POINT('Ctrl Pts',(-3.20879856093728,4.91171884717559,130.));
#53257=CARTESIAN_POINT('Ctrl Pts',(-3.33544390790157,4.80592591755381,130.));
#53258=CARTESIAN_POINT('Ctrl Pts',(-3.41766258017248,4.73724471909174,130.));
#53259=CARTESIAN_POINT('Ctrl Pts',(-3.49793277631496,4.6661221713314,130.));
#53260=CARTESIAN_POINT('Ctrl Pts',(-3.57619172699311,4.59267182290119,130.));
#53261=CARTESIAN_POINT('Ctrl Pts',(-3.62721998191113,4.54477898673313,130.));
#53262=CARTESIAN_POINT('Ctrl Pts',(-3.67739297975411,4.49589635854078,130.));
#53263=CARTESIAN_POINT('Ctrl Pts',(-3.72669148950679,4.44605450340122,130.));
#53264=CARTESIAN_POINT('Ctrl Pts',(-3.74722649737596,4.42529316816736,130.));
#53265=CARTESIAN_POINT('Ctrl Pts',(-3.76760975587872,4.40436539092426,130.));
#53266=CARTESIAN_POINT('Ctrl Pts',(-3.78783979790461,4.38327335155342,130.));
#53267=CARTESIAN_POINT('Ctrl Pts',(-3.80599703519715,4.36434243863936,130.));
#53268=CARTESIAN_POINT('Ctrl Pts',(-3.82402508596036,4.34528516998115,130.));
#53269=CARTESIAN_POINT('Ctrl Pts',(-3.8419196208096,4.32610718559679,130.));
#53270=CARTESIAN_POINT('Ctrl Pts',(-3.95373953775787,4.20626720991925,130.));
#53271=CARTESIAN_POINT('Ctrl Pts',(-4.06039477934112,4.0816687766888,130.));
#53272=CARTESIAN_POINT('Ctrl Pts',(-4.16169333226532,3.95274377575036,130.));
#53273=CARTESIAN_POINT('Ctrl Pts',(-4.26401219978641,3.82252019692935,130.));
#53274=CARTESIAN_POINT('Ctrl Pts',(-4.36086631611474,3.68788169668274,130.));
#53275=CARTESIAN_POINT('Ctrl Pts',(-4.45201053252839,3.54924911468795,130.));
#53276=CARTESIAN_POINT('Ctrl Pts',(-4.53334388495471,3.42553909673154,130.));
#53277=CARTESIAN_POINT('Ctrl Pts',(-4.61012992925456,3.29864786635624,130.));
#53278=CARTESIAN_POINT('Ctrl Pts',(-4.68215943876187,3.16886588604444,130.));
#53279=CARTESIAN_POINT('Ctrl Pts',(-4.69302130707921,3.14929509082797,130.));
#53280=CARTESIAN_POINT('Ctrl Pts',(-4.70377084455898,3.12966591564697,130.));
#53281=CARTESIAN_POINT('Ctrl Pts',(-4.71440565460736,3.10998302703064,130.));
#53282=CARTESIAN_POINT('Ctrl Pts',(-4.79134796001078,2.96757833712556,130.));
#53283=CARTESIAN_POINT('Ctrl Pts',(-4.86232208226549,2.82230393704696,130.));
#53284=CARTESIAN_POINT('Ctrl Pts',(-4.92714211255705,2.67456634541395,130.));
#53285=CARTESIAN_POINT('Ctrl Pts',(-4.99165161938617,2.52753649779587,130.));
#53286=CARTESIAN_POINT('Ctrl Pts',(-5.05006608621869,2.37806623720806,130.));
#53287=CARTESIAN_POINT('Ctrl Pts',(-5.10215320174004,2.22654123991806,130.));
#53288=CARTESIAN_POINT('Ctrl Pts',(-5.15352370275379,2.07710092346008,130.));
#53289=CARTESIAN_POINT('Ctrl Pts',(-5.19873989699047,1.92566131722251,130.));
#53290=CARTESIAN_POINT('Ctrl Pts',(-5.23752848087705,1.77258862010428,130.));
#53291=CARTESIAN_POINT('Ctrl Pts',(-5.26873343336441,1.64944346340934,130.));
#53292=CARTESIAN_POINT('Ctrl Pts',(-5.29577752888173,1.52524116094855,130.));
#53293=CARTESIAN_POINT('Ctrl Pts',(-5.31849325398757,1.40017510822192,130.));
#53294=CARTESIAN_POINT('Ctrl Pts',(-5.32868054202697,1.34408691833846,130.));
#53295=CARTESIAN_POINT('Ctrl Pts',(-5.33799698071074,1.28782506394763,130.));
#53296=CARTESIAN_POINT('Ctrl Pts',(-5.34642591588743,1.23140734783872,130.));
#53297=CARTESIAN_POINT('Ctrl Pts',(-5.35149623877264,1.19746996059804,130.));
#53298=CARTESIAN_POINT('Ctrl Pts',(-5.35624540188262,1.16347618014318,130.));
#53299=CARTESIAN_POINT('Ctrl Pts',(-5.36066960833698,1.12942993355321,130.));
#53300=CARTESIAN_POINT('Ctrl Pts',(-5.36337465687219,1.1086133757326,130.));
#53301=CARTESIAN_POINT('Ctrl Pts',(-5.36595716110829,1.08778520479147,130.));
#53302=CARTESIAN_POINT('Ctrl Pts',(-5.36841592606578,1.06695188444939,130.));
#53303=CARTESIAN_POINT('Ctrl Pts',(-5.38643209853856,0.914299354031173,
130.));
#53304=CARTESIAN_POINT('Ctrl Pts',(-5.39782132330128,0.76127519594384,130.));
#53305=CARTESIAN_POINT('Ctrl Pts',(-5.40237196850048,0.60822166947751,130.));
#53306=CARTESIAN_POINT('Ctrl Pts',(-5.40579165332522,0.493206149937382,
130.));
#53307=CARTESIAN_POINT('Ctrl Pts',(-5.40534852701692,0.37817386832857,130.));
#53308=CARTESIAN_POINT('Ctrl Pts',(-5.4009333780326,0.263271286956652,130.));
#53309=CARTESIAN_POINT('Ctrl Pts',(-5.39498435461679,0.10845020401096,130.));
#53310=CARTESIAN_POINT('Ctrl Pts',(-5.38182560150715,-0.0461364505366216,
130.));
#53311=CARTESIAN_POINT('Ctrl Pts',(-5.36166329395989,-0.200029125946722,
130.));
#53312=CARTESIAN_POINT('Ctrl Pts',(-5.34151584033518,-0.353808425946975,
130.));
#53313=CARTESIAN_POINT('Ctrl Pts',(-5.31437470356353,-0.506895541187959,
130.));
#53314=CARTESIAN_POINT('Ctrl Pts',(-5.28039992254779,-0.658807623106542,
130.));
#53315=CARTESIAN_POINT('Ctrl Pts',(-5.26472627071547,-0.728889519440523,
130.));
#53316=CARTESIAN_POINT('Ctrl Pts',(-5.24759763676859,-0.798720925805533,
130.));
#53317=CARTESIAN_POINT('Ctrl Pts',(-5.22902684970209,-0.868251994011044,
130.));
#53318=CARTESIAN_POINT('Ctrl Pts',(-5.22301676236688,-0.890754421664162,
130.));
#53319=CARTESIAN_POINT('Ctrl Pts',(-5.21685561466066,-0.913225379026263,
130.));
#53320=CARTESIAN_POINT('Ctrl Pts',(-5.21054380404271,-0.935663135660378,
130.));
#53321=CARTESIAN_POINT('Ctrl Pts',(-5.20486822320544,-0.955839169019444,
130.));
#53322=CARTESIAN_POINT('Ctrl Pts',(-5.19907277575825,-0.975981308264116,
130.));
#53323=CARTESIAN_POINT('Ctrl Pts',(-5.19316007549178,-0.996081558145602,
130.));
#53324=CARTESIAN_POINT('Ctrl Pts',(-5.15023736011681,-1.14199751291171,
130.));
#53325=CARTESIAN_POINT('Ctrl Pts',(-5.1011075998424,-1.28582149559654,130.));
#53326=CARTESIAN_POINT('Ctrl Pts',(-5.04599926784503,-1.42713283539364,
130.));
#53327=CARTESIAN_POINT('Ctrl Pts',(-4.99026887878914,-1.5700392827395,130.));
#53328=CARTESIAN_POINT('Ctrl Pts',(-4.9284237967488,-1.71037686011977,130.));
#53329=CARTESIAN_POINT('Ctrl Pts',(-4.86065301345585,-1.84768459305006,
130.));
#53330=CARTESIAN_POINT('Ctrl Pts',(-4.7928822301629,-1.98499232598035,130.));
#53331=CARTESIAN_POINT('Ctrl Pts',(-4.71918527961721,-2.11927098094242,
130.));
#53332=CARTESIAN_POINT('Ctrl Pts',(-4.63971068055132,-2.25002196879991,
130.));
#53333=CARTESIAN_POINT('Ctrl Pts',(-4.5849160685212,-2.34016963530484,130.));
#53334=CARTESIAN_POINT('Ctrl Pts',(-4.52737412606546,-2.4286395222737,130.));
#53335=CARTESIAN_POINT('Ctrl Pts',(-4.46715124519521,-2.51531152444212,
130.));
#53336=CARTESIAN_POINT('Ctrl Pts',(-4.43566885186282,-2.56062058345327,
130.));
#53337=CARTESIAN_POINT('Ctrl Pts',(-4.40345369451756,-2.60543813700367,
130.));
#53338=CARTESIAN_POINT('Ctrl Pts',(-4.37051460776245,-2.64974581524745,
130.));
#53339=CARTESIAN_POINT('Ctrl Pts',(-4.3498704560937,-2.67751508634336,130.));
#53340=CARTESIAN_POINT('Ctrl Pts',(-4.32894193686738,-2.70508406168616,
130.));
#53341=CARTESIAN_POINT('Ctrl Pts',(-4.30773114742818,-2.73244804114046,
130.));
#53342=CARTESIAN_POINT('Ctrl Pts',(-4.29561742812669,-2.74807591614397,
130.));
#53343=CARTESIAN_POINT('Ctrl Pts',(-4.28341758933611,-2.76362923604917,
130.));
#53344=CARTESIAN_POINT('Ctrl Pts',(-4.27113373590674,-2.77910551783698,
130.));
#53345=CARTESIAN_POINT('Ctrl Pts',(-4.17940507365103,-2.89467337553329,
130.));
#53346=CARTESIAN_POINT('Ctrl Pts',(-4.08296782193032,-3.00598297629126,
130.));
#53347=CARTESIAN_POINT('Ctrl Pts',(-3.98206514775803,-3.11276944435602,
130.));
#53348=CARTESIAN_POINT('Ctrl Pts',(-3.88164013777467,-3.21905039488049,
130.));
#53349=CARTESIAN_POINT('Ctrl Pts',(-3.77679132028946,-3.32085136116889,
130.));
#53350=CARTESIAN_POINT('Ctrl Pts',(-3.66772668560753,-3.41787103111659,
130.));
#53351=CARTESIAN_POINT('Ctrl Pts',(-3.55974446398038,-3.51392782838216,
130.));
#53352=CARTESIAN_POINT('Ctrl Pts',(-3.44762915219098,-3.60529811873874,
130.));
#53353=CARTESIAN_POINT('Ctrl Pts',(-3.33155962241286,-3.69164424731295,
130.));
#53354=CARTESIAN_POINT('Ctrl Pts',(-3.21783010743005,-3.7762495984517,130.));
#53355=CARTESIAN_POINT('Ctrl Pts',(-3.10030370603907,-3.85603155384217,
130.));
#53356=CARTESIAN_POINT('Ctrl Pts',(-2.97913416561654,-3.93062466590592,
130.));
#53357=CARTESIAN_POINT('Ctrl Pts',(-2.93884537173577,-3.95542682745891,
130.));
#53358=CARTESIAN_POINT('Ctrl Pts',(-2.89815371868312,-3.97965491914145,
130.));
#53359=CARTESIAN_POINT('Ctrl Pts',(-2.85706463458608,-4.00329423553871,
130.));
#53360=CARTESIAN_POINT('Ctrl Pts',(-3.49129836376668,-3.46410432834522,
-10.0471983845063));
#53361=CARTESIAN_POINT('Ctrl Pts',(-2.91414933031449,-4.04578411773647,
-10.0007944088984));
#53362=CARTESIAN_POINT('Ctrl Pts',(-1.46740602186593,-4.90364861172812,
-9.90798645768269));
#53363=CARTESIAN_POINT('Ctrl Pts',(1.92453937789233,-5.07348089440844,-9.72237055525127));
#53364=CARTESIAN_POINT('Ctrl Pts',(5.43970692864372,-2.05961707410548,-9.49035067721199));
#53365=CARTESIAN_POINT('Ctrl Pts',(4.67141455431437,3.47170793039274,-9.21192682356487));
#53366=CARTESIAN_POINT('Ctrl Pts',(-0.394303111254869,5.8022423708097,-8.93350296991773));
#53367=CARTESIAN_POINT('Ctrl Pts',(-5.09502701080405,2.80733175830066,-8.65507911627061));
#53368=CARTESIAN_POINT('Ctrl Pts',(-5.11582220422363,-2.76998183349922,
-8.37665526262347));
#53369=CARTESIAN_POINT('Ctrl Pts',(-0.435410493021885,-5.80062512701066,
-8.09823140897635));
#53370=CARTESIAN_POINT('Ctrl Pts',(4.64466218789312,-3.50245220498147,-7.81980755532921));
#53371=CARTESIAN_POINT('Ctrl Pts',(5.45739468419239,2.01424609607877,-7.54138370168209));
#53372=CARTESIAN_POINT('Ctrl Pts',(1.25572029180289,5.68000375627327,-7.26295984803495));
#53373=CARTESIAN_POINT('Ctrl Pts',(-4.09966034597428,4.1270561564691,-6.98453599438783));
#53374=CARTESIAN_POINT('Ctrl Pts',(-5.68827338584756,-1.21792801260327,
-6.70611214074069));
#53375=CARTESIAN_POINT('Ctrl Pts',(-2.05044135574297,-5.44383565780062,
-6.42768828709357));
#53376=CARTESIAN_POINT('Ctrl Pts',(3.47134289591715,-4.66792459610127,-6.14926443344644));
#53377=CARTESIAN_POINT('Ctrl Pts',(5.803635743461,0.3969206476142,-5.8708405797993));
#53378=CARTESIAN_POINT('Ctrl Pts',(2.80350181475234,5.09706699486434,-5.59241672615218));
#53379=CARTESIAN_POINT('Ctrl Pts',(-2.77250943461248,5.11399248292585,-5.31399287250505));
#53380=CARTESIAN_POINT('Ctrl Pts',(-5.80111878332751,0.43214162495672,-5.03556901885792));
#53381=CARTESIAN_POINT('Ctrl Pts',(-3.49961605198755,-4.64676344512396,
-4.75714516521079));
#53382=CARTESIAN_POINT('Ctrl Pts',(2.01736012333282,-5.4561876061593,-4.47872131156366));
#53383=CARTESIAN_POINT('Ctrl Pts',(5.68077069634635,-1.25242520393326,-4.20029745791653));
#53384=CARTESIAN_POINT('Ctrl Pts',(4.12464623088233,4.10207481179193,-3.9218736042694));
#53385=CARTESIAN_POINT('Ctrl Pts',(-1.22123428830395,5.68755759612714,-3.64344975062227));
#53386=CARTESIAN_POINT('Ctrl Pts',(-5.44503554290356,2.04726950927692,-3.36502589697514));
#53387=CARTESIAN_POINT('Ctrl Pts',(-4.66589704313019,-3.47406523478677,
-3.08660204332801));
#53388=CARTESIAN_POINT('Ctrl Pts',(0.400302865534793,-5.80340263407658,
-2.80817818968088));
#53389=CARTESIAN_POINT('Ctrl Pts',(5.09870148282997,-2.80052989457494,-2.52975433603375));
#53390=CARTESIAN_POINT('Ctrl Pts',(5.11237470052847,2.77549084296867,-2.25133048238662));
#53391=CARTESIAN_POINT('Ctrl Pts',(0.42875946485938,5.80136965084335,-1.97290662873949));
#53392=CARTESIAN_POINT('Ctrl Pts',(-4.64880320297601,3.49690624434093,-1.69448277509236));
#53393=CARTESIAN_POINT('Ctrl Pts',(-5.45501040680013,-2.02054100754454,
-1.41605892144523));
#53394=CARTESIAN_POINT('Ctrl Pts',(-1.24911288418635,-5.68149993443013,
-1.1376350677981));
#53395=CARTESIAN_POINT('Ctrl Pts',(4.10447898256108,-4.12225384754937,-0.859211214150975));
#53396=CARTESIAN_POINT('Ctrl Pts',(5.68684458676181,1.22455018188017,-0.580787360503842));
#53397=CARTESIAN_POINT('Ctrl Pts',(2.04409447042155,5.44622826349031,-0.302363506856717));
#53398=CARTESIAN_POINT('Ctrl Pts',(-3.47678507055683,4.66387071809777,-0.0239396532095809));
#53399=CARTESIAN_POINT('Ctrl Pts',(-5.80316825208324,-0.403686437716624,
0.254484200437544));
#53400=CARTESIAN_POINT('Ctrl Pts',(-2.79755665155426,-5.10033344825063,
0.532908054084678));
#53401=CARTESIAN_POINT('Ctrl Pts',(2.7784711114303,-5.11075559823943,0.811331907731805));
#53402=CARTESIAN_POINT('Ctrl Pts',(5.80161865024956,-0.425376937628951,
1.08975576137894));
#53403=CARTESIAN_POINT('Ctrl Pts',(3.49419519287011,4.65084126326794,1.36817961502607));
#53404=CARTESIAN_POINT('Ctrl Pts',(-2.02372117571978,5.45383141515521,1.64660346867319));
#53405=CARTESIAN_POINT('Ctrl Pts',(-5.68222725659244,1.24580010693086,1.92502732232033));
#53406=CARTESIAN_POINT('Ctrl Pts',(-4.11986005471321,-4.10688174063604,
2.20345117596745));
#53407=CARTESIAN_POINT('Ctrl Pts',(1.22786565484881,-5.68612965343156,2.48187502961459));
#53408=CARTESIAN_POINT('Ctrl Pts',(5.44741913497888,-2.040918731811,2.76029888326171));
#53409=CARTESIAN_POINT('Ctrl Pts',(4.6618428064117,3.47950372184003,3.03872273690884));
#53410=CARTESIAN_POINT('Ctrl Pts',(-0.407069872025434,5.80293189872846,
3.31714659055597));
#53411=CARTESIAN_POINT('Ctrl Pts',(-5.10196368020262,2.79458245680537,3.59557044420311));
#53412=CARTESIAN_POINT('Ctrl Pts',(-5.10913475841737,-2.78145043499297,
3.87399429785023));
#53413=CARTESIAN_POINT('Ctrl Pts',(-0.421994265891336,-5.80186567765455,
4.15241815149737));
#53414=CARTESIAN_POINT('Ctrl Pts',(4.65287774260152,-3.49148295347327,4.43084200514448));
#53415=CARTESIAN_POINT('Ctrl Pts',(5.45265056950567,2.02690065589327,4.70926585879163));
#53416=CARTESIAN_POINT('Ctrl Pts',(1.24248690619172,5.68295264716619,4.98768971243874));
#53417=CARTESIAN_POINT('Ctrl Pts',(-4.10928310262335,4.11746486135404,5.26611356608589));
#53418=CARTESIAN_POINT('Ctrl Pts',(-5.68541278715194,-1.23118071040779,
5.544537419733));
#53419=CARTESIAN_POINT('Ctrl Pts',(-2.03774229941179,-5.44860815467391,
5.82296127338016));
#53420=CARTESIAN_POINT('Ctrl Pts',(3.48222119030037,-4.65981330997436,6.10138512702726));
#53421=CARTESIAN_POINT('Ctrl Pts',(5.8026935727219,0.410453167953449,6.37980898067441));
#53422=CARTESIAN_POINT('Ctrl Pts',(2.79160731206521,5.10359217779156,6.65823283432152));
#53423=CARTESIAN_POINT('Ctrl Pts',(-2.78442881302834,5.10751218179347,6.93665668796867));
#53424=CARTESIAN_POINT('Ctrl Pts',(-5.80211073277071,0.41861145070098,7.21508054161579));
#53425=CARTESIAN_POINT('Ctrl Pts',(-3.48876952718026,-4.65491264023392,
7.49350439526292));
#53426=CARTESIAN_POINT('Ctrl Pts',(2.03007944704129,-5.45146787027966,7.77192824891004));
#53427=CARTESIAN_POINT('Ctrl Pts',(5.68367610587452,-1.23917328308113,8.05035210255719));
#53428=CARTESIAN_POINT('Ctrl Pts',(4.11506826830211,4.1116830676992,8.32877595620429));
#53429=CARTESIAN_POINT('Ctrl Pts',(-1.23449534743867,5.68469398817063,8.60719980985145));
#53430=CARTESIAN_POINT('Ctrl Pts',(-5.4497953221667,2.03456517430157,8.88562366349855));
#53431=CARTESIAN_POINT('Ctrl Pts',(-4.6577822294781,-3.48493747501288,9.16404751714571));
#53432=CARTESIAN_POINT('Ctrl Pts',(0.413836324351832,-5.80245327414518,
9.44247137079281));
#53433=CARTESIAN_POINT('Ctrl Pts',(5.10521894046314,-2.78863121834486,9.72089522443996));
#53434=CARTESIAN_POINT('Ctrl Pts',(5.10588786891966,2.78740624452375,9.99931907808708));
#53435=CARTESIAN_POINT('Ctrl Pts',(0.415228493207719,5.80235381551483,10.2777429317342));
#53436=CARTESIAN_POINT('Ctrl Pts',(-4.6569459554733,3.48605491491343,10.5561667853813));
#53437=CARTESIAN_POINT('Ctrl Pts',(-5.45028331787931,-2.03325754808326,
10.8345906390285));
#53438=CARTESIAN_POINT('Ctrl Pts',(-1.23585923872538,-5.68439763247154,
11.1130144926756));
#53439=CARTESIAN_POINT('Ctrl Pts',(4.11408163504771,-4.11267027637206,11.3914383463227));
#53440=CARTESIAN_POINT('Ctrl Pts',(5.683973256732,1.23780956481465,11.6698621999699));
#53441=CARTESIAN_POINT('Ctrl Pts',(2.03138735756037,5.45098063705376,11.948286053617));
#53442=CARTESIAN_POINT('Ctrl Pts',(-3.48765257505427,4.65574956561328,12.2267099072641));
#53443=CARTESIAN_POINT('Ctrl Pts',(-5.80221100307997,-0.417219340070512,
12.5051337609113));
#53444=CARTESIAN_POINT('Ctrl Pts',(-2.78565417665601,-5.10684396766439,
12.7835576145584));
#53445=CARTESIAN_POINT('Ctrl Pts',(2.79038272846711,-5.10426182034811,13.0619814682055));
#53446=CARTESIAN_POINT('Ctrl Pts',(5.80259492580427,-0.411845394561442,
13.3404053218526));
#53447=CARTESIAN_POINT('Ctrl Pts',(3.48333911759557,4.65897768762844,13.6188291754998));
#53448=CARTESIAN_POINT('Ctrl Pts',(-2.03643495793874,5.4490969127073,13.8972530291469));
#53449=CARTESIAN_POINT('Ctrl Pts',(-5.68511722671199,1.2325447742511,14.175676882794));
#53450=CARTESIAN_POINT('Ctrl Pts',(-4.11027088637907,-4.11647880385354,
14.4541007364412));
#53451=CARTESIAN_POINT('Ctrl Pts',(1.2411233614091,-5.68325059308101,14.7325245900883));
#53452=CARTESIAN_POINT('Ctrl Pts',(5.45216409893207,-2.0282088502685,15.0109484437354));
#53453=CARTESIAN_POINT('Ctrl Pts',(4.65371531907096,3.49036648950155,15.2893722973825));
#53454=CARTESIAN_POINT('Ctrl Pts',(-0.420602213959508,5.80196675960862,
15.5677961510297));
#53455=CARTESIAN_POINT('Ctrl Pts',(-5.10846725884286,2.78267618801067,15.8462200046768));
#53456=CARTESIAN_POINT('Ctrl Pts',(-5.10263403663162,-2.79335826384653,
16.1246438583239));
#53457=CARTESIAN_POINT('Ctrl Pts',(-0.408462155912262,-5.8028340635571,
16.4030677119711));
#53458=CARTESIAN_POINT('Ctrl Pts',(4.66100783600869,-3.48062213614987,16.6814915656182));
#53459=CARTESIAN_POINT('Ctrl Pts',(5.4479086551669,2.03961167552763,16.9599154192653));
#53460=CARTESIAN_POINT('Ctrl Pts',(1.22922989078505,5.68583488835121,17.2383392729125));
#53461=CARTESIAN_POINT('Ctrl Pts',(-4.11887457330181,4.10787009913883,17.5167631265596));
#53462=CARTESIAN_POINT('Ctrl Pts',(-5.68252599746333,-1.24443673609558,
17.7951869802067));
#53463=CARTESIAN_POINT('Ctrl Pts',(-2.02502965350643,-5.45334570739934,
18.0736108338538));
#53464=CARTESIAN_POINT('Ctrl Pts',(3.49307921743211,-4.65167949054264,18.352034687501));
#53465=CARTESIAN_POINT('Ctrl Pts',(5.80172054381419,0.4239849448688,18.6304585411481));
#53466=CARTESIAN_POINT('Ctrl Pts',(2.77969725342115,5.11008881344677,18.9088823947953));
#53467=CARTESIAN_POINT('Ctrl Pts',(-2.79633284965052,5.10100451832347,19.1873062484423));
#53468=CARTESIAN_POINT('Ctrl Pts',(-5.803071228692,0.40507877841031,19.4657301020895));
#53469=CARTESIAN_POINT('Ctrl Pts',(-3.47790397149999,-4.66303639992394,
19.7441539557366));
#53470=CARTESIAN_POINT('Ctrl Pts',(2.04278769977008,-5.44671854566206,20.0225778093838));
#53471=CARTESIAN_POINT('Ctrl Pts',(5.68655061714523,-1.22591458945406,20.3010016630309));
#53472=CARTESIAN_POINT('Ctrl Pts',(4.10546791546748,4.12126894257805,20.579425516678));
#53473=CARTESIAN_POINT('Ctrl Pts',(-1.2477496877477,5.68179947012534,20.8578493703251));
#53474=CARTESIAN_POINT('Ctrl Pts',(-5.45452546205389,2.02184976835486,21.1362732239723));
#53475=CARTESIAN_POINT('Ctrl Pts',(-4.64964208072038,-3.49579075792379,
21.4146970776194));
#53476=CARTESIAN_POINT('Ctrl Pts',(0.427367531648445,-5.80147235578038,
21.6931209312665));
#53477=CARTESIAN_POINT('Ctrl Pts',(5.1117086309249,-2.77671737390015,21.9715447849137));
#53478=CARTESIAN_POINT('Ctrl Pts',(5.09937326597762,2.79930648486794,22.2499686385608));
#53479=CARTESIAN_POINT('Ctrl Pts',(0.401695263205706,5.80330642112832,22.5283924922079));
#53480=CARTESIAN_POINT('Ctrl Pts',(-4.66506337868458,3.47518462456994,22.8068163458551));
#53481=CARTESIAN_POINT('Ctrl Pts',(-5.44552658459737,-2.04596302958645,
23.0852401995022));
#53482=CARTESIAN_POINT('Ctrl Pts',(-1.222598871385,-5.68726441285079,23.3636640531493));
#53483=CARTESIAN_POINT('Ctrl Pts',(4.12366191086833,-4.10306433618151,23.6420879067964));
#53484=CARTESIAN_POINT('Ctrl Pts',(5.68107101131397,1.25106221523925,23.9205117604436));
#53485=CARTESIAN_POINT('Ctrl Pts',(2.01866919589476,5.45570336249478,24.1989356140907));
#53486=CARTESIAN_POINT('Ctrl Pts',(-3.49850111005493,4.64760309029668,24.4773594677378));
#53487=CARTESIAN_POINT('Ctrl Pts',(-5.80122219559149,-0.430749973148619,
24.755783321385));
#53488=CARTESIAN_POINT('Ctrl Pts',(-2.77373655046063,-5.11332671072659,
25.0342071750321));
#53489=CARTESIAN_POINT('Ctrl Pts',(2.80227916848797,-5.09774028014861,25.3126310286793));
#53490=CARTESIAN_POINT('Ctrl Pts',(5.80353964078615,-0.39831161144852,25.5910548823263));
#53491=CARTESIAN_POINT('Ctrl Pts',(3.47246409628408,4.66708877160151,25.8694787359735));
#53492=CARTESIAN_POINT('Ctrl Pts',(-2.04913766389717,5.44433277237802,26.1479025896206));
#53493=CARTESIAN_POINT('Ctrl Pts',(-5.68797627522524,1.21928273770528,26.4263264432677));
#53494=CARTESIAN_POINT('Ctrl Pts',(-4.10065936209809,-4.12605347735923,
26.7047502969149));
#53495=CARTESIAN_POINT('Ctrl Pts',(1.2543743174442,-5.68034062127683,26.983174150562));
#53496=CARTESIAN_POINT('Ctrl Pts',(5.45687940832144,-2.01548793720741,27.2615980042091));
#53497=CARTESIAN_POINT('Ctrl Pts',(4.64556251996484,3.50121027290405,27.5400218578563));
#53498=CARTESIAN_POINT('Ctrl Pts',(-0.434132268219488,5.80097006333265,
27.8184457115034));
#53499=CARTESIAN_POINT('Ctrl Pts',(-5.11494305230171,2.77075478411592,28.0968695651505));
#53500=CARTESIAN_POINT('Ctrl Pts',(-5.09610556139159,-2.8052508994999,28.3752934187976));
#53501=CARTESIAN_POINT('Ctrl Pts',(-0.394927824289227,-5.80377088758623,
28.6537172724448));
#53502=CARTESIAN_POINT('Ctrl Pts',(4.6691125779863,-3.46974238756726,28.9321411260919));
#53503=CARTESIAN_POINT('Ctrl Pts',(5.4431371094098,2.0523116016232,29.210564979739));
#53504=CARTESIAN_POINT('Ctrl Pts',(1.215966189542,5.68868620402655,29.4889888333862));
#53505=CARTESIAN_POINT('Ctrl Pts',(-4.12844364123772,4.09825299403475,29.7674126870333));
#53506=CARTESIAN_POINT('Ctrl Pts',(-5.67960830026223,-1.25768599323653,
30.0458365406804));
#53507=CARTESIAN_POINT('Ctrl Pts',(-2.01230599337432,-5.4580535991341,30.3242603943276));
#53508=CARTESIAN_POINT('Ctrl Pts',(3.50391824555016,-4.64352037041854,30.6026842479747));
#53509=CARTESIAN_POINT('Ctrl Pts',(5.80071595908955,0.437514415711182,30.8811081016218));
#53510=CARTESIAN_POINT('Ctrl Pts',(2.76777207587959,5.11655765510094,31.1595319552689));
#53511=CARTESIAN_POINT('Ctrl Pts',(-2.80822167689368,5.0944691102622,31.4379558089161));
#53512=CARTESIAN_POINT('Ctrl Pts',(-5.80400016144989,0.391543902877945,
31.7163796625632));
#53513=CARTESIAN_POINT('Ctrl Pts',(-3.46701949934472,-4.67113479715094,
31.9948035162103));
#53514=CARTESIAN_POINT('Ctrl Pts',(2.05548484168548,-5.44193959609919,32.2732273698575));
#53515=CARTESIAN_POINT('Ctrl Pts',(5.68939419901335,-1.21264922802275,32.5516512235046));
#53516=CARTESIAN_POINT('Ctrl Pts',(4.09584523280961,4.13083240169122,32.8300750771517));
#53517=CARTESIAN_POINT('Ctrl Pts',(-1.26099724149055,5.67887404851917,33.1084989307988));
#53518=CARTESIAN_POINT('Ctrl Pts',(-5.45922593453371,2.00912336547695,33.386922784446));
#53519=CARTESIAN_POINT('Ctrl Pts',(-4.64147664235183,-3.50662502707285,
33.6653466380932));
#53520=CARTESIAN_POINT('Ctrl Pts',(0.440896414474084,-5.80045988294852,
33.9437704917402));
#53521=CARTESIAN_POINT('Ctrl Pts',(5.11817051857534,-2.76478842676563,34.2221943453874));
#53522=CARTESIAN_POINT('Ctrl Pts',(5.09283092731677,2.81119149965931,34.5006181990345));
#53523=CARTESIAN_POINT('Ctrl Pts',(0.388159848365178,5.80422746229918,34.7790420526816));
#53524=CARTESIAN_POINT('Ctrl Pts',(-4.67315542840794,3.46429543254218,35.0574659063288));
#53525=CARTESIAN_POINT('Ctrl Pts',(-5.44074023285332,-2.05865738300537,
35.3358897599759));
#53526=CARTESIAN_POINT('Ctrl Pts',(-1.20933185427489,-5.69010025994507,
35.614313613623));
#53527=CARTESIAN_POINT('Ctrl Pts',(4.13321975790782,-4.09343607924097,35.8927374672701));
#53528=CARTESIAN_POINT('Ctrl Pts',(5.67813786629717,1.26430806108067,36.1711613209173));
#53529=CARTESIAN_POINT('Ctrl Pts',(2.00594005459731,5.46039641412169,36.4495851745644));
#53530=CARTESIAN_POINT('Ctrl Pts',(-3.50933061655186,4.63943133645954,36.7280090282115));
#53531=CARTESIAN_POINT('Ctrl Pts',(-5.80020183499662,-0.444278263358354,
37.0064328818587));
#53532=CARTESIAN_POINT('Ctrl Pts',(-2.76180383778841,-5.11978164217659,
37.2848567355058));
#53533=CARTESIAN_POINT('Ctrl Pts',(2.81416036678732,-5.09119101311223,37.5632805891529));
#53534=CARTESIAN_POINT('Ctrl Pts',(5.80445279005691,-0.384775661901064,
37.8417044428));
#53535=CARTESIAN_POINT('Ctrl Pts',(3.46157018808544,4.67517447107051,38.1201282964472));
#53536=CARTESIAN_POINT('Ctrl Pts',(-2.06182922450441,5.4395390200798,38.3985521500943));
#53537=CARTESIAN_POINT('Ctrl Pts',(-5.69080438658164,1.20601406942624,38.6769760037414));
#53538=CARTESIAN_POINT('Ctrl Pts',(-4.0910255341479,-4.13560570907586,38.9553998573886));
#53539=CARTESIAN_POINT('Ctrl Pts',(1.26761845088123,-5.6773997538465,39.2338237110357));
#53540=CARTESIAN_POINT('Ctrl Pts',(5.46156503750013,-2.00275606181767,39.5122475646828));
#53541=CARTESIAN_POINT('Ctrl Pts',(4.63738445343698,3.51203501306753,39.79067141833));
#53542=CARTESIAN_POINT('Ctrl Pts',(-0.447659961214595,5.79994181532161,
40.0690952719771));
#53543=CARTESIAN_POINT('Ctrl Pts',(-5.12139102535709,2.75881830996228,40.3475191256242));
#53544=CARTESIAN_POINT('Ctrl Pts',(-5.08954936820597,-2.81712827726845,
40.6259429792714));
#53545=CARTESIAN_POINT('Ctrl Pts',(-0.381391344636143,-5.80467614464644,
40.9043668329184));
#53546=CARTESIAN_POINT('Ctrl Pts',(4.67719192445218,-3.45884376690104,41.1827906865657));
#53547=CARTESIAN_POINT('Ctrl Pts',(5.43833595818706,2.06500036510422,41.4612145402126));
#53548=CARTESIAN_POINT('Ctrl Pts',(1.20269587460476,5.69150657868371,41.7396383938599));
#53549=CARTESIAN_POINT('Ctrl Pts',(-4.13799025438433,4.08861359834987,42.018062247507));
#53550=CARTESIAN_POINT('Ctrl Pts',(-5.67665971141812,-1.27092840976715,
42.2964861011541));
#53551=CARTESIAN_POINT('Ctrl Pts',(-1.99957138822013,-5.46273180427181,
42.5749099548013));
#53552=CARTESIAN_POINT('Ctrl Pts',(3.51473821570051,-4.6353359939799,42.8533338084484));
#53553=CARTESIAN_POINT('Ctrl Pts',(5.79967982401188,0.45104150689311,43.1317576620956));
#53554=CARTESIAN_POINT('Ctrl Pts',(2.75583184430228,5.12299866756965,43.4101815157427));
#53555=CARTESIAN_POINT('Ctrl Pts',(-2.82009523009366,5.08790599315611,43.6886053693897));
#53556=CARTESIAN_POINT('Ctrl Pts',(-5.80489752599187,0.378006897721008,
43.967029223037));
#53557=CARTESIAN_POINT('Ctrl Pts',(-3.45611616991583,-4.67920778786726,
44.245453076684));
#53558=CARTESIAN_POINT('Ctrl Pts',(2.06817080372702,-5.43713104758401,44.5238769303312));
#53559=CARTESIAN_POINT('Ctrl Pts',(5.69220683601255,-1.19937727093821,44.8023007839783));
#53560=CARTESIAN_POINT('Ctrl Pts',(4.08620027266672,4.14037339302263,45.0807246376255));
#53561=CARTESIAN_POINT('Ctrl Pts',(-1.27423793661312,5.67591773926357,45.3591484912725));
#53562=CARTESIAN_POINT('Ctrl Pts',(-5.46389671404001,1.99638603488747,45.6375723449197));
#53563=CARTESIAN_POINT('Ctrl Pts',(-4.63328595878473,-3.51744022353175,
45.9159961985668));
#53564=CARTESIAN_POINT('Ctrl Pts',(0.454422899244266,-5.79941586115651,
46.1944200522139));
#53565=CARTESIAN_POINT('Ctrl Pts',(5.12460456826788,-2.75284444182363,46.4728439058611));
#53566=CARTESIAN_POINT('Ctrl Pts',(5.08626088852126,2.82306122425459,46.7512677595082));
#53567=CARTESIAN_POINT('Ctrl Pts',(0.374622322305924,5.8051169340179,47.0296916131553));
#53568=CARTESIAN_POINT('Ctrl Pts',(-4.68122206063041,3.45338739805693,47.3081154668025));
#53569=CARTESIAN_POINT('Ctrl Pts',(-5.43592428868028,-2.07134053929494,
47.5865393204495));
#53570=CARTESIAN_POINT('Ctrl Pts',(-1.19605825955486,-5.69290515833011,
47.8649631740968));
#53571=CARTESIAN_POINT('Ctrl Pts',(4.14275512418048,-4.08378555791893,48.1433870277438));
#53572=CARTESIAN_POINT('Ctrl Pts',(5.67517383763514,1.27754703029398,48.421810881391));
#53573=CARTESIAN_POINT('Ctrl Pts',(1.99320000290249,5.46505976640885,48.7002347350381));
#53574=CARTESIAN_POINT('Ctrl Pts',(-3.52014103564295,4.63123434854828,48.9786585886852));
#53575=CARTESIAN_POINT('Ctrl Pts',(-5.79914992684515,-0.457804137118822,
49.2570824423324));
#53576=CARTESIAN_POINT('Ctrl Pts',(-2.7498561035418,-5.1262087269058,49.5355062959795));
#53577=CARTESIAN_POINT('Ctrl Pts',(2.82602625874287,-5.08461405486067,49.8139301496266));
#53578=CARTESIAN_POINT('Ctrl Pts',(5.80533436864992,-0.371237619541609,
50.0923540032738));
#53579=CARTESIAN_POINT('Ctrl Pts',(3.4506574522521,4.68323474205681,50.3707778569208));
#53580=CARTESIAN_POINT('Ctrl Pts',(-2.07450957073036,5.43471568188616,50.649201710568));
#53581=CARTESIAN_POINT('Ctrl Pts',(-5.69360154539906,1.19273884158297,50.9276255642152));
#53582=CARTESIAN_POINT('Ctrl Pts',(-4.08136945492725,-4.14513544704848,
51.2060494178623));
#53583=CARTESIAN_POINT('Ctrl Pts',(1.28085568968505,-5.67442800678559,51.4844732715094));
#53584=CARTESIAN_POINT('Ctrl Pts',(5.4662209609829,-1.99001329334819,51.7628971251566));
#53585=CARTESIAN_POINT('Ctrl Pts',(4.62918116396803,3.52284065111588,52.0413209788037));
#53586=CARTESIAN_POINT('Ctrl Pts',(-0.461185219367196,5.79888202116823,
52.3197448324508));
#53587=CARTESIAN_POINT('Ctrl Pts',(-5.12781114293802,2.74686683047278,52.5981686860979));
#53588=CARTESIAN_POINT('Ctrl Pts',(-5.08296549273427,-2.82899033255045,
52.8765925397451));
#53589=CARTESIAN_POINT('Ctrl Pts',(-0.367852790578618,-5.80554982981413,
53.1550163933922));
#53590=CARTESIAN_POINT('Ctrl Pts',(4.68524583146246,-3.4479263334292,53.4334402470393));
#53591=CARTESIAN_POINT('Ctrl Pts',(5.43350522761236,2.0776778969562,53.7118641006865));
#53592=CARTESIAN_POINT('Ctrl Pts',(1.18941901815086,5.69429599698262,53.9902879543335));
#53593=CARTESIAN_POINT('Ctrl Pts',(-4.14751436081733,4.07895196451306,54.2687118079807));
#53594=CARTESIAN_POINT('Ctrl Pts',(-5.67368024696851,-1.28416391366144,
54.5471356616279));
#53595=CARTESIAN_POINT('Ctrl Pts',(-1.98682590730801,-5.46738029736734,
54.8255595152749));
#53596=CARTESIAN_POINT('Ctrl Pts',(3.52553906903275,-4.627126405742,55.1039833689222));
#53597=CARTESIAN_POINT('Ctrl Pts',(5.7986121442169,0.464566144840059,55.3824072225692));
#53598=CARTESIAN_POINT('Ctrl Pts',(2.74387662363257,5.12941181581999,55.6608310762164));
#53599=CARTESIAN_POINT('Ctrl Pts',(-2.83195344466994,5.08131520270228,55.9392549298634));
#53600=CARTESIAN_POINT('Ctrl Pts',(-5.80576331743716,0.364467836567547,
56.2176787835106));
#53601=CARTESIAN_POINT('Ctrl Pts',(-3.44519404251673,-4.68725532816361,
56.4961026371577));
#53602=CARTESIAN_POINT('Ctrl Pts',(2.08084551689526,-5.43229292627044,56.7745264908049));
#53603=CARTESIAN_POINT('Ctrl Pts',(5.69498851284468,-1.18609879038724,57.052950344452));
#53604=CARTESIAN_POINT('Ctrl Pts',(4.07653308749828,4.14989186467828,57.3313741980992));
#53605=CARTESIAN_POINT('Ctrl Pts',(-1.2874717010986,5.67293055843817,57.6097980517462));
#53606=CARTESIAN_POINT('Ctrl Pts',(-5.46853777516823,1.98363784586525,57.8882219053935));
#53607=CARTESIAN_POINT('Ctrl Pts',(-4.62507007456854,-3.52823628847641,
58.1666457590405));
#53608=CARTESIAN_POINT('Ctrl Pts',(0.467946912388112,-5.79834029608278,
58.4450696126877));
#53609=CARTESIAN_POINT('Ctrl Pts',(5.13101074500744,-2.7408854840378,58.7234934663347));
#53610=CARTESIAN_POINT('Ctrl Pts',(5.07966318532585,2.83491559409379,59.001917319982));
#53611=CARTESIAN_POINT('Ctrl Pts',(0.361082758659297,5.80597483144648,59.2803411736289));
#53612=CARTESIAN_POINT('Ctrl Pts',(-4.68926323147709,3.44246058044367,59.5587650272763));
#53613=CARTESIAN_POINT('Ctrl Pts',(-5.43107877827254,-2.08401242947076,
59.8371888809232));
#53614=CARTESIAN_POINT('Ctrl Pts',(-1.18277815942064,-5.69567909274991,
60.1156127345705));
#53615=CARTESIAN_POINT('Ctrl Pts',(4.15226795782324,-4.07411282470503,60.3940365882174));
#53616=CARTESIAN_POINT('Ctrl Pts',(5.67217894144929,1.29077905087206,60.6724604418648));
#53617=CARTESIAN_POINT('Ctrl Pts',(1.98044911010386,5.469693393992,60.9508842955118));
#53618=CARTESIAN_POINT('Ctrl Pts',(-3.53093230852989,4.62301217114679,61.229308149159));
#53619=CARTESIAN_POINT('Ctrl Pts',(-5.79806647685838,-0.47132752086214,
61.507732002806));
#53620=CARTESIAN_POINT('Ctrl Pts',(-2.73789341270518,-5.13260792995689,
61.7861558564532));
#53621=CARTESIAN_POINT('Ctrl Pts',(2.83787677981535,-5.07800944116647,62.0645797101003));
#53622=CARTESIAN_POINT('Ctrl Pts',(5.80618437177022,-0.357697558004235,
62.3430035637474));
#53623=CARTESIAN_POINT('Ctrl Pts',(3.4397259481389,4.69126954072045,62.6214274173947));
#53624=CARTESIAN_POINT('Ctrl Pts',(-2.08717863360625,5.42986278403133,62.8998512710416));
#53625=CARTESIAN_POINT('Ctrl Pts',(-5.69636773646354,1.17945712637986,63.178275124689));
#53626=CARTESIAN_POINT('Ctrl Pts',(-4.07169117695603,-4.15464263944444,
63.4566989783358));
#53627=CARTESIAN_POINT('Ctrl Pts',(1.29408596185757,-5.67142539625746,63.7351228319832));
#53628=CARTESIAN_POINT('Ctrl Pts',(5.47084715344585,-1.97725970110767,64.0135466856302));
#53629=CARTESIAN_POINT('Ctrl Pts',(4.62095269617623,3.53362712827672,64.2919705392774));
#53630=CARTESIAN_POINT('Ctrl Pts',(-0.474707969112876,5.79779068663673,
64.5703943929245));
#53631=CARTESIAN_POINT('Ctrl Pts',(-5.1342033701254,2.73490041065189,64.8488182465717));
#53632=CARTESIAN_POINT('Ctrl Pts',(-5.07635397078635,-2.84083700082785,
65.1272421002188));
#53633=CARTESIAN_POINT('Ctrl Pts',(-0.354312235753313,-5.80639193833713,
65.4056659538659));
#53634=CARTESIAN_POINT('Ctrl Pts',(4.69327425521161,-3.4369901465322,65.684089807513));
#53635=CARTESIAN_POINT('Ctrl Pts',(5.42864494396021,2.09034412822534,65.9625136611601));
#53636=CARTESIAN_POINT('Ctrl Pts',(1.1761356923939,5.69705444375144,66.2409375148073));
#53637=CARTESIAN_POINT('Ctrl Pts',(-4.15701590873452,4.06926814507461,66.5193613684544));
#53638=CARTESIAN_POINT('Ctrl Pts',(-5.67066992311886,-1.29739243293082,
66.7977852221016));
#53639=CARTESIAN_POINT('Ctrl Pts',(-1.97406961996107,-5.47199905313755,
67.0762090757487));
#53640=CARTESIAN_POINT('Ctrl Pts',(3.53632074680071,-4.61889165035702,67.3546329293958));
#53641=CARTESIAN_POINT('Ctrl Pts',(5.79751292551162,0.478088255991047,67.633056783043));
#53642=CARTESIAN_POINT('Ctrl Pts',(2.73190647889548,5.13579706497058,67.91148063669));
#53643=CARTESIAN_POINT('Ctrl Pts',(-2.843796256125,5.07469677474826,68.1899044903372));
#53644=CARTESIAN_POINT('Ctrl Pts',(-5.80659753107665,0.350926793057335,
68.4683283439843));
#53645=CARTESIAN_POINT('Ctrl Pts',(-3.43425317655358,-4.69527737426908,
68.7467521976315));
#53646=CARTESIAN_POINT('Ctrl Pts',(2.09350891225194,-5.42742525847318,69.0251760512785));
#53647=CARTESIAN_POINT('Ctrl Pts',(5.69773921438019,-1.17281385859187,69.3035999049257));
#53648=CARTESIAN_POINT('Ctrl Pts',(4.06684372988438,4.15938776488691,69.5820237585728));
#53649=CARTESIAN_POINT('Ctrl Pts',(-1.30069846296805,5.66991252229023,69.8604476122199));
#53650=CARTESIAN_POINT('Ctrl Pts',(-5.47314909267551,1.97087886774828,70.1388714658671));
#53651=CARTESIAN_POINT('Ctrl Pts',(-4.61682903438977,-3.5390131631864,70.4172953195142));
#53652=CARTESIAN_POINT('Ctrl Pts',(0.481468380347833,-5.79723319357744,
70.6957191731614));
#53653=CARTESIAN_POINT('Ctrl Pts',(5.13738901395058,-2.72891161845354,70.9741430268085));
#53654=CARTESIAN_POINT('Ctrl Pts',(5.07303785361562,2.84675454470068,71.2525668804556));
#53655=CARTESIAN_POINT('Ctrl Pts',(0.347541231067252,5.80680114991893,71.5309907341027));
#53656=CARTESIAN_POINT('Ctrl Pts',(-4.69727889721183,3.43151503913349,71.8094145877499));
#53657=CARTESIAN_POINT('Ctrl Pts',(-5.42620372798489,-2.09667298461008,
72.087838441397));
#53658=CARTESIAN_POINT('Ctrl Pts',(-1.16949162610311,-5.69842204811702,
72.3662622950442));
#53659=CARTESIAN_POINT('Ctrl Pts',(4.16175820709524,-4.06441793220953,72.6446861486912));
#53660=CARTESIAN_POINT('Ctrl Pts',(5.66915319402907,1.30400405084528,72.9231100023384));
#53661=CARTESIAN_POINT('Ctrl Pts',(1.96768744555408,5.47429727166879,73.2015338559855));
#53662=CARTESIAN_POINT('Ctrl Pts',(-3.54170437651841,4.61476484897565,73.4799577096326));
#53663=CARTESIAN_POINT('Ctrl Pts',(-5.7969514909293,-0.484848341034039,
73.7583815632798));
#53664=CARTESIAN_POINT('Ctrl Pts',(-2.72591583034415,-5.13897921652443,
74.0368054169269));
#53665=CARTESIAN_POINT('Ctrl Pts',(2.84971186554951,-5.07137720795222,74.315229270574));
#53666=CARTESIAN_POINT('Ctrl Pts',(5.80700279479466,-0.344155550933751,
74.5936531242212));
#53667=CARTESIAN_POINT('Ctrl Pts',(3.42877573520264,4.69927882335965,74.8720769778683));
#53668=CARTESIAN_POINT('Ctrl Pts',(-2.09983634422443,5.42498035291051,75.1505008315154));
#53669=CARTESIAN_POINT('Ctrl Pts',(-5.6991029447297,1.16616899605683,75.4289246851625));
#53670=CARTESIAN_POINT('Ctrl Pts',(-4.06199075287477,-4.16412723455357,
75.7073485388097));
#53671=CARTESIAN_POINT('Ctrl Pts',(1.30730919543873,-5.66839193859359,75.9857723924568));
#53672=CARTESIAN_POINT('Ctrl Pts',(5.475443589727,-1.96449535446343,76.264196246104));
#53673=CARTESIAN_POINT('Ctrl Pts',(4.61269909481645,3.54439438588181,76.542620099751));
#53674=CARTESIAN_POINT('Ctrl Pts',(-0.488228136900599,5.79666781766301,
76.8210439533983));
#53675=CARTESIAN_POINT('Ctrl Pts',(-5.14056767215146,2.72291911558574,77.0994678070453));
#53676=CARTESIAN_POINT('Ctrl Pts',(-5.06971483832266,-2.85266821766606,
77.3778916606925));
#53677=CARTESIAN_POINT('Ctrl Pts',(-0.340769753807865,-5.80720246563535,
77.6563155143396));
#53678=CARTESIAN_POINT('Ctrl Pts',(4.70127715203259,-3.42603526569229,77.9347393679867));
#53679=CARTESIAN_POINT('Ctrl Pts',(5.42375513366596,2.1029989900195,78.2131632216339));
#53680=CARTESIAN_POINT('Ctrl Pts',(1.16284596958247,5.69978190398691,78.4915870752809));
#53681=CARTESIAN_POINT('Ctrl Pts',(-4.16649484645678,4.05956219270503,78.7700109289282));
#53682=CARTESIAN_POINT('Ctrl Pts',(-5.66762875624243,-1.31061389562501,
79.0484347825752));
#53683=CARTESIAN_POINT('Ctrl Pts',(-1.96130259556129,-5.47658804646063,
79.3268586362224));
#53684=CARTESIAN_POINT('Ctrl Pts',(3.54708319036234,-4.61063177261423,79.6052824898694));
#53685=CARTESIAN_POINT('Ctrl Pts',(5.79638217387485,0.491607766798655,79.8837063435167));
#53686=CARTESIAN_POINT('Ctrl Pts',(2.71992147519714,5.14215438029163,80.1621301971638));
#53687=CARTESIAN_POINT('Ctrl Pts',(-2.85562360004527,5.06805074529212,80.4405540508108));
#53688=CARTESIAN_POINT('Ctrl Pts',(-5.80740016237305,0.33738384084066,80.7189779044581));
#53689=CARTESIAN_POINT('Ctrl Pts',(-3.42329363153413,-4.70327388255127,
80.997401758105));
#53690=CARTESIAN_POINT('Ctrl Pts',(2.10616092092011,-5.42252807066782,81.2758256117524));
#53691=CARTESIAN_POINT('Ctrl Pts',(5.7004589256578,-1.15952254780973,81.5542494653993));
#53692=CARTESIAN_POINT('Ctrl Pts',(4.05713225252595,4.16886104199992,81.8326733190467));
#53693=CARTESIAN_POINT('Ctrl Pts',(-1.31391815028062,5.6668636472351,82.1110971726936));
#53694=CARTESIAN_POINT('Ctrl Pts',(-5.47773064148054,1.95810916993311,82.3895210263409));
#53695=CARTESIAN_POINT('Ctrl Pts',(-4.60856288307185,-3.54977078904587,
82.6679448799879));
#53696=CARTESIAN_POINT('Ctrl Pts',(0.494987229579467,-5.79609455966206,
82.946368733635));
#53697=CARTESIAN_POINT('Ctrl Pts',(5.14373934040566,-2.71692291019715,83.2247925872822));
#53698=CARTESIAN_POINT('Ctrl Pts',(5.06638492942612,2.85857801168262,83.5032164409293));
#53699=CARTESIAN_POINT('Ctrl Pts',(0.333997813182944,5.80759588494068,83.7816402945764));
#53700=CARTESIAN_POINT('Ctrl Pts',(-4.70526901423705,3.42055083365993,84.0600641482237));
#53701=CARTESIAN_POINT('Ctrl Pts',(-5.42129916433304,-2.10932213585141,
84.3384880018706));
#53702=CARTESIAN_POINT('Ctrl Pts',(-1.15619873186854,-5.70113400951219,
84.6169118555179));
#53703=CARTESIAN_POINT('Ctrl Pts',(4.1712258203786,-4.05470093316368,84.8953357091649));
#53704=CARTESIAN_POINT('Ctrl Pts',(5.66609661183164,1.31722195828223,85.1737595628121));
#53705=CARTESIAN_POINT('Ctrl Pts',(1.95491507866457,5.47887137439827,85.4521834164592));
#53706=CARTESIAN_POINT('Ctrl Pts',(-3.55245718101874,4.60649242689272,85.7306072701064));
#53707=CARTESIAN_POINT('Ctrl Pts',(-5.79580497512237,-0.498366524094111,
86.0090311237535));
#53708=CARTESIAN_POINT('Ctrl Pts',(-2.71392342160519,-5.14532255195471,
86.2874549774007));
#53709=CARTESIAN_POINT('Ctrl Pts',(2.86153145157372,-5.06471739129104,86.5658788310476));
#53710=CARTESIAN_POINT('Ctrl Pts',(5.80778963327165,-0.330611671985869,
86.844302684695));
#53711=CARTESIAN_POINT('Ctrl Pts',(3.4178068730022,4.70726254641164,87.1227265383419));
#53712=CARTESIAN_POINT('Ctrl Pts',(-2.11248263373895,5.42006841507948,87.4011503919893));
#53713=CARTESIAN_POINT('Ctrl Pts',(-5.70180715532063,1.15287452288852,87.6795742456361));
#53714=CARTESIAN_POINT('Ctrl Pts',(-4.05226823544451,-4.173589180789,87.9579980992835));
#53715=CARTESIAN_POINT('Ctrl Pts',(1.32052531850694,-5.66532765029288,88.2364219529305));
#53716=CARTESIAN_POINT('Ctrl Pts',(5.48001024482615,-1.95172032284121,88.5148458065777));
#53717=CARTESIAN_POINT('Ctrl Pts',(4.60442040478046,3.5551423653677,88.7932696602248));
#53718=CARTESIAN_POINT('Ctrl Pts',(-0.501745649193681,5.79551342035425,
89.071693513872));
#53719=CARTESIAN_POINT('Ctrl Pts',(-5.14690401440058,2.71092301044105,89.3501173675189));
#53720=CARTESIAN_POINT('Ctrl Pts',(-5.06304813145374,-2.86448391871446,
89.6285412211663));
#53721=CARTESIAN_POINT('Ctrl Pts',(-0.327225418400649,-5.80798140730008,
89.9069650748132));
#53722=CARTESIAN_POINT('Ctrl Pts',(4.70925447839735,-3.41506175049384,90.1853889284604));
#53723=CARTESIAN_POINT('Ctrl Pts',(5.41883582332552,2.11564241350824,90.4638127821077));
#53724=CARTESIAN_POINT('Ctrl Pts',(1.14954992199983,5.70247836285427,90.7422366357546));
#53725=CARTESIAN_POINT('Ctrl Pts',(-4.17595112242768,4.04983416019552,91.0206604894019));
#53726=CARTESIAN_POINT('Ctrl Pts',(-5.66455676288018,-1.3238282298317,91.2990843430488));
#53727=CARTESIAN_POINT('Ctrl Pts',(-1.94852490354921,-5.48114725237695,
91.5775081966962));
#53728=CARTESIAN_POINT('Ctrl Pts',(3.55782634118013,-4.60234681743952,91.8559320503431));
#53729=CARTESIAN_POINT('Ctrl Pts',(5.79521989545676,0.505124603729757,92.1343559039904));
#53730=CARTESIAN_POINT('Ctrl Pts',(2.70792167772444,5.14848372720567,92.4127797576374));
#53731=CARTESIAN_POINT('Ctrl Pts',(-2.86743541210141,5.06137715048165,92.6912036112847));
#53732=CARTESIAN_POINT('Ctrl Pts',(-5.8081712069608,0.323839053578139,92.9696274649316));
#53733=CARTESIAN_POINT('Ctrl Pts',(-3.41231546706785,-4.71124480951695,
93.2480513185789));
#53734=CARTESIAN_POINT('Ctrl Pts',(2.11880147408499,-5.4176013894902,93.526475172226));
#53735=CARTESIAN_POINT('Ctrl Pts',(5.70314763188498,-1.14622493033275,93.8048990258731));
#53736=CARTESIAN_POINT('Ctrl Pts',(4.04739870824418,4.17831164449162,94.0833228795204));
#53737=CARTESIAN_POINT('Ctrl Pts',(-1.32713069113358,5.66378394985563,94.3617467331672));
#53738=CARTESIAN_POINT('Ctrl Pts',(-5.48228239666421,1.94532882187493,94.6401705868147));
#53739=CARTESIAN_POINT('Ctrl Pts',(-4.6002716655748,-3.56050910754356,94.9185944404615));
#53740=CARTESIAN_POINT('Ctrl Pts',(0.508503386553553,-5.7949244005297,95.1970182941089));
#53741=CARTESIAN_POINT('Ctrl Pts',(5.15006168983296,-2.70491942447578,95.4754421477558));
#53742=CARTESIAN_POINT('Ctrl Pts',(5.05970444894282,2.87038593073113,95.7538660014031));
#53743=CARTESIAN_POINT('Ctrl Pts',(0.320452578669648,5.80835903218928,96.0322898550501));
#53744=CARTESIAN_POINT('Ctrl Pts',(-4.71323353909406,3.40956802365781,96.3107137086973));
#53745=CARTESIAN_POINT('Ctrl Pts',(-5.41636511399308,-2.12195981439559,
96.5891375623444));
#53746=CARTESIAN_POINT('Ctrl Pts',(-1.14289954901735,-5.70381496218517,
96.8675614159915));
#53747=CARTESIAN_POINT('Ctrl Pts',(4.18067074617859,-4.04496188041834,97.1459852696388));
#53748=CARTESIAN_POINT('Ctrl Pts',(5.66300921148187,1.33043270129022,97.4244091232857));
#53749=CARTESIAN_POINT('Ctrl Pts',(1.94213207890468,5.4834156773019,97.702832976933));
#53750=CARTESIAN_POINT('Ctrl Pts',(-3.56319066354585,4.59819494989182,97.9812568305801));
#53751=CARTESIAN_POINT('Ctrl Pts',(-5.79462693567359,-0.511881996516395,
98.2596806842271));
#53752=CARTESIAN_POINT('Ctrl Pts',(-2.70191625171569,-5.15163790174596,
98.5381045378744));
#53753=CARTESIAN_POINT('Ctrl Pts',(2.87333547360048,-5.05803002740593,98.8165283915213));
#53754=CARTESIAN_POINT('Ctrl Pts',(5.80854488292173,-0.31706599482648,99.0949522451687));
#53755=CARTESIAN_POINT('Ctrl Pts',(3.40681942119772,4.71522066645252,99.3733760988158));
#53756=CARTESIAN_POINT('Ctrl Pts',(-2.12511743336623,5.41512699725444,99.6517999524627));
#53757=CARTESIAN_POINT('Ctrl Pts',(-5.70448035352804,1.1395737791842,99.9302238061101));
#53758=CARTESIAN_POINT('Ctrl Pts',(-4.0425236775464,-4.18302842668654,100.208647659757));
#53759=CARTESIAN_POINT('Ctrl Pts',(1.33373425917899,-5.66223254802231,100.487071513404));
#53760=CARTESIAN_POINT('Ctrl Pts',(5.48454709390498,-1.93893467572513,100.765495367051));
#53761=CARTESIAN_POINT('Ctrl Pts',(4.59611667109638,3.56587100827567,101.043919220699));
#53762=CARTESIAN_POINT('Ctrl Pts',(-0.515260432469941,5.79432750098943,
101.322343074346));
#53763=CARTESIAN_POINT('Ctrl Pts',(-5.15321236240903,2.69891216046496,101.600766927993));
#53764=CARTESIAN_POINT('Ctrl Pts',(-5.05635388644005,-2.87628403970705,
101.87919078164));
#53765=CARTESIAN_POINT('Ctrl Pts',(-0.313679303199746,-5.8087287590948,
102.157614635287));
#53766=CARTESIAN_POINT('Ctrl Pts',(4.71720619091674,-3.40406966062208,102.436038488934));
#53767=CARTESIAN_POINT('Ctrl Pts',(5.41388703969527,2.12827432992347,102.714462342581));
#53768=CARTESIAN_POINT('Ctrl Pts',(1.13624762196393,5.70514380568731,102.992886196228));
#53769=CARTESIAN_POINT('Ctrl Pts',(-4.1853846852139,4.0400841004573,103.271310049876));
#53770=CARTESIAN_POINT('Ctrl Pts',(-5.66145395974103,-1.33703536367746,
103.549733903523));
#53771=CARTESIAN_POINT('Ctrl Pts',(-1.93573661342329,-5.48567664608875,
103.82815775717));
#53772=CARTESIAN_POINT('Ctrl Pts',(3.56855014082175,-4.59403682989503,104.106581610817));
#53773=CARTESIAN_POINT('Ctrl Pts',(5.79402609657907,0.518638693265626,104.385005464464));
#53774=CARTESIAN_POINT('Ctrl Pts',(2.69590715174485,5.15478507128686,104.663429318111));
#53775=CARTESIAN_POINT('Ctrl Pts',(-2.87923162804837,5.05467602661504,104.941853171758));
#53776=CARTESIAN_POINT('Ctrl Pts',(-5.80891066064616,0.310292504940642,
105.220277025406));
#53777=CARTESIAN_POINT('Ctrl Pts',(-3.4013187428654,-4.71919011181193,105.498700879052));
#53778=CARTESIAN_POINT('Ctrl Pts',(2.13143050299427,-5.4126452417369,105.7771247327));
#53779=CARTESIAN_POINT('Ctrl Pts',(5.70580531843759,-1.13292107848706,106.055548586347));
#53780=CARTESIAN_POINT('Ctrl Pts',(4.03764314998017,4.18773952095986,106.333972439994));
#53781=CARTESIAN_POINT('Ctrl Pts',(-1.34033601366353,5.66067344690254,106.612396293641));
#53782=CARTESIAN_POINT('Ctrl Pts',(-5.48680433346917,1.93253789308644,106.890820147288));
#53783=CARTESIAN_POINT('Ctrl Pts',(-4.59195542699491,-3.57122806027332,
107.169244000935));
#53784=CARTESIAN_POINT('Ctrl Pts',(0.522016777754955,-5.79372272254491,
107.447667854582));
#53785=CARTESIAN_POINT('Ctrl Pts',(5.15635602784475,-2.69290122657703,107.72609170823));
#53786=CARTESIAN_POINT('Ctrl Pts',(5.05299644850137,2.88217823762239,108.004515561877));
#53787=CARTESIAN_POINT('Ctrl Pts',(0.306905601200556,5.8090905875139,108.282939415524));
#53788=CARTESIAN_POINT('Ctrl Pts',(-4.72117242846357,3.39856666886297,108.561363269171));
#53789=CARTESIAN_POINT('Ctrl Pts',(-5.41140160380157,-2.13458595150567,
108.839787122818));
#53790=CARTESIAN_POINT('Ctrl Pts',(-1.1295941498845,-5.70646489155393,109.118210976465));
#53791=CARTESIAN_POINT('Ctrl Pts',(4.19009293312384,-4.03520082694487,109.396634830112));
#53792=CARTESIAN_POINT('Ctrl Pts',(5.65989100977229,1.34363620801531,109.675058683759));
#53793=CARTESIAN_POINT('Ctrl Pts',(1.92933851580168,5.48793015566298,109.953482537407));
#53794=CARTESIAN_POINT('Ctrl Pts',(-3.5739047657201,4.58987246310338,110.231906391054));
#53795=CARTESIAN_POINT('Ctrl Pts',(-5.79341737899019,-0.525394684789773,
110.510330244701));
#53796=CARTESIAN_POINT('Ctrl Pts',(-2.68989438598306,-5.1579252315488,110.788754098348));
#53797=CARTESIAN_POINT('Ctrl Pts',(2.88512386742743,-5.05131515266979,111.067177951995));
#53798=CARTESIAN_POINT('Ctrl Pts',(5.80926853963687,-0.303518593130995,
111.345601805642));
#53799=CARTESIAN_POINT('Ctrl Pts',(3.39581343955041,4.72315314019781,111.62402565929));
#53800=CARTESIAN_POINT('Ctrl Pts',(-2.13774067438488,5.41015612631201,111.902449512937));
#53801=CARTESIAN_POINT('Ctrl Pts',(-5.70712252481211,1.12626683728736,112.180873366584));
#53802=CARTESIAN_POINT('Ctrl Pts',(-4.03275713218176,-4.19244492090577,
112.459297220231));
#53803=CARTESIAN_POINT('Ctrl Pts',(1.34693594561081,-5.65910664861623,112.737721073878));
#53804=CARTESIAN_POINT('Ctrl Pts',(5.48905411228744,-1.92613848265676,113.016144927525));
#53805=CARTESIAN_POINT('Ctrl Pts',(4.58778793892862,3.57658025625215,113.294568781172));
#53806=CARTESIAN_POINT('Ctrl Pts',(-0.528772413221697,5.79311006601865,
113.572992634819));
#53807=CARTESIAN_POINT('Ctrl Pts',(-5.1594926818655,2.68688663098524,113.851416488466));
#53808=CARTESIAN_POINT('Ctrl Pts',(-5.04963213969196,-2.88806851646232,
114.129840342114));
#53809=CARTESIAN_POINT('Ctrl Pts',(-0.300131481883046,-5.80944451695458,
114.408264195761));
#53810=CARTESIAN_POINT('Ctrl Pts',(4.72513224634132,-3.39305905586345,114.686688049408));
#53811=CARTESIAN_POINT('Ctrl Pts',(5.40890880969165,2.14089467055971,114.965111903055));
#53812=CARTESIAN_POINT('Ctrl Pts',(1.12293914182643,5.70777821798859,115.243535756702));
#53813=CARTESIAN_POINT('Ctrl Pts',(-4.19479548350608,4.03031206652138,115.521959610349));
#53814=CARTESIAN_POINT('Ctrl Pts',(-5.65832036370105,-1.3502352253282,115.800383463996));
#53815=CARTESIAN_POINT('Ctrl Pts',(-1.92293779473958,-5.49017620296048,
116.078807317644));
#53816=CARTESIAN_POINT('Ctrl Pts',(3.57925453095985,-4.58570185517924,116.35723117129));
#53817=CARTESIAN_POINT('Ctrl Pts',(5.79280078373477,0.532149961902354,116.635655024938));
#53818=CARTESIAN_POINT('Ctrl Pts',(2.68387796260612,5.16105837826204,116.914078878585));
#53819=CARTESIAN_POINT('Ctrl Pts',(-2.89101218372597,5.04794741013998,117.192502732232));
#53820=CARTESIAN_POINT('Ctrl Pts',(-5.80961851940719,0.296744268608284,
117.470926585879));
#53821=CARTESIAN_POINT('Ctrl Pts',(-3.39030351873854,-4.72710974622134,
117.749350439526));
#53822=CARTESIAN_POINT('Ctrl Pts',(2.14404793895791,-5.40765965436446,118.027774293173));
#53823=CARTESIAN_POINT('Ctrl Pts',(5.70843197086043,-1.11961106463314,118.306198146821));
#53824=CARTESIAN_POINT('Ctrl Pts',(4.02786563079502,4.19714462012598,118.584622000468));
#53825=CARTESIAN_POINT('Ctrl Pts',(-1.35353404604633,5.65753215529382,118.863045854115));
#53826=CARTESIAN_POINT('Ctrl Pts',(-5.49129642730031,1.91973645313823,119.141469707762));
#53827=CARTESIAN_POINT('Ctrl Pts',(-4.58361421256499,-3.58192758893474,
119.419893561409));
#53828=CARTESIAN_POINT('Ctrl Pts',(0.535527329685027,-5.79248953224288,
119.698317415056));
#53829=CARTESIAN_POINT('Ctrl Pts',(5.16262232020387,-2.68086838186981,119.976741268703));
#53830=CARTESIAN_POINT('Ctrl Pts',(5.04626096459074,2.89395486822036,120.25516512235));
#53831=CARTESIAN_POINT('Ctrl Pts',(0.29335695445051,5.80979054693031,120.533588975998));
#53832=CARTESIAN_POINT('Ctrl Pts',(-4.72908563915093,3.38754682912243,120.812012829645));
#53833=CARTESIAN_POINT('Ctrl Pts',(-5.40640866078271,-2.14720047852628,
121.090436683292));
#53834=CARTESIAN_POINT('Ctrl Pts',(-1.11628260678685,-5.7090837831698,121.368860536939));
#53835=CARTESIAN_POINT('Ctrl Pts',(4.19949232986848,-4.02541782590159,121.647284390586));
#53836=CARTESIAN_POINT('Ctrl Pts',(5.65674202384814,1.35683240677064,121.925708244233));
#53837=CARTESIAN_POINT('Ctrl Pts',(1.9165344585906,5.49241478468641,122.20413209788));
#53838=CARTESIAN_POINT('Ctrl Pts',(-3.58459942860632,4.58152501224816,122.482555951528));
#53839=CARTESIAN_POINT('Ctrl Pts',(-5.79217631289823,-0.538904516276096,
122.760979805174));
#53840=CARTESIAN_POINT('Ctrl Pts',(-2.67785788744019,-5.1641845055458,123.039403658822));
#53841=CARTESIAN_POINT('Ctrl Pts',(2.89689656449083,-5.04457280666451,123.317827512469));
#53842=CARTESIAN_POINT('Ctrl Pts',(5.80996060787651,-0.289969534807391,
123.596251366116));
#53843=CARTESIAN_POINT('Ctrl Pts',(3.3847889720702,4.73105991359457,123.874675219763));
#53844=CARTESIAN_POINT('Ctrl Pts',(-2.15035225820507,5.40515584988507,124.15309907341));
#53845=CARTESIAN_POINT('Ctrl Pts',(-5.70973371131906,1.11295373068523,124.431522927057));
#53846=CARTESIAN_POINT('Ctrl Pts',(-4.02296854575556,-4.20183853879829,
124.709946780705));
#53847=CARTESIAN_POINT('Ctrl Pts',(1.36013010449734,-5.65595010773044,124.988370634352));
#53848=CARTESIAN_POINT('Ctrl Pts',(5.49353165593364,-1.91333155142861,125.266794487999));
#53849=CARTESIAN_POINT('Ctrl Pts',(4.57943353516515,3.58726955670461,125.545218341646));
#53850=CARTESIAN_POINT('Ctrl Pts',(-0.542280161447921,5.79186205548623,
125.823642195293));
#53851=CARTESIAN_POINT('Ctrl Pts',(-5.16574749997522,2.67484472491793,126.10206604894));
#53852=CARTESIAN_POINT('Ctrl Pts',(-5.04287809139271,-2.89983395694199,
126.380489902587));
#53853=CARTESIAN_POINT('Ctrl Pts',(-0.286591160200441,-5.81013496081811,
126.658913756234));
#53854=CARTESIAN_POINT('Ctrl Pts',(4.73304984475302,-3.38201813095182,126.937337609882));
#53855=CARTESIAN_POINT('Ctrl Pts',(5.40386860173048,2.15348096294236,127.215761463529));
#53856=CARTESIAN_POINT('Ctrl Pts',(1.10968603140598,5.71042388849744,127.494185317176));
#53857=CARTESIAN_POINT('Ctrl Pts',(-4.2042995484988,4.02043823411284,127.772609170823));
#53858=CARTESIAN_POINT('Ctrl Pts',(-5.65493680070571,-1.36327691301718,
128.05103302447));
#53859=CARTESIAN_POINT('Ctrl Pts',(-1.91054242683083,-5.49493073827346,
128.329456878117));
#53860=CARTESIAN_POINT('Ctrl Pts',(3.59072126358126,-4.5768037590934,128.607880731764));
#53861=CARTESIAN_POINT('Ctrl Pts',(5.79006558455199,0.54463932997096,128.886304585412));
#53862=CARTESIAN_POINT('Ctrl Pts',(2.67464333335573,5.16925071277719,129.164728439058));
#53863=CARTESIAN_POINT('Ctrl Pts',(-2.90822559480448,5.03732645866885,129.443152292706));
#53864=CARTESIAN_POINT('Ctrl Pts',(-5.31707737445595,1.08293508440448,129.675172170745));
#53865=CARTESIAN_POINT('Ctrl Pts',(-4.603565324725,-2.23746205360027,129.860788073176));
#53866=CARTESIAN_POINT('Ctrl Pts',(-3.52404725972245,-3.52728314116456,
129.953596024392));
#53867=CARTESIAN_POINT('Ctrl Pts',(-2.85706463458608,-4.00329423553871,
130.));
#53868=CARTESIAN_POINT('Ctrl Pts',(-3.72756542462615,-3.69853108392275,
-9.85503696991097));
#53869=CARTESIAN_POINT('Ctrl Pts',(-3.11135891409689,-4.31957496079135,
-9.80863299430312));
#53870=CARTESIAN_POINT('Ctrl Pts',(-1.56670996892205,-5.23549382352855,
-9.7158250430874));
#53871=CARTESIAN_POINT('Ctrl Pts',(2.05477896642027,-5.41681918703043,-9.53020914065599));
#53872=CARTESIAN_POINT('Ctrl Pts',(5.80782888043916,-2.19899779207675,-9.2981892626167));
#53873=CARTESIAN_POINT('Ctrl Pts',(4.98754376236452,3.70664924546102,-9.01976540896959));
#53874=CARTESIAN_POINT('Ctrl Pts',(-0.420986833893069,6.19489822788983,
-8.74134155532244));
#53875=CARTESIAN_POINT('Ctrl Pts',(-5.43982339639458,2.99731266347737,-8.46291770167533));
#53876=CARTESIAN_POINT('Ctrl Pts',(-5.46202586547939,-2.9574351526511,-8.18449384802818));
#53877=CARTESIAN_POINT('Ctrl Pts',(-0.46487608052925,-6.1931715401536,-7.90606999438107));
#53878=CARTESIAN_POINT('Ctrl Pts',(4.95898097978158,-3.73947408110051,-7.62764614073393));
#53879=CARTESIAN_POINT('Ctrl Pts',(5.82671362163038,2.15055641831008,-7.34922228708681));
#53880=CARTESIAN_POINT('Ctrl Pts',(1.34069880457724,6.06438734465265,-7.07079843343967));
#53881=CARTESIAN_POINT('Ctrl Pts',(-4.37709716160729,4.40634693213311,-6.79237457979254));
#53882=CARTESIAN_POINT('Ctrl Pts',(-6.07321660587955,-1.30034900384963,
-6.51395072614541));
#53883=CARTESIAN_POINT('Ctrl Pts',(-2.18920112420409,-5.81223701358888,
-6.23552687249829));
#53884=CARTESIAN_POINT('Ctrl Pts',(3.70625950796275,-4.98381762778274,-5.95710301885116));
#53885=CARTESIAN_POINT('Ctrl Pts',(6.19638589441884,0.423781507110357,-5.67867916520402));
#53886=CARTESIAN_POINT('Ctrl Pts',(2.99322353569123,5.44200143254548,-5.4002553115569));
#53887=CARTESIAN_POINT('Ctrl Pts',(-2.96013380442341,5.46007232122862,-5.12183145790976));
#53888=CARTESIAN_POINT('Ctrl Pts',(-6.19369860373471,0.461385997955999,
-4.84340760426264));
#53889=CARTESIAN_POINT('Ctrl Pts',(-3.73644599677842,-4.9612244356498,-4.5649837506155));
#53890=CARTESIAN_POINT('Ctrl Pts',(2.15388118151106,-5.82542485685804,-4.28655989696838));
#53891=CARTESIAN_POINT('Ctrl Pts',(6.06520618595503,-1.3371807278235,-4.00813604332125));
#53892=CARTESIAN_POINT('Ctrl Pts',(4.40377391935758,4.3796750218653,-3.72971218967412));
#53893=CARTESIAN_POINT('Ctrl Pts',(-1.30387902554989,6.0724523764339,-3.45128833602699));
#53894=CARTESIAN_POINT('Ctrl Pts',(-5.81351809866303,2.1858146289845,-3.17286448237986));
#53895=CARTESIAN_POINT('Ctrl Pts',(-4.98165286397166,-3.70916607600341,
-2.89444062873273));
#53896=CARTESIAN_POINT('Ctrl Pts',(0.427392610277646,-6.19613700979456,
-2.6160167750856));
#53897=CARTESIAN_POINT('Ctrl Pts',(5.44374653141498,-2.99005049639645,-2.33759292143847));
#53898=CARTESIAN_POINT('Ctrl Pts',(5.45834505844533,2.96331697399165,-2.05916906779134));
#53899=CARTESIAN_POINT('Ctrl Pts',(0.45777495652505,6.1939664482386,-1.78074521414421));
#53900=CARTESIAN_POINT('Ctrl Pts',(-4.96340223028426,3.73355280798775,-1.50232136049708));
#53901=CARTESIAN_POINT('Ctrl Pts',(-5.82416799274277,-2.15727732608879,
-1.22389750684995));
#53902=CARTESIAN_POINT('Ctrl Pts',(-1.33364425305754,-6.06598477385677,
-0.945473653202821));
#53903=CARTESIAN_POINT('Ctrl Pts',(4.38224189037673,-4.40121963597495,-0.667049799555694));
#53904=CARTESIAN_POINT('Ctrl Pts',(6.07169111549865,1.30741931599734,-0.388625945908561));
#53905=CARTESIAN_POINT('Ctrl Pts',(2.18242472533663,5.81479153437582,-0.110202092261436));
#53906=CARTESIAN_POINT('Ctrl Pts',(-3.71206997155193,4.97948941119768,0.1682217613857));
#53907=CARTESIAN_POINT('Ctrl Pts',(-6.19588676643994,-0.431005159353265,
0.446645615032825));
#53908=CARTESIAN_POINT('Ctrl Pts',(-2.98687604473746,-5.445488937031,0.725069468679958));
#53909=CARTESIAN_POINT('Ctrl Pts',(2.96649892652511,-5.45661638644921,1.00349332232709));
#53910=CARTESIAN_POINT('Ctrl Pts',(6.19423229821208,-0.454163523115957,
1.28191717597421));
#53911=CARTESIAN_POINT('Ctrl Pts',(3.73065829119942,4.96557821247941,1.56034102962135));
#53912=CARTESIAN_POINT('Ctrl Pts',(-2.16067270617363,5.82290921505217,1.83876488326847));
#53913=CARTESIAN_POINT('Ctrl Pts',(-6.06676131618066,1.33010728982196,2.11718873691561));
#53914=CARTESIAN_POINT('Ctrl Pts',(-4.39866384770363,-4.38480725059255,
2.39561259056273));
#53915=CARTESIAN_POINT('Ctrl Pts',(1.31095915737338,-6.07092780039778,2.67403644420987));
#53916=CARTESIAN_POINT('Ctrl Pts',(5.81606299585617,-2.17903407457897,2.95246029785699));
#53917=CARTESIAN_POINT('Ctrl Pts',(4.97732426439622,3.71497260245568,3.23088415150413));
#53918=CARTESIAN_POINT('Ctrl Pts',(-0.434617561225553,6.1956344183157,3.50930800515125));
#53919=CARTESIAN_POINT('Ctrl Pts',(-5.44722949186912,2.98370057694384,3.78773185879839));
#53920=CARTESIAN_POINT('Ctrl Pts',(-5.45488585933577,-2.96967987021536,
4.06615571244551));
#53921=CARTESIAN_POINT('Ctrl Pts',(-0.450551935420432,-6.19449604273283,
4.34457956609265));
#53922=CARTESIAN_POINT('Ctrl Pts',(4.96775250672782,-3.72776250609439,4.62300341973977));
#53923=CARTESIAN_POINT('Ctrl Pts',(5.82164845789067,2.16406735169747,4.9014272733869));
#53924=CARTESIAN_POINT('Ctrl Pts',(1.32656987444429,6.06753579619937,5.17985112703403));
#53925=CARTESIAN_POINT('Ctrl Pts',(-4.38737112024312,4.39610656413154,5.45827498068116));
#53926=CARTESIAN_POINT('Ctrl Pts',(-6.07016242153879,-1.31449855309236,
5.73669883432829));
#53927=CARTESIAN_POINT('Ctrl Pts',(-2.1756426830818,-5.81733248022635,6.01512268797542));
#53928=CARTESIAN_POINT('Ctrl Pts',(3.71787397049125,-4.97515742559844,6.29354654162255));
#53929=CARTESIAN_POINT('Ctrl Pts',(6.19537996404417,0.438229815352393,6.57197039526968));
#53930=CARTESIAN_POINT('Ctrl Pts',(2.98052409487006,5.44896819497442,6.85039424891681));
#53931=CARTESIAN_POINT('Ctrl Pts',(-2.97285980439152,5.45315347788571,7.12881810256394));
#53932=CARTESIAN_POINT('Ctrl Pts',(-6.19475768149381,0.446940194564266,
7.40724195621107));
#53933=CARTESIAN_POINT('Ctrl Pts',(-3.72486545377224,-4.96992511223639,
7.68566580985821));
#53934=CARTESIAN_POINT('Ctrl Pts',(2.16746126156735,-5.8203857217154,7.96408966350532));
#53935=CARTESIAN_POINT('Ctrl Pts',(6.06830821361728,-1.32303200811196,8.24251351715246));
#53936=CARTESIAN_POINT('Ctrl Pts',(4.3935477861451,4.38993349844886,8.52093737079958));
#53937=CARTESIAN_POINT('Ctrl Pts',(-1.31803750196012,6.06939497918618,8.79936122444673));
#53938=CARTESIAN_POINT('Ctrl Pts',(-5.81859998704997,2.17225055199571,9.07778507809384));
#53939=CARTESIAN_POINT('Ctrl Pts',(-4.97298889554354,-3.72077407467108,
9.35620893174098));
#53940=CARTESIAN_POINT('Ctrl Pts',(0.441841920507206,-6.19512340371251,
9.6346327853881));
#53941=CARTESIAN_POINT('Ctrl Pts',(5.45070504575508,-2.97734659959565,9.91305663903523));
#53942=CARTESIAN_POINT('Ctrl Pts',(5.45141924268827,2.9760387279724,10.1914804926824));
#53943=CARTESIAN_POINT('Ctrl Pts',(0.443328301775111,6.19501721440619,10.4699043463295));
#53944=CARTESIAN_POINT('Ctrl Pts',(-4.97209602826647,3.7219671352177,10.7483281999766));
#53945=CARTESIAN_POINT('Ctrl Pts',(-5.81912100695569,-2.17085443462954,
11.0267520536238));
#53946=CARTESIAN_POINT('Ctrl Pts',(-1.31949369202748,-6.06907856817188,
11.3051759072709));
#53947=CARTESIAN_POINT('Ctrl Pts',(4.39249438433867,-4.3909875146141,11.583599760918));
#53948=CARTESIAN_POINT('Ctrl Pts',(6.06862547360082,1.32157600277364,11.8620236145652));
#53949=CARTESIAN_POINT('Ctrl Pts',(2.1688576824738,5.81986551589623,12.1404474682123));
#53950=CARTESIAN_POINT('Ctrl Pts',(-3.7236729140094,4.97081867496857,12.4188713218594));
#53951=CARTESIAN_POINT('Ctrl Pts',(-6.19486473740788,-0.445453875462067,
12.6972951755065));
#53952=CARTESIAN_POINT('Ctrl Pts',(-2.97416809220076,-5.45244004362073,
12.9757190291537));
#53953=CARTESIAN_POINT('Ctrl Pts',(2.97921663987744,-5.44968315433302,13.2541428828008));
#53954=CARTESIAN_POINT('Ctrl Pts',(6.1952746413817,-0.439716258280684,13.5325667364479));
#53955=CARTESIAN_POINT('Ctrl Pts',(3.71906755141604,4.97426525408005,13.8109905900951));
#53956=CARTESIAN_POINT('Ctrl Pts',(-2.1742468697305,5.81785431404147,14.0894144437422));
#53957=CARTESIAN_POINT('Ctrl Pts',(-6.06984685960131,1.31595492739377,14.3678382973893));
#53958=CARTESIAN_POINT('Ctrl Pts',(-4.38842575040887,-4.39505377704208,
14.6462621510364));
#53959=CARTESIAN_POINT('Ctrl Pts',(1.32511405433002,-6.06785390504426,14.9246860046836));
#53960=CARTESIAN_POINT('Ctrl Pts',(5.82112906633488,-2.1654640756695,15.2031098583307));
#53961=CARTESIAN_POINT('Ctrl Pts',(4.96864676461137,3.72657048752075,15.4815337119778));
#53962=CARTESIAN_POINT('Ctrl Pts',(-0.449065678989183,6.19460396521824,
15.759957565625));
#53963=CARTESIAN_POINT('Ctrl Pts',(-5.45417318798152,2.97098857376587,16.0383814192721));
#53964=CARTESIAN_POINT('Ctrl Pts',(-5.44794521341013,-2.98239353902625,
16.3168052729192));
#53965=CARTESIAN_POINT('Ctrl Pts',(-0.436104065308916,-6.19552996233291,
16.5952291265663));
#53966=CARTESIAN_POINT('Ctrl Pts',(4.97643278893975,-3.71616670335292,16.8736529802135));
#53967=CARTESIAN_POINT('Ctrl Pts',(5.81658564340332,2.17763856571702,17.1520768338606));
#53968=CARTESIAN_POINT('Ctrl Pts',(1.31241571541379,6.07061308764435,17.4305006875077));
#53969=CARTESIAN_POINT('Ctrl Pts',(-4.39761167568901,4.38586249440032,17.7089245411549));
#53970=CARTESIAN_POINT('Ctrl Pts',(-6.06708027377879,-1.3286516554266,17.987348394802));
#53971=CARTESIAN_POINT('Ctrl Pts',(-2.16206973273641,-5.82239063793635,
18.2657722484491));
#53972=CARTESIAN_POINT('Ctrl Pts',(3.72946679422009,-4.96647316521026,18.5441961020963));
#53973=CARTESIAN_POINT('Ctrl Pts',(6.19434108723227,0.452677329860728,18.8226199557434));
#53974=CARTESIAN_POINT('Ctrl Pts',(2.9678080453718,5.45590447824831,19.1010438093905));
#53975=CARTESIAN_POINT('Ctrl Pts',(-2.98556942433889,5.44620542051037,19.3794676630377));
#53976=CARTESIAN_POINT('Ctrl Pts',(-6.19578317717296,0.432491724087773,
19.6578915166847));
#53977=CARTESIAN_POINT('Ctrl Pts',(-3.71326459201449,-4.97859863210875,
19.9363153703319));
#53978=CARTESIAN_POINT('Ctrl Pts',(2.18102952143619,-5.81531499547251,20.214739223979));
#53979=CARTESIAN_POINT('Ctrl Pts',(6.07137725204052,-1.30887605729064,20.4931630776262));
#53980=CARTESIAN_POINT('Ctrl Pts',(4.38329774745979,4.40016807940991,20.7715869312733));
#53981=CARTESIAN_POINT('Ctrl Pts',(-1.33218880486076,6.06630458006745,21.0500107849204));
#53982=CARTESIAN_POINT('Ctrl Pts',(-5.82365023027184,2.15867465482835,21.3284346385676));
#53983=CARTESIAN_POINT('Ctrl Pts',(-4.96429787750409,-3.73236183312285,
21.6068584922147));
#53984=CARTESIAN_POINT('Ctrl Pts',(0.456288826848907,-6.19407610353931,
21.8852823458618));
#53985=CARTESIAN_POINT('Ctrl Pts',(5.4576339138326,-2.96462650809979,22.163706199509));
#53986=CARTESIAN_POINT('Ctrl Pts',(5.44446377622514,2.9887442947358,22.4421300531561));
#53987=CARTESIAN_POINT('Ctrl Pts',(0.428879235845219,6.19603428581577,22.7205539068032));
#53988=CARTESIAN_POINT('Ctrl Pts',(-4.9807627828508,3.7103612183873,22.9989777604504));
#53989=CARTESIAN_POINT('Ctrl Pts',(-5.81404237068101,-2.18441973573531,
23.2774016140974));
#53990=CARTESIAN_POINT('Ctrl Pts',(-1.30533595422747,-6.07213935253009,
23.5558254677446));
#53991=CARTESIAN_POINT('Ctrl Pts',(4.40272298733576,-4.38073151045905,23.8342493213917));
#53992=CARTESIAN_POINT('Ctrl Pts',(6.06552682417391,1.3357255014301,24.1126731750389));
#53993=CARTESIAN_POINT('Ctrl Pts',(2.15527884309945,5.82490784291321,24.391097028686));
#53994=CARTESIAN_POINT('Ctrl Pts',(-3.73525560324502,4.96212090223225,24.6695208823331));
#53995=CARTESIAN_POINT('Ctrl Pts',(-6.19380901422938,-0.459900168726112,
24.9479447359802));
#53996=CARTESIAN_POINT('Ctrl Pts',(-2.96144396303136,-5.45936149414647,
25.2263685896274));
#53997=CARTESIAN_POINT('Ctrl Pts',(2.99191814913776,-5.44272028114656,25.5047924432745));
#53998=CARTESIAN_POINT('Ctrl Pts',(6.196283288176,-0.425266601809134,25.7832162969216));
#53999=CARTESIAN_POINT('Ctrl Pts',(3.70745658345825,4.98292524043012,26.0616401505688));
#54000=CARTESIAN_POINT('Ctrl Pts',(-2.18780920746171,5.81276776946144,26.3400640042159));
#54001=CARTESIAN_POINT('Ctrl Pts',(-6.07289938885401,1.30179540742797,26.618487857863));
#54002=CARTESIAN_POINT('Ctrl Pts',(-4.37816378427055,-4.40527639859808,
26.8969117115101));
#54003=CARTESIAN_POINT('Ctrl Pts',(1.33926174393233,-6.06474700636252,27.1753355651573));
#54004=CARTESIAN_POINT('Ctrl Pts',(5.82616347543284,-2.15188229870415,27.4537594188044));
#54005=CARTESIAN_POINT('Ctrl Pts',(4.95994224013495,3.73814810360272,27.7321832724515));
#54006=CARTESIAN_POINT('Ctrl Pts',(-0.463511354264669,6.19353981939337,
28.0106071260987));
#54007=CARTESIAN_POINT('Ctrl Pts',(-5.46108721860255,2.95826041124837,28.2890309797457));
#54008=CARTESIAN_POINT('Ctrl Pts',(-5.4409749358673,-2.99509098646564,28.567454833393));
#54009=CARTESIAN_POINT('Ctrl Pts',(-0.421653823207863,-6.19653018416905,
28.8458786870401));
#54010=CARTESIAN_POINT('Ctrl Pts',(4.98508600411173,-3.70455068821481,29.1243025406872));
#54011=CARTESIAN_POINT('Ctrl Pts',(5.81149119224705,2.19119793546338,29.4027263943343));
#54012=CARTESIAN_POINT('Ctrl Pts',(1.2982544180955,6.07365736075385,29.6811502479814));
#54013=CARTESIAN_POINT('Ctrl Pts',(-4.40782831232883,4.37559456976717,29.9595741016286));
#54014=CARTESIAN_POINT('Ctrl Pts',(-6.0639651268984,-1.34279753116531,30.2379979552757));
#54015=CARTESIAN_POINT('Ctrl Pts',(-2.14848502279716,-5.82741712740386,
30.5164218089228));
#54016=CARTESIAN_POINT('Ctrl Pts',(3.74103933321266,-4.95776189195283,30.79484566257));
#54017=CARTESIAN_POINT('Ctrl Pts',(6.19326851912278,0.467122382236926,31.0732695162171));
#54018=CARTESIAN_POINT('Ctrl Pts',(2.95507585383304,5.46281108661433,31.3516933698642));
#54019=CARTESIAN_POINT('Ctrl Pts',(-2.99826280564106,5.43922774098064,31.6301172235114));
#54020=CARTESIAN_POINT('Ctrl Pts',(-6.19677497371092,0.418040901269345,
31.9085410771585));
#54021=CARTESIAN_POINT('Ctrl Pts',(-3.7016435336448,-4.98724507316104,32.1869649308056));
#54022=CARTESIAN_POINT('Ctrl Pts',(2.1945859185882,-5.81021263947181,32.4653887844528));
#54023=CARTESIAN_POINT('Ctrl Pts',(6.07441326797193,-1.29471298743398,32.7438126380998));
#54024=CARTESIAN_POINT('Ctrl Pts',(4.37302386782237,4.41037872766044,33.022236491747));
#54025=CARTESIAN_POINT('Ctrl Pts',(-1.3463328619271,6.0631811860474,33.3006603453941));
#54026=CARTESIAN_POINT('Ctrl Pts',(-5.82866879840025,2.14508701653312,33.5790841990412));
#54027=CARTESIAN_POINT('Ctrl Pts',(-4.95557985842688,-3.74392929109215,
33.8575080526884));
#54028=CARTESIAN_POINT('Ctrl Pts',(0.470733251415439,-6.19299511350976,
34.1359319063355));
#54029=CARTESIAN_POINT('Ctrl Pts',(5.46453309759574,-2.95189029186794,34.4143557599827));
#54030=CARTESIAN_POINT('Ctrl Pts',(5.43747869708053,3.00143360558567,34.6927796136298));
#54031=CARTESIAN_POINT('Ctrl Pts',(0.414427837221952,6.19701765671836,34.9712034672769));
#54032=CARTESIAN_POINT('Ctrl Pts',(-4.98940244684405,3.69873512073661,35.249627320924));
#54033=CARTESIAN_POINT('Ctrl Pts',(-5.80893211157042,-2.19797315568457,
35.5280511745712));
#54034=CARTESIAN_POINT('Ctrl Pts',(-1.29117111664705,-6.07516711025136,
35.8064750282183));
#54035=CARTESIAN_POINT('Ctrl Pts',(4.41292764372606,-4.37045167930985,36.0848988818654));
#54036=CARTESIAN_POINT('Ctrl Pts',(6.06239518407591,1.34986773501598,36.3633227355126));
#54037=CARTESIAN_POINT('Ctrl Pts',(2.14168828106728,5.82991848799643,36.6417465891597));
#54038=CARTESIAN_POINT('Ctrl Pts',(-3.74681797625863,4.95339614029897,36.9201704428068));
#54039=CARTESIAN_POINT('Ctrl Pts',(-6.19271960264728,-0.47434396057257,
37.1985942964539));
#54040=CARTESIAN_POINT('Ctrl Pts',(-2.94870372643611,-5.46625325096137,
37.4770181501011));
#54041=CARTESIAN_POINT('Ctrl Pts',(3.00460338522167,-5.43572780476161,37.7554420037482));
#54042=CARTESIAN_POINT('Ctrl Pts',(6.19725823310897,-0.410814632293651,
38.0338658573953));
#54043=CARTESIAN_POINT('Ctrl Pts',(3.69582545047869,4.99155812442748,38.3122897110425));
#54044=CARTESIAN_POINT('Ctrl Pts',(-2.20135964560103,5.80764960897808,38.5907135646896));
#54045=CARTESIAN_POINT('Ctrl Pts',(-6.07591888733587,1.28762880693885,38.8691374183368));
#54046=CARTESIAN_POINT('Ctrl Pts',(-4.36787800510409,-4.4154750596591,39.1475612719838));
#54047=CARTESIAN_POINT('Ctrl Pts',(1.35340214923009,-6.06160712125117,39.425985125631));
#54048=CARTESIAN_POINT('Ctrl Pts',(5.83116619576758,-2.13828881755513,39.7044089792781));
#54049=CARTESIAN_POINT('Ctrl Pts',(4.95121073831148,3.74970538773023,39.9828328329253));
#54050=CARTESIAN_POINT('Ctrl Pts',(-0.477954508481131,6.19244198662903,
40.2612566865723));
#54051=CARTESIAN_POINT('Ctrl Pts',(-5.46797154612653,2.94551615862052,40.5396805402195));
#54052=CARTESIAN_POINT('Ctrl Pts',(-5.43397506461897,-3.00777214347152,
40.8181043938666));
#54053=CARTESIAN_POINT('Ctrl Pts',(-0.407201287712849,-6.19749670280094,
41.0965282475137));
#54054=CARTESIAN_POINT('Ctrl Pts',(4.99371210517841,-3.69291452386027,41.3749521011609));
#54055=CARTESIAN_POINT('Ctrl Pts',(5.80636513213084,2.2047453871862,41.653375954808));
#54056=CARTESIAN_POINT('Ctrl Pts',(1.28408605951368,6.07666859896988,41.9317998084552));
#54057=CARTESIAN_POINT('Ctrl Pts',(-4.41802097459366,4.36530284608003,42.2102236621023));
#54058=CARTESIAN_POINT('Ctrl Pts',(-6.06081699784108,-1.35693610336823,
42.4886475157494));
#54059=CARTESIAN_POINT('Ctrl Pts',(-2.13488862715202,-5.83241192128959,
42.7670713693965));
#54060=CARTESIAN_POINT('Ctrl Pts',(3.75259152452537,-4.9490236532072,43.0454952230437));
#54061=CARTESIAN_POINT('Ctrl Pts',(6.19216226554937,0.481564893913621,43.3239190766908));
#54062=CARTESIAN_POINT('Ctrl Pts',(2.94232758950492,5.46968798250703,43.602342930338));
#54063=CARTESIAN_POINT('Ctrl Pts',(-3.01093987925787,5.43222047724852,43.880766783985));
#54064=CARTESIAN_POINT('Ctrl Pts',(-6.19773306571321,0.403587804708005,
44.1591906376322));
#54065=CARTESIAN_POINT('Ctrl Pts',(-3.69000234187092,-4.99586438836475,
44.4376144912793));
#54066=CARTESIAN_POINT('Ctrl Pts',(2.2081303792894,-5.80507868146529,44.7160383449265));
#54067=CARTESIAN_POINT('Ctrl Pts',(6.07741624489852,-1.28054287557562,44.9944621985735));
#54068=CARTESIAN_POINT('Ctrl Pts',(4.36272620311297,4.42056538766427,45.2728860522208));
#54069=CARTESIAN_POINT('Ctrl Pts',(-1.36046959622891,6.06002481411424,45.5513099058677));
#54070=CARTESIAN_POINT('Ctrl Pts',(-5.83365566413891,2.13148771101397,45.8297337595151));
#54071=CARTESIAN_POINT('Ctrl Pts',(-4.94683488572972,-3.75547638566279,
46.108157613162));
#54072=CARTESIAN_POINT('Ctrl Pts',(0.485175115642611,-6.19188043950342,
46.3865814668093));
#54073=CARTESIAN_POINT('Ctrl Pts',(5.47140255951946,-2.93913802017323,46.6650053204563));
#54074=CARTESIAN_POINT('Ctrl Pts',(5.43046404324665,3.01410659150414,46.9434291741035));
#54075=CARTESIAN_POINT('Ctrl Pts',(0.399974184507209,6.19796732176539,47.2218530277506));
#54076=CARTESIAN_POINT('Ctrl Pts',(-4.99801497325478,3.68708890550052,47.5002768813978));
#54077=CARTESIAN_POINT('Ctrl Pts',(-5.80379025741878,-2.2115146207598,47.7787007350449));
#54078=CARTESIAN_POINT('Ctrl Pts',(-1.2769992563293,-6.07816182486761,48.057124588692));
#54079=CARTESIAN_POINT('Ctrl Pts',(4.42310829800586,-4.36014807707895,48.3355484423391));
#54080=CARTESIAN_POINT('Ctrl Pts',(6.05923057033998,1.36400262661085,48.6139722959862));
#54081=CARTESIAN_POINT('Ctrl Pts',(2.12808607029709,5.83489742389285,48.8923961496335));
#54082=CARTESIAN_POINT('Ctrl Pts',(-3.75835997016207,4.94464443662301,49.1708200032804));
#54083=CARTESIAN_POINT('Ctrl Pts',(-6.19159650858692,-0.488785172441089,
49.4492438569277));
#54084=CARTESIAN_POINT('Ctrl Pts',(-2.93594745170962,-5.47311527658095,
49.7276677105747));
#54085=CARTESIAN_POINT('Ctrl Pts',(3.0172722791337,-5.42870576321049,50.006091564222));
#54086=CARTESIAN_POINT('Ctrl Pts',(6.19819947087785,-0.39636042833906,50.284515417869));
#54087=CARTESIAN_POINT('Ctrl Pts',(3.68417421573959,5.00016385911732,50.5629392715162));
#54088=CARTESIAN_POINT('Ctrl Pts',(-2.21489811044685,5.80249986042937,50.8413631251632));
#54089=CARTESIAN_POINT('Ctrl Pts',(-6.0789053386238,1.2734552029793,51.1197869788105));
#54090=CARTESIAN_POINT('Ctrl Pts',(-4.35756846885422,-4.4256497047542,51.3982108324575));
#54091=CARTESIAN_POINT('Ctrl Pts',(1.36753519331326,-6.05843426678821,51.6766346861046));
#54092=CARTESIAN_POINT('Ctrl Pts',(5.83613720012922,-2.12468370615766,51.9550585397519));
#54093=CARTESIAN_POINT('Ctrl Pts',(4.94245230663171,3.76124227704283,52.2334823933989));
#54094=CARTESIAN_POINT('Ctrl Pts',(-0.492395063081671,6.19131047289637,
52.5119062470461));
#54095=CARTESIAN_POINT('Ctrl Pts',(-5.47482613310915,2.93275588519888,52.7903301006932));
#54096=CARTESIAN_POINT('Ctrl Pts',(-5.42694563773782,-3.02043694107034,
53.0687539543404));
#54097=CARTESIAN_POINT('Ctrl Pts',(-0.392746537431982,-6.19842951297174,
53.3471778079874));
#54098=CARTESIAN_POINT('Ctrl Pts',(5.0023110452221,-3.68125827357881,53.6256016616347));
#54099=CARTESIAN_POINT('Ctrl Pts',(5.80120749093557,2.21828084720058,53.9040255152817));
#54100=CARTESIAN_POINT('Ctrl Pts',(1.26991071673034,6.07964678591425,54.1824493689289));
#54101=CARTESIAN_POINT('Ctrl Pts',(-4.42818960704527,4.35498737931578,54.4608732225759));
#54102=CARTESIAN_POINT('Ctrl Pts',(-6.05763590372964,-1.37106729513512,
54.7392970762232));
#54103=CARTESIAN_POINT('Ctrl Pts',(-2.12128061975243,-5.83737499242651,
55.0177209298702));
#54104=CARTESIAN_POINT('Ctrl Pts',(3.76412330532518,-4.94025849650115,55.2961447835174));
#54105=CARTESIAN_POINT('Ctrl Pts',(6.19102233252913,0.496004786337269,55.5745686371645));
#54106=CARTESIAN_POINT('Ctrl Pts',(2.92956332172572,5.47653512852268,55.8529924908116));
#54107=CARTESIAN_POINT('Ctrl Pts',(-3.02360057623841,5.42518366742681,56.1314163444588));
#54108=CARTESIAN_POINT('Ctrl Pts',(-6.1986574479688,0.389132513014424,56.4098401981059));
#54109=CARTESIAN_POINT('Ctrl Pts',(-3.6783410800095,-5.0044565308391,56.688264051753));
#54110=CARTESIAN_POINT('Ctrl Pts',(2.22166282987091,-5.79991314937677,56.9666879054002));
#54111=CARTESIAN_POINT('Ctrl Pts',(6.08038616648687,-1.2663657987875,57.2451117590473));
#54112=CARTESIAN_POINT('Ctrl Pts',(4.35240480934116,4.43072800401557,57.5235356126944));
#54113=CARTESIAN_POINT('Ctrl Pts',(-1.37459893087578,6.05683548143575,57.8019594663416));
#54114=CARTESIAN_POINT('Ctrl Pts',(-5.83861080036407,2.11787681223804,58.0803833199886));
#54115=CARTESIAN_POINT('Ctrl Pts',(-4.93806300697687,-3.7670030540299,58.3588071736358));
#54116=CARTESIAN_POINT('Ctrl Pts',(0.499614340980781,-6.19073208758301,
58.6372310272829));
#54117=CARTESIAN_POINT('Ctrl Pts',(5.47824226224044,-2.9263697623756,58.9156548809301));
#54118=CARTESIAN_POINT('Ctrl Pts',(5.42341985287656,3.02676318356225,59.1940787345772));
#54119=CARTESIAN_POINT('Ctrl Pts',(0.385518356315185,6.1988832757915,59.4725025882243));
#54120=CARTESIAN_POINT('Ctrl Pts',(-5.00660031523891,3.6754226360235,59.7509264418715));
#54121=CARTESIAN_POINT('Ctrl Pts',(-5.79861683619302,-2.22504405730817,
60.0293502955185));
#54122=CARTESIAN_POINT('Ctrl Pts',(-1.26282045035567,-6.08112348009042,
60.3077741491658));
#54123=CARTESIAN_POINT('Ctrl Pts',(4.43326489480233,-4.34982075980811,60.5861980028128));
#54124=CARTESIAN_POINT('Ctrl Pts',(6.05603300017853,1.37813009933466,60.86462185646));
#54125=CARTESIAN_POINT('Ctrl Pts',(2.11447228477175,5.83984462352173,61.1430457101071));
#54126=CARTESIAN_POINT('Ctrl Pts',(-3.76988152217794,4.93586583880535,61.4214695637542));
#54127=CARTESIAN_POINT('Ctrl Pts',(-6.19043973815677,-0.503223725785225,
61.6998934174013));
#54128=CARTESIAN_POINT('Ctrl Pts',(-2.92317520823401,-5.47994753368219,
61.9783172710485));
#54129=CARTESIAN_POINT('Ctrl Pts',(3.02992476196705,-5.42165419468657,62.2567411246955));
#54130=CARTESIAN_POINT('Ctrl Pts',(6.19910699636319,-0.381904068562471,
62.5351649783428));
#54131=CARTESIAN_POINT('Ctrl Pts',(3.67250294261256,5.0087423976929,62.8135888319898));
#54132=CARTESIAN_POINT('Ctrl Pts',(-2.22842452836309,5.79731855182492,63.0920126856371));
#54133=CARTESIAN_POINT('Ctrl Pts',(-6.08185872647424,1.25927467264003,63.3704365392841));
#54134=CARTESIAN_POINT('Ctrl Pts',(-4.34723523159504,-4.43580027854311,
63.6488603929313));
#54135=CARTESIAN_POINT('Ctrl Pts',(1.38166079931146,-6.05522846023084,63.9272842465784));
#54136=CARTESIAN_POINT('Ctrl Pts',(5.8410764614801,-2.11106703851077,64.2057081002255));
#54137=CARTESIAN_POINT('Ctrl Pts',(4.9336669927334,3.77275870879084,64.4841319538727));
#54138=CARTESIAN_POINT('Ctrl Pts',(-0.506832939523575,6.19014528434975,
64.7625558075197));
#54139=CARTESIAN_POINT('Ctrl Pts',(-5.48165094226821,2.91997966038697,65.040979661167));
#54140=CARTESIAN_POINT('Ctrl Pts',(-5.41988669345709,-3.03308531037791,
65.319403514814));
#54141=CARTESIAN_POINT('Ctrl Pts',(-0.378289650985128,-6.19932860960775,
65.5978273684612));
#54142=CARTESIAN_POINT('Ctrl Pts',(5.01088277747282,-3.66958200076937,65.8762512221083));
#54143=CARTESIAN_POINT('Ctrl Pts',(5.79601829671383,2.2318042418864,66.1546750757555));
#54144=CARTESIAN_POINT('Ctrl Pts',(1.25572846684602,6.08259190538837,66.4330989294025));
#54145=CARTESIAN_POINT('Ctrl Pts',(-4.43833415437589,4.34464822558098,66.7115227830498));
#54146=CARTESIAN_POINT('Ctrl Pts',(-6.0544218618662,-1.38519102960575,66.9899466366968));
#54147=CARTESIAN_POINT('Ctrl Pts',(-2.10766107461286,-5.84230631382042,
67.268370490344));
#54148=CARTESIAN_POINT('Ctrl Pts',(3.7756346128904,-4.93146646950858,67.5467943439911));
#54149=CARTESIAN_POINT('Ctrl Pts',(6.18984872626208,0.510441980968776,67.8252181976383));
#54150=CARTESIAN_POINT('Ctrl Pts',(2.9167831199209,5.48335248741942,68.1036420512853));
#54151=CARTESIAN_POINT('Ctrl Pts',(-3.03624482772044,5.41811734978899,68.3820659049325));
#54152=CARTESIAN_POINT('Ctrl Pts',(-6.19954811544985,0.374675104811834,
68.6604897585795));
#54153=CARTESIAN_POINT('Ctrl Pts',(-3.66665981148688,-5.01302145385108,
68.9389136122268));
#54154=CARTESIAN_POINT('Ctrl Pts',(2.23518319672922,-5.79471607130176,69.2173374658739));
#54155=CARTESIAN_POINT('Ctrl Pts',(6.08332301658356,-1.25218183417913,69.4957613195209));
#54156=CARTESIAN_POINT('Ctrl Pts',(4.34205974264528,4.44086652143958,69.7741851731683));
#54157=CARTESIAN_POINT('Ctrl Pts',(-1.38872078901773,6.05361320535872,70.0526090268151));
#54158=CARTESIAN_POINT('Ctrl Pts',(-5.84353418012459,2.10425439423563,70.3310328804625));
#54159=CARTESIAN_POINT('Ctrl Pts',(-4.9292642698789,-3.77850923349922,70.6094567341095));
#54160=CARTESIAN_POINT('Ctrl Pts',(0.514050848894259,-6.18955006399452,
70.8878805877567));
#54161=CARTESIAN_POINT('Ctrl Pts',(5.4850521685573,-2.91358558792228,71.1663044414038));
#54162=CARTESIAN_POINT('Ctrl Pts',(5.41634616428379,3.03940331292046,71.4447282950509));
#54163=CARTESIAN_POINT('Ctrl Pts',(0.371060431271426,6.19976551381493,71.7231521486979));
#54164=CARTESIAN_POINT('Ctrl Pts',(-5.01515842610055,3.66373637575853,72.0015760023452));
#54165=CARTESIAN_POINT('Ctrl Pts',(-5.79341187603146,-2.23856139174275,
72.2799998559922));
#54166=CARTESIAN_POINT('Ctrl Pts',(-1.24863477584512,-6.08405205981133,
72.5584237096394));
#54167=CARTESIAN_POINT('Ctrl Pts',(4.44339737887316,-4.3394697836679,72.8368475632866));
#54168=CARTESIAN_POINT('Ctrl Pts',(6.05280249098336,1.39225007634737,73.1152714169336));
#54169=CARTESIAN_POINT('Ctrl Pts',(2.10084699853723,5.8447600599752,73.3936952705809));
#54170=CARTESIAN_POINT('Ctrl Pts',(-3.78138256963996,4.92706039459298,73.6721191242278));
#54171=CARTESIAN_POINT('Ctrl Pts',(-6.18924929764864,-0.517659542073067,
73.9505429778751));
#54172=CARTESIAN_POINT('Ctrl Pts',(-2.91038706547802,-5.48674998510428,
74.2289668315222));
#54173=CARTESIAN_POINT('Ctrl Pts',(3.04256076490452,-5.41457313754346,74.5073906851693));
#54174=CARTESIAN_POINT('Ctrl Pts',(6.19998080462899,-0.367445631592474,
74.7858145388165));
#54175=CARTESIAN_POINT('Ctrl Pts',(3.66081169457798,5.017293693495,75.0642383924636));
#54176=CARTESIAN_POINT('Ctrl Pts',(-2.24193882577889,5.79210571134614,75.3426622461107));
#54177=CARTESIAN_POINT('Ctrl Pts',(-6.08477903482368,1.24508729304965,75.6210860997579));
#54178=CARTESIAN_POINT('Ctrl Pts',(-4.33687834952939,-4.44592672581621,
75.8995099534049));
#54179=CARTESIAN_POINT('Ctrl Pts',(1.39577889039483,-6.05198971901576,76.1779338070522));
#54180=CARTESIAN_POINT('Ctrl Pts',(5.84598395295547,-2.09743888867607,76.4563576606991));
#54181=CARTESIAN_POINT('Ctrl Pts',(4.92485484440009,3.78425462033575,76.7347815143464));
#54182=CARTESIAN_POINT('Ctrl Pts',(-0.521268059278363,6.18894642732675,
77.0132053679934));
#54183=CARTESIAN_POINT('Ctrl Pts',(-5.48844593648309,2.90718755367551,77.2916292216407));
#54184=CARTESIAN_POINT('Ctrl Pts',(-5.41279827017078,-3.04571718259916,
77.5700530752877));
#54185=CARTESIAN_POINT('Ctrl Pts',(-0.363830707003893,-6.20019398781887,
77.8484769289348));
#54186=CARTESIAN_POINT('Ctrl Pts',(5.01942725530845,-3.65788576893953,78.126900782582));
#54187=CARTESIAN_POINT('Ctrl Pts',(5.79079757768992,2.24531549768938,78.4053246362291));
#54188=CARTESIAN_POINT('Ctrl Pts',(1.24153938699856,6.08550394137369,78.6837484898763));
#54189=CARTESIAN_POINT('Ctrl Pts',(-4.4484545614091,4.33428544111047,78.9621723435234));
#54190=CARTESIAN_POINT('Ctrl Pts',(-6.05117488973208,-1.39930722996069,
79.2405961971704));
#54191=CARTESIAN_POINT('Ctrl Pts',(-2.09403006581055,-5.8472058586495,79.5190200508177));
#54192=CARTESIAN_POINT('Ctrl Pts',(3.78712538461051,-4.92264762004982,79.7974439044648));
#54193=CARTESIAN_POINT('Ctrl Pts',(6.18864145313159,0.524876399283552,80.0758677581119));
#54194=CARTESIAN_POINT('Ctrl Pts',(2.90398705360255,5.49014002211714,80.354291611759));
#54195=CARTESIAN_POINT('Ctrl Pts',(-3.04887256493131,5.41102156276922,80.6327154654062));
#54196=CARTESIAN_POINT('Ctrl Pts',(-6.20040506331207,0.360215658734639,
80.9111393190533));
#54197=CARTESIAN_POINT('Ctrl Pts',(-3.65495859983791,-5.02155911081553,
81.1895631727004));
#54198=CARTESIAN_POINT('Ctrl Pts',(2.24869140632625,-5.78948747550755,81.4679870263477));
#54199=CARTESIAN_POINT('Ctrl Pts',(6.08622677921486,-1.23799105889803,81.7464108799947));
#54200=CARTESIAN_POINT('Ctrl Pts',(4.33169105929267,4.45098088479241,82.0248347336419));
#54201=CARTESIAN_POINT('Ctrl Pts',(-1.40283509384545,6.05035800340937,82.3032585872889));
#54202=CARTESIAN_POINT('Ctrl Pts',(-5.84842577664184,2.09062053109955,82.5816824409361));
#54203=CARTESIAN_POINT('Ctrl Pts',(-4.92043872229259,-3.78999486148822,
82.8601062945833));
#54204=CARTESIAN_POINT('Ctrl Pts',(0.528484560862153,-6.18833437516702,
83.1385301482302));
#54205=CARTESIAN_POINT('Ctrl Pts',(5.49183224143067,-2.90078556634683,83.4169540018776));
#54206=CARTESIAN_POINT('Ctrl Pts',(5.40924301594254,3.05202691082846,83.6953778555245));
#54207=CARTESIAN_POINT('Ctrl Pts',(0.35660048801342,6.20061403103695,83.9738017091718));
#54208=CARTESIAN_POINT('Ctrl Pts',(-5.02368925929172,3.65203018826795,84.2522255628188));
#54209=CARTESIAN_POINT('Ctrl Pts',(-5.78817540524418,-2.25206655054194,
84.530649416466));
#54210=CARTESIAN_POINT('Ctrl Pts',(-1.23444230995443,-6.08694754810143,
84.8090732701131));
#54211=CARTESIAN_POINT('Ctrl Pts',(4.45350569510733,-4.32909520495806,85.0874971237602));
#54212=CARTESIAN_POINT('Ctrl Pts',(6.04953906032532,1.40636248084973,85.3659209774074));
#54213=CARTESIAN_POINT('Ctrl Pts',(2.08721028570223,5.84964370651772,85.6443448310545));
#54214=CARTESIAN_POINT('Ctrl Pts',(-3.79286304999338,4.91822815187942,85.9227686847017));
#54215=CARTESIAN_POINT('Ctrl Pts',(-6.1880251935374,-0.532092542787492,
86.2011925383488));
#54216=CARTESIAN_POINT('Ctrl Pts',(-2.89758309299682,-5.49352259384837,
86.4796163919959));
#54217=CARTESIAN_POINT('Ctrl Pts',(3.05518021921827,-5.40746263029544,86.758040245643));
#54218=CARTESIAN_POINT('Ctrl Pts',(6.20082089092238,-0.352985196069277,
87.0364640992902));
#54219=CARTESIAN_POINT('Ctrl Pts',(3.6491005352253,5.0258177000128,87.3148879529372));
#54220=CARTESIAN_POINT('Ctrl Pts',(-2.2554409291893,5.78686136734597,87.5933118065845));
#54221=CARTESIAN_POINT('Ctrl Pts',(-6.08766624778842,1.23089314137383,87.8717356602316));
#54222=CARTESIAN_POINT('Ctrl Pts',(-4.32649787898883,-4.45602899149562,
88.1501595138786));
#54223=CARTESIAN_POINT('Ctrl Pts',(1.40988938977465,-6.04871806075837,88.4285833675259));
#54224=CARTESIAN_POINT('Ctrl Pts',(5.85085964786324,-2.08379933077759,88.7070072211729));
#54225=CARTESIAN_POINT('Ctrl Pts',(4.91601590956152,3.79572994915096,88.9854310748201));
#54226=CARTESIAN_POINT('Ctrl Pts',(-0.535700343832902,6.1877139083478,89.2638549284673));
#54227=CARTESIAN_POINT('Ctrl Pts',(-5.49521107879562,2.89437963464127,89.5422787821142));
#54228=CARTESIAN_POINT('Ctrl Pts',(-5.40568040643315,-3.05833248902866,
89.8207026357616));
#54229=CARTESIAN_POINT('Ctrl Pts',(-0.349369784131343,-6.20102564289808,
90.0991264894084));
#54230=CARTESIAN_POINT('Ctrl Pts',(5.02794443225523,-3.64616964170593,90.3775503430558));
#54231=CARTESIAN_POINT('Ctrl Pts',(5.7855453622596,2.25881454112108,90.6559741967028));
#54232=CARTESIAN_POINT('Ctrl Pts',(1.22734355436289,6.08838287803152,90.93439805035));
#54233=CARTESIAN_POINT('Ctrl Pts',(-4.45855077309947,4.32389908226804,91.2128219039971));
#54234=CARTESIAN_POINT('Ctrl Pts',(-6.04789500498758,-1.41341581942115,
91.4912457576442));
#54235=CARTESIAN_POINT('Ctrl Pts',(-2.08038766748531,-5.852073600265,91.7696696112914));
#54236=CARTESIAN_POINT('Ctrl Pts',(3.79859555798657,-4.91380199609103,92.0480934649385));
#54237=CARTESIAN_POINT('Ctrl Pts',(6.18740051970406,0.539307962772255,92.3265173185856));
#54238=CARTESIAN_POINT('Ctrl Pts',(2.89117519236893,5.49689769569843,92.6049411722327));
#54239=CARTESIAN_POINT('Ctrl Pts',(-3.0614837191883,5.40389634496153,92.8833650258799));
#54240=CARTESIAN_POINT('Ctrl Pts',(-6.20122828689443,0.345754253428334,
93.161788879527));
#54241=CARTESIAN_POINT('Ctrl Pts',(-3.64323750870601,-5.03006945529593,
93.4402127331742));
#54242=CARTESIAN_POINT('Ctrl Pts',(2.26218738519033,-5.78422739043248,93.7186365868212));
#54243=CARTESIAN_POINT('Ctrl Pts',(6.08909743858714,-1.22379355012835,93.9970604404684));
#54244=CARTESIAN_POINT('Ctrl Pts',(4.32129881567914,4.46107103906154,94.2754842941155));
#54245=CARTESIAN_POINT('Ctrl Pts',(-1.41694176859032,6.04706989329276,94.5539081477627));
#54246=CARTESIAN_POINT('Ctrl Pts',(-5.85328556331033,2.07697529698528,94.8323320014097));
#54247=CARTESIAN_POINT('Ctrl Pts',(-4.91158641222056,-3.80145987552598,
95.110755855057));
#54248=CARTESIAN_POINT('Ctrl Pts',(0.542915398379021,-6.18708502771268,
95.389179708704));
#54249=CARTESIAN_POINT('Ctrl Pts',(5.49858244398346,-2.88796976726925,95.6676035623512));
#54250=CARTESIAN_POINT('Ctrl Pts',(5.40211044648703,3.06463390862584,95.9460274159983));
#54251=CARTESIAN_POINT('Ctrl Pts',(0.342138605189483,6.20142882284257,96.2244512696454));
#54252=CARTESIAN_POINT('Ctrl Pts',(-5.03219276841277,3.64030413722229,96.5028751232926));
#54253=CARTESIAN_POINT('Ctrl Pts',(-5.78290745231255,-2.26555946025075,
96.7812989769397));
#54254=CARTESIAN_POINT('Ctrl Pts',(-1.2202431298768,-6.0898099292123,97.0597228305868));
#54255=CARTESIAN_POINT('Ctrl Pts',(4.4635897885253,-4.31869708010603,97.3381466842341));
#54256=CARTESIAN_POINT('Ctrl Pts',(6.04624272595434,1.42046723608385,97.6165705378809));
#54257=CARTESIAN_POINT('Ctrl Pts',(2.07356222043732,5.85449553658713,97.8949943915284));
#54258=CARTESIAN_POINT('Ctrl Pts',(-3.80432290079535,4.90936915870336,98.1734182451752));
#54259=CARTESIAN_POINT('Ctrl Pts',(-6.18676743248101,-0.546522649426795,
98.4518420988226));
#54260=CARTESIAN_POINT('Ctrl Pts',(-2.88476336043193,-5.50026532307788,
98.7302659524695));
#54261=CARTESIAN_POINT('Ctrl Pts',(3.06778305627027,-5.40032271161683,99.0086898061168));
#54262=CARTESIAN_POINT('Ctrl Pts',(6.20162725067434,-0.338522840644003,
99.2871136597637));
#54263=CARTESIAN_POINT('Ctrl Pts',(3.637369528252,5.03431437088382,99.5655375134111));
#54264=CARTESIAN_POINT('Ctrl Pts',(-2.2689307651559,5.78158554834853,99.8439613670581));
#54265=CARTESIAN_POINT('Ctrl Pts',(-6.09052034966483,1.21669229481527,100.122385220705));
#54266=CARTESIAN_POINT('Ctrl Pts',(-4.31609387643315,-4.4661070206344,100.400809074352));
#54267=CARTESIAN_POINT('Ctrl Pts',(1.42399222070312,-6.04541350325356,100.679232928));
#54268=CARTESIAN_POINT('Ctrl Pts',(5.85570351968426,-2.07014843900163,100.957656781647));
#54269=CARTESIAN_POINT('Ctrl Pts',(4.90715023629299,3.80718463282164,101.236080635294));
#54270=CARTESIAN_POINT('Ctrl Pts',(-0.550129714689517,6.18644773411688,
101.514504488941));
#54271=CARTESIAN_POINT('Ctrl Pts',(-5.50194633240983,2.88155597294684,101.792928342588));
#54272=CARTESIAN_POINT('Ctrl Pts',(-5.39853314095852,-3.07093116105133,
102.071352196235));
#54273=CARTESIAN_POINT('Ctrl Pts',(-0.334906961020913,-6.20182357032214,
102.349776049882));
#54274=CARTESIAN_POINT('Ctrl Pts',(5.03643426198777,-3.63443368279287,102.628199903529));
#54275=CARTESIAN_POINT('Ctrl Pts',(5.78026167898992,2.27230129875968,102.906623757177));
#54276=CARTESIAN_POINT('Ctrl Pts',(1.21314104615092,6.09122869970316,103.185047610824));
#54277=CARTESIAN_POINT('Ctrl Pts',(-4.46862273453304,4.31348920554555,103.463471464471));
#54278=CARTESIAN_POINT('Ctrl Pts',(-6.04458222547238,-1.42751672124976,
103.741895318118));
#54279=CARTESIAN_POINT('Ctrl Pts',(-2.06673395383878,-5.85690951219101,
104.020319171765));
#54280=CARTESIAN_POINT('Ctrl Pts',(3.81004507063194,-4.90492964574384,104.298743025412));
#54281=CARTESIAN_POINT('Ctrl Pts',(6.18612593272902,0.553736592940906,104.577166879059));
#54282=CARTESIAN_POINT('Ctrl Pts',(2.87834760590436,5.50362547140775,104.855590732706));
#54283=CARTESIAN_POINT('Ctrl Pts',(-3.07407822189872,5.39674173512051,105.134014586354));
#54284=CARTESIAN_POINT('Ctrl Pts',(-6.20201778171941,0.3312909675493,105.412438440001));
#54285=CARTESIAN_POINT('Ctrl Pts',(-3.63149660184265,-5.03855244100415,
105.690862293648));
#54286=CARTESIAN_POINT('Ctrl Pts',(2.27567105991644,-5.77893584468655,105.969286147295));
#54287=CARTESIAN_POINT('Ctrl Pts',(6.09193497908663,-1.20958938509078,106.247710000942));
#54288=CARTESIAN_POINT('Ctrl Pts',(4.31088306832845,4.47113692936624,106.526133854589));
#54289=CARTESIAN_POINT('Ctrl Pts',(-1.43104073652573,6.04374889289317,106.804557708236));
#54290=CARTESIAN_POINT('Ctrl Pts',(-5.85811351369734,2.06331876610964,107.082981561883));
#54291=CARTESIAN_POINT('Ctrl Pts',(-4.90270738781089,-3.81290421325383,
107.361405415531));
#54292=CARTESIAN_POINT('Ctrl Pts',(0.557343282954733,-6.18580202842678,
107.639829269178));
#54293=CARTESIAN_POINT('Ctrl Pts',(5.50530273950077,-2.87513826039528,107.918253122825));
#54294=CARTESIAN_POINT('Ctrl Pts',(5.39494849471189,3.07722423774255,108.196676976472));
#54295=CARTESIAN_POINT('Ctrl Pts',(0.327674861458482,6.20220988480007,108.475100830119));
#54296=CARTESIAN_POINT('Ctrl Pts',(-5.04066890721283,3.6285582863999,108.753524683766));
#54297=CARTESIAN_POINT('Ctrl Pts',(-5.77760804588923,-2.27904004748059,
109.031948537413));
#54298=CARTESIAN_POINT('Ctrl Pts',(-1.20603731284231,-6.0926391875751,109.310372391061));
#54299=CARTESIAN_POINT('Ctrl Pts',(4.47364960427921,-4.3082754656679,109.588796244708));
#54300=CARTESIAN_POINT('Ctrl Pts',(6.04291350579938,1.4345642653332,109.867220098355));
#54301=CARTESIAN_POINT('Ctrl Pts',(2.05990287697488,5.85931552379407,110.145643952002));
#54302=CARTESIAN_POINT('Ctrl Pts',(-3.81576205971545,4.90048346324935,110.424067805649));
#54303=CARTESIAN_POINT('Ctrl Pts',(-6.18547602132036,-0.560949783505152,
110.702491659296));
#54304=CARTESIAN_POINT('Ctrl Pts',(-2.87192793751032,-5.50697813611887,
110.980915512943));
#54305=CARTESIAN_POINT('Ctrl Pts',(3.08036920751339,-5.39315342034202,111.259339366591));
#54306=CARTESIAN_POINT('Ctrl Pts',(6.2023998794988,-0.324058643977884,111.537763220238));
#54307=CARTESIAN_POINT('Ctrl Pts',(3.62561873746359,5.04278365989433,111.816187073885));
#54308=CARTESIAN_POINT('Ctrl Pts',(-2.28240826030677,5.7762782830493,112.094610927532));
#54309=CARTESIAN_POINT('Ctrl Pts',(-6.09334132492911,1.20248483061314,112.373034781179));
#54310=CARTESIAN_POINT('Ctrl Pts',(-4.30566639845044,-4.47616075841778,
112.651458634826));
#54311=CARTESIAN_POINT('Ctrl Pts',(1.43808730647429,-6.04207606447495,112.929882488473));
#54312=CARTESIAN_POINT('Ctrl Pts',(5.86051554207254,-2.05648628759585,113.20830634212));
#54313=CARTESIAN_POINT('Ctrl Pts',(4.89825787281534,3.81861860904526,113.486730195767));
#54314=CARTESIAN_POINT('Ctrl Pts',(-0.564556093366052,6.18514791152054,
113.765154049415));
#54315=CARTESIAN_POINT('Ctrl Pts',(-5.50865166069243,2.86871663834093,114.043577903062));
#54316=CARTESIAN_POINT('Ctrl Pts',(-5.39135651262125,-3.0835131301423,114.322001756709));
#54317=CARTESIAN_POINT('Ctrl Pts',(-0.320442316336498,-6.20258776575104,
114.600425610356));
#54318=CARTESIAN_POINT('Ctrl Pts',(5.04489669832976,-3.62267795603275,114.878849464003));
#54319=CARTESIAN_POINT('Ctrl Pts',(5.77494655661886,2.2857756972502,115.15727331765));
#54320=CARTESIAN_POINT('Ctrl Pts',(1.19893193961059,6.09404139091007,115.435697171297));
#54321=CARTESIAN_POINT('Ctrl Pts',(-4.47867039092821,4.30305586756279,115.714121024945));
#54322=CARTESIAN_POINT('Ctrl Pts',(-6.0412365692046,-1.4416098587512,115.992544878592));
#54323=CARTESIAN_POINT('Ctrl Pts',(-2.05306899913409,-5.86171356812484,
116.270968732239));
#54324=CARTESIAN_POINT('Ctrl Pts',(3.82147386027209,-4.89603061726545,116.549392585886));
#54325=CARTESIAN_POINT('Ctrl Pts',(6.18481769913886,0.568162211311366,116.827816439533));
#54326=CARTESIAN_POINT('Ctrl Pts',(2.8655043639789,5.51032331265255,117.10624029318));
#54327=CARTESIAN_POINT('Ctrl Pts',(-3.08665600456044,5.3895577721604,117.384664146827));
#54328=CARTESIAN_POINT('Ctrl Pts',(-6.20277354349289,0.316825879763828,
117.663088000474));
#54329=CARTESIAN_POINT('Ctrl Pts',(-3.61973594310723,-5.04700802180085,
117.941511854122));
#54330=CARTESIAN_POINT('Ctrl Pts',(2.28914235716608,-5.77361286705054,118.219935707769));
#54331=CARTESIAN_POINT('Ctrl Pts',(6.0947393852799,-1.19537864104265,118.498359561416));
#54332=CARTESIAN_POINT('Ctrl Pts',(4.30044387389252,4.48117850095767,118.776783415063));
#54333=CARTESIAN_POINT('Ctrl Pts',(-1.44513192096696,6.0403950202735,119.05520726871));
#54334=CARTESIAN_POINT('Ctrl Pts',(-5.86290960154331,2.04965101275129,119.333631122357));
#54335=CARTESIAN_POINT('Ctrl Pts',(-4.89380169735742,-3.824327812426,119.612054976004));
#54336=CARTESIAN_POINT('Ctrl Pts',(0.571768136116752,-6.18448538428672,
119.890478829651));
#54337=CARTESIAN_POINT('Ctrl Pts',(5.51199309142856,-2.8622911155176,120.168902683299));
#54338=CARTESIAN_POINT('Ctrl Pts',(5.38775719957539,3.08979782970226,120.447326536946));
#54339=CARTESIAN_POINT('Ctrl Pts',(0.31320933548108,6.20295721265561,120.725750390593));
#54340=CARTESIAN_POINT('Ctrl Pts',(-5.04911762957415,3.61679269969782,121.00417424424));
#54341=CARTESIAN_POINT('Ctrl Pts',(-5.77227721482724,-2.29250823892995,
121.282598097887));
#54342=CARTESIAN_POINT('Ctrl Pts',(-1.19182493606175,-6.09543530776335,
121.561021951534));
#54343=CARTESIAN_POINT('Ctrl Pts',(4.48368508754851,-4.29783041839939,121.839445805182));
#54344=CARTESIAN_POINT('Ctrl Pts',(6.03955141816593,1.44865349205967,122.117869658828));
#54345=CARTESIAN_POINT('Ctrl Pts',(2.04623232923532,5.86410364166548,122.396293512476));
#54346=CARTESIAN_POINT('Ctrl Pts',(-3.82718046383023,4.89157111433223,122.674717366123));
#54347=CARTESIAN_POINT('Ctrl Pts',(-6.18415096841107,-0.575373867468753,
122.95314121977));
#54348=CARTESIAN_POINT('Ctrl Pts',(-2.85907689153052,-5.51366099473004,
123.231565073417));
#54349=CARTESIAN_POINT('Ctrl Pts',(3.09293859974396,-5.38595479873152,123.509988927064));
#54350=CARTESIAN_POINT('Ctrl Pts',(6.203138782157,-0.309592678574449,123.788412780711));
#54351=CARTESIAN_POINT('Ctrl Pts',(3.61384820984823,5.0512255093335,124.066836634358));
#54352=CARTESIAN_POINT('Ctrl Pts',(-2.29587330938013,5.77093962230462,124.345260488006));
#54353=CARTESIAN_POINT('Ctrl Pts',(-6.09612921857968,1.18827078452085,124.623684341653));
#54354=CARTESIAN_POINT('Ctrl Pts',(-4.29521538781869,-4.48619007176196,
124.9021081953));
#54355=CARTESIAN_POINT('Ctrl Pts',(1.45217435528767,-6.03870591061202,125.180532048947));
#54356=CARTESIAN_POINT('Ctrl Pts',(5.86529609507713,-2.04281267134551,125.458955902594));
#54357=CARTESIAN_POINT('Ctrl Pts',(4.88933810046496,3.83003128783364,125.737379756241));
#54358=CARTESIAN_POINT('Ctrl Pts',(-0.578977953088837,6.18381544421881,
126.015803609888));
#54359=CARTESIAN_POINT('Ctrl Pts',(-5.51532976187251,2.85585981889264,126.294227463536));
#54360=CARTESIAN_POINT('Ctrl Pts',(-5.384145396786,-3.09607477471346,126.572651317182));
#54361=CARTESIAN_POINT('Ctrl Pts',(-0.305985678809838,-6.20332493410653,
126.85107517083));
#54362=CARTESIAN_POINT('Ctrl Pts',(5.05335010534642,-3.6108898572602,127.129499024477));
#54363=CARTESIAN_POINT('Ctrl Pts',(5.76956526204834,2.29921374333548,127.407922878124));
#54364=CARTESIAN_POINT('Ctrl Pts',(1.18478194982891,6.09686610220261,127.686346731771));
#54365=CARTESIAN_POINT('Ctrl Pts',(-4.4888176256727,4.29251384208693,127.964770585418));
#54366=CARTESIAN_POINT('Ctrl Pts',(-6.03762402993717,-1.45553411816505,
128.243194439065));
#54367=CARTESIAN_POINT('Ctrl Pts',(-2.03983479797794,-5.86678985768713,
128.521618292712));
#54368=CARTESIAN_POINT('Ctrl Pts',(3.8337165824916,-4.88653035923571,128.80004214636));
#54369=CARTESIAN_POINT('Ctrl Pts',(6.1818974004875,0.58149677391166,129.078466000007));
#54370=CARTESIAN_POINT('Ctrl Pts',(2.85564479853464,5.51907004802257,129.356889853654));
#54371=CARTESIAN_POINT('Ctrl Pts',(-3.1050343009106,5.37821806774232,129.635313707301));
#54372=CARTESIAN_POINT('Ctrl Pts',(-5.67690060144359,1.15622068272167,129.86733358534));
#54373=CARTESIAN_POINT('Ctrl Pts',(-4.91510296356909,-2.38887809660516,
130.052949487772));
#54374=CARTESIAN_POINT('Ctrl Pts',(-3.76253054062033,-3.76598540426341,
130.145757438987));
#54375=CARTESIAN_POINT('Ctrl Pts',(-3.05041111877786,-4.27420965560272,
130.192161414595));
#54376=CARTESIAN_POINT('Ctrl Pts',(-3.96383248548561,-3.93295783950028,
-9.66287555531569));
#54377=CARTESIAN_POINT('Ctrl Pts',(-3.30856849787929,-4.59336580384622,
-9.61647157970784));
#54378=CARTESIAN_POINT('Ctrl Pts',(-1.66601391597817,-5.567339035329,-9.52366362849213));
#54379=CARTESIAN_POINT('Ctrl Pts',(2.18501855494821,-5.7601574796524,-9.3380477260607));
#54380=CARTESIAN_POINT('Ctrl Pts',(6.17595083223459,-2.33837851004803,-9.10602784802143));
#54381=CARTESIAN_POINT('Ctrl Pts',(5.30367297041469,3.9415905605293,-8.82760399437431));
#54382=CARTESIAN_POINT('Ctrl Pts',(-0.447670556531286,6.58755408496995,
-8.54918014072716));
#54383=CARTESIAN_POINT('Ctrl Pts',(-5.7846197819851,3.18729356865408,-8.27075628708006));
#54384=CARTESIAN_POINT('Ctrl Pts',(-5.80822952673516,-3.14488847180297,
-7.9923324334329));
#54385=CARTESIAN_POINT('Ctrl Pts',(-0.494341668036604,-6.58571795329654,
-7.71390857978579));
#54386=CARTESIAN_POINT('Ctrl Pts',(5.27329977167003,-3.97649595721956,-7.43548472613864));
#54387=CARTESIAN_POINT('Ctrl Pts',(6.19603255906839,2.28686674054138,-7.15706087249153));
#54388=CARTESIAN_POINT('Ctrl Pts',(1.42567731735158,6.44877093303202,-6.87863701884439));
#54389=CARTESIAN_POINT('Ctrl Pts',(-4.65453397724029,4.68563770779713,-6.60021316519726));
#54390=CARTESIAN_POINT('Ctrl Pts',(-6.45815982591155,-1.38276999509599,
-6.32178931155014));
#54391=CARTESIAN_POINT('Ctrl Pts',(-2.32796089266521,-6.18063836937714,
-6.043365457903));
#54392=CARTESIAN_POINT('Ctrl Pts',(3.94117612000835,-5.29971065946422,-5.76494160425588));
#54393=CARTESIAN_POINT('Ctrl Pts',(6.58913604537669,0.450642366606509,-5.48651775060875));
#54394=CARTESIAN_POINT('Ctrl Pts',(3.18294525663012,5.78693587022664,-5.20809389696161));
#54395=CARTESIAN_POINT('Ctrl Pts',(-3.14775817423433,5.80615215953137,-4.92967004331449));
#54396=CARTESIAN_POINT('Ctrl Pts',(-6.58627842414191,0.490630370955284,
-4.65124618966736));
#54397=CARTESIAN_POINT('Ctrl Pts',(-3.9732759415693,-5.27568542617564,-4.37282233602023));
#54398=CARTESIAN_POINT('Ctrl Pts',(2.29040223968931,-6.19466210755678,-4.0943984823731));
#54399=CARTESIAN_POINT('Ctrl Pts',(6.4496416755637,-1.42193625171373,-3.81597462872597));
#54400=CARTESIAN_POINT('Ctrl Pts',(4.68290160783284,4.65727523193867,-3.53755077507883));
#54401=CARTESIAN_POINT('Ctrl Pts',(-1.38652376279582,6.45734715674067,-3.25912692143171));
#54402=CARTESIAN_POINT('Ctrl Pts',(-6.1820006544225,2.32435974869207,-2.98070306778457));
#54403=CARTESIAN_POINT('Ctrl Pts',(-5.29740868481312,-3.94426691722004,
-2.70227921413745));
#54404=CARTESIAN_POINT('Ctrl Pts',(0.454482355020498,-6.58887138551255,
-2.42385536049032));
#54405=CARTESIAN_POINT('Ctrl Pts',(5.78879157999998,-3.17957109821796,-2.14543150684319));
#54406=CARTESIAN_POINT('Ctrl Pts',(5.80431541636219,3.15114310501463,-1.86700765319606));
#54407=CARTESIAN_POINT('Ctrl Pts',(0.486790448190714,6.58656324563387,-1.58858379954893));
#54408=CARTESIAN_POINT('Ctrl Pts',(-5.27800125759252,3.97019937163456,-1.3101599459018));
#54409=CARTESIAN_POINT('Ctrl Pts',(-6.19332557868541,-2.29401364463305,
-1.03173609225467));
#54410=CARTESIAN_POINT('Ctrl Pts',(-1.41817562192872,-6.45046961328342,
-0.753312238607539));
#54411=CARTESIAN_POINT('Ctrl Pts',(4.66000479819239,-4.68018542440052,-0.474888384960414));
#54412=CARTESIAN_POINT('Ctrl Pts',(6.4565376442355,1.39028845011451,-0.196464531313281));
#54413=CARTESIAN_POINT('Ctrl Pts',(2.32075498025171,6.18335480526133,0.0819593223338455));
#54414=CARTESIAN_POINT('Ctrl Pts',(-3.94735487254703,5.29510810429758,0.360383175980979));
#54415=CARTESIAN_POINT('Ctrl Pts',(-6.58860528079665,-0.458323880989896,
0.638807029628107));
#54416=CARTESIAN_POINT('Ctrl Pts',(-3.17619543792065,-5.79064442581137,
0.917230883275238));
#54417=CARTESIAN_POINT('Ctrl Pts',(3.15452674161993,-5.80247717465899,1.19565473692237));
#54418=CARTESIAN_POINT('Ctrl Pts',(6.58684594617458,-0.482950108602965,
1.4740785905695));
#54419=CARTESIAN_POINT('Ctrl Pts',(3.96712138952872,5.28031516169088,1.75250244421663));
#54420=CARTESIAN_POINT('Ctrl Pts',(-2.29762423662747,6.19198701494913,2.03092629786376));
#54421=CARTESIAN_POINT('Ctrl Pts',(-6.45129537576889,1.41441447271307,2.30935015151089));
#54422=CARTESIAN_POINT('Ctrl Pts',(-4.67746764069405,-4.66273276054907,
2.58777400515801));
#54423=CARTESIAN_POINT('Ctrl Pts',(1.39405265989795,-6.45572594736398,2.86619785880515));
#54424=CARTESIAN_POINT('Ctrl Pts',(6.18470685673347,-2.31714941734695,3.14462171245227));
#54425=CARTESIAN_POINT('Ctrl Pts',(5.29280572238075,3.95044148307134,3.42304556609941));
#54426=CARTESIAN_POINT('Ctrl Pts',(-0.462165250425673,6.58833693790293,
3.70146941974653));
#54427=CARTESIAN_POINT('Ctrl Pts',(-5.79249530353563,3.17281869708231,3.97989327339367));
#54428=CARTESIAN_POINT('Ctrl Pts',(-5.80063696025417,-3.15790930543777,
4.25831712704079));
#54429=CARTESIAN_POINT('Ctrl Pts',(-0.479109604949533,-6.5871264078111,
4.53674098068793));
#54430=CARTESIAN_POINT('Ctrl Pts',(5.28262727085413,-3.96404205871552,4.81516483433505));
#54431=CARTESIAN_POINT('Ctrl Pts',(6.19064634627567,2.30123404750168,5.09358868798219));
#54432=CARTESIAN_POINT('Ctrl Pts',(1.41065284269685,6.45211894523253,5.3720125416293));
#54433=CARTESIAN_POINT('Ctrl Pts',(-4.66545913786288,4.67474826690904,5.65043639527645));
#54434=CARTESIAN_POINT('Ctrl Pts',(-6.45491205592566,-1.39781639577693,
5.92886024892357));
#54435=CARTESIAN_POINT('Ctrl Pts',(-2.31354306675181,-6.18605680577878,
6.20728410257071));
#54436=CARTESIAN_POINT('Ctrl Pts',(3.95352675068213,-5.29050154122254,6.48570795621782));
#54437=CARTESIAN_POINT('Ctrl Pts',(6.58806635536644,0.466006462751344,6.76413180986496));
#54438=CARTESIAN_POINT('Ctrl Pts',(3.16944087767492,5.79434421215727,7.04255566351209));
#54439=CARTESIAN_POINT('Ctrl Pts',(-3.1612907957547,5.79879477397794,7.32097951715922));
#54440=CARTESIAN_POINT('Ctrl Pts',(-6.58740463021691,0.47526893842755,7.59940337080635));
#54441=CARTESIAN_POINT('Ctrl Pts',(-3.96096138036421,-5.28493758423886,
7.87782722445348));
#54442=CARTESIAN_POINT('Ctrl Pts',(2.30484307609341,-6.18930357315113,8.1562510781006));
#54443=CARTESIAN_POINT('Ctrl Pts',(6.45294032136004,-1.40689073314278,8.43467493174774));
#54444=CARTESIAN_POINT('Ctrl Pts',(4.6720273039881,4.66818392919851,8.71309878539486));
#54445=CARTESIAN_POINT('Ctrl Pts',(-1.40157965648158,6.45409597020173,8.991522639042));
#54446=CARTESIAN_POINT('Ctrl Pts',(-6.18740465193323,2.30993592968984,9.26994649268913));
#54447=CARTESIAN_POINT('Ctrl Pts',(-5.28819556160898,-3.95661067432928,
9.54837034633626));
#54448=CARTESIAN_POINT('Ctrl Pts',(0.469847516662575,-6.58779353327983,
9.82679419998338));
#54449=CARTESIAN_POINT('Ctrl Pts',(5.79619115104702,-3.16606198084645,10.1052180536305));
#54450=CARTESIAN_POINT('Ctrl Pts',(5.79695061645688,3.16467121142106,10.3836419072777));
#54451=CARTESIAN_POINT('Ctrl Pts',(0.471428110342511,6.58768061329754,10.6620657609248));
#54452=CARTESIAN_POINT('Ctrl Pts',(-5.28724610105964,3.95787935552199,10.9404896145719));
#54453=CARTESIAN_POINT('Ctrl Pts',(-6.18795869603207,-2.30845132117582,
11.218913468219));
#54454=CARTESIAN_POINT('Ctrl Pts',(-1.4031281453296,-6.45375950387221,11.4973373218662));
#54455=CARTESIAN_POINT('Ctrl Pts',(4.67090713362965,-4.66930475285615,11.7757611755133));
#54456=CARTESIAN_POINT('Ctrl Pts',(6.45327769046963,1.40534244073263,12.0541850291604));
#54457=CARTESIAN_POINT('Ctrl Pts',(2.30632800738723,6.1887503947387,12.3326088828076));
#54458=CARTESIAN_POINT('Ctrl Pts',(-3.95969325296453,5.28588778432387,12.6110327364547));
#54459=CARTESIAN_POINT('Ctrl Pts',(-6.58751847173579,-0.473688410853622,
12.8894565901018));
#54460=CARTESIAN_POINT('Ctrl Pts',(-3.16268200774551,-5.79803611957706,
13.1678804437489));
#54461=CARTESIAN_POINT('Ctrl Pts',(3.16805055128777,-5.79510448831792,13.4463042973961));
#54462=CARTESIAN_POINT('Ctrl Pts',(6.58795435695914,-0.467587121999925,
13.7247281510432));
#54463=CARTESIAN_POINT('Ctrl Pts',(3.95479598523653,5.28955282053166,14.0031520046903));
#54464=CARTESIAN_POINT('Ctrl Pts',(-2.31205878152226,6.18661171537565,14.2815758583375));
#54465=CARTESIAN_POINT('Ctrl Pts',(-6.45457649249062,1.39936508053644,14.5599997119846));
#54466=CARTESIAN_POINT('Ctrl Pts',(-4.66658061443868,-4.67362875023062,
14.8384235656317));
#54467=CARTESIAN_POINT('Ctrl Pts',(1.40910474725094,-6.45245721700749,15.1168474192789));
#54468=CARTESIAN_POINT('Ctrl Pts',(6.19009403373768,-2.30271930107051,15.3952712729259));
#54469=CARTESIAN_POINT('Ctrl Pts',(5.28357821015179,3.96277448553996,15.6736951265731));
#54470=CARTESIAN_POINT('Ctrl Pts',(-0.477529144018868,6.58724117082786,
15.9521189802202));
#54471=CARTESIAN_POINT('Ctrl Pts',(-5.79987911712016,3.15930095952108,16.2305428338674));
#54472=CARTESIAN_POINT('Ctrl Pts',(-5.79325639018865,-3.17142881420597,
16.5089666875145));
#54473=CARTESIAN_POINT('Ctrl Pts',(-0.463745974705563,-6.58822586110871,
16.7873905411617));
#54474=CARTESIAN_POINT('Ctrl Pts',(5.2918577418708,-3.95171127055596,17.0658143948087));
#54475=CARTESIAN_POINT('Ctrl Pts',(6.18526263163975,2.31566545590642,17.3442382484559));
#54476=CARTESIAN_POINT('Ctrl Pts',(1.39560154004253,6.45539128693748,17.622662102103));
#54477=CARTESIAN_POINT('Ctrl Pts',(-4.67634877807622,4.6638548896618,17.9010859557501));
#54478=CARTESIAN_POINT('Ctrl Pts',(-6.45163455009424,-1.41286657475762,
18.1795098093973));
#54479=CARTESIAN_POINT('Ctrl Pts',(-2.29910981196639,-6.19143556847337,
18.4579336630444));
#54480=CARTESIAN_POINT('Ctrl Pts',(3.96585437100808,-5.28126683987788,18.7363575166915));
#54481=CARTESIAN_POINT('Ctrl Pts',(6.58696163065034,0.481369714852657,19.0147813703387));
#54482=CARTESIAN_POINT('Ctrl Pts',(3.15591883732246,5.80172014304984,19.2932052239858));
#54483=CARTESIAN_POINT('Ctrl Pts',(-3.17480599902726,5.79140632269727,19.5716290776329));
#54484=CARTESIAN_POINT('Ctrl Pts',(-6.58849512565393,0.459904669765239,
19.85005293128));
#54485=CARTESIAN_POINT('Ctrl Pts',(-3.94862521252898,-5.29416086429357,
20.1284767849272));
#54486=CARTESIAN_POINT('Ctrl Pts',(2.3192713431023,-6.18391144528296,20.4069006385743));
#54487=CARTESIAN_POINT('Ctrl Pts',(6.45620388693581,-1.39183752512723,20.6853244922214));
#54488=CARTESIAN_POINT('Ctrl Pts',(4.6611275794521,4.67906721624177,20.9637483458686));
#54489=CARTESIAN_POINT('Ctrl Pts',(-1.41662792197383,6.45080969000957,21.2421721995157));
#54490=CARTESIAN_POINT('Ctrl Pts',(-6.19277499848978,2.29549954130184,21.5205960531628));
#54491=CARTESIAN_POINT('Ctrl Pts',(-5.27895367428779,-3.96893290832191,
21.79901990681));
#54492=CARTESIAN_POINT('Ctrl Pts',(0.48521012204937,-6.58667985129825,22.0774437604571));
#54493=CARTESIAN_POINT('Ctrl Pts',(5.80355919674031,-3.15253564229943,22.3558676141042));
#54494=CARTESIAN_POINT('Ctrl Pts',(5.78955428647267,3.17818210460365,22.6342914677513));
#54495=CARTESIAN_POINT('Ctrl Pts',(0.456063208484729,6.58876215050323,22.9127153213985));
#54496=CARTESIAN_POINT('Ctrl Pts',(-5.29646218701701,3.94553781220464,23.1911391750456));
#54497=CARTESIAN_POINT('Ctrl Pts',(-6.18255815676466,-2.32287644188415,
23.4695630286927));
#54498=CARTESIAN_POINT('Ctrl Pts',(-1.38807303706995,-6.4570142922094,23.7479868823399));
#54499=CARTESIAN_POINT('Ctrl Pts',(4.68178406380318,-4.65839868473658,24.026410735987));
#54500=CARTESIAN_POINT('Ctrl Pts',(6.44998263703386,1.42038878762094,24.3048345896342));
#54501=CARTESIAN_POINT('Ctrl Pts',(2.29188849030413,6.19411232333165,24.5832584432812));
#54502=CARTESIAN_POINT('Ctrl Pts',(-3.9720100964351,5.27663871416782,24.8616822969284));
#54503=CARTESIAN_POINT('Ctrl Pts',(-6.58639583286728,-0.489050364303604,
25.1401061505755));
#54504=CARTESIAN_POINT('Ctrl Pts',(-3.14915137560207,-5.80539627756634,
25.4185300042227));
#54505=CARTESIAN_POINT('Ctrl Pts',(3.18155712978754,-5.78770028214451,25.6969538578698));
#54506=CARTESIAN_POINT('Ctrl Pts',(6.58902693556586,-0.452221592169745,
25.9753777115169));
#54507=CARTESIAN_POINT('Ctrl Pts',(3.94244907063243,5.29876170925873,26.2538015651641));
#54508=CARTESIAN_POINT('Ctrl Pts',(-2.32648075102626,6.18120276654486,26.5322254188111));
#54509=CARTESIAN_POINT('Ctrl Pts',(-6.45782250248278,1.38430807715065,26.8106492724583));
#54510=CARTESIAN_POINT('Ctrl Pts',(-4.65566820644302,-4.68449931983693,
27.0890731261054));
#54511=CARTESIAN_POINT('Ctrl Pts',(1.42414917042049,-6.44915339144822,27.3674969797525));
#54512=CARTESIAN_POINT('Ctrl Pts',(6.19544754254423,-2.28827666020089,27.6459208333997));
#54513=CARTESIAN_POINT('Ctrl Pts',(5.27432196030506,3.97508593430139,27.9243446870468));
#54514=CARTESIAN_POINT('Ctrl Pts',(-0.49289044030986,6.5861095754541,28.202768540694));
#54515=CARTESIAN_POINT('Ctrl Pts',(-5.80723138490337,3.14576603838083,28.481192394341));
#54516=CARTESIAN_POINT('Ctrl Pts',(-5.78584431034302,-3.18493107343138,
28.7596162479882));
#54517=CARTESIAN_POINT('Ctrl Pts',(-0.448379822126494,-6.58928948075187,
29.0380401016353));
#54518=CARTESIAN_POINT('Ctrl Pts',(5.30105943023716,-3.93935898886236,29.3164639552825));
#54519=CARTESIAN_POINT('Ctrl Pts',(6.17984527508429,2.33008426930356,29.5948878089296));
#54520=CARTESIAN_POINT('Ctrl Pts',(1.380542646649,6.45862851748116,29.8733116625768));
#54521=CARTESIAN_POINT('Ctrl Pts',(-4.68721298341994,4.65293614549958,30.1517355162238));
#54522=CARTESIAN_POINT('Ctrl Pts',(-6.44832195353458,-1.42790906909408,
30.430159369871));
#54523=CARTESIAN_POINT('Ctrl Pts',(-2.28466405221999,-6.19678065567362,
30.7085832235181));
#54524=CARTESIAN_POINT('Ctrl Pts',(3.97816042087516,-5.27200341348711,30.9870070771652));
#54525=CARTESIAN_POINT('Ctrl Pts',(6.58582107915601,0.496730348762664,31.2654309308124));
#54526=CARTESIAN_POINT('Ctrl Pts',(3.14237963178648,5.80906451812772,31.5438547844595));
#54527=CARTESIAN_POINT('Ctrl Pts',(-3.18830393438844,5.78398637169907,31.8222786381066));
#54528=CARTESIAN_POINT('Ctrl Pts',(-6.58954978597194,0.44453789966075,32.1007024917539));
#54529=CARTESIAN_POINT('Ctrl Pts',(-3.93626756794489,-5.30335534917115,
32.3791263454008));
#54530=CARTESIAN_POINT('Ctrl Pts',(2.33368699549094,-6.17848568284443,32.6575501990481));
#54531=CARTESIAN_POINT('Ctrl Pts',(6.4594323369305,-1.3767767468452,32.9359740526951));
#54532=CARTESIAN_POINT('Ctrl Pts',(4.65020250283515,4.68992505362966,33.2143979063423));
#54533=CARTESIAN_POINT('Ctrl Pts',(-1.43166848236366,6.44748832357563,33.4928217599894));
#54534=CARTESIAN_POINT('Ctrl Pts',(-6.19811166226677,2.28105066758929,33.7712456136365));
#54535=CARTESIAN_POINT('Ctrl Pts',(-5.26968307450193,-3.98123355511144,
34.0496694672837));
#54536=CARTESIAN_POINT('Ctrl Pts',(0.500570088356797,-6.58553034407101,
34.3280933209308));
#54537=CARTESIAN_POINT('Ctrl Pts',(5.81089567661615,-3.13899215697025,34.6065171745779));
#54538=CARTESIAN_POINT('Ctrl Pts',(5.78212646684429,3.19167571151203,34.8849410282251));
#54539=CARTESIAN_POINT('Ctrl Pts',(0.440695826078731,6.58980785113753,35.1633648818722));
#54540=CARTESIAN_POINT('Ctrl Pts',(-5.30564946528016,3.93317480893105,35.4417887355193));
#54541=CARTESIAN_POINT('Ctrl Pts',(-6.17712399028752,-2.33728892836378,
35.7202125891665));
#54542=CARTESIAN_POINT('Ctrl Pts',(-1.3730103790192,-6.46023396055767,35.9986364428136));
#54543=CARTESIAN_POINT('Ctrl Pts',(4.6926355295443,-4.64746727937873,36.2770602964607));
#54544=CARTESIAN_POINT('Ctrl Pts',(6.44665250185466,1.43542740895129,36.5554841501079));
#54545=CARTESIAN_POINT('Ctrl Pts',(2.27743650753725,6.19944056187117,36.833908003755));
#54546=CARTESIAN_POINT('Ctrl Pts',(-3.9843053359654,5.26736094413842,37.1123318574021));
#54547=CARTESIAN_POINT('Ctrl Pts',(-6.58523737029794,-0.504409657786784,
37.3907557110492));
#54548=CARTESIAN_POINT('Ctrl Pts',(-3.1356036150838,-5.81272485974614,37.6691795646963));
#54549=CARTESIAN_POINT('Ctrl Pts',(3.19504640365602,-5.78026459641099,37.9476034183435));
#54550=CARTESIAN_POINT('Ctrl Pts',(6.59006367616103,-0.436853602686241,
38.2260272719906));
#54551=CARTESIAN_POINT('Ctrl Pts',(3.93008071287194,5.30794177778444,38.5044511256378));
#54552=CARTESIAN_POINT('Ctrl Pts',(-2.34089006669765,6.17576019787637,38.7828749792849));
#54553=CARTESIAN_POINT('Ctrl Pts',(-6.4610333880901,1.36924354445145,39.061298832932));
#54554=CARTESIAN_POINT('Ctrl Pts',(-4.64473047606029,-4.69534441024232,
39.3397226865791));
#54555=CARTESIAN_POINT('Ctrl Pts',(1.43918584757895,-6.44581448865584,39.6181465402263));
#54556=CARTESIAN_POINT('Ctrl Pts',(6.20076735403504,-2.27382157329258,39.8965703938733));
#54557=CARTESIAN_POINT('Ctrl Pts',(5.26503702318596,3.98737576239292,40.1749942475206));
#54558=CARTESIAN_POINT('Ctrl Pts',(-0.508249055747655,6.58494215793644,
40.4534181011676));
#54559=CARTESIAN_POINT('Ctrl Pts',(-5.81455206689598,3.13221400727876,40.7318419548148));
#54560=CARTESIAN_POINT('Ctrl Pts',(-5.77840076103197,-3.19841600967458,
41.0102658084619));
#54561=CARTESIAN_POINT('Ctrl Pts',(-0.433011230789567,-6.59031726095543,
41.2886896621091));
#54562=CARTESIAN_POINT('Ctrl Pts',(5.31023228590465,-3.9269852808195,41.5671135157562));
#54563=CARTESIAN_POINT('Ctrl Pts',(6.17439430607461,2.34449040926819,41.8455373694033));
#54564=CARTESIAN_POINT('Ctrl Pts',(1.36547624442261,6.46183061925605,42.1239612230505));
#54565=CARTESIAN_POINT('Ctrl Pts',(-4.69805169480298,4.6419920938102,42.4023850766975));
#54566=CARTESIAN_POINT('Ctrl Pts',(-6.44497428426404,-1.4429437969693,42.6808089303448));
#54567=CARTESIAN_POINT('Ctrl Pts',(-2.2702058660839,-6.20209203830737,42.9592327839917));
#54568=CARTESIAN_POINT('Ctrl Pts',(3.99044483335022,-5.2627113124345,43.237656637639));
#54569=CARTESIAN_POINT('Ctrl Pts',(6.58464470708685,0.512088280934132,43.516080491286));
#54570=CARTESIAN_POINT('Ctrl Pts',(3.12882333470756,5.8163772974444,43.7945043449333));
#54571=CARTESIAN_POINT('Ctrl Pts',(-3.20178452842208,5.77653496134093,44.0729281985803));
#54572=CARTESIAN_POINT('Ctrl Pts',(-6.59056860543455,0.429168711694992,
44.3513520522275));
#54573=CARTESIAN_POINT('Ctrl Pts',(-3.92388851382601,-5.31252098886223,
44.6297759058746));
#54574=CARTESIAN_POINT('Ctrl Pts',(2.34808995485178,-6.17302631534656,44.9081997595216));
#54575=CARTESIAN_POINT('Ctrl Pts',(6.46262565378449,-1.36170848021304,45.1866236131689));
#54576=CARTESIAN_POINT('Ctrl Pts',(4.63925213355924,4.70075738230592,45.465047466816));
#54577=CARTESIAN_POINT('Ctrl Pts',(-1.4467012558447,6.4441318889649,45.7434713204631));
#54578=CARTESIAN_POINT('Ctrl Pts',(-6.20341461423781,2.26658938714048,46.0218951741103));
#54579=CARTESIAN_POINT('Ctrl Pts',(-5.26038381267472,-3.99351254779384,
46.3003190277573));
#54580=CARTESIAN_POINT('Ctrl Pts',(0.51592733204096,-6.58434501785033,46.5787428814046));
#54581=CARTESIAN_POINT('Ctrl Pts',(5.81820055077105,-3.12543159852284,46.8571667350516));
#54582=CARTESIAN_POINT('Ctrl Pts',(5.77466719797205,3.2051519587537,47.1355905886988));
#54583=CARTESIAN_POINT('Ctrl Pts',(0.425326046708484,6.59081770951289,47.4140144423458));
#54584=CARTESIAN_POINT('Ctrl Pts',(-5.31480788587913,3.92079041294412,47.6924382959931));
#54585=CARTESIAN_POINT('Ctrl Pts',(-6.17165622615728,-2.35168870222466,
47.9708621496401));
#54586=CARTESIAN_POINT('Ctrl Pts',(-1.35794025310373,-6.46341849140512,
48.2492860032874));
#54587=CARTESIAN_POINT('Ctrl Pts',(4.70346147183124,-4.63651059623897,48.5277098569344));
#54588=CARTESIAN_POINT('Ctrl Pts',(6.44328730304483,1.45045822292773,48.8061337105815));
#54589=CARTESIAN_POINT('Ctrl Pts',(2.26297213769171,6.20473508137685,49.0845575642287));
#54590=CARTESIAN_POINT('Ctrl Pts',(-3.9965789046812,5.25805452469773,49.3629814178758));
#54591=CARTESIAN_POINT('Ctrl Pts',(-6.58404309032867,-0.519766207763357,
49.641405271523));
#54592=CARTESIAN_POINT('Ctrl Pts',(-3.12203879987747,-5.82002182625609,
49.91982912517));
#54593=CARTESIAN_POINT('Ctrl Pts',(3.20851829952456,-5.7727974715603,50.1982529788172));
#54594=CARTESIAN_POINT('Ctrl Pts',(6.59106457310578,-0.421483237136511,
50.4766768324643));
#54595=CARTESIAN_POINT('Ctrl Pts',(3.91769097922709,5.31709297617784,50.7551006861114));
#54596=CARTESIAN_POINT('Ctrl Pts',(-2.35528665016334,6.17028403897258,51.0335245397587));
#54597=CARTESIAN_POINT('Ctrl Pts',(-6.46420913184854,1.35417156437564,51.3119483934057));
#54598=CARTESIAN_POINT('Ctrl Pts',(-4.6337674827812,-4.70616396245993,51.5903722470528));
#54599=CARTESIAN_POINT('Ctrl Pts',(1.45421469694148,-6.44244052679083,51.8687961006999));
#54600=CARTESIAN_POINT('Ctrl Pts',(6.20605343927554,-2.25935411896713,52.1472199543472));
#54601=CARTESIAN_POINT('Ctrl Pts',(5.25572344929541,3.99964390296978,52.4256438079942));
#54602=CARTESIAN_POINT('Ctrl Pts',(-0.523604906796155,6.58373892462452,
52.7040676616414));
#54603=CARTESIAN_POINT('Ctrl Pts',(-5.82184112328028,3.11864493992497,52.9824915152884));
#54604=CARTESIAN_POINT('Ctrl Pts',(-5.77092578274138,-3.21188354959022,
53.2609153689357));
#54605=CARTESIAN_POINT('Ctrl Pts',(-0.417640284285345,-6.59130919612937,
53.5393392225827));
#54606=CARTESIAN_POINT('Ctrl Pts',(5.31937625898175,-3.91459021372843,53.8177630762299));
#54607=CARTESIAN_POINT('Ctrl Pts',(6.16890975425877,2.35888379744498,54.096186929877));
#54608=CARTESIAN_POINT('Ctrl Pts',(1.35040241530983,6.46499757484586,54.3746107835242));
#54609=CARTESIAN_POINT('Ctrl Pts',(-4.70886485327322,4.63102279411851,54.6530346371712));
#54610=CARTESIAN_POINT('Ctrl Pts',(-6.44159156049077,-1.45797067660881,
54.9314584908185));
#54611=CARTESIAN_POINT('Ctrl Pts',(-2.25573533219686,-6.20736968748566,
55.2098823444655));
#54612=CARTESIAN_POINT('Ctrl Pts',(4.0027075416176,-5.25339058726029,55.4883061981127));
#54613=CARTESIAN_POINT('Ctrl Pts',(6.58343252084137,0.527443427834472,55.7667300517598));
#54614=CARTESIAN_POINT('Ctrl Pts',(3.11525001981887,5.82365844122538,56.0451539054069));
#54615=CARTESIAN_POINT('Ctrl Pts',(-3.2152477078069,5.76905213215134,56.323577759054));
#54616=CARTESIAN_POINT('Ctrl Pts',(-6.59155157850042,0.413797189461302,
56.6020016127012));
#54617=CARTESIAN_POINT('Ctrl Pts',(-3.91148811750227,-5.32165773351459,
56.8804254663483));
#54618=CARTESIAN_POINT('Ctrl Pts',(2.36248014284657,-6.1675333724831,57.1588493199955));
#54619=CARTESIAN_POINT('Ctrl Pts',(6.46578382012906,-1.34663280718776,57.4372731736426));
#54620=CARTESIAN_POINT('Ctrl Pts',(4.62827653118404,4.71156414335287,57.7156970272897));
#54621=CARTESIAN_POINT('Ctrl Pts',(-1.46172616065295,6.44074040443335,57.9941208809369));
#54622=CARTESIAN_POINT('Ctrl Pts',(-6.20868382555991,2.25211577861082,58.2725447345839));
#54623=CARTESIAN_POINT('Ctrl Pts',(-5.25105593938519,-4.00576981958337,
58.5509685882311));
#54624=CARTESIAN_POINT('Ctrl Pts',(0.531281769573442,-6.58312387908324,
58.8293924418782));
#54625=CARTESIAN_POINT('Ctrl Pts',(5.82547377947346,-3.11185404071339,59.1078162955253));
#54626=CARTESIAN_POINT('Ctrl Pts',(5.76717652042727,3.21861077303071,59.3862401491726));
#54627=CARTESIAN_POINT('Ctrl Pts',(0.409953953971075,6.59179172013654,59.6646640028195));
#54628=CARTESIAN_POINT('Ctrl Pts',(-5.32393739900074,3.90838469160332,59.9430878564668));
#54629=CARTESIAN_POINT('Ctrl Pts',(-6.1661548941135,-2.36607568514559,60.2215117101138));
#54630=CARTESIAN_POINT('Ctrl Pts',(-1.34286274129069,-6.46656786743093,
60.499935563761));
#54631=CARTESIAN_POINT('Ctrl Pts',(4.71426183178142,-4.62552869491119,60.7783594174081));
#54632=CARTESIAN_POINT('Ctrl Pts',(6.43988705890778,1.46548114779727,61.0567832710552));
#54633=CARTESIAN_POINT('Ctrl Pts',(2.24849545943964,6.20999585305146,61.3352071247024));
#54634=CARTESIAN_POINT('Ctrl Pts',(-4.00883073582598,5.24871950646391,61.6136309783494));
#54635=CARTESIAN_POINT('Ctrl Pts',(-6.58281299945516,-0.535119930708313,
61.8920548319967));
#54636=CARTESIAN_POINT('Ctrl Pts',(-3.10845700376283,-5.82728713740749,
62.1704786856437));
#54637=CARTESIAN_POINT('Ctrl Pts',(3.22197274411874,-5.76529894820667,62.448902539291));
#54638=CARTESIAN_POINT('Ctrl Pts',(6.59202962095616,-0.406110579120708,
62.7273263929379));
#54639=CARTESIAN_POINT('Ctrl Pts',(3.90527993708621,5.32621525466534,63.0057502465852));
#54640=CARTESIAN_POINT('Ctrl Pts',(-2.36967042311993,6.1647743196185,63.2841741002322));
#54641=CARTESIAN_POINT('Ctrl Pts',(-6.46734971648495,1.33909221890021,63.5625979538794));
#54642=CARTESIAN_POINT('Ctrl Pts',(-4.62277928623404,-4.71695791764177,
63.8410218075266));
#54643=CARTESIAN_POINT('Ctrl Pts',(1.46923563676534,-6.43903152420423,64.1194456611737));
#54644=CARTESIAN_POINT('Ctrl Pts',(6.21130576951436,-2.24487437591387,64.3978695148208));
#54645=CARTESIAN_POINT('Ctrl Pts',(5.24638128929058,4.01189028930497,64.6762933684679));
#54646=CARTESIAN_POINT('Ctrl Pts',(-0.538957909934277,6.58249988206277,
64.9547172221151));
#54647=CARTESIAN_POINT('Ctrl Pts',(-5.82909851441101,3.10505891012206,65.2331410757622));
#54648=CARTESIAN_POINT('Ctrl Pts',(-5.76341941612784,-3.22533361992796,
65.5115649294094));
#54649=CARTESIAN_POINT('Ctrl Pts',(-0.402267066216936,-6.59226528087837,
65.7899887830564));
#54650=CARTESIAN_POINT('Ctrl Pts',(5.32849129973403,-3.90217385500653,66.0684126367037));
#54651=CARTESIAN_POINT('Ctrl Pts',(6.16339164946744,2.37326435554747,66.3468364903507));
#54652=CARTESIAN_POINT('Ctrl Pts',(1.33532124129813,6.46812936702529,66.6252603439979));
#54653=CARTESIAN_POINT('Ctrl Pts',(-4.71965240001728,4.62002830608733,66.9036841976449));
#54654=CARTESIAN_POINT('Ctrl Pts',(-6.43817380061354,-1.47298962628067,
67.1821080512921));
#54655=CARTESIAN_POINT('Ctrl Pts',(-2.24125252926465,-6.2126135745033,67.4605319049392));
#54656=CARTESIAN_POINT('Ctrl Pts',(4.0149484789801,-5.24404128866014,67.7389557585864));
#54657=CARTESIAN_POINT('Ctrl Pts',(6.58218452701253,0.542795705946505,68.0173796122336));
#54658=CARTESIAN_POINT('Ctrl Pts',(3.10165976094634,5.83090790986826,68.2958034658805));
#54659=CARTESIAN_POINT('Ctrl Pts',(-3.22869339931589,5.76153792482971,68.5742273195278));
#54660=CARTESIAN_POINT('Ctrl Pts',(-6.59249869982305,0.398423416566328,
68.8526511731748));
#54661=CARTESIAN_POINT('Ctrl Pts',(-3.89906644642019,-5.33076553343308,
69.1310750268221));
#54662=CARTESIAN_POINT('Ctrl Pts',(2.3768574812065,-6.16200688413035,69.409498880469));
#54663=CARTESIAN_POINT('Ctrl Pts',(6.46890681878693,-1.33154980976638,69.6879227341164));
#54664=CARTESIAN_POINT('Ctrl Pts',(4.61727575540617,4.72234527799222,69.9663465877634));
#54665=CARTESIAN_POINT('Ctrl Pts',(-1.47674311506742,6.43731388842723,70.2447704414106));
#54666=CARTESIAN_POINT('Ctrl Pts',(-6.21391926757366,2.23762992072296,70.5231942950576));
#54667=CARTESIAN_POINT('Ctrl Pts',(-5.24169950536803,-4.01800530381204,
70.8016181487048));
#54668=CARTESIAN_POINT('Ctrl Pts',(0.546633317440691,-6.5818669344116,71.0800420023519));
#54669=CARTESIAN_POINT('Ctrl Pts',(5.83271532316402,-3.098259557391,71.358465855999));
#54670=CARTESIAN_POINT('Ctrl Pts',(5.75965447495197,3.23205208114023,71.6368897096462));
#54671=CARTESIAN_POINT('Ctrl Pts',(0.394579631475598,6.59272987771093,71.9153135632933));
#54672=CARTESIAN_POINT('Ctrl Pts',(-5.33303795498926,3.89595771238356,72.1937374169405));
#54673=CARTESIAN_POINT('Ctrl Pts',(-6.16062002407802,-2.38044979887542,
72.4721612705875));
#54674=CARTESIAN_POINT('Ctrl Pts',(-1.32777792558714,-6.46968207150563,
72.7505851242348));
#54675=CARTESIAN_POINT('Ctrl Pts',(4.72503655065108,-4.61452163512627,73.0290089778817));
#54676=CARTESIAN_POINT('Ctrl Pts',(6.43645178793764,1.48049610184946,73.3074328315291));
#54677=CARTESIAN_POINT('Ctrl Pts',(2.23400655152038,6.21522284828162,73.585856685176));
#54678=CARTESIAN_POINT('Ctrl Pts',(-4.0210607627615,5.2393559402103,73.8642805388233));
#54679=CARTESIAN_POINT('Ctrl Pts',(-6.58154710436798,-0.550470743112097,
74.1427043924703));
#54680=CARTESIAN_POINT('Ctrl Pts',(-3.09485830061189,-5.83452075368412,
74.4211282461175));
#54681=CARTESIAN_POINT('Ctrl Pts',(3.23540966425953,-5.7577690671347,74.6995520997645));
#54682=CARTESIAN_POINT('Ctrl Pts',(6.59295881446331,-0.390735712251194,
74.9779759534118));
#54683=CARTESIAN_POINT('Ctrl Pts',(3.89284765395332,5.33530856363034,75.2563998070588));
#54684=CARTESIAN_POINT('Ctrl Pts',(-2.38404130733335,6.15923106978178,75.534823660706));
#54685=CARTESIAN_POINT('Ctrl Pts',(-6.47045512491767,1.32400559004247,75.8132475143532));
#54686=CARTESIAN_POINT('Ctrl Pts',(-4.61176594618401,-4.72772621707885,
76.0916713680002));
#54687=CARTESIAN_POINT('Ctrl Pts',(1.48424858535093,-6.43558749943792,76.3700952216474));
#54688=CARTESIAN_POINT('Ctrl Pts',(6.21652431618393,-2.23038242288872,76.6485190752944));
#54689=CARTESIAN_POINT('Ctrl Pts',(5.23701059398374,4.0241148547897,76.9269429289418));
#54690=CARTESIAN_POINT('Ctrl Pts',(-0.554307981656129,6.58122503699047,
77.2053667825887));
#54691=CARTESIAN_POINT('Ctrl Pts',(-5.83632420081472,3.09145599176529,77.483790636236));
#54692=CARTESIAN_POINT('Ctrl Pts',(-5.75588170201891,-3.23876614753225,
77.762214489883));
#54693=CARTESIAN_POINT('Ctrl Pts',(-0.386891660199915,-6.5931855100024,
78.0406383435301));
#54694=CARTESIAN_POINT('Ctrl Pts',(5.33757735858429,-3.88973627218676,78.3190621971773));
#54695=CARTESIAN_POINT('Ctrl Pts',(6.15784002171388,2.38763200535924,78.5974860508244));
#54696=CARTESIAN_POINT('Ctrl Pts',(1.32023280441466,6.47122597876048,78.8759099044716));
#54697=CARTESIAN_POINT('Ctrl Pts',(-4.73041427636142,4.60900868951591,79.1543337581187));
#54698=CARTESIAN_POINT('Ctrl Pts',(-6.43472102322171,-1.48800056429638,
79.4327576117657));
#54699=CARTESIAN_POINT('Ctrl Pts',(-2.22675753605982,-6.21782367083837,
79.711181465413));
#54700=CARTESIAN_POINT('Ctrl Pts',(4.02716757885868,-5.23466346748542,79.98960531906));
#54701=CARTESIAN_POINT('Ctrl Pts',(6.58090073238833,0.558145031768453,80.2680291727073));
#54702=CARTESIAN_POINT('Ctrl Pts',(3.08805263200795,5.83812566394266,80.5464530263542));
#54703=CARTESIAN_POINT('Ctrl Pts',(-3.24212152981735,5.75399238024632,80.8248768800015));
#54704=CARTESIAN_POINT('Ctrl Pts',(-6.59340996425109,0.383047476628627,
81.1033007336486));
#54705=CARTESIAN_POINT('Ctrl Pts',(-3.88662356814169,-5.3398443390798,81.3817245872957));
#54706=CARTESIAN_POINT('Ctrl Pts',(2.39122189173239,-6.15644688034727,81.6601484409429));
#54707=CARTESIAN_POINT('Ctrl Pts',(6.47199463277192,-1.31645956998633,81.93857229459));
#54708=CARTESIAN_POINT('Ctrl Pts',(4.6062498660594,4.73310072758491,82.2169961482372));
#54709=CARTESIAN_POINT('Ctrl Pts',(-1.49175203741027,6.43385235958365,82.4954200018842));
#54710=CARTESIAN_POINT('Ctrl Pts',(-6.21912091180313,2.22313189226599,82.7738438555314));
#54711=CARTESIAN_POINT('Ctrl Pts',(-5.23231456151334,-4.03021893393057,
83.0522677091786));
#54712=CARTESIAN_POINT('Ctrl Pts',(0.561981892144835,-6.58057419067199,
83.3306915628256));
#54713=CARTESIAN_POINT('Ctrl Pts',(5.83992514245569,-3.08464822249653,83.6091154164727));
#54714=CARTESIAN_POINT('Ctrl Pts',(5.75210110245894,3.24547580997431,83.8875392701199));
#54715=CARTESIAN_POINT('Ctrl Pts',(0.379203162843909,6.59363217713319,84.165963123767));
#54716=CARTESIAN_POINT('Ctrl Pts',(-5.3421095043464,3.883509542876,84.4443869774141));
#54717=CARTESIAN_POINT('Ctrl Pts',(-6.15505164615532,-2.39481096523249,
84.7228108310613));
#54718=CARTESIAN_POINT('Ctrl Pts',(-1.31268588804032,-6.47276108669066,
85.0012346847084));
#54719=CARTESIAN_POINT('Ctrl Pts',(4.73578556983606,-4.60348947675244,85.2796585383555));
#54720=CARTESIAN_POINT('Ctrl Pts',(6.43298150881899,1.49550300341722,85.5580823920027));
#54721=CARTESIAN_POINT('Ctrl Pts',(2.21950549273989,6.22041603863717,85.8365062456497));
#54722=CARTESIAN_POINT('Ctrl Pts',(-4.03326891896803,5.22996387686611,86.114930099297));
#54723=CARTESIAN_POINT('Ctrl Pts',(-6.58024541195241,-0.565818561480864,
86.393353952944));
#54724=CARTESIAN_POINT('Ctrl Pts',(-3.08124276438845,-5.84172263574204,
86.6717778065911));
#54725=CARTESIAN_POINT('Ctrl Pts',(3.24882898686282,-5.75020786929984,86.9502016602383));
#54726=CARTESIAN_POINT('Ctrl Pts',(6.59385214857313,-0.375358720152691,
87.2286255138854));
#54727=CARTESIAN_POINT('Ctrl Pts',(3.88039419744838,5.34437285361397,87.5070493675325));
#54728=CARTESIAN_POINT('Ctrl Pts',(-2.39839922463963,6.15365431961246,87.7854732211798));
#54729=CARTESIAN_POINT('Ctrl Pts',(-6.47352534025624,1.30891175985915,88.0638970748268));
#54730=CARTESIAN_POINT('Ctrl Pts',(-4.60072752253314,-4.73846880220224,
88.342320928474));
#54731=CARTESIAN_POINT('Ctrl Pts',(1.49925346104233,-6.43210847122385,88.6207447821212));
#54732=CARTESIAN_POINT('Ctrl Pts',(6.22170905090035,-2.21587833871397,88.8991686357682));
#54733=CARTESIAN_POINT('Ctrl Pts',(5.22761141434257,4.03631753293422,89.1775924894154));
#54734=CARTESIAN_POINT('Ctrl Pts',(-0.569655038472113,6.57991439634137,
89.4560163430625));
#54735=CARTESIAN_POINT('Ctrl Pts',(-5.84351814319067,3.07783625884149,89.7344401967096));
#54736=CARTESIAN_POINT('Ctrl Pts',(-5.74831268141256,-3.25218105934286,
90.0128640503567));
#54737=CARTESIAN_POINT('Ctrl Pts',(-0.371514149862039,-6.59406987849609,
90.2912879040039));
#54738=CARTESIAN_POINT('Ctrl Pts',(5.34663438611311,-3.87727753291801,90.5697117576509));
#54739=CARTESIAN_POINT('Ctrl Pts',(6.15225490119367,2.40198666873391,90.8481356112982));
#54740=CARTESIAN_POINT('Ctrl Pts',(1.30513718672595,6.47428739320878,91.1265594649451));
#54741=CARTESIAN_POINT('Ctrl Pts',(-4.74115042377128,4.59796400434054,91.4049833185925));
#54742=CARTESIAN_POINT('Ctrl Pts',(-6.43123324709496,-1.50300340901059,
91.6834071722394));
#54743=CARTESIAN_POINT('Ctrl Pts',(-2.21225043142142,-6.22299994815304,
91.9618310258866));
#54744=CARTESIAN_POINT('Ctrl Pts',(4.03936477479301,-5.22525717474255,92.2402548795338));
#54745=CARTESIAN_POINT('Ctrl Pts',(6.57958114395136,0.573491321814751,92.5186787331809));
#54746=CARTESIAN_POINT('Ctrl Pts',(3.07442870701341,5.8453116641912,92.797102586828));
#54747=CARTESIAN_POINT('Ctrl Pts',(-3.2555320262752,5.74641553944141,93.0755264404753));
#54748=CARTESIAN_POINT('Ctrl Pts',(-6.59428536682807,0.367669453278525,
93.3539502941222));
#54749=CARTESIAN_POINT('Ctrl Pts',(-3.87415955034417,-5.34889410107492,
93.6323741477694));
#54750=CARTESIAN_POINT('Ctrl Pts',(2.40557329629567,-6.15085339137476,93.9107980014166));
#54751=CARTESIAN_POINT('Ctrl Pts',(6.4750472452893,-1.30136216992396,94.1892218550636));
#54752=CARTESIAN_POINT('Ctrl Pts',(4.5951989231141,4.74383043363146,94.4676457087109));
#54753=CARTESIAN_POINT('Ctrl Pts',(-1.50675284604706,6.43035583672989,94.7460695623579));
#54754=CARTESIAN_POINT('Ctrl Pts',(-6.22428872995647,2.20862177209563,95.0244934160051));
#54755=CARTESIAN_POINT('Ctrl Pts',(-5.22290115886631,-4.04241064350841,
95.3029172696522));
#54756=CARTESIAN_POINT('Ctrl Pts',(0.577327410204486,-6.57924565489567,
95.5813411232994));
#54757=CARTESIAN_POINT('Ctrl Pts',(5.84710319813395,-3.07102011006271,95.8597649769464));
#54758=CARTESIAN_POINT('Ctrl Pts',(5.74451644403124,3.25888188652056,96.1381888305936));
#54759=CARTESIAN_POINT('Ctrl Pts',(0.363824631709314,6.59449861349584,96.4166126842407));
#54760=CARTESIAN_POINT('Ctrl Pts',(-5.35115199773147,3.87104025078679,96.6950365378879));
#54761=CARTESIAN_POINT('Ctrl Pts',(-6.14944979063202,-2.40915910610592,
96.973460391535));
#54762=CARTESIAN_POINT('Ctrl Pts',(-1.29758671073624,-6.47580489623943,
97.2518842451821));
#54763=CARTESIAN_POINT('Ctrl Pts',(4.74650883087199,-4.59243227979371,97.5303080988292));
#54764=CARTESIAN_POINT('Ctrl Pts',(6.42947624042683,1.51050177087747,97.8087319524763));
#54765=CARTESIAN_POINT('Ctrl Pts',(2.20499236196995,6.22557539587235,98.0871558061237));
#54766=CARTESIAN_POINT('Ctrl Pts',(-4.04545513804484,5.2205433675149,98.3655796597704));
#54767=CARTESIAN_POINT('Ctrl Pts',(-6.57890792928845,-0.581163302337195,
98.6440035134179));
#54768=CARTESIAN_POINT('Ctrl Pts',(-3.06761046914817,-5.8488927444098,98.9224273670648));
#54769=CARTESIAN_POINT('Ctrl Pts',(3.26223063894007,-5.74261539582774,99.2008512207121));
#54770=CARTESIAN_POINT('Ctrl Pts',(6.59470961842695,-0.359979686461526,
99.4792750743591));
#54771=CARTESIAN_POINT('Ctrl Pts',(3.8679196353063,5.35340807531511,99.7576989280063));
#54772=CARTESIAN_POINT('Ctrl Pts',(-2.41274409694558,6.14804409944263,100.036122781653));
#54773=CARTESIAN_POINT('Ctrl Pts',(-6.47656034580163,1.29381081044633,100.314546635301));
#54774=CARTESIAN_POINT('Ctrl Pts',(-4.58966407531989,-4.74918561458226,
100.592970488948));
#54775=CARTESIAN_POINT('Ctrl Pts',(1.51425018222724,-6.42859445848481,100.871394342595));
#54776=CARTESIAN_POINT('Ctrl Pts',(6.22685994546354,-2.20136220227813,101.149818196242));
#54777=CARTESIAN_POINT('Ctrl Pts',(5.2181838014896,4.04849825736762,101.428242049889));
#54778=CARTESIAN_POINT('Ctrl Pts',(-0.584998996909095,6.57856796724433,
101.706665903536));
#54779=CARTESIAN_POINT('Ctrl Pts',(-5.85068030241062,3.06419978542872,101.985089757183));
#54780=CARTESIAN_POINT('Ctrl Pts',(-5.74071239547699,-3.26557828239561,
102.26351361083));
#54781=CARTESIAN_POINT('Ctrl Pts',(-0.356134618842078,-6.59491838154948,
102.541937464478));
#54782=CARTESIAN_POINT('Ctrl Pts',(5.35566233305879,-3.86479770496367,102.820361318125));
#54783=CARTESIAN_POINT('Ctrl Pts',(6.14663631828457,2.4163282675959,103.098785171772));
#54784=CARTESIAN_POINT('Ctrl Pts',(1.29003447033791,6.47731359371901,103.377209025419));
#54785=CARTESIAN_POINT('Ctrl Pts',(-4.7518607838522,4.58689431063379,103.655632879066));
#54786=CARTESIAN_POINT('Ctrl Pts',(-6.42771049120372,-1.51799807882206,
103.934056732713));
#54787=CARTESIAN_POINT('Ctrl Pts',(-2.19773129425428,-6.22814237829327,
104.21248058636));
#54788=CARTESIAN_POINT('Ctrl Pts',(4.05154000044214,-5.21582246159265,104.490904440007));
#54789=CARTESIAN_POINT('Ctrl Pts',(6.57822576887897,0.588834492616189,104.769328293655));
#54790=CARTESIAN_POINT('Ctrl Pts',(3.06078806006388,5.85246587152864,105.047752147302));
#54791=CARTESIAN_POINT('Ctrl Pts',(-3.26892481574906,5.73880744362598,105.326176000949));
#54792=CARTESIAN_POINT('Ctrl Pts',(-6.59512490279267,0.352289430157958,
105.604599854596));
#54793=CARTESIAN_POINT('Ctrl Pts',(-3.86167446081989,-5.35791477019638,
105.883023708243));
#54794=CARTESIAN_POINT('Ctrl Pts',(2.4199116168386,-6.1452264476362,106.16144756189));
#54795=CARTESIAN_POINT('Ctrl Pts',(6.47806463973569,-1.28625769169451,106.439871415537));
#54796=CARTESIAN_POINT('Ctrl Pts',(4.58412298667673,4.75453433777263,106.718295269185));
#54797=CARTESIAN_POINT('Ctrl Pts',(-1.52174545938792,6.42682433888381,106.996719122832));
#54798=CARTESIAN_POINT('Ctrl Pts',(-6.22942269392552,2.19409963913285,107.275142976479));
#54799=CARTESIAN_POINT('Ctrl Pts',(-5.21345934862686,-4.05458036623436,
107.553566830126));
#54800=CARTESIAN_POINT('Ctrl Pts',(0.59266978815451,-6.57788133430863,107.831990683773));
#54801=CARTESIAN_POINT('Ctrl Pts',(5.8542494511568,-3.05737529421354,108.11041453742));
#54802=CARTESIAN_POINT('Ctrl Pts',(5.7369005409224,3.27227023786272,108.388838391067));
#54803=CARTESIAN_POINT('Ctrl Pts',(0.348444121716408,6.59532918208624,108.667262244714));
#54804=CARTESIAN_POINT('Ctrl Pts',(-5.36016538596209,3.85854990393683,108.945686098361));
#54805=CARTESIAN_POINT('Ctrl Pts',(-6.14381448797689,-2.42349414345551,
109.224109952009));
#54806=CARTESIAN_POINT('Ctrl Pts',(-1.28248047580012,-6.47881348359625,
109.502533805656));
#54807=CARTESIAN_POINT('Ctrl Pts',(4.7572062754346,-4.58135010439092,109.780957659303));
#54808=CARTESIAN_POINT('Ctrl Pts',(6.42593600182647,1.52549232265109,110.05938151295));
#54809=CARTESIAN_POINT('Ctrl Pts',(2.19046723814809,6.23070089192516,110.337805366597));
#54810=CARTESIAN_POINT('Ctrl Pts',(-4.05761935371081,5.21109446339532,110.616229220244));
#54811=CARTESIAN_POINT('Ctrl Pts',(-6.57753466365052,-0.596504882220527,
110.894653073892));
#54812=CARTESIAN_POINT('Ctrl Pts',(-3.05396148903758,-5.85603104068893,
111.173076927538));
#54813=CARTESIAN_POINT('Ctrl Pts',(3.27561454759935,-5.73499168801425,111.451500781186));
#54814=CARTESIAN_POINT('Ctrl Pts',(6.59553121936074,-0.344598694824773,
111.729924634833));
#54815=CARTESIAN_POINT('Ctrl Pts',(3.85542403537677,5.36241417959085,112.00834848848));
#54816=CARTESIAN_POINT('Ctrl Pts',(-2.42707584622865,6.14240043978659,112.286772342127));
#54817=CARTESIAN_POINT('Ctrl Pts',(-6.47956012504612,1.2787028239389,112.565196195774));
#54818=CARTESIAN_POINT('Ctrl Pts',(-4.57857566471911,-4.75987659592976,
112.843620049421));
#54819=CARTESIAN_POINT('Ctrl Pts',(1.52923866733776,-6.42504548033368,113.122043903069));
#54820=CARTESIAN_POINT('Ctrl Pts',(6.23197697185764,-2.18683409253494,113.400467756716));
#54821=CARTESIAN_POINT('Ctrl Pts',(5.20872780670208,4.06065696183837,113.678891610363));
#54822=CARTESIAN_POINT('Ctrl Pts',(-0.600339773510414,6.57718575702242,
113.95731546401));
#54823=CARTESIAN_POINT('Ctrl Pts',(-5.85781063951934,3.05054664569663,114.235739317657));
#54824=CARTESIAN_POINT('Ctrl Pts',(-5.73308088555054,-3.27895774382228,
114.514163171304));
#54825=CARTESIAN_POINT('Ctrl Pts',(-0.340753150789953,-6.5957310145475,
114.792587024951));
#54826=CARTESIAN_POINT('Ctrl Pts',(5.36466115031821,-3.85229685620206,115.071010878598));
#54827=CARTESIAN_POINT('Ctrl Pts',(6.14098430354606,2.43065672394069,115.349434732246));
#54828=CARTESIAN_POINT('Ctrl Pts',(1.27492473739474,6.48030456383154,115.627858585892));
#54829=CARTESIAN_POINT('Ctrl Pts',(-4.76254529835031,4.5757996686042,115.90628243954));
#54830=CARTESIAN_POINT('Ctrl Pts',(-6.42415277470816,-1.53298449217421,
116.184706293187));
#54831=CARTESIAN_POINT('Ctrl Pts',(-2.18320020352859,-6.2332509332892,116.463130146834));
#54832=CARTESIAN_POINT('Ctrl Pts',(4.06369318958433,-5.20635937935165,116.741554000481));
#54833=CARTESIAN_POINT('Ctrl Pts',(6.57683461454295,0.604174460720374,117.019977854128));
#54834=CARTESIAN_POINT('Ctrl Pts',(3.04713076535168,5.85958824704307,117.298401707775));
#54835=CARTESIAN_POINT('Ctrl Pts',(-3.28229982539491,5.73116813418082,117.576825561423));
#54836=CARTESIAN_POINT('Ctrl Pts',(-6.59592856757859,0.336907490919371,
117.85524941507));
#54837=CARTESIAN_POINT('Ctrl Pts',(-3.84916836747591,-5.36690629738036,
118.133673268717));
#54838=CARTESIAN_POINT('Ctrl Pts',(2.43423677537425,-6.13956607973662,118.412097122364));
#54839=CARTESIAN_POINT('Ctrl Pts',(6.48104679969937,-1.27114621745216,118.690520976011));
#54840=CARTESIAN_POINT('Ctrl Pts',(4.57302211699003,4.76521238178937,118.968944829658));
#54841=CARTESIAN_POINT('Ctrl Pts',(-1.53672979588759,6.42325788525319,119.247368683305));
#54842=CARTESIAN_POINT('Ctrl Pts',(-6.23452277578633,2.17956557236435,119.525792536953));
#54843=CARTESIAN_POINT('Ctrl Pts',(-5.20398918214985,-4.06672803591727,
119.8042163906));
#54844=CARTESIAN_POINT('Ctrl Pts',(0.608008942548482,-6.57648123633055,
120.082640244247));
#54845=CARTESIAN_POINT('Ctrl Pts',(5.86136386265324,-3.04371384916539,120.361064097894));
#54846=CARTESIAN_POINT('Ctrl Pts',(5.72925343456004,3.28564079118416,120.639487951541));
#54847=CARTESIAN_POINT('Ctrl Pts',(0.333061716511642,6.59612387838091,120.917911805188));
#54848=CARTESIAN_POINT('Ctrl Pts',(-5.36914961999736,3.84603857027319,121.196335658835));
#54849=CARTESIAN_POINT('Ctrl Pts',(-6.13814576887177,-2.43781599933361,
121.474759512482));
#54850=CARTESIAN_POINT('Ctrl Pts',(-1.26736726533664,-6.4817868323569,121.753183366129));
#54851=CARTESIAN_POINT('Ctrl Pts',(4.76787784522852,-4.57024301089718,122.031607219777));
#54852=CARTESIAN_POINT('Ctrl Pts',(6.42236081248373,1.5404745773487,122.310031073424));
#54853=CARTESIAN_POINT('Ctrl Pts',(2.17593019988002,6.23579249864457,122.588454927071));
#54854=CARTESIAN_POINT('Ctrl Pts',(-4.06976149905412,5.20161721641628,122.866878780718));
#54855=CARTESIAN_POINT('Ctrl Pts',(-6.57612562392392,-0.611843218661398,
123.145302634365));
#54856=CARTESIAN_POINT('Ctrl Pts',(-3.04029589562085,-5.86313748391429,
123.423726488012));
#54857=CARTESIAN_POINT('Ctrl Pts',(3.28898063499709,-5.72733679079851,123.702150341659));
#54858=CARTESIAN_POINT('Ctrl Pts',(6.5963169564375,-0.329215822341513,123.980574195307));
#54859=CARTESIAN_POINT('Ctrl Pts',(3.84290744762627,5.37139110507242,124.258998048954));
#54860=CARTESIAN_POINT('Ctrl Pts',(-2.4413943605552,6.13672339472416,124.537421902601));
#54861=CARTESIAN_POINT('Ctrl Pts',(-6.48252472584031,1.26358783835648,124.815845756248));
#54862=CARTESIAN_POINT('Ctrl Pts',(-4.56746222988183,-4.77054160472563,
125.094269609895));
#54863=CARTESIAN_POINT('Ctrl Pts',(1.54421860607799,-6.42146171349359,125.372693463542));
#54864=CARTESIAN_POINT('Ctrl Pts',(6.23706053422062,-2.17229379126241,125.651117317189));
#54865=CARTESIAN_POINT('Ctrl Pts',(5.19924266576478,4.07279301896267,125.929541170837));
#54866=CARTESIAN_POINT('Ctrl Pts',(-0.615675744729761,6.57576883295141,
126.207965024483));
#54867=CARTESIAN_POINT('Ctrl Pts',(-5.86491202376979,3.03687491286735,126.486388878131));
#54868=CARTESIAN_POINT('Ctrl Pts',(-5.72541270217929,-3.29231559248493,
126.764812731778));
#54869=CARTESIAN_POINT('Ctrl Pts',(-0.325380197419233,-6.59651490739494,
127.043236585425));
#54870=CARTESIAN_POINT('Ctrl Pts',(5.37365036593983,-3.83976158356861,127.321660439072));
#54871=CARTESIAN_POINT('Ctrl Pts',(6.1352619223662,2.44494652372861,127.600084292719));
#54872=CARTESIAN_POINT('Ctrl Pts',(1.25987786825185,6.48330831590777,127.878508146366));
#54873=CARTESIAN_POINT('Ctrl Pts',(-4.77333570284661,4.56458945006103,128.156932000013));
#54874=CARTESIAN_POINT('Ctrl Pts',(-6.42031125916862,-1.54779132331292,
128.435355853661));
#54875=CARTESIAN_POINT('Ctrl Pts',(-2.16912716912506,-6.23864897710079,
128.713779707308));
#54876=CARTESIAN_POINT('Ctrl Pts',(4.07671190140194,-5.19625695937802,128.992203560955));
#54877=CARTESIAN_POINT('Ctrl Pts',(6.57372921642299,0.618354217852361,129.270627414602));
#54878=CARTESIAN_POINT('Ctrl Pts',(3.03664626371355,5.86888938326796,129.549051268249));
#54879=CARTESIAN_POINT('Ctrl Pts',(-3.30184300701674,5.71910967681579,129.827475121896));
#54880=CARTESIAN_POINT('Ctrl Pts',(-6.03672382843121,1.22950628103885,130.059494999936));
#54881=CARTESIAN_POINT('Ctrl Pts',(-5.22664060241318,-2.54029413961005,
130.245110902367));
#54882=CARTESIAN_POINT('Ctrl Pts',(-4.00101382151821,-4.00468766736226,
130.337918853583));
#54883=CARTESIAN_POINT('Ctrl Pts',(-3.24375760296964,-4.54512507566672,
130.384322829191));
#54884=CARTESIAN_POINT('Ctrl Pts',(-4.20009954634508,-4.16738459507781,
-9.47071414072041));
#54885=CARTESIAN_POINT('Ctrl Pts',(-3.50577808166169,-4.8671566469011,-9.42431016511256));
#54886=CARTESIAN_POINT('Ctrl Pts',(-1.76531786303429,-5.89918424712944,
-9.33150221389684));
#54887=CARTESIAN_POINT('Ctrl Pts',(2.31525814347615,-6.10349577227439,-9.14588631146544));
#54888=CARTESIAN_POINT('Ctrl Pts',(6.54407278403002,-2.4777592280193,-8.91386643342614));
#54889=CARTESIAN_POINT('Ctrl Pts',(5.61980217846484,4.17653187559757,-8.63544257977903));
#54890=CARTESIAN_POINT('Ctrl Pts',(-0.47435427916949,6.98020994205008,-8.35701872613188));
#54891=CARTESIAN_POINT('Ctrl Pts',(-6.12941616757563,3.37727447383079,-8.07859487248477));
#54892=CARTESIAN_POINT('Ctrl Pts',(-6.15443318799092,-3.33234179095485,
-7.80017101883763));
#54893=CARTESIAN_POINT('Ctrl Pts',(-0.523807255543973,-6.97826436643947,
-7.5217471651905));
#54894=CARTESIAN_POINT('Ctrl Pts',(5.58761856355849,-4.21351783333861,-7.24332331154338));
#54895=CARTESIAN_POINT('Ctrl Pts',(6.56535149650638,2.42317706277268,-6.96489945789624));
#54896=CARTESIAN_POINT('Ctrl Pts',(1.51065583012593,6.8331545214114,-6.68647560424912));
#54897=CARTESIAN_POINT('Ctrl Pts',(-4.9319707928733,4.96492848346115,-6.40805175060197));
#54898=CARTESIAN_POINT('Ctrl Pts',(-6.84310304594355,-1.46519098634236,
-6.12962789695486));
#54899=CARTESIAN_POINT('Ctrl Pts',(-2.46672066112633,-6.5490397251654,-5.85120404330772));
#54900=CARTESIAN_POINT('Ctrl Pts',(4.17609273205395,-5.61560369114569,-5.5727801896606));
#54901=CARTESIAN_POINT('Ctrl Pts',(6.98188619633454,0.477503226102664,-5.29435633601347));
#54902=CARTESIAN_POINT('Ctrl Pts',(3.37266697756901,6.13187030790779,-5.01593248236633));
#54903=CARTESIAN_POINT('Ctrl Pts',(-3.33538254404525,6.15223199783412,-4.73750862871921));
#54904=CARTESIAN_POINT('Ctrl Pts',(-6.97885824454911,0.519874743954567,
-4.45908477507207));
#54905=CARTESIAN_POINT('Ctrl Pts',(-4.21010588636016,-5.59014641670148,
-4.18066092142495));
#54906=CARTESIAN_POINT('Ctrl Pts',(2.42692329786755,-6.56389935825552,-3.90223706777781));
#54907=CARTESIAN_POINT('Ctrl Pts',(6.83407716517237,-1.50669177560396,-3.62381321413069));
#54908=CARTESIAN_POINT('Ctrl Pts',(4.9620292963081,4.93487544201203,-3.34538936048356));
#54909=CARTESIAN_POINT('Ctrl Pts',(-1.46916850004176,6.84224193704743,-3.06696550683643));
#54910=CARTESIAN_POINT('Ctrl Pts',(-6.55048321018197,2.46290486839966,-2.7885416531893));
#54911=CARTESIAN_POINT('Ctrl Pts',(-5.61316450565459,-4.17936775843667,
-2.51011779954216));
#54912=CARTESIAN_POINT('Ctrl Pts',(0.48157209976335,-6.98160576123052,-2.23169394589504));
#54913=CARTESIAN_POINT('Ctrl Pts',(6.13383662858499,-3.36909170003948,-1.95327009224791));
#54914=CARTESIAN_POINT('Ctrl Pts',(6.15028577427905,3.33896923603762,-1.67484623860078));
#54915=CARTESIAN_POINT('Ctrl Pts',(0.515805939856379,6.97916004302912,-1.39642238495365));
#54916=CARTESIAN_POINT('Ctrl Pts',(-5.59260028490076,4.20684593528139,-1.11799853130652));
#54917=CARTESIAN_POINT('Ctrl Pts',(-6.56248316462805,-2.43074996317731,
-0.839574677659391));
#54918=CARTESIAN_POINT('Ctrl Pts',(-1.50270699079991,-6.83495445271005,
-0.56115082401226));
#54919=CARTESIAN_POINT('Ctrl Pts',(4.93776770600804,-4.95915121282611,-0.282726970365132));
#54920=CARTESIAN_POINT('Ctrl Pts',(6.84138417297234,1.47315758423168,-0.004303116718001));
#54921=CARTESIAN_POINT('Ctrl Pts',(2.4590852351668,6.55191807614683,0.274120736929126));
#54922=CARTESIAN_POINT('Ctrl Pts',(-4.18263977354214,5.61072679739748,0.55254459057626));
#54923=CARTESIAN_POINT('Ctrl Pts',(-6.98132379515334,-0.485642602626536,
0.830968444223388));
#54924=CARTESIAN_POINT('Ctrl Pts',(-3.36551483110386,-6.13579991459174,
1.10939229787052));
#54925=CARTESIAN_POINT('Ctrl Pts',(3.34255455671475,-6.14833796286877,1.38781615151765));
#54926=CARTESIAN_POINT('Ctrl Pts',(6.97945959413709,-0.511736694089966,
1.66624000516478));
#54927=CARTESIAN_POINT('Ctrl Pts',(4.20358448785803,5.59505211090234,1.94466385881191));
#54928=CARTESIAN_POINT('Ctrl Pts',(-2.43457576708131,6.5610648148461,2.22308771245903));
#54929=CARTESIAN_POINT('Ctrl Pts',(-6.8358294353571,1.49872165560417,2.50151156610617));
#54930=CARTESIAN_POINT('Ctrl Pts',(-4.95627143368447,-4.94065827050558,
2.77993541975329));
#54931=CARTESIAN_POINT('Ctrl Pts',(1.47714616242253,-6.84052409433019,3.05835927340044));
#54932=CARTESIAN_POINT('Ctrl Pts',(6.55335071761077,-2.45526476011491,3.33678312704754));
#54933=CARTESIAN_POINT('Ctrl Pts',(5.60828718036528,4.18591036368699,3.61520698069469));
#54934=CARTESIAN_POINT('Ctrl Pts',(-0.489712939625793,6.98103945749017,
3.89363083434181));
#54935=CARTESIAN_POINT('Ctrl Pts',(-6.13776111520212,3.36193681722077,4.17205468798895));
#54936=CARTESIAN_POINT('Ctrl Pts',(-6.14638806117258,-3.34613874066016,
4.45047854163607));
#54937=CARTESIAN_POINT('Ctrl Pts',(-0.507667274478622,-6.97975677288937,
4.72890239528321));
#54938=CARTESIAN_POINT('Ctrl Pts',(5.59750203498042,-4.20032161133665,5.00732624893033));
#54939=CARTESIAN_POINT('Ctrl Pts',(6.55964423466067,2.43840074330588,5.28575010257747));
#54940=CARTESIAN_POINT('Ctrl Pts',(1.49473581094941,6.83670209426571,5.56417395622459));
#54941=CARTESIAN_POINT('Ctrl Pts',(-4.94354715548264,4.95338996968654,5.84259780987173));
#54942=CARTESIAN_POINT('Ctrl Pts',(-6.83966169031252,-1.4811342384615,6.12102166351884));
#54943=CARTESIAN_POINT('Ctrl Pts',(-2.45144345042182,-6.55478113133121,
6.399445517166));
#54944=CARTESIAN_POINT('Ctrl Pts',(4.18917953087302,-5.60584565684663,6.67786937081309));
#54945=CARTESIAN_POINT('Ctrl Pts',(6.98075274668871,0.493783110150294,6.95629322446026));
#54946=CARTESIAN_POINT('Ctrl Pts',(3.35835766047978,6.13972022934013,7.23471707810736));
#54947=CARTESIAN_POINT('Ctrl Pts',(-3.34972178711789,6.14443607007018,7.5131409317545));
#54948=CARTESIAN_POINT('Ctrl Pts',(-6.98005157894001,0.503597682290836,
7.79156478540162));
#54949=CARTESIAN_POINT('Ctrl Pts',(-4.1970573069562,-5.59995005624133,8.06998863904877));
#54950=CARTESIAN_POINT('Ctrl Pts',(2.44222489061947,-6.55822142458687,8.34841249269588));
#54951=CARTESIAN_POINT('Ctrl Pts',(6.83757242910279,-1.49074945817361,8.62683634634303));
#54952=CARTESIAN_POINT('Ctrl Pts',(4.9505068218311,4.94643435994816,8.90526019999013));
#54953=CARTESIAN_POINT('Ctrl Pts',(-1.48512181100304,6.83879696121727,9.18368405363728));
#54954=CARTESIAN_POINT('Ctrl Pts',(-6.55620931681649,2.44762130738398,9.46210790728441));
#54955=CARTESIAN_POINT('Ctrl Pts',(-5.60340222767442,-4.19244727398749,
9.74053176093154));
#54956=CARTESIAN_POINT('Ctrl Pts',(0.497853112817942,-6.98046366284714,
10.0189556145787));
#54957=CARTESIAN_POINT('Ctrl Pts',(6.14167725633898,-3.35477736209725,10.2973794682258));
#54958=CARTESIAN_POINT('Ctrl Pts',(6.14248199022549,3.35330369486973,10.5758033218729));
#54959=CARTESIAN_POINT('Ctrl Pts',(0.499527918909906,6.98034401218888,10.8542271755201));
#54960=CARTESIAN_POINT('Ctrl Pts',(-5.6023961738528,4.19379157582627,11.1326510291672));
#54961=CARTESIAN_POINT('Ctrl Pts',(-6.55679638510844,-2.4460482077221,11.4110748828143));
#54962=CARTESIAN_POINT('Ctrl Pts',(-1.48676259863171,-6.83844043957255,
11.6894987364615));
#54963=CARTESIAN_POINT('Ctrl Pts',(4.94931988292061,-4.94762199109819,11.9679225901086));
#54964=CARTESIAN_POINT('Ctrl Pts',(6.83792990733845,1.48910887869161,12.2463464437557));
#54965=CARTESIAN_POINT('Ctrl Pts',(2.44379833230066,6.55763527358118,12.5247702974028));
#54966=CARTESIAN_POINT('Ctrl Pts',(-4.19571359191966,5.60095689367916,12.80319415105));
#54967=CARTESIAN_POINT('Ctrl Pts',(-6.98017220606371,-0.501922946245178,
13.0816180046971));
#54968=CARTESIAN_POINT('Ctrl Pts',(-3.35119592329026,-6.1436321955334,13.3600418583442));
#54969=CARTESIAN_POINT('Ctrl Pts',(3.3568844626981,-6.14052582230283,13.6384657119914));
#54970=CARTESIAN_POINT('Ctrl Pts',(6.98063407253657,-0.495457985719165,
13.9168895656385));
#54971=CARTESIAN_POINT('Ctrl Pts',(4.190524419057,5.60484038698326,14.1953134192856));
#54972=CARTESIAN_POINT('Ctrl Pts',(-2.44987069331402,6.55536911670982,14.4737372729327));
#54973=CARTESIAN_POINT('Ctrl Pts',(-6.83930612537993,1.4827752336791,14.7521611265799));
#54974=CARTESIAN_POINT('Ctrl Pts',(-4.94473547846849,-4.95220372341915,
15.030584980227));
#54975=CARTESIAN_POINT('Ctrl Pts',(1.49309544017187,-6.83706052897074,15.3090088338741));
#54976=CARTESIAN_POINT('Ctrl Pts',(6.55905900114047,-2.43997452647152,15.5874326875213));
#54977=CARTESIAN_POINT('Ctrl Pts',(5.59850965569222,4.19897848355916,15.8658565411684));
#54978=CARTESIAN_POINT('Ctrl Pts',(-0.505992609048554,6.97987837643749,
16.1442803948155));
#54979=CARTESIAN_POINT('Ctrl Pts',(-6.1455850462588,3.34761334527627,16.4227042484627));
#54980=CARTESIAN_POINT('Ctrl Pts',(-6.13856756696716,-3.36046408938568,
16.7011281021098));
#54981=CARTESIAN_POINT('Ctrl Pts',(-0.491387884102221,-6.98092175988452,
16.9795519557569));
#54982=CARTESIAN_POINT('Ctrl Pts',(5.60728269480187,-4.18725583775901,17.257975809404));
#54983=CARTESIAN_POINT('Ctrl Pts',(6.55393961987617,2.45369234609581,17.5363996630512));
#54984=CARTESIAN_POINT('Ctrl Pts',(1.47878736467127,6.84016948623062,17.8148235166983));
#54985=CARTESIAN_POINT('Ctrl Pts',(-4.95508588046342,4.94184728492329,18.0932473703454));
#54986=CARTESIAN_POINT('Ctrl Pts',(-6.8361888264097,-1.49708149408864,18.3716712239925));
#54987=CARTESIAN_POINT('Ctrl Pts',(-2.43614989119636,-6.56048049901039,
18.6500950776397));
#54988=CARTESIAN_POINT('Ctrl Pts',(4.20224194779605,-5.59606051454548,18.9285189312868));
#54989=CARTESIAN_POINT('Ctrl Pts',(6.97958217406843,0.510062099844575,19.2069427849339));
#54990=CARTESIAN_POINT('Ctrl Pts',(3.34402962927311,6.14753580785139,19.4853666385811));
#54991=CARTESIAN_POINT('Ctrl Pts',(-3.36404257371562,6.13660722488416,19.7637904922282));
#54992=CARTESIAN_POINT('Ctrl Pts',(-6.9812070741349,0.487317615442708,20.0422143458754));
#54993=CARTESIAN_POINT('Ctrl Pts',(-4.18398583304347,-5.60972309647839,
20.3206381995225));
#54994=CARTESIAN_POINT('Ctrl Pts',(2.45751316476841,-6.55250789509341,20.5990620531696));
#54995=CARTESIAN_POINT('Ctrl Pts',(6.84103052183109,-1.47479899296382,20.8774859068167));
#54996=CARTESIAN_POINT('Ctrl Pts',(4.9389574114444,4.95796635307363,21.1559097604638));
#54997=CARTESIAN_POINT('Ctrl Pts',(-1.50106703908689,6.83531479995168,21.434333614111));
#54998=CARTESIAN_POINT('Ctrl Pts',(-6.56189976670772,2.43232442777533,21.7127574677581));
#54999=CARTESIAN_POINT('Ctrl Pts',(-5.5936094710715,-4.20550398352098,21.9911813214053));
#55000=CARTESIAN_POINT('Ctrl Pts',(0.514131417249838,-6.97928359905718,
22.2696051750524));
#55001=CARTESIAN_POINT('Ctrl Pts',(6.149484479648,-3.34044477649908,22.5480290286995));
#55002=CARTESIAN_POINT('Ctrl Pts',(6.13464479672021,3.36761991447152,22.8264528823466));
#55003=CARTESIAN_POINT('Ctrl Pts',(0.483247181124235,6.98149001519067,23.1048767359938));
#55004=CARTESIAN_POINT('Ctrl Pts',(-5.61216159118322,4.180714406022,23.3833005896409));
#55005=CARTESIAN_POINT('Ctrl Pts',(-6.5510739428483,-2.46133314803299,23.661724443288));
#55006=CARTESIAN_POINT('Ctrl Pts',(-1.47081011991242,-6.84188923188871,
23.9401482969351));
#55007=CARTESIAN_POINT('Ctrl Pts',(4.96084514027061,-4.93606585901412,24.2185721505823));
#55008=CARTESIAN_POINT('Ctrl Pts',(6.8344384498938,1.50505207381178,24.4969960042294));
#55009=CARTESIAN_POINT('Ctrl Pts',(2.42849813750882,6.56331680375008,24.7754198578766));
#55010=CARTESIAN_POINT('Ctrl Pts',(-4.20876458962517,5.5911565261034,25.0538437115237));
#55011=CARTESIAN_POINT('Ctrl Pts',(-6.97898265150518,-0.5182005598811,25.3322675651708));
#55012=CARTESIAN_POINT('Ctrl Pts',(-3.33685878817279,-6.15143106098621,
25.6106914188179));
#55013=CARTESIAN_POINT('Ctrl Pts',(3.37119611043732,-6.13268028314246,25.889115272465));
#55014=CARTESIAN_POINT('Ctrl Pts',(6.98177058295572,-0.479176582530357,
26.1675391261122));
#55015=CARTESIAN_POINT('Ctrl Pts',(4.1774415578066,5.61459817808735,26.4459629797593));
#55016=CARTESIAN_POINT('Ctrl Pts',(-2.4651522945908,6.54963776362828,26.7243868334065));
#55017=CARTESIAN_POINT('Ctrl Pts',(-6.84274561611155,1.46682074687334,27.0028106870536));
#55018=CARTESIAN_POINT('Ctrl Pts',(-4.93317262861548,-4.96372224107578,
27.2812345407007));
#55019=CARTESIAN_POINT('Ctrl Pts',(1.50903659690863,-6.83355977653392,27.5596583943478));
#55020=CARTESIAN_POINT('Ctrl Pts',(6.56473160965562,-2.42467102169763,27.838082247995));
#55021=CARTESIAN_POINT('Ctrl Pts',(5.58870168047518,4.21202376500006,28.1165061016421));
#55022=CARTESIAN_POINT('Ctrl Pts',(-0.52226952635505,6.97867933151483,28.3949299552892));
#55023=CARTESIAN_POINT('Ctrl Pts',(-6.1533755512042,3.33327166551328,28.6733538089363));
#55024=CARTESIAN_POINT('Ctrl Pts',(-6.13071368481874,-3.37477116039712,
28.9517776625835));
#55025=CARTESIAN_POINT('Ctrl Pts',(-0.475105821045126,-6.9820487773347,
29.2302015162306));
#55026=CARTESIAN_POINT('Ctrl Pts',(5.61703285636259,-4.17416728950991,29.5086253698778));
#55027=CARTESIAN_POINT('Ctrl Pts',(6.54819935792153,2.46897060314373,29.7870492235249));
#55028=CARTESIAN_POINT('Ctrl Pts',(1.4628308752025,6.84359967420847,30.065473077172));
#55029=CARTESIAN_POINT('Ctrl Pts',(-4.96659765451106,4.93027772123201,30.3438969308191));
#55030=CARTESIAN_POINT('Ctrl Pts',(-6.83267878017075,-1.51302060702285,
30.6223207844663));
#55031=CARTESIAN_POINT('Ctrl Pts',(-2.42084308164284,-6.56614418394338,
30.9007446381133));
#55032=CARTESIAN_POINT('Ctrl Pts',(4.21528150853767,-5.5862449350214,31.1791684917606));
#55033=CARTESIAN_POINT('Ctrl Pts',(6.97837363918924,0.526338315288408,31.4575923454076));
#55034=CARTESIAN_POINT('Ctrl Pts',(3.32968340973994,6.15531794964111,31.7360161990548));
#55035=CARTESIAN_POINT('Ctrl Pts',(-3.37834506313583,6.12874500241751,32.0144400527019));
#55036=CARTESIAN_POINT('Ctrl Pts',(-6.98232459823295,0.471034898052151,
32.292863906349));
#55037=CARTESIAN_POINT('Ctrl Pts',(-4.17089160224498,-5.61946562518125,
32.5712877599962));
#55038=CARTESIAN_POINT('Ctrl Pts',(2.47278807239367,-6.54675872621704,32.8497116136433));
#55039=CARTESIAN_POINT('Ctrl Pts',(6.84445140588907,-1.45884050625643,33.1281354672904));
#55040=CARTESIAN_POINT('Ctrl Pts',(4.92738113784791,4.96947137959889,33.4065593209376));
#55041=CARTESIAN_POINT('Ctrl Pts',(-1.51700410280022,6.83179546110386,33.6849831745847));
#55042=CARTESIAN_POINT('Ctrl Pts',(-6.56755452613331,2.41701431864547,33.9634070282318));
#55043=CARTESIAN_POINT('Ctrl Pts',(-5.58378629057699,-4.21853781913074,
34.2418308818789));
#55044=CARTESIAN_POINT('Ctrl Pts',(0.530406925298152,-6.97806557463225,
34.5202547355261));
#55045=CARTESIAN_POINT('Ctrl Pts',(6.15725825563656,-3.32609402207256,34.7986785891732));
#55046=CARTESIAN_POINT('Ctrl Pts',(6.12677423660805,3.38191781743839,35.0771024428204));
#55047=CARTESIAN_POINT('Ctrl Pts',(0.466963814935509,6.98259804555671,35.3555262964674));
#55048=CARTESIAN_POINT('Ctrl Pts',(-5.62189648371627,4.16761449712548,35.6339501501146));
#55049=CARTESIAN_POINT('Ctrl Pts',(-6.54531586900461,-2.47660470104297,
35.9123740037618));
#55050=CARTESIAN_POINT('Ctrl Pts',(-1.45484964139136,-6.84530081086397,
36.1907978574088));
#55051=CARTESIAN_POINT('Ctrl Pts',(4.97234341536255,-4.92448287944761,36.4692217110561));
#55052=CARTESIAN_POINT('Ctrl Pts',(6.8309098196334,1.52098708288659,36.7476455647031));
#55053=CARTESIAN_POINT('Ctrl Pts',(2.41318473400722,6.56896263574592,37.0260694183503));
#55054=CARTESIAN_POINT('Ctrl Pts',(-4.22179269567218,5.58132574797784,37.3044932719974));
#55055=CARTESIAN_POINT('Ctrl Pts',(-6.97775513794859,-0.534475355000993,
37.5829171256445));
#55056=CARTESIAN_POINT('Ctrl Pts',(-3.3225035037315,-6.15919646853093,37.8613409792916));
#55057=CARTESIAN_POINT('Ctrl Pts',(3.38548942209037,-6.12480138806036,38.1397648329388));
#55058=CARTESIAN_POINT('Ctrl Pts',(6.98286911921309,-0.462892573078836,
38.4181886865859));
#55059=CARTESIAN_POINT('Ctrl Pts',(4.16433597526518,5.62432543114141,38.696612540233));
#55060=CARTESIAN_POINT('Ctrl Pts',(-2.48042048779425,6.54387078677464,38.9750363938802));
#55061=CARTESIAN_POINT('Ctrl Pts',(-6.84614788884433,1.45085828196406,39.2534602475273));
#55062=CARTESIAN_POINT('Ctrl Pts',(-4.92158294701648,-4.97521376082556,
39.5318841011744));
#55063=CARTESIAN_POINT('Ctrl Pts',(1.52496954592781,-6.83002185606051,39.8103079548215));
#55064=CARTESIAN_POINT('Ctrl Pts',(6.57036851230249,-2.40935432903004,40.0887318084687));
#55065=CARTESIAN_POINT('Ctrl Pts',(5.57886330806047,4.22504613705561,40.3671556621158));
#55066=CARTESIAN_POINT('Ctrl Pts',(-0.538543603014195,6.97744232924386,
40.6455795157629));
#55067=CARTESIAN_POINT('Ctrl Pts',(-6.16113258766541,3.318911855937,40.9240033694101));
#55068=CARTESIAN_POINT('Ctrl Pts',(-6.12282645744497,-3.38905987587764,
41.2024272230572));
#55069=CARTESIAN_POINT('Ctrl Pts',(-0.458821173866272,-6.98313781910993,
41.4808510767043));
#55070=CARTESIAN_POINT('Ctrl Pts',(5.62675246663088,-4.16105603777872,41.7592749303515));
#55071=CARTESIAN_POINT('Ctrl Pts',(6.54242348001838,2.48423543135017,42.0376987839985));
#55072=CARTESIAN_POINT('Ctrl Pts',(1.44686642933153,6.84699263954222,42.3161226376458));
#55073=CARTESIAN_POINT('Ctrl Pts',(-4.9780824150123,4.91868134154035,42.5945464912928));
#55074=CARTESIAN_POINT('Ctrl Pts',(-6.82913157068701,-1.52895149057037,
42.87297034494));
#55075=CARTESIAN_POINT('Ctrl Pts',(-2.40552310501578,-6.57177215532517,
43.151394198587));
#55076=CARTESIAN_POINT('Ctrl Pts',(4.22829814217506,-5.5763989716618,43.4298180522343));
#55077=CARTESIAN_POINT('Ctrl Pts',(6.97712714862434,0.542611667954641,43.7082419058813));
#55078=CARTESIAN_POINT('Ctrl Pts',(3.3153190799102,6.16306661238177,43.9866657595286));
#55079=CARTESIAN_POINT('Ctrl Pts',(-3.39262917758629,6.12084944543334,44.2650896131756));
#55080=CARTESIAN_POINT('Ctrl Pts',(-6.98340414515589,0.454749618681986,
44.5435134668228));
#55081=CARTESIAN_POINT('Ctrl Pts',(-4.15777468578111,-5.62917758935972,
44.8219373204699));
#55082=CARTESIAN_POINT('Ctrl Pts',(2.48804953041416,-6.54097394922784,45.100361174117));
#55083=CARTESIAN_POINT('Ctrl Pts',(6.84783506267045,-1.44287408485045,45.3787850277641));
#55084=CARTESIAN_POINT('Ctrl Pts',(4.9157780640055,4.98094937694757,45.6572088814113));
#55085=CARTESIAN_POINT('Ctrl Pts',(-1.5329329154605,6.82823896381557,45.9356327350584));
#55086=CARTESIAN_POINT('Ctrl Pts',(-6.57317356433671,2.40169106326698,46.2140565887055));
#55087=CARTESIAN_POINT('Ctrl Pts',(-5.57393273961971,-4.23154870992487,
46.4924804423526));
#55088=CARTESIAN_POINT('Ctrl Pts',(0.546679548439304,-6.97680959619725,
46.7709042959998));
#55089=CARTESIAN_POINT('Ctrl Pts',(6.16499854202264,-3.31172517687243,47.0493281496469));
#55090=CARTESIAN_POINT('Ctrl Pts',(6.11887035269745,3.39619732600324,47.327752003294));
#55091=CARTESIAN_POINT('Ctrl Pts',(0.450677908909769,6.98366809726039,47.6061758569412));
#55092=CARTESIAN_POINT('Ctrl Pts',(-5.6316007985035,4.1544919203877,47.8845997105883));
#55093=CARTESIAN_POINT('Ctrl Pts',(-6.53952219489578,-2.49186278368952,
48.1630235642354));
#55094=CARTESIAN_POINT('Ctrl Pts',(-1.43888124987817,-6.84867515794263,
48.4414474178826));
#55095=CARTESIAN_POINT('Ctrl Pts',(4.98381464565661,-4.91287311539898,48.7198712715296));
#55096=CARTESIAN_POINT('Ctrl Pts',(6.82734403574969,1.53691381924461,48.9982951251769));
#55097=CARTESIAN_POINT('Ctrl Pts',(2.3978582050863,6.57457273886085,49.2767189788239));
#55098=CARTESIAN_POINT('Ctrl Pts',(-4.23479783920031,5.57146461277246,49.5551428324711));
#55099=CARTESIAN_POINT('Ctrl Pts',(-6.97648967207044,-0.550747243085628,
49.8335666861182));
#55100=CARTESIAN_POINT('Ctrl Pts',(-3.30813014804529,-6.16692837593123,
50.1119905397654));
#55101=CARTESIAN_POINT('Ctrl Pts',(3.3997643199154,-6.11688917991012,50.3904143934124));
#55102=CARTESIAN_POINT('Ctrl Pts',(6.9839296753337,-0.446606045933962,50.6688382470596));
#55103=CARTESIAN_POINT('Ctrl Pts',(4.1512077427146,5.63402209323835,50.9472621007067));
#55104=CARTESIAN_POINT('Ctrl Pts',(-2.49567518987983,6.53806821751579,51.2256859543539));
#55105=CARTESIAN_POINT('Ctrl Pts',(-6.84951292507326,1.43488792577199,51.504109808001));
#55106=CARTESIAN_POINT('Ctrl Pts',(-4.90996649670818,-4.98667822016567,
51.7825336616481));
#55107=CARTESIAN_POINT('Ctrl Pts',(1.5408942005697,-6.82644678679344,52.0609575152952));
#55108=CARTESIAN_POINT('Ctrl Pts',(6.57596967842187,-2.3940245317766,52.3393813689425));
#55109=CARTESIAN_POINT('Ctrl Pts',(5.56899459195911,4.23804552889673,52.6178052225894));
#55110=CARTESIAN_POINT('Ctrl Pts',(-0.554814750510634,6.97616737635267,
52.8962290762368));
#55111=CARTESIAN_POINT('Ctrl Pts',(-6.16885611345141,3.30453399465108,53.1746529298836));
#55112=CARTESIAN_POINT('Ctrl Pts',(-6.11490592774493,-3.4033301581101,53.453076783531));
#55113=CARTESIAN_POINT('Ctrl Pts',(-0.442534031138704,-6.98418887928699,
53.7315006371779));
#55114=CARTESIAN_POINT('Ctrl Pts',(5.63644147274139,-4.14792215387804,54.0099244908252));
#55115=CARTESIAN_POINT('Ctrl Pts',(6.53661201758198,2.49948674768936,54.2883483444722));
#55116=CARTESIAN_POINT('Ctrl Pts',(1.43089411388931,6.85034836377748,54.5667721981195));
#55117=CARTESIAN_POINT('Ctrl Pts',(-4.98954009950117,4.90705820892124,54.8451960517665));
#55118=CARTESIAN_POINT('Ctrl Pts',(-6.8255472172519,-1.54487405808249,55.1236199054137));
#55119=CARTESIAN_POINT('Ctrl Pts',(-2.39019004464128,-6.57736438254481,
55.4020437590608));
#55120=CARTESIAN_POINT('Ctrl Pts',(4.24129177791002,-5.56652267801944,55.6804676127079));
#55121=CARTESIAN_POINT('Ctrl Pts',(6.97584270915361,0.558882069331685,55.9588914663551));
#55122=CARTESIAN_POINT('Ctrl Pts',(3.30093671791202,6.17078175392806,56.2373153200021));
#55123=CARTESIAN_POINT('Ctrl Pts',(-3.40689483937537,6.11292059687588,56.5157391736494));
#55124=CARTESIAN_POINT('Ctrl Pts',(-6.98444570903205,0.43846186590818,56.7941630272964));
#55125=CARTESIAN_POINT('Ctrl Pts',(-4.14463515499503,-5.63885893619008,
57.0725868809436));
#55126=CARTESIAN_POINT('Ctrl Pts',(2.50329745582221,-6.53515359558943,57.3510107345907));
#55127=CARTESIAN_POINT('Ctrl Pts',(6.85118147377125,-1.42689981558801,57.6294345882378));
#55128=CARTESIAN_POINT('Ctrl Pts',(4.90414825302692,4.99240028269017,57.907858441885));
#55129=CARTESIAN_POINT('Ctrl Pts',(-1.54885339043013,6.82464532743094,58.1862822955321));
#55130=CARTESIAN_POINT('Ctrl Pts',(-6.57875685075575,2.3863547449836,58.4647061491792));
#55131=CARTESIAN_POINT('Ctrl Pts',(-5.56404887179351,-4.24453658513685,
58.7431300028264));
#55132=CARTESIAN_POINT('Ctrl Pts',(0.562949198166103,-6.97551567058348,
59.0215538564735));
#55133=CARTESIAN_POINT('Ctrl Pts',(6.17270529670647,-3.29733831905118,59.2999777101206));
#55134=CARTESIAN_POINT('Ctrl Pts',(6.11093318797799,3.41045836249916,59.5784015637678));
#55135=CARTESIAN_POINT('Ctrl Pts',(0.434389551626964,6.98470016448157,59.8568254174148));
#55136=CARTESIAN_POINT('Ctrl Pts',(-5.64127448276255,4.14134674718315,60.1352492710621));
#55137=CARTESIAN_POINT('Ctrl Pts',(-6.53369295203398,-2.507107312983,60.4136731247091));
#55138=CARTESIAN_POINT('Ctrl Pts',(-1.42290503222572,-6.85201225477145,
60.6920969783564));
#55139=CARTESIAN_POINT('Ctrl Pts',(4.99525876876051,-4.90123663001426,60.9705208320033));
#55140=CARTESIAN_POINT('Ctrl Pts',(6.82374111763702,1.55283219625988,61.2489446856506));
#55141=CARTESIAN_POINT('Ctrl Pts',(2.38251863410754,6.5801470825812,61.5273685392976));
#55142=CARTESIAN_POINT('Ctrl Pts',(-4.24777994947404,5.56157317412246,61.8057923929448));
#55143=CARTESIAN_POINT('Ctrl Pts',(-6.97518626075355,-0.567016135631398,
62.0842162465919));
#55144=CARTESIAN_POINT('Ctrl Pts',(-3.29373879929166,-6.17462674113279,
62.3626401002391));
#55145=CARTESIAN_POINT('Ctrl Pts',(3.41402072627044,-6.10894370172678,62.6410639538862));
#55146=CARTESIAN_POINT('Ctrl Pts',(6.98495224554912,-0.430317089678943,
62.9194878075333));
#55147=CARTESIAN_POINT('Ctrl Pts',(4.13805693155986,5.64368811163779,63.1979116611804));
#55148=CARTESIAN_POINT('Ctrl Pts',(-2.51091631787676,6.53223008741208,63.4763355148276));
#55149=CARTESIAN_POINT('Ctrl Pts',(-6.85284070649566,1.41890976516039,63.7547593684747));
#55150=CARTESIAN_POINT('Ctrl Pts',(-4.89832334087304,-4.99811555674043,
64.0331832221217));
#55151=CARTESIAN_POINT('Ctrl Pts',(1.55681047421923,-6.82283458817761,64.3116070757691));
#55152=CARTESIAN_POINT('Ctrl Pts',(6.58153507754862,-2.37868171331697,64.5900309294159));
#55153=CARTESIAN_POINT('Ctrl Pts',(5.55909558584776,4.2510218698191,64.8684547830634));
#55154=CARTESIAN_POINT('Ctrl Pts',(-0.571082880344979,6.97485447977578,
65.1468786367103));
#55155=CARTESIAN_POINT('Ctrl Pts',(-6.17654608655382,3.29013815985714,65.4253024903575));
#55156=CARTESIAN_POINT('Ctrl Pts',(-6.10695213879858,-3.41758192947802,
65.7037263440046));
#55157=CARTESIAN_POINT('Ctrl Pts',(-0.426244481448751,-6.98520195214898,
65.9821501976518));
#55158=CARTESIAN_POINT('Ctrl Pts',(5.64609982199524,-4.1347657092437,66.2605740512988));
#55159=CARTESIAN_POINT('Ctrl Pts',(6.53076500222105,2.51472446920854,66.538997904946));
#55160=CARTESIAN_POINT('Ctrl Pts',(1.41491401575025,6.85366682866222,66.8174217585931));
#55161=CARTESIAN_POINT('Ctrl Pts',(-5.00097064565866,4.8954083865937,67.0958456122403));
#55162=CARTESIAN_POINT('Ctrl Pts',(-6.82192573936089,-1.5607882229556,67.3742694658874));
#55163=CARTESIAN_POINT('Ctrl Pts',(-2.37484398391645,-6.58292083518617,
67.6526933195345));
#55164=CARTESIAN_POINT('Ctrl Pts',(4.2542623450698,-5.55661610781171,67.9311171731817));
#55165=CARTESIAN_POINT('Ctrl Pts',(6.97452032776297,0.575149430924237,68.2095410268288));
#55166=CARTESIAN_POINT('Ctrl Pts',(3.28653640197177,6.17846333231709,68.4879648804759));
#55167=CARTESIAN_POINT('Ctrl Pts',(-3.42114197091134,6.10495849987044,68.7663887341231));
#55168=CARTESIAN_POINT('Ctrl Pts',(-6.98544928419626,0.422171728320822,
69.0448125877702));
#55169=CARTESIAN_POINT('Ctrl Pts',(-4.1314730813535,-5.64850961301508,69.3232364414172));
#55170=CARTESIAN_POINT('Ctrl Pts',(2.51853176568377,-6.52929769695893,69.6016602950645));
#55171=CARTESIAN_POINT('Ctrl Pts',(6.85449062099032,-1.41091778535363,69.8800841487114));
#55172=CARTESIAN_POINT('Ctrl Pts',(4.89249176816705,5.00382403454488,70.1585080023588));
#55173=CARTESIAN_POINT('Ctrl Pts',(-1.56476544111709,6.82101457149574,70.4369318560057));
#55174=CARTESIAN_POINT('Ctrl Pts',(-6.58430435502274,2.37100544721029,70.715355709653));
#55175=CARTESIAN_POINT('Ctrl Pts',(-5.55413474085716,-4.25750137412486,
70.9937795633));
#55176=CARTESIAN_POINT('Ctrl Pts',(0.579215785987118,-6.97418380482868,
71.2722034169472));
#55177=CARTESIAN_POINT('Ctrl Pts',(6.18037847777074,-3.28293352685973,71.5506272705943));
#55178=CARTESIAN_POINT('Ctrl Pts',(6.10296278562014,3.42470084936001,71.8290511242415));
#55179=CARTESIAN_POINT('Ctrl Pts',(0.418098831679774,6.98569424160693,72.1074749778885));
#55180=CARTESIAN_POINT('Ctrl Pts',(-5.65091748387798,4.1281790490086,72.3858988315358));
#55181=CARTESIAN_POINT('Ctrl Pts',(-6.52782817212458,-2.52233820600809,
72.6643226851828));
#55182=CARTESIAN_POINT('Ctrl Pts',(-1.40692107532915,-6.85531208319993,
72.9427465388299));
#55183=CARTESIAN_POINT('Ctrl Pts',(5.006675722429,-4.88957348658464,73.2211703924772));
#55184=CARTESIAN_POINT('Ctrl Pts',(6.82010108489192,1.56874212735155,73.4995942461242));
#55185=CARTESIAN_POINT('Ctrl Pts',(2.36716610450353,6.58568563658803,73.7780180997714));
#55186=CARTESIAN_POINT('Ctrl Pts',(-4.26073895588305,5.55165148582763,74.0564419534185));
#55187=CARTESIAN_POINT('Ctrl Pts',(-6.97384491108733,-0.583281944151123,
74.3348658070656));
#55188=CARTESIAN_POINT('Ctrl Pts',(-3.27932953574576,-6.18229152226397,
74.6132896607128));
#55189=CARTESIAN_POINT('Ctrl Pts',(3.42825856361453,-6.10096499672593,74.8917135143599));
#55190=CARTESIAN_POINT('Ctrl Pts',(6.98593682429763,-0.414025792909914,
75.170137368007));
#55191=CARTESIAN_POINT('Ctrl Pts',(4.12488361332866,5.65332343376568,75.4485612216542));
#55192=CARTESIAN_POINT('Ctrl Pts',(-2.52614378888781,6.52635642821742,75.7269850753012));
#55193=CARTESIAN_POINT('Ctrl Pts',(-6.85613121501166,1.40292388703529,76.0054089289485));
#55194=CARTESIAN_POINT('Ctrl Pts',(-4.88665354283862,-5.00952570834149,
76.2838327825954));
#55195=CARTESIAN_POINT('Ctrl Pts',(1.57271828030703,-6.81918527986008,76.5622566362427));
#55196=CARTESIAN_POINT('Ctrl Pts',(6.58706467941239,-2.36332595710137,76.8406804898898));
#55197=CARTESIAN_POINT('Ctrl Pts',(5.54916634356738,4.26397508924365,77.1191043435369));
#55198=CARTESIAN_POINT('Ctrl Pts',(-0.587347904033891,6.9735036466542,77.397528197184));
#55199=CARTESIAN_POINT('Ctrl Pts',(-6.18420246514635,3.27572442985507,77.6759520508313));
#55200=CARTESIAN_POINT('Ctrl Pts',(-6.09896513386704,-3.43181511246536,
77.9543759044783));
#55201=CARTESIAN_POINT('Ctrl Pts',(-0.409952613395948,-6.98617703218592,
78.2327997581254));
#55202=CARTESIAN_POINT('Ctrl Pts',(5.65572746186015,-4.12158677543401,78.5112236117726));
#55203=CARTESIAN_POINT('Ctrl Pts',(6.52488246573783,2.52994851302911,78.7896474654196));
#55204=CARTESIAN_POINT('Ctrl Pts',(1.39892622183076,6.85694801614726,79.0680713190669));
#55205=CARTESIAN_POINT('Ctrl Pts',(-5.01237399131375,4.88373193792135,79.3464951727139));
#55206=CARTESIAN_POINT('Ctrl Pts',(-6.81826715671135,-1.57669389863207,
79.6249190263612));
#55207=CARTESIAN_POINT('Ctrl Pts',(-2.35948500630908,-6.58844148302724,
79.9033428800081));
#55208=CARTESIAN_POINT('Ctrl Pts',(4.26720977310686,-5.54667931492101,80.1817667336555));
#55209=CARTESIAN_POINT('Ctrl Pts',(6.97316001164507,0.591413664253351,80.4601905873024));
#55210=CARTESIAN_POINT('Ctrl Pts',(3.27211821041336,6.18611130576817,80.7386144409497));
#55211=CARTESIAN_POINT('Ctrl Pts',(-3.43537049470339,6.09696319772341,81.0170382945967));
#55212=CARTESIAN_POINT('Ctrl Pts',(-6.9864148651901,0.405879294522616,81.2954621482438));
#55213=CARTESIAN_POINT('Ctrl Pts',(-4.11828853644548,-5.65812956734407,
81.573886001891));
#55214=CARTESIAN_POINT('Ctrl Pts',(2.53375237713854,-6.52340628518699,81.8523098555382));
#55215=CARTESIAN_POINT('Ctrl Pts',(6.85776248632897,-1.39492808107462,82.1307337091853));
#55216=CARTESIAN_POINT('Ctrl Pts',(4.88080867282612,5.01522057037741,82.4091575628324));
#55217=CARTESIAN_POINT('Ctrl Pts',(-1.5806689809751,6.81734671575793,82.6875814164794));
#55218=CARTESIAN_POINT('Ctrl Pts',(-6.58981604696442,2.35564325343243,82.9660052701267));
#55219=CARTESIAN_POINT('Ctrl Pts',(-5.54419040073409,-4.27044300637292,
83.2444291237738));
#55220=CARTESIAN_POINT('Ctrl Pts',(0.595479223427524,-6.97281400617696,
83.522852977421));
#55221=CARTESIAN_POINT('Ctrl Pts',(6.1880180434807,-3.26851087864622,83.801276831068));
#55222=CARTESIAN_POINT('Ctrl Pts',(6.09495918897536,3.43892470912016,84.0797006847152));
#55223=CARTESIAN_POINT('Ctrl Pts',(0.401805837674386,6.98665032322945,84.3581245383623));
#55224=CARTESIAN_POINT('Ctrl Pts',(-5.66052974940107,4.11498889748403,84.6365483920093));
#55225=CARTESIAN_POINT('Ctrl Pts',(-6.52192788706646,-2.53755537992303,
84.9149722456567));
#55226=CARTESIAN_POINT('Ctrl Pts',(-1.39092946612621,-6.8585746252799,85.1933960993035));
#55227=CARTESIAN_POINT('Ctrl Pts',(5.01806544456479,-4.87788374854682,85.4718199529509));
#55228=CARTESIAN_POINT('Ctrl Pts',(6.81642395731267,1.58464352598471,85.7502438065978));
#55229=CARTESIAN_POINT('Ctrl Pts',(2.35180069977754,6.59118837075661,86.0286676602452));
#55230=CARTESIAN_POINT('Ctrl Pts',(-4.27367478794267,5.5416996018528,86.307091513892));
#55231=CARTESIAN_POINT('Ctrl Pts',(-6.97246563036744,-0.59954458017424,
86.5855153675394));
#55232=CARTESIAN_POINT('Ctrl Pts',(-3.26490243578007,-6.1899226776357,86.8639392211865));
#55233=CARTESIAN_POINT('Ctrl Pts',(3.44247775450736,-6.09295310830424,87.1423630748335));
#55234=CARTESIAN_POINT('Ctrl Pts',(6.98688340622387,-0.397732244236107,
87.4207869284808));
#55235=CARTESIAN_POINT('Ctrl Pts',(4.11168785967147,5.66292800721513,87.6992107821278));
#55236=CARTESIAN_POINT('Ctrl Pts',(-2.54135752008998,6.52044727187894,87.977634635775));
#55237=CARTESIAN_POINT('Ctrl Pts',(-6.85938443272403,1.38693037834446,88.2560584894221));
#55238=CARTESIAN_POINT('Ctrl Pts',(-4.87495716607746,-5.02090861290885,
88.5344823430691));
#55239=CARTESIAN_POINT('Ctrl Pts',(1.58861753231004,-6.81549888168934,88.8129061967165));
#55240=CARTESIAN_POINT('Ctrl Pts',(6.59255845393744,-2.34795734665035,89.0913300503635));
#55241=CARTESIAN_POINT('Ctrl Pts',(5.53920691912364,4.27690511671748,89.3697539040107));
#55242=CARTESIAN_POINT('Ctrl Pts',(-0.603609733111337,6.97211488433493,
89.6481777576577));
#55243=CARTESIAN_POINT('Ctrl Pts',(-6.19182520758571,3.26129288304171,89.9266016113048));
#55244=CARTESIAN_POINT('Ctrl Pts',(-6.09094495639199,-3.44602962965707,
90.2050254649521));
#55245=CARTESIAN_POINT('Ctrl Pts',(-0.393658515592726,-6.98711411409408,
90.483449318599));
#55246=CARTESIAN_POINT('Ctrl Pts',(5.66532433997098,-4.10838542413011,90.7618731722463));
#55247=CARTESIAN_POINT('Ctrl Pts',(6.51896444012776,2.54515879634676,91.0402970258934));
#55248=CARTESIAN_POINT('Ctrl Pts',(1.38293081908901,6.86019190838603,91.3187208795406));
#55249=CARTESIAN_POINT('Ctrl Pts',(-5.02375007444307,4.87202892641306,91.5971447331876));
#55250=CARTESIAN_POINT('Ctrl Pts',(-6.81457148920236,-1.59259099860004,
91.8755685868349));
#55251=CARTESIAN_POINT('Ctrl Pts',(-2.34411319535752,-6.59392629604109,
92.1539924404817));
#55252=CARTESIAN_POINT('Ctrl Pts',(4.28013399159945,-5.53671235339405,92.4324162941292));
#55253=CARTESIAN_POINT('Ctrl Pts',(6.97176176819866,0.607674680857242,92.7108401477761));
#55254=CARTESIAN_POINT('Ctrl Pts',(3.25768222165789,6.19372563268397,92.9892640014233));
#55255=CARTESIAN_POINT('Ctrl Pts',(-3.44958033336209,6.08893473392128,93.2676878550705));
#55256=CARTESIAN_POINT('Ctrl Pts',(-6.98734244676171,0.389584653128723,
93.5461117087175));
#55257=CARTESIAN_POINT('Ctrl Pts',(-4.10508159198234,-5.6677187468539,93.8245355623647));
#55258=CARTESIAN_POINT('Ctrl Pts',(2.548959207401,-6.51747939231703,94.1029594160119));
#55259=CARTESIAN_POINT('Ctrl Pts',(6.86099705199147,-1.37893078971957,94.3813832696589));
#55260=CARTESIAN_POINT('Ctrl Pts',(4.86909903054906,5.02658982820138,94.6598071233061));
#55261=CARTESIAN_POINT('Ctrl Pts',(-1.5965639235038,6.81364178016702,94.9382309769533));
#55262=CARTESIAN_POINT('Ctrl Pts',(-6.59529189660259,2.34026824720598,95.2166548306002));
#55263=CARTESIAN_POINT('Ctrl Pts',(-5.53421590551207,-4.28336141149082,
95.4950786842477));
#55264=CARTESIAN_POINT('Ctrl Pts',(0.611739422029957,-6.97140628207867,
95.7735025378944));
#55265=CARTESIAN_POINT('Ctrl Pts',(6.19562395228444,-3.25407045285617,96.051926391542));
#55266=CARTESIAN_POINT('Ctrl Pts',(6.08692244157545,3.45312986441528,96.3303502451886));
#55267=CARTESIAN_POINT('Ctrl Pts',(0.385510658229152,6.98756840414912,96.6087740988361));
#55268=CARTESIAN_POINT('Ctrl Pts',(-5.67011122705018,4.10177636435128,96.8871979524832));
#55269=CARTESIAN_POINT('Ctrl Pts',(-6.51599212895148,-2.55275875196109,
97.1656218061301));
#55270=CARTESIAN_POINT('Ctrl Pts',(-1.37493029159568,-6.86179986326655,
97.4440456597775));
#55271=CARTESIAN_POINT('Ctrl Pts',(5.0294278732187,-4.8661674794814,97.7224695134245));
#55272=CARTESIAN_POINT('Ctrl Pts',(6.8127097548993,1.6005363056711,98.0008933670716));
#55273=CARTESIAN_POINT('Ctrl Pts',(2.33642250350259,6.59665525515757,98.2793172207188));
#55274=CARTESIAN_POINT('Ctrl Pts',(-4.28658737529433,5.53171757632644,98.5577410743658));
#55275=CARTESIAN_POINT('Ctrl Pts',(-6.97104842609587,-0.615803955247596,
98.8361649280132));
#55276=CARTESIAN_POINT('Ctrl Pts',(-3.25045757786441,-6.19752016574172,
99.11458878166));
#55277=CARTESIAN_POINT('Ctrl Pts',(3.45667822160986,-6.08490808003864,99.3930126353075));
#55278=CARTESIAN_POINT('Ctrl Pts',(6.98779198617956,-0.381436532279055,
99.6714364889542));
#55279=CARTESIAN_POINT('Ctrl Pts',(4.09846974236059,5.67250177974641,99.9498603426018));
#55280=CARTESIAN_POINT('Ctrl Pts',(-2.55655742873526,6.51450265053672,100.228284196249));
#55281=CARTESIAN_POINT('Ctrl Pts',(-6.86260034193842,1.3709293260774,100.506708049896));
#55282=CARTESIAN_POINT('Ctrl Pts',(-4.86323427420664,-5.03226420853012,
100.785131903543));
#55283=CARTESIAN_POINT('Ctrl Pts',(1.60450814375138,-6.81177541371608,101.06355575719));
#55284=CARTESIAN_POINT('Ctrl Pts',(6.59801637124282,-2.33257596555462,101.341979610837));
#55285=CARTESIAN_POINT('Ctrl Pts',(5.52921736668622,4.28981188191358,101.620403464484));
#55286=CARTESIAN_POINT('Ctrl Pts',(-0.619868279128679,6.97068820037178,
101.898827318132));
#55287=CARTESIAN_POINT('Ctrl Pts',(-6.19941427241141,3.2468435979106,102.177251171778));
#55288=CARTESIAN_POINT('Ctrl Pts',(-6.08289164999546,-3.46022540373989,
102.455675025426));
#55289=CARTESIAN_POINT('Ctrl Pts',(-0.37736227666324,-6.98801319277683,
102.734098879073));
#55290=CARTESIAN_POINT('Ctrl Pts',(5.6748904041298,-4.09516172713445,103.01252273272));
#55291=CARTESIAN_POINT('Ctrl Pts',(6.51301095757923,2.5603552364321,103.290946586367));
#55292=CARTESIAN_POINT('Ctrl Pts',(1.3669278945249,6.86339848773486,103.569370440014));
#55293=CARTESIAN_POINT('Ctrl Pts',(-5.03509883317134,4.86029941572203,103.847794293661));
#55294=CARTESIAN_POINT('Ctrl Pts',(-6.81083875693507,-1.60847943639435,
104.126218147308));
#55295=CARTESIAN_POINT('Ctrl Pts',(-2.32872863466976,-6.59937524439553,
104.404642000956));
#55296=CARTESIAN_POINT('Ctrl Pts',(4.29303493025233,-5.52671527744145,104.683065854603));
#55297=CARTESIAN_POINT('Ctrl Pts',(6.97032560502893,0.623932392291463,104.96148970825));
#55298=CARTESIAN_POINT('Ctrl Pts',(3.24322851422338,6.20130627164954,105.239913561897));
#55299=CARTESIAN_POINT('Ctrl Pts',(-3.4637714095994,6.08087315213145,105.518337415544));
#55300=CARTESIAN_POINT('Ctrl Pts',(-6.98823202386593,0.37328789276662,105.796761269191));
#55301=CARTESIAN_POINT('Ctrl Pts',(-4.09185231979714,-5.6772770993886,106.075185122838));
#55302=CARTESIAN_POINT('Ctrl Pts',(2.56415217376077,-6.51151705058585,106.353608976486));
#55303=CARTESIAN_POINT('Ctrl Pts',(6.86419430038473,-1.36292599829824,106.632032830133));
#55304=CARTESIAN_POINT('Ctrl Pts',(4.85736290502502,5.03793174617901,106.91045668378));
#55305=CARTESIAN_POINT('Ctrl Pts',(-1.61245018225011,6.80989978487445,107.188880537427));
#55306=CARTESIAN_POINT('Ctrl Pts',(-6.60073187415369,2.32488051215605,107.467304391074));
#55307=CARTESIAN_POINT('Ctrl Pts',(-5.52421130944283,-4.29625651921488,
107.745728244721));
#55308=CARTESIAN_POINT('Ctrl Pts',(0.627996293354289,-6.96996064019049,
108.024152098368));
#55309=CARTESIAN_POINT('Ctrl Pts',(6.20319616281283,-3.2396123280318,108.302575952016));
#55310=CARTESIAN_POINT('Ctrl Pts',(6.07885258713292,3.46731623798289,108.580999805663));
#55311=CARTESIAN_POINT('Ctrl Pts',(0.369213381974334,6.98844847937241,108.85942365931));
#55312=CARTESIAN_POINT('Ctrl Pts',(-5.67966186471135,4.08854152147376,109.137847512957));
#55313=CARTESIAN_POINT('Ctrl Pts',(-6.51002093006455,-2.56794823943043,
109.416271366604));
#55314=CARTESIAN_POINT('Ctrl Pts',(-1.35892363875792,-6.86498777961741,
109.694695220251));
#55315=CARTESIAN_POINT('Ctrl Pts',(5.04076294658997,-4.85442474311395,109.973119073898));
#55316=CARTESIAN_POINT('Ctrl Pts',(6.80895849785357,1.61642037996899,110.251542927545));
#55317=CARTESIAN_POINT('Ctrl Pts',(2.32103159932129,6.60208626005625,110.529966781192));
#55318=CARTESIAN_POINT('Ctrl Pts',(-4.29947664770616,5.52170546354129,110.80839063484));
#55319=CARTESIAN_POINT('Ctrl Pts',(-6.96959330598069,-0.632059980935899,
111.086814488487));
#55320=CARTESIAN_POINT('Ctrl Pts',(-3.23599504056484,-6.20508394525901,
111.365238342134));
#55321=CARTESIAN_POINT('Ctrl Pts',(3.47085988768531,-6.07682995568647,111.643662195781));
#55322=CARTESIAN_POINT('Ctrl Pts',(6.98866255922268,-0.365138745671669,
111.922086049428));
#55323=CARTESIAN_POINT('Ctrl Pts',(4.08522933328995,5.68204469928737,112.200509903075));
#55324=CARTESIAN_POINT('Ctrl Pts',(-2.57174343215052,6.50852259652388,112.478933756722));
#55325=CARTESIAN_POINT('Ctrl Pts',(-6.86577892516314,1.35492081726468,112.75735761037));
#55326=CARTESIAN_POINT('Ctrl Pts',(-4.85148493098777,-5.04359243344176,
113.035781464017));
#55327=CARTESIAN_POINT('Ctrl Pts',(1.62039002820123,-6.80801489619239,113.314205317664));
#55328=CARTESIAN_POINT('Ctrl Pts',(6.60343840164274,-2.31718189747404,113.592629171311));
#55329=CARTESIAN_POINT('Ctrl Pts',(5.5191977405888,4.30269531463148,113.871053024958));
#55330=CARTESIAN_POINT('Ctrl Pts',(-0.636123453654769,6.9692236025243,114.149476878605));
#55331=CARTESIAN_POINT('Ctrl Pts',(-6.20696961834626,3.23237665305234,114.427900732252));
#55332=CARTESIAN_POINT('Ctrl Pts',(-6.07480525847982,-3.47440235750226,
114.706324585899));
#55333=CARTESIAN_POINT('Ctrl Pts',(-0.361063985243409,-6.98887426334396,
114.984748439546));
#55334=CARTESIAN_POINT('Ctrl Pts',(5.68442560230666,-4.08191575637137,115.263172293194));
#55335=CARTESIAN_POINT('Ctrl Pts',(6.50702205047326,2.57553775063117,115.541596146841));
#55336=CARTESIAN_POINT('Ctrl Pts',(1.35091753517889,6.86656773675302,115.820020000488));
#55337=CARTESIAN_POINT('Ctrl Pts',(-5.04642020577243,4.84854346964561,116.098443854135));
#55338=CARTESIAN_POINT('Ctrl Pts',(-6.80706898021171,-1.62435912559722,
116.376867707782));
#55339=CARTESIAN_POINT('Ctrl Pts',(-2.3133314079231,-6.60478829845354,116.655291561429));
#55340=CARTESIAN_POINT('Ctrl Pts',(4.30591251889657,-5.51668814143787,116.933715415077));
#55341=CARTESIAN_POINT('Ctrl Pts',(6.96885152994704,0.640186710129389,117.212139268724));
#55342=CARTESIAN_POINT('Ctrl Pts',(3.22875716672446,6.20885318143358,117.490563122371));
#55343=CARTESIAN_POINT('Ctrl Pts',(-3.47794364622938,6.07277849620123,117.768986976018));
#55344=CARTESIAN_POINT('Ctrl Pts',(-6.9890835916643,0.356989102074914,118.047410829665));
#55345=CARTESIAN_POINT('Ctrl Pts',(-4.07860079184459,-5.68680457295987,
118.325834683312));
#55346=CARTESIAN_POINT('Ctrl Pts',(2.57933119358243,-6.5055192924227,118.604258536959));
#55347=CARTESIAN_POINT('Ctrl Pts',(6.86735421411885,-1.34691379386167,118.882682390606));
#55348=CARTESIAN_POINT('Ctrl Pts',(4.84560036008754,5.04924626262106,119.161106244254));
#55349=CARTESIAN_POINT('Ctrl Pts',(-1.62832767080822,6.80612075023288,119.439530097901));
#55350=CARTESIAN_POINT('Ctrl Pts',(-6.60613595002934,2.30948013197741,119.717953951548));
#55351=CARTESIAN_POINT('Ctrl Pts',(-5.51417666694228,-4.30912825940853,
119.996377805195));
#55352=CARTESIAN_POINT('Ctrl Pts',(0.644249748980212,-6.96847708837439,
120.274801658842));
#55353=CARTESIAN_POINT('Ctrl Pts',(6.21073463387792,-3.22513658281319,120.553225512489));
#55354=CARTESIAN_POINT('Ctrl Pts',(6.0707496695447,3.48148375266606,120.831649366136));
#55355=CARTESIAN_POINT('Ctrl Pts',(0.352914097542206,6.98929054410621,121.110073219783));
#55356=CARTESIAN_POINT('Ctrl Pts',(-5.68918161042058,4.07528444084858,121.38849707343));
#55357=CARTESIAN_POINT('Ctrl Pts',(-6.5040143229163,-2.58312375973728,121.666920927078));
#55358=CARTESIAN_POINT('Ctrl Pts',(-1.34290959461152,-6.86813835695045,
121.945344780725));
#55359=CARTESIAN_POINT('Ctrl Pts',(5.05207060290854,-4.84265560339497,122.223768634372));
#55360=CARTESIAN_POINT('Ctrl Pts',(6.80517020680153,1.63229566263774,122.502192488019));
#55361=CARTESIAN_POINT('Ctrl Pts',(2.30562807052473,6.60748135562364,122.780616341666));
#55362=CARTESIAN_POINT('Ctrl Pts',(-4.31234253427801,5.51166331850034,123.059040195313));
#55363=CARTESIAN_POINT('Ctrl Pts',(-6.96810027943676,-0.648312569854052,
123.337464048961));
#55364=CARTESIAN_POINT('Ctrl Pts',(-3.22151489971119,-6.21261397309853,
123.615887902608));
#55365=CARTESIAN_POINT('Ctrl Pts',(3.48502267025022,-6.0687187828655,123.894311756255));
#55366=CARTESIAN_POINT('Ctrl Pts',(6.98949513071799,-0.348838966108577,
124.172735609902));
#55367=CARTESIAN_POINT('Ctrl Pts',(4.07196668540431,5.69155670081135,124.451159463549));
#55368=CARTESIAN_POINT('Ctrl Pts',(-2.58691541173027,6.5025071671437,124.729583317196));
#55369=CARTESIAN_POINT('Ctrl Pts',(-6.86892023310093,1.33890489219211,125.008007170843));
#55370=CARTESIAN_POINT('Ctrl Pts',(-4.83970907194496,-5.0548931376893,125.28643102449));
#55371=CARTESIAN_POINT('Ctrl Pts',(1.63626285686831,-6.80421751637518,125.564854878138));
#55372=CARTESIAN_POINT('Ctrl Pts',(6.60882497336411,-2.30177491117929,125.843278731785));
#55373=CARTESIAN_POINT('Ctrl Pts',(5.50914723106459,4.31555475009168,126.121702585432));
#55374=CARTESIAN_POINT('Ctrl Pts',(-0.652373536370679,6.96772222168401,
126.400126439079));
#55375=CARTESIAN_POINT('Ctrl Pts',(-6.21449428566708,3.21789000684206,126.678550292726));
#55376=CARTESIAN_POINT('Ctrl Pts',(-6.06668000757257,-3.48855641025641,
126.956974146373));
#55377=CARTESIAN_POINT('Ctrl Pts',(-0.344774716028633,-6.98970488068336,
127.23539800002));
#55378=CARTESIAN_POINT('Ctrl Pts',(5.69395062653325,-4.068633309877,127.513821853667));
#55379=CARTESIAN_POINT('Ctrl Pts',(6.50095858268405,2.59067930412174,127.792245707314));
#55380=CARTESIAN_POINT('Ctrl Pts',(1.3349737866748,6.86975052961293,128.070669560962));
#55381=CARTESIAN_POINT('Ctrl Pts',(-5.05785378002051,4.83666505803512,128.349093414609));
#55382=CARTESIAN_POINT('Ctrl Pts',(-6.80299848840007,-1.64004852846079,
128.627517268256));
#55383=CARTESIAN_POINT('Ctrl Pts',(-2.29841954027217,-6.61050809651445,
128.905941121903));
#55384=CARTESIAN_POINT('Ctrl Pts',(4.31970722031227,-5.50598355952033,129.18436497555));
#55385=CARTESIAN_POINT('Ctrl Pts',(6.96556103235851,0.655211661793067,129.462788829197));
#55386=CARTESIAN_POINT('Ctrl Pts',(3.21764772889245,6.21870871851334,129.741212682844));
#55387=CARTESIAN_POINT('Ctrl Pts',(-3.49865171312285,6.06000128588926,130.019636536492));
#55388=CARTESIAN_POINT('Ctrl Pts',(-6.39654705541885,1.30279187935603,130.251656414531));
#55389=CARTESIAN_POINT('Ctrl Pts',(-5.53817824125726,-2.69171018261493,
130.437272316962));
#55390=CARTESIAN_POINT('Ctrl Pts',(-4.23949710241608,-4.24338993046111,
130.530080268178));
#55391=CARTESIAN_POINT('Ctrl Pts',(-3.43710408716141,-4.81604049573073,
130.576484243786));
#55392=CARTESIAN_POINT('Ctrl Pts',(-2.85711522928025,-4.00149011032068,
-10.));
#55393=CARTESIAN_POINT('Ctrl Pts',(-2.41648365696274,-4.31442211364657,
-9.96932881922757));
#55394=CARTESIAN_POINT('Ctrl Pts',(-1.17990489524751,-4.91804358772338,
-9.89225366284727));
#55395=CARTESIAN_POINT('Ctrl Pts',(1.92453937789233,-5.07348089440844,-9.72237055525127));
#55396=CARTESIAN_POINT('Ctrl Pts',(5.43970692864372,-2.05961707410548,-9.49035067721199));
#55397=CARTESIAN_POINT('Ctrl Pts',(4.67141455431437,3.47170793039274,-9.21192682356487));
#55398=CARTESIAN_POINT('Ctrl Pts',(-0.394303111254869,5.8022423708097,-8.93350296991773));
#55399=CARTESIAN_POINT('Ctrl Pts',(-4.31724444146487,3.30287017342899,-8.70114717405969));
#55400=CARTESIAN_POINT('Ctrl Pts',(-4.90982483510101,0.82872126176219,-8.56159932941736));
#55401=CARTESIAN_POINT('Ctrl Pts',(-4.91001919821333,6.39834157814545E-5,
-8.51485943599074));
#55402=CARTESIAN_POINT('Ctrl Pts',(-5.90701629014678,0.000721185244744792,
126.811624807795));
#55403=CARTESIAN_POINT('Ctrl Pts',(-5.90589710669071,-1.0324812503633,126.860074587321));
#55404=CARTESIAN_POINT('Ctrl Pts',(-5.6483729107334,-2.06620547501384,126.908524366847));
#55405=CARTESIAN_POINT('Ctrl Pts',(-5.1376648386644,-2.95434008581106,126.956974146373));
#55406=CARTESIAN_POINT('Ctrl Pts',(-4.15937824372468,-4.65560590039867,
127.049782097589));
#55407=CARTESIAN_POINT('Ctrl Pts',(-2.25207647987663,-5.82265539054102,
127.142590048805));
#55408=CARTESIAN_POINT('Ctrl Pts',(-0.29197137419231,-5.91933487381112,
127.23539800002));
#55409=CARTESIAN_POINT('Ctrl Pts',(1.66813373149212,-6.01601435708123,127.328205951236));
#55410=CARTESIAN_POINT('Ctrl Pts',(3.68104217901263,-5.04232383347917,127.421013902452));
#55411=CARTESIAN_POINT('Ctrl Pts',(4.82199772879814,-3.44559313601152,127.513821853667));
#55412=CARTESIAN_POINT('Ctrl Pts',(5.96295327858346,-1.84886243854414,127.606629804883));
#55413=CARTESIAN_POINT('Ctrl Pts',(6.23195593063374,0.370908432788888,127.699437756099));
#55414=CARTESIAN_POINT('Ctrl Pts',(5.50545979065741,2.19397240603706,127.792245707315));
#55415=CARTESIAN_POINT('Ctrl Pts',(4.77896365068096,4.01703637928555,127.88505365853));
#55416=CARTESIAN_POINT('Ctrl Pts',(3.05696871867794,5.44339345444921,127.977861609746));
#55417=CARTESIAN_POINT('Ctrl Pts',(1.13049999156036,5.81772441343478,128.070669560962));
#55418=CARTESIAN_POINT('Ctrl Pts',(-0.79596873555699,6.19205537242031,128.163477512177));
#55419=CARTESIAN_POINT('Ctrl Pts',(-2.92691125778872,5.51436021522773,128.256285463393));
#55420=CARTESIAN_POINT('Ctrl Pts',(-4.28323997030115,4.09606037221553,128.349093414609));
#55421=CARTESIAN_POINT('Ctrl Pts',(-5.31857665971544,3.01341878945275,128.419937212337));
#55422=CARTESIAN_POINT('Ctrl Pts',(-5.90255806307964,1.49923850233953,128.490781010066));
#55423=CARTESIAN_POINT('Ctrl Pts',(-5.91642361182645,-0.00541095714722729,
128.561624807795));
#55424=CARTESIAN_POINT('Origin',(0.,0.,-13.2351405640096));
#55425=CARTESIAN_POINT('Ctrl Pts',(2.85706463458369,-4.00329423554042,-10.));
#55426=CARTESIAN_POINT('Ctrl Pts',(3.52391651473643,-3.52737645103792,-9.95360512071162));
#55427=CARTESIAN_POINT('Ctrl Pts',(4.6032797975914,-2.23787345781402,-9.86081536213486));
#55428=CARTESIAN_POINT('Ctrl Pts',(5.31710770646798,1.0817198372055,-9.67523584498136));
#55429=CARTESIAN_POINT('Ctrl Pts',(2.91000325553484,5.03585724930024,-9.44326144853946));
#55430=CARTESIAN_POINT('Ctrl Pts',(-2.67142550958262,5.17047615300083,-9.16489217280919));
#55431=CARTESIAN_POINT('Ctrl Pts',(-4.84847440842237,1.94359242658305,-8.97051854463248));
#55432=CARTESIAN_POINT('Ctrl Pts',(-4.92512433492993,0.157117410974401,
-8.86893467503253));
#55433=CARTESIAN_POINT('Ctrl Pts',(-4.9240923050422,0.00237935796991912,
-8.86014056400933));
#55434=CARTESIAN_POINT('Ctrl Pts',(3.4371040871608,-4.81604049573117,-10.5764842437858));
#55435=CARTESIAN_POINT('Ctrl Pts',(4.23933981366781,-4.24350218404385,-10.5300893644975));
#55436=CARTESIAN_POINT('Ctrl Pts',(5.53783474658711,-2.69220510984897,-10.4372996059207));
#55437=CARTESIAN_POINT('Ctrl Pts',(6.39658354541614,1.30132991344342,-10.2517200887672));
#55438=CARTESIAN_POINT('Ctrl Pts',(3.50079027340594,6.05823379856682,-10.0197456923253));
#55439=CARTESIAN_POINT('Ctrl Pts',(-3.21377662457789,6.22018294683352,-9.74137641659503));
#55440=CARTESIAN_POINT('Ctrl Pts',(-6.96458399641983,0.660629702264095,
-9.46300714086476));
#55441=CARTESIAN_POINT('Ctrl Pts',(-4.3248127554248,-5.50138505625064,-9.18463786513449));
#55442=CARTESIAN_POINT('Ctrl Pts',(2.29049378023627,-6.61276642800579,-8.90626858940423));
#55443=CARTESIAN_POINT('Ctrl Pts',(6.80029139153989,-1.64926970870278,-8.62789931367396));
#55444=CARTESIAN_POINT('Ctrl Pts',(5.06509383187957,4.82841021736868,-8.3495300379437));
#55445=CARTESIAN_POINT('Ctrl Pts',(-1.32276848152976,6.87163827279611,-8.07116076221342));
#55446=CARTESIAN_POINT('Ctrl Pts',(-6.49543867311718,2.60324077919988,-7.79279148648315));
#55447=CARTESIAN_POINT('Ctrl Pts',(-5.70232919786885,-4.05608148955149,
-7.51442221075289));
#55448=CARTESIAN_POINT('Ctrl Pts',(0.328315906814816,-6.99003262884612,
-7.23605293502261));
#55449=CARTESIAN_POINT('Ctrl Pts',(6.05737171330259,-3.50376713762688,-6.95768365929234));
#55450=CARTESIAN_POINT('Ctrl Pts',(6.22288606259671,3.20061689120149,-6.67931438356208));
#55451=CARTESIAN_POINT('Ctrl Pts',(0.672806576516693,6.96531258652612,-6.4009451078318));
#55452=CARTESIAN_POINT('Ctrl Pts',(-5.49522514782519,4.33251896898317,-6.12257583210154));
#55453=CARTESIAN_POINT('Ctrl Pts',(-6.61601726927951,-2.27959531258102,
-5.84420655637128));
#55454=CARTESIAN_POINT('Ctrl Pts',(-1.66014241893913,-6.79795287504758,
-5.565837280641));
#55455=CARTESIAN_POINT('Ctrl Pts',(4.82053563726988,-5.0725406571401,-5.28746800491073));
#55456=CARTESIAN_POINT('Ctrl Pts',(6.87365889457675,1.31188753052232,-5.00909872918046));
#55457=CARTESIAN_POINT('Ctrl Pts',(2.61347841437683,6.49137623247661,-4.73072945345019));
#55458=CARTESIAN_POINT('Ctrl Pts',(-4.047123996549,5.70867950871538,-4.45236017771992));
#55459=CARTESIAN_POINT('Ctrl Pts',(-6.99053269373454,-0.3173128977453,-4.17399090198966));
#55460=CARTESIAN_POINT('Ctrl Pts',(-3.51329185906621,-6.05186045779054,
-3.89562162625939));
#55461=CARTESIAN_POINT('Ctrl Pts',(3.19082973901377,-6.22790817328656,-3.61725235052912));
#55462=CARTESIAN_POINT('Ctrl Pts',(6.96424488227746,-0.683760135240154,
-3.33888307479885));
#55463=CARTESIAN_POINT('Ctrl Pts',(4.34115529651584,5.48840645098574,-3.06051379906858));
#55464=CARTESIAN_POINT('Ctrl Pts',(-2.26918930552874,6.61959323301065,-2.78214452333831));
#55465=CARTESIAN_POINT('Ctrl Pts',(-6.79533377574579,1.67083020092733,-2.50377524760804));
#55466=CARTESIAN_POINT('Ctrl Pts',(-5.08011463276461,-4.81255337613399,
-2.22540597187778));
#55467=CARTESIAN_POINT('Ctrl Pts',(1.30107731735387,-6.87571323530137,-1.9470366961475));
#55468=CARTESIAN_POINT('Ctrl Pts',(6.48725855983418,-2.62368272834031,-1.66866742041724));
#55469=CARTESIAN_POINT('Ctrl Pts',(5.715036454269,4.03814227174553,-1.39029814468696));
#55470=CARTESIAN_POINT('Ctrl Pts',(-0.306320093554309,6.99102300674048,
-1.1119288689567));
#55471=CARTESIAN_POINT('Ctrl Pts',(-6.04632841794436,3.5228039035726,-0.833559593226426));
#55472=CARTESIAN_POINT('Ctrl Pts',(-6.23291796674688,-3.18103258398395,
-0.555190317496161));
#55473=CARTESIAN_POINT('Ctrl Pts',(-0.694710370832787,-6.96316107678336,
-0.276821041765888));
#55474=CARTESIAN_POINT('Ctrl Pts',(5.48157331859047,-4.34978029715457,0.0015482339643776));
#55475=CARTESIAN_POINT('Ctrl Pts',(6.62315328652935,2.25877737365066,0.27991750969465));
#55476=CARTESIAN_POINT('Ctrl Pts',(1.68151360901781,6.79269804004795,0.558286785424916));
#55477=CARTESIAN_POINT('Ctrl Pts',(-4.80455908671799,5.08767595890522,0.836656061155189));
#55478=CARTESIAN_POINT('Ctrl Pts',(-6.87775064266443,-1.29026384042682,
1.11502533688545));
#55479=CARTESIAN_POINT('Ctrl Pts',(-2.63388051878106,-6.48312487103019,
1.39339461261573));
#55480=CARTESIAN_POINT('Ctrl Pts',(4.02915054287043,-5.72137925534322,1.67176388834599));
#55481=CARTESIAN_POINT('Ctrl Pts',(6.99149604335227,0.295326525009105,1.95013316407626));
#55482=CARTESIAN_POINT('Ctrl Pts',(3.53230723199496,6.04078143118759,2.22850243980653));
#55483=CARTESIAN_POINT('Ctrl Pts',(-3.17122756047482,6.23791234631183,2.5068717155368));
#55484=CARTESIAN_POINT('Ctrl Pts',(-6.96206005518643,0.705658889664277,
2.78524099126707));
#55485=CARTESIAN_POINT('Ctrl Pts',(-4.35839454142477,-5.47472663261496,
3.06361026699734));
#55486=CARTESIAN_POINT('Ctrl Pts',(2.24835985613929,-6.62669696288323,3.34197954272761));
#55487=CARTESIAN_POINT('Ctrl Pts',(6.79004550846843,-1.69219285943192,3.62034881845788));
#55488=CARTESIAN_POINT('Ctrl Pts',(5.09522470478115,4.79655291729097,3.89871809418815));
#55489=CARTESIAN_POINT('Ctrl Pts',(-1.27944717303976,6.87977104357299,4.17708736991841));
#55490=CARTESIAN_POINT('Ctrl Pts',(-6.47897515162715,2.64407179652568,4.45545664564868));
#55491=CARTESIAN_POINT('Ctrl Pts',(-5.72770790931377,-4.02014885124534,
4.73382592137895));
#55492=CARTESIAN_POINT('Ctrl Pts',(0.284332226209421,-6.99195179229115,
5.01219519710922));
#55493=CARTESIAN_POINT('Ctrl Pts',(6.03521950757322,-3.54180182618849,5.29056447283949));
#55494=CARTESIAN_POINT('Ctrl Pts',(6.24289130157187,3.16141469556638,5.56893374856976));
#55495=CARTESIAN_POINT('Ctrl Pts',(0.716605663635154,6.96094181870749,5.84730302430003));
#55496=CARTESIAN_POINT('Ctrl Pts',(-5.46786640944469,4.36699800882151,6.12567230003029));
#55497=CARTESIAN_POINT('Ctrl Pts',(-6.63022425359814,-2.23793677917492,
6.40404157576057));
#55498=CARTESIAN_POINT('Ctrl Pts',(-1.70286792561071,-6.78737618734301,
6.68241085149083));
#55499=CARTESIAN_POINT('Ctrl Pts',(4.78853488756881,-5.10276085184492,6.96078012722111));
#55500=CARTESIAN_POINT('Ctrl Pts',(6.88177443307402,1.26862734200135,7.23914940295137));
#55501=CARTESIAN_POINT('Ctrl Pts',(2.6542565363518,6.47480941185285,7.51751867868164));
#55502=CARTESIAN_POINT('Ctrl Pts',(-4.01113721911641,5.73402240054953,7.79588795441191));
#55503=CARTESIAN_POINT('Ctrl Pts',(-6.99239025243653,-0.273337224349726,
8.07425723014218));
#55504=CARTESIAN_POINT('Ctrl Pts',(-3.5512876626729,-6.02964266084915,8.35262650587245));
#55505=CARTESIAN_POINT('Ctrl Pts',(3.15159401352083,-6.24785482021824,8.63099578160272));
#55506=CARTESIAN_POINT('Ctrl Pts',(6.95980637011251,-0.727550665676303,
8.90936505733298));
#55507=CARTESIAN_POINT('Ctrl Pts',(4.37559067807077,5.46099266604204,9.18773433306327));
#55508=CARTESIAN_POINT('Ctrl Pts',(-2.22750816853013,6.63373514995257,9.4661036087935));
#55509=CARTESIAN_POINT('Ctrl Pts',(-6.78469008327218,1.71353878115812,9.74447288452382));
#55510=CARTESIAN_POINT('Ctrl Pts',(-5.11028438146206,-4.78050501737731,
10.022842160254));
#55511=CARTESIAN_POINT('Ctrl Pts',(1.25780437406543,-6.88376080621389,10.3012114359844));
#55512=CARTESIAN_POINT('Ctrl Pts',(6.47062766200786,-2.66443471307583,10.5795807117146));
#55513=CARTESIAN_POINT('Ctrl Pts',(5.74032271343675,4.00211566876656,10.8579499874449));
#55514=CARTESIAN_POINT('Ctrl Pts',(-0.262341546617244,6.99281142270426,
11.1363192631751));
#55515=CARTESIAN_POINT('Ctrl Pts',(-6.02405090480507,3.56076471799275,11.4146885389054));
#55516=CARTESIAN_POINT('Ctrl Pts',(-6.25280288997779,-3.14176553862156,
11.6930578146357));
#55517=CARTESIAN_POINT('Ctrl Pts',(-0.738493868724291,-6.95865371220909,
11.9714270903659));
#55518=CARTESIAN_POINT('Ctrl Pts',(5.45410541940353,-4.38417252792563,12.2497963660962));
#55519=CARTESIAN_POINT('Ctrl Pts',(6.63722964326527,2.21707404999144,12.5281656418265));
#55520=CARTESIAN_POINT('Ctrl Pts',(1.72420539968851,6.78198720289781,12.8065349175568));
#55521=CARTESIAN_POINT('Ctrl Pts',(-4.77246332657172,5.11779527502935,13.084904193287));
#55522=CARTESIAN_POINT('Ctrl Pts',(-6.88573015808093,-1.24697829599372,
13.3632734690173));
#55523=CARTESIAN_POINT('Ctrl Pts',(-2.67460630153053,-6.4664299124322,13.6416427447476));
#55524=CARTESIAN_POINT('Ctrl Pts',(3.99308422250307,-5.74660883239687,13.9200120204778));
#55525=CARTESIAN_POINT('Ctrl Pts',(6.99321530205292,0.251345220200505,14.1983812962081));
#55526=CARTESIAN_POINT('Ctrl Pts',(3.57023296871443,6.01844425326751,14.4767505719383));
#55527=CARTESIAN_POINT('Ctrl Pts',(-3.13192929517096,6.25773549861567,14.7551198476687));
#55528=CARTESIAN_POINT('Ctrl Pts',(-6.95748384784736,0.749435245720291,
15.0334891233989));
#55529=CARTESIAN_POINT('Ctrl Pts',(-4.39274353716615,-5.44720468655893,
15.3118583991292));
#55530=CARTESIAN_POINT('Ctrl Pts',(2.2066344493589,-6.64070772489554,15.5902276748594));
#55531=CARTESIAN_POINT('Ctrl Pts',(6.77926755290319,-1.73486775482704,15.8685969505897));
#55532=CARTESIAN_POINT('Ctrl Pts',(5.12529351397489,4.7644098350364,16.14696622632));
#55533=CARTESIAN_POINT('Ctrl Pts',(-1.23614913455534,6.88768248380563,16.4253355020503));
#55534=CARTESIAN_POINT('Ctrl Pts',(-6.46221617350552,2.68477127656499,16.7037047777805));
#55535=CARTESIAN_POINT('Ctrl Pts',(-5.75288074188647,-3.9840429026576,16.9820740535108));
#55536=CARTESIAN_POINT('Ctrl Pts',(0.240348272289746,-6.99360188948385,
17.2604433292411));
#55537=CARTESIAN_POINT('Ctrl Pts',(6.01282272009998,-3.57969239142614,17.5388126049713));
#55538=CARTESIAN_POINT('Ctrl Pts',(6.26265263393503,3.12208530749102,17.8171818807016));
#55539=CARTESIAN_POINT('Ctrl Pts',(0.760374769609702,6.95629677992002,18.0955511564318));
#55540=CARTESIAN_POINT('Ctrl Pts',(-5.44029048457163,4.40130368459892,18.3739204321622));
#55541=CARTESIAN_POINT('Ctrl Pts',(-6.64416938624315,-2.1961893924464,18.6522897078924));
#55542=CARTESIAN_POINT('Ctrl Pts',(-1.74552582020905,-6.77653114001317,
18.9306589836227));
#55543=CARTESIAN_POINT('Ctrl Pts',(4.75634456268516,-5.13277907975786,19.2090282593529));
#55544=CARTESIAN_POINT('Ctrl Pts',(6.88961777856047,1.22531691652745,19.4873975350832));
#55545=CARTESIAN_POINT('Ctrl Pts',(2.69492961304441,6.45798645564707,19.7657668108135));
#55546=CARTESIAN_POINT('Ctrl Pts',(-3.97499173158654,5.75913842639707,20.0441360865438));
#55547=CARTESIAN_POINT('Ctrl Pts',(-6.99397118404114,-0.22935073007701,
20.322505362274));
#55548=CARTESIAN_POINT('Ctrl Pts',(-3.58914296273775,-6.00718631920259,
20.6008746380043));
#55549=CARTESIAN_POINT('Ctrl Pts',(3.11223359992263,-6.26755428377747,20.8792439137345));
#55550=CARTESIAN_POINT('Ctrl Pts',(6.9550925113623,-0.771312413342824,21.1576131894649));
#55551=CARTESIAN_POINT('Ctrl Pts',(4.40985294905754,5.43336283053807,21.4359824651951));
#55552=CARTESIAN_POINT('Ctrl Pts',(-2.18573890508088,6.64761461874863,21.7143517409254));
#55553=CARTESIAN_POINT('Ctrl Pts',(-6.77377797099395,1.75617956948081,21.9927210166556));
#55554=CARTESIAN_POINT('Ctrl Pts',(-5.1402519538691,-4.74826752946058,22.2710902923859));
#55555=CARTESIAN_POINT('Ctrl Pts',(1.21448166869439,-6.89153603756012,22.5494595681161));
#55556=CARTESIAN_POINT('Ctrl Pts',(6.45374076931547,-2.70508128585077,22.8278288438465));
#55557=CARTESIAN_POINT('Ctrl Pts',(5.76538187045557,3.96593073167031,23.1061981195766));
#55558=CARTESIAN_POINT('Ctrl Pts',(-0.218352620755356,6.99432318481166,
23.384567395307));
#55559=CARTESIAN_POINT('Ctrl Pts',(-6.00153506451229,3.59858465928122,23.6629366710372));
#55560=CARTESIAN_POINT('Ctrl Pts',(-6.27244043602289,-3.10237419682568,
23.9413059467676));
#55561=CARTESIAN_POINT('Ctrl Pts',(-0.782248149874517,-6.95387104515194,
24.2196752224977));
#55562=CARTESIAN_POINT('Ctrl Pts',(5.42642174158814,-4.41839130940257,24.4980444982281));
#55563=CARTESIAN_POINT('Ctrl Pts',(6.651043413893,2.17528301310316,24.7764137739583));
#55564=CARTESIAN_POINT('Ctrl Pts',(1.76682897629888,6.77100805265326,25.0547830496886));
#55565=CARTESIAN_POINT('Ctrl Pts',(-4.74017875533462,5.14771211783052,25.3331523254189));
#55566=CARTESIAN_POINT('Ctrl Pts',(-6.89343725606137,-1.20364341784837,
25.6115216011491));
#55567=CARTESIAN_POINT('Ctrl Pts',(-2.71522626988215,-6.44947912500898,
25.8898908768794));
#55568=CARTESIAN_POINT('Ctrl Pts',(3.95685992531394,-5.77161105862387,26.1682601526097));
#55569=CARTESIAN_POINT('Ctrl Pts',(6.99465789092502,0.207353971519667,26.4466294283399));
#55570=CARTESIAN_POINT('Ctrl Pts',(3.60801745771017,5.99586897000287,26.7249987040702));
#55571=CARTESIAN_POINT('Ctrl Pts',(-3.09250712257939,6.27731107858934,27.0033679798005));
#55572=CARTESIAN_POINT('Ctrl Pts',(-6.95263238430926,0.79318195216411,27.2817372555308));
#55573=CARTESIAN_POINT('Ctrl Pts',(-4.42691874452137,-5.41946723488482,
27.560106531261));
#55574=CARTESIAN_POINT('Ctrl Pts',(2.16482174236717,-6.65445576319799,27.8384758069913));
#55575=CARTESIAN_POINT('Ctrl Pts',(6.76822139184016,-1.77747401433098,28.1168450827215));
#55576=CARTESIAN_POINT('Ctrl Pts',(5.15515955319559,4.73207826030814,28.3952143584518));
#55577=CARTESIAN_POINT('Ctrl Pts',(-1.19280219078862,6.89532142936314,28.6735836341821));
#55578=CARTESIAN_POINT('Ctrl Pts',(-6.44520153326523,2.72536454005337,28.9519529099124));
#55579=CARTESIAN_POINT('Ctrl Pts',(-5.77782597549934,-3.9477793349464,29.2303221856426));
#55580=CARTESIAN_POINT('Ctrl Pts',(0.19635480956596,-6.99497530155361,29.5086914613729));
#55581=CARTESIAN_POINT('Ctrl Pts',(5.99018804968463,-3.61744133470055,29.7870607371032));
#55582=CARTESIAN_POINT('Ctrl Pts',(6.28216619943336,3.08263240158176,30.0654300128334));
#55583=CARTESIAN_POINT('Ctrl Pts',(0.804113793176059,6.95137653189703,30.3437992885637));
#55584=CARTESIAN_POINT('Ctrl Pts',(-5.41249932762432,4.43543523332839,30.622168564294));
#55585=CARTESIAN_POINT('Ctrl Pts',(-6.65785165822602,-2.15435511874011,
30.9005378400242));
#55586=CARTESIAN_POINT('Ctrl Pts',(-1.78811465725532,-6.76541799544518,
31.1789071157545));
#55587=CARTESIAN_POINT('Ctrl Pts',(4.72396606441094,-5.16259424154934,31.4572763914848));
#55588=CARTESIAN_POINT('Ctrl Pts',(6.89718855280647,1.18195801432204,31.735645667215));
#55589=CARTESIAN_POINT('Ctrl Pts',(2.73549607129591,6.44090800466125,32.0140149429453));
#55590=CARTESIAN_POINT('Ctrl Pts',(-3.93868898302102,5.78402660571449,32.2923842186756));
#55591=CARTESIAN_POINT('Ctrl Pts',(-6.99527541591257,-0.185355162091369,
32.5707534944059));
#55592=CARTESIAN_POINT('Ctrl Pts',(-3.62685626695024,-5.98449231760461,
32.8491227701361));
#55593=CARTESIAN_POINT('Ctrl Pts',(3.07275005824958,-6.28700578654989,33.1274920458664));
#55594=CARTESIAN_POINT('Ctrl Pts',(6.95010349102055,-0.815043645879572,
33.4058613215966));
#55595=CARTESIAN_POINT('Ctrl Pts',(4.44394075476531,5.40551803703592,33.6842305973269));
#55596=CARTESIAN_POINT('Ctrl Pts',(-2.14388316810245,6.66123109058015,33.9625998730572));
#55597=CARTESIAN_POINT('Ctrl Pts',(-6.76259787040012,1.79875087876129,34.2409691487875));
#55598=CARTESIAN_POINT('Ctrl Pts',(-5.17001616450826,-4.71584218770179,
34.5193384245177));
#55599=CARTESIAN_POINT('Ctrl Pts',(1.17111091526254,-6.8990386217746,34.797707700248));
#55600=CARTESIAN_POINT('Ctrl Pts',(6.43659854981351,-2.74562083855788,35.0760769759783));
#55601=CARTESIAN_POINT('Ctrl Pts',(5.79021293393728,3.92958889201531,35.3544462517086));
#55602=CARTESIAN_POINT('Ctrl Pts',(-0.17435505629461,6.99555823325981,35.6328155274388));
#55603=CARTESIAN_POINT('Ctrl Pts',(-5.97878178784655,3.63626223117903,35.9111848031691));
#55604=CARTESIAN_POINT('Ctrl Pts',(-6.29182982797216,-3.06286011701881,
36.1895540788993));
#55605=CARTESIAN_POINT('Ctrl Pts',(-0.82597148324852,-6.94881326482767,
36.4679233546296));
#55606=CARTESIAN_POINT('Ctrl Pts',(5.39852338038214,-4.45243528780061,36.7462926303599));
#55607=CARTESIAN_POINT('Ctrl Pts',(6.66459405190411,2.13340591634808,37.0246619060902));
#55608=CARTESIAN_POINT('Ctrl Pts',(1.8093826525488,6.75976102367829,37.3030311818204));
#55609=CARTESIAN_POINT('Ctrl Pts',(-4.70770665026849,5.17742530372023,37.5814004575507));
#55610=CARTESIAN_POINT('Ctrl Pts',(-6.90087163169291,-1.16026092043159,
37.8597697332809));
#55611=CARTESIAN_POINT('Ctrl Pts',(-2.75573881680387,-6.43227317937797,
38.1381390090112));
#55612=CARTESIAN_POINT('Ctrl Pts',(3.92047908443075,-5.79638494487086,38.4165082847415));
#55613=CARTESIAN_POINT('Ctrl Pts',(6.99582375289604,0.163354519375268,38.6948775604718));
#55614=CARTESIAN_POINT('Ctrl Pts',(3.64565920412922,5.97305647453065,38.973246836202));
#55615=CARTESIAN_POINT('Ctrl Pts',(-3.0529626023439,6.29663831177191,39.2516161119323));
#55616=CARTESIAN_POINT('Ctrl Pts',(-6.94750585650865,0.836897278262201,
39.5299853876626));
#55617=CARTESIAN_POINT('Ctrl Pts',(-4.46091881143022,-5.39151537495839,
39.8083546633928));
#55618=CARTESIAN_POINT('Ctrl Pts',(2.12292338938355,-6.66794053388248,40.0867239391231));
#55619=CARTESIAN_POINT('Ctrl Pts',(6.75690746229423,-1.82000995232913,40.3650932148533));
#55620=CARTESIAN_POINT('Ctrl Pts',(5.18482164086506,4.69955947222737,40.6434624905837));
#55621=CARTESIAN_POINT('Ctrl Pts',(-1.14940805665755,6.90268757802897,40.9218317663139));
#55622=CARTESIAN_POINT('Ctrl Pts',(-6.42793190404972,2.76584998101567,41.2002010420442));
#55623=CARTESIAN_POINT('Ctrl Pts',(-5.80254262325399,-3.91135958279285,
41.4785703177744));
#55624=CARTESIAN_POINT('Ctrl Pts',(0.1523535785339,-6.99607197416468,41.7569395935047));
#55625=CARTESIAN_POINT('Ctrl Pts',(5.9673163918137,-3.65504716256524,42.0353088692351));
#55626=CARTESIAN_POINT('Ctrl Pts',(6.30143122605941,3.04305753869823,42.3136781449652));
#55627=CARTESIAN_POINT('Ctrl Pts',(0.847821003904525,6.94618126929632,42.5920474206956));
#55628=CARTESIAN_POINT('Ctrl Pts',(-5.38449403809326,4.46939130467704,42.8704166964258));
#55629=CARTESIAN_POINT('Ctrl Pts',(-6.67127052824044,-2.11243561312889,
43.1487859721561));
#55630=CARTESIAN_POINT('Ctrl Pts',(-1.83063275182428,-6.75403719330394,
43.4271552478863));
#55631=CARTESIAN_POINT('Ctrl Pts',(4.69140067372388,-5.19220515765391,43.7055245236166));
#55632=CARTESIAN_POINT('Ctrl Pts',(6.90448645629252,1.13855235077613,43.9838937993469));
#55633=CARTESIAN_POINT('Ctrl Pts',(2.77595430619153,6.42357473456341,44.2622630750771));
#55634=CARTESIAN_POINT('Ctrl Pts',(-3.90223040965128,5.8086859538606,44.5406323508074));
#55635=CARTESIAN_POINT('Ctrl Pts',(-6.99630289645201,-0.141352260972383,
44.8190016265377));
#55636=CARTESIAN_POINT('Ctrl Pts',(-3.66442608327355,-5.96156155388915,
45.0973709022679));
#55637=CARTESIAN_POINT('Ctrl Pts',(3.0331449505737,-6.30620855898327,45.3757401779983));
#55638=CARTESIAN_POINT('Ctrl Pts',(6.94483950646594,-0.858742633164764,
45.6541094537285));
#55639=CARTESIAN_POINT('Ctrl Pts',(4.47785274659151,5.37745938714813,45.9324787294588));
#55640=CARTESIAN_POINT('Ctrl Pts',(-2.1019426135168,6.67458402674401,46.210848005189));
#55641=CARTESIAN_POINT('Ctrl Pts',(-6.75115022380455,1.84125102476782,46.4892172809194));
#55642=CARTESIAN_POINT('Ctrl Pts',(-5.19957583582988,-4.68323027493191,
46.7675865566495));
#55643=CARTESIAN_POINT('Ctrl Pts',(1.12769382962969,-6.90626826203556,47.0459558323799));
#55644=CARTESIAN_POINT('Ctrl Pts',(6.41920168169281,-2.78605176734692,47.32432510811));
#55645=CARTESIAN_POINT('Ctrl Pts',(5.81481492150043,3.89309158757929,47.6026943838405));
#55646=CARTESIAN_POINT('Ctrl Pts',(-0.130350593893225,6.99651651918698,
47.8810636595706));
#55647=CARTESIAN_POINT('Ctrl Pts',(-5.95579197498666,3.67379594306342,48.159432935301));
#55648=CARTESIAN_POINT('Ctrl Pts',(-6.31097029873081,-3.02322486248083,
48.4378022110312));
#55649=CARTESIAN_POINT('Ctrl Pts',(-0.869662139037468,-6.94348057133521,
48.7161714867615));
#55650=CARTESIAN_POINT('Ctrl Pts',(5.37041143951732,-4.4863031162513,48.9945407624917));
#55651=CARTESIAN_POINT('Ctrl Pts',(6.6778810212001,2.09144441649309,49.2729100382221));
#55652=CARTESIAN_POINT('Ctrl Pts',(1.85186474490403,6.74824656093464,49.5512793139522));
#55653=CARTESIAN_POINT('Ctrl Pts',(-4.6750482960543,5.20693365716757,49.8296485896825));
#55654=CARTESIAN_POINT('Ctrl Pts',(-6.90803299085227,-1.11683252006797,
50.1080178654128));
#55655=CARTESIAN_POINT('Ctrl Pts',(-2.79614233951396,-6.41481275625112,
50.3863871411431));
#55656=CARTESIAN_POINT('Ctrl Pts',(3.88394313917433,-5.82092951101844,50.6647564168733));
#55657=CARTESIAN_POINT('Ctrl Pts',(6.99671284184141,0.119348604500108,50.9431256926036));
#55658=CARTESIAN_POINT('Ctrl Pts',(3.68315671876607,5.95000766937262,51.2214949683339));
#55659=CARTESIAN_POINT('Ctrl Pts',(-3.01329729894889,6.31571643352771,51.4998642440641));
#55660=CARTESIAN_POINT('Ctrl Pts',(-6.94210446726436,0.880579494522117,
51.7782335197944));
#55661=CARTESIAN_POINT('Ctrl Pts',(-4.49474239276128,-5.36335021262824,
52.0566027955247));
#55662=CARTESIAN_POINT('Ctrl Pts',(2.0809410480163,-6.68116150345623,52.334972071255));
#55663=CARTESIAN_POINT('Ctrl Pts',(6.74532621187403,-1.86247388598872,52.6133413469853));
#55664=CARTESIAN_POINT('Ctrl Pts',(5.21427860347363,4.66685475732229,52.8917106227154));
#55665=CARTESIAN_POINT('Ctrl Pts',(-1.10596844894738,6.90978063837902,53.1700798984458));
#55666=CARTESIAN_POINT('Ctrl Pts',(-6.41040796909065,2.80622599774214,53.448449174176));
#55667=CARTESIAN_POINT('Ctrl Pts',(-5.82702970729528,-3.87478508705741,
53.7268184499063));
#55668=CARTESIAN_POINT('Ctrl Pts',(0.108346319997076,-6.99689186392985,
54.0051877256365));
#55669=CARTESIAN_POINT('Ctrl Pts',(5.94420865134965,-3.69250838723553,54.2835570013669));
#55670=CARTESIAN_POINT('Ctrl Pts',(6.32044695163845,3.00336228452527,54.5619262770971));
#55671=CARTESIAN_POINT('Ctrl Pts',(0.891494672623838,6.94071119765604,54.8402955528274));
#55672=CARTESIAN_POINT('Ctrl Pts',(-5.3562757239408,4.50317055525407,55.1186648285575));
#55673=CARTESIAN_POINT('Ctrl Pts',(-6.68442546540088,-2.07043253405773,
55.397034104288));
#55674=CARTESIAN_POINT('Ctrl Pts',(-1.87307842178917,-6.7423891838437,55.6754033800181));
#55675=CARTESIAN_POINT('Ctrl Pts',(4.65864967899578,-5.22161065658646,55.9537726557485));
#55676=CARTESIAN_POINT('Ctrl Pts',(6.9115112002945,1.09510164313103,56.2321419314787));
#55677=CARTESIAN_POINT('Ctrl Pts',(2.81630271709793,6.40598733110295,56.510511207209));
#55678=CARTESIAN_POINT('Ctrl Pts',(-3.86561745387344,5.83311549524726,56.7888804829392));
#55679=CARTESIAN_POINT('Ctrl Pts',(-6.99705358500964,-0.0973437675893806,
57.0672497586697));
#55680=CARTESIAN_POINT('Ctrl Pts',(-3.70185092534808,-5.93839493525681,
57.3456190343996));
#55681=CARTESIAN_POINT('Ctrl Pts',(2.99341984377602,-6.32516184136598,57.6239883101302));
#55682=CARTESIAN_POINT('Ctrl Pts',(6.93930076595538,-0.902407646352917,
57.9023575858602));
#55683=CARTESIAN_POINT('Ctrl Pts',(4.51158758288953,5.34918799094799,58.1807268615907));
#55684=CARTESIAN_POINT('Ctrl Pts',(-2.05991890060161,6.68767289896333,58.4590961373207));
#55685=CARTESIAN_POINT('Ctrl Pts',(-6.73943548410595,1.88367832608374,58.7374654130512));
#55686=CARTESIAN_POINT('Ctrl Pts',(-5.22892979837629,-4.65043308136325,
59.0158346887813));
#55687=CARTESIAN_POINT('Ctrl Pts',(1.0842321294891,-6.91322467231963,59.2942039645118));
#55688=CARTESIAN_POINT('Ctrl Pts',(6.40155085321885,-2.82637247266478,59.5725732402418));
#55689=CARTESIAN_POINT('Ctrl Pts',(5.8391868598262,3.85644026229077,59.8509425159723));
#55690=CARTESIAN_POINT('Ctrl Pts',(-0.0863409744825115,6.99719800468092,
60.1293117917024));
#55691=CARTESIAN_POINT('Ctrl Pts',(-5.93256653546964,3.71118431000278,60.4076810674328));
#55692=CARTESIAN_POINT('Ctrl Pts',(-6.32986109105182,-2.98347000128584,
60.686050343163));
#55693=CARTESIAN_POINT('Ctrl Pts',(-0.913318388725055,-6.93787317564979,
60.9644196188933));
#55694=CARTESIAN_POINT('Ctrl Pts',(5.34208703117528,-4.5199934548551,61.2427888946235));
#55695=CARTESIAN_POINT('Ctrl Pts',(6.69090379611385,2.04940017364437,61.5211581703538));
#55696=CARTESIAN_POINT('Ctrl Pts',(1.89427357266239,6.73646511996448,61.7995274460842));
#55697=CARTESIAN_POINT('Ctrl Pts',(-4.64220498474165,5.23623601074521,62.0778967218143));
#55698=CARTESIAN_POINT('Ctrl Pts',(-6.91492105021739,-1.07335993489815,
62.3562659975447));
#55699=CARTESIAN_POINT('Ctrl Pts',(-2.83643523954384,-6.39709854640821,
62.6346352732749));
#55700=CARTESIAN_POINT('Ctrl Pts',(3.84725353500179,-5.84524378601966,62.9130045490052));
#55701=CARTESIAN_POINT('Ctrl Pts',(6.99732512258652,0.0753379678828323,
63.1913738247354));
#55702=CARTESIAN_POINT('Ctrl Pts',(3.7205085181213,5.92672346639955,63.4697431004658));
#55703=CARTESIAN_POINT('Ctrl Pts',(-2.97351278165681,6.33454468907653,63.7481123761959));
#55704=CARTESIAN_POINT('Ctrl Pts',(-6.93642843026943,0.924226872761883,
64.0264816519263));
#55705=CARTESIAN_POINT('Ctrl Pts',(-4.52838815036582,-5.33497286218137,
64.3048509276565));
#55706=CARTESIAN_POINT('Ctrl Pts',(2.03887637919601,-6.69411814886327,64.5832202033868));
#55707=CARTESIAN_POINT('Ctrl Pts',(6.7334780987638,-1.90486413532633,64.861589479117));
#55708=CARTESIAN_POINT('Ctrl Pts',(5.24352927562737,4.63396540947642,65.1399587548474));
#55709=CARTESIAN_POINT('Ctrl Pts',(-1.06248508624185,6.91660032979344,65.4183280305775));
#55710=CARTESIAN_POINT('Ctrl Pts',(-6.39263042168039,2.84649099285255,65.6966973063079));
#55711=CARTESIAN_POINT('Ctrl Pts',(-5.85128625885058,-3.83805729472223,
65.975066582038));
#55712=CARTESIAN_POINT('Ctrl Pts',(0.0643347749972447,-6.99743493841216,
66.2534358577685));
#55713=CARTESIAN_POINT('Ctrl Pts',(5.92086574249491,-3.72982352664781,66.5318051334986));
#55714=CARTESIAN_POINT('Ctrl Pts',(6.33921262385881,2.96354820951057,66.810174409229));
#55715=CARTESIAN_POINT('Ctrl Pts',(0.935133071489911,6.93496653338645,67.0885436849591));
#55716=CARTESIAN_POINT('Ctrl Pts',(-5.32784550155691,4.53677164866438,67.3669129606895));
#55717=CARTESIAN_POINT('Ctrl Pts',(-6.69731594926383,-2.02834754327791,
67.6452822364197));
#55718=CARTESIAN_POINT('Ctrl Pts',(-1.91544998788864,-6.73047442789003,
67.92365151215));
#55719=CARTESIAN_POINT('Ctrl Pts',(4.62571437594122,-5.25080957498887,68.2020207878803));
#55720=CARTESIAN_POINT('Ctrl Pts',(6.91826250689525,1.05160761040976,68.4803900636105));
#55721=CARTESIAN_POINT('Ctrl Pts',(2.85653970772702,6.38814649008333,68.7587593393409));
#55722=CARTESIAN_POINT('Ctrl Pts',(-3.8288515641914,5.85731426337825,69.0371286150711));
#55723=CARTESIAN_POINT('Ctrl Pts',(-6.99752745188624,-0.053331423033017,
69.3154978908014));
#55724=CARTESIAN_POINT('Ctrl Pts',(-3.73912931254947,-5.91499337823953,
69.5938671665316));
#55725=CARTESIAN_POINT('Ctrl Pts',(2.95357630948563,-6.34386488385672,69.8722364422619));
#55726=CARTESIAN_POINT('Ctrl Pts',(6.9334874886159,-0.946036957941923,70.1506057179922));
#55727=CARTESIAN_POINT('Ctrl Pts',(4.54514392902107,5.32070496692563,70.4289749937224));
#55728=CARTESIAN_POINT('Ctrl Pts',(-2.01781369192432,6.70049718940818,70.7073442694526));
#55729=CARTESIAN_POINT('Ctrl Pts',(-6.72745411477015,1.92603110417443,70.985713545183));
#55730=CARTESIAN_POINT('Ctrl Pts',(-5.25807689082814,-4.61745190453829,
71.2640828209132));
#55731=CARTESIAN_POINT('Ctrl Pts',(1.04072753429877,-6.91990757741292,71.5424520966435));
#55732=CARTESIAN_POINT('Ctrl Pts',(6.38364676270434,-2.86658135931959,71.8208213723738));
#55733=CARTESIAN_POINT('Ctrl Pts',(5.86332778469723,3.81963636617187,72.099190648104));
#55734=CARTESIAN_POINT('Ctrl Pts',(-0.0423279391977326,6.9976026627802,
72.3775599238344));
#55735=CARTESIAN_POINT('Ctrl Pts',(-5.90910638815427,3.74842585281589,72.6559291995646));
#55736=CARTESIAN_POINT('Ctrl Pts',(-6.34850145756637,-2.94359710623954,
72.9342984752948));
#55737=CARTESIAN_POINT('Ctrl Pts',(-0.956938505156228,-6.93199129961475,
73.2126677510252));
#55738=CARTESIAN_POINT('Ctrl Pts',(5.31355127594381,-4.5535049707342,73.4910370267554));
#55739=CARTESIAN_POINT('Ctrl Pts',(6.70366186143025,2.00727485118249,73.7694063024857));
#55740=CARTESIAN_POINT('Ctrl Pts',(1.93660745801957,6.72441716687232,74.0477755782159));
#55741=CARTESIAN_POINT('Ctrl Pts',(-4.6091780156978,5.26533120517534,74.3261448539462));
#55742=CARTESIAN_POINT('Ctrl Pts',(-6.9215355372788,-1.0298448848113,74.6045141296765));
#55743=CARTESIAN_POINT('Ctrl Pts',(-2.87661592280069,-6.37913125066994,
74.8828834054067));
#55744=CARTESIAN_POINT('Ctrl Pts',(3.81041172344989,-5.86932680793801,75.1612526811371));
#55745=CARTESIAN_POINT('Ctrl Pts',(6.99766057090778,0.0313243506992304,
75.4396219568672));
#55746=CARTESIAN_POINT('Ctrl Pts',(3.75771312446028,5.9032047867954,75.7179912325976));
#55747=CARTESIAN_POINT('Ctrl Pts',(-2.93361062444756,6.35312233352339,75.9963605083277));
#55748=CARTESIAN_POINT('Ctrl Pts',(-6.93047797008259,0.967837686176782,
76.2747297840582));
#55749=CARTESIAN_POINT('Ctrl Pts',(-4.56185475312959,-5.30638444629986,
76.5530990597882));
#55750=CARTESIAN_POINT('Ctrl Pts',(1.99673104711092,-6.70680995750503,76.8314683355187));
#55751=CARTESIAN_POINT('Ctrl Pts',(6.72136359170614,-1.94717902327247,77.1098376112488));
#55752=CARTESIAN_POINT('Ctrl Pts',(5.2725725000929,4.60089272987844,77.3882068869792));
#55753=CARTESIAN_POINT('Ctrl Pts',(-1.01895968885651,6.92314638246727,77.6665761627094));
#55754=CARTESIAN_POINT('Ctrl Pts',(-6.3745999651453,2.88664337335853,77.9449454384397));
#55755=CARTESIAN_POINT('Ctrl Pts',(-5.87531131826721,-3.80117765883502,
78.22331471417));
#55756=CARTESIAN_POINT('Ctrl Pts',(0.0203206847462305,-6.99770117612603,
78.5016839899002));
#55757=CARTESIAN_POINT('Ctrl Pts',(5.89728858875571,-3.76699110451776,78.7800532656305));
#55758=CARTESIAN_POINT('Ctrl Pts',(6.35772750030168,2.92361688880281,79.0584225413607));
#55759=CARTESIAN_POINT('Ctrl Pts',(0.978734474053595,6.9289475037616,79.3367918170911));
#55760=CARTESIAN_POINT('Ctrl Pts',(-5.29920449571548,4.57019325556077,79.6151610928212));
#55761=CARTESIAN_POINT('Ctrl Pts',(-6.70994146984795,-1.98618230578136,
79.8935303685517));
#55762=CARTESIAN_POINT('Ctrl Pts',(-1.95774577379312,-6.71829339682188,
80.1718996442817));
#55763=CARTESIAN_POINT('Ctrl Pts',(4.59259606756707,-5.27980075767568,80.4502689200122));
#55764=CARTESIAN_POINT('Ctrl Pts',(6.9247401089954,1.00807197335037,80.7286381957424));
#55765=CARTESIAN_POINT('Ctrl Pts',(2.89666368619801,6.37005291733483,81.0070074714725));
#55766=CARTESIAN_POINT('Ctrl Pts',(-3.79193419515991,5.88128130088692,81.2853767472031));
#55767=CARTESIAN_POINT('Ctrl Pts',(-6.99772447833453,-0.00931696854672991,
81.563746022933));
#55768=CARTESIAN_POINT('Ctrl Pts',(-3.7762597700471,-5.89135780866416,81.8421152986636));
#55769=CARTESIAN_POINT('Ctrl Pts',(2.91361592401662,-6.36231694651414,82.1204845743937));
#55770=CARTESIAN_POINT('Ctrl Pts',(6.92739990443582,-0.989628841842616,
82.3988538501239));
#55771=CARTESIAN_POINT('Ctrl Pts',(4.57852045740981,5.2920114419439,82.6772231258543));
#55772=CARTESIAN_POINT('Ctrl Pts',(-1.9756286532773,6.71305639071614,82.9555924015846));
#55773=CARTESIAN_POINT('Ctrl Pts',(-6.71520658981113,1.96830768345331,83.2339616773148));
#55774=CARTESIAN_POINT('Ctrl Pts',(-5.28701596005046,-4.58428804927831,
83.5123309530451));
#55775=CARTESIAN_POINT('Ctrl Pts',(0.997181765214038,-6.92631671292251,
83.7907002287754));
#55776=CARTESIAN_POINT('Ctrl Pts',(6.36549011848205,-2.90667683654248,84.0690695045055));
#55777=CARTESIAN_POINT('Ctrl Pts',(5.88723674103532,3.78268135528068,84.347438780236));
#55778=CARTESIAN_POINT('Ctrl Pts',(0.00168677069072056,6.99773047747545,
84.6258080559661));
#55779=CARTESIAN_POINT('Ctrl Pts',(-5.88541246118538,3.78551909813028,84.9041773316965));
#55780=CARTESIAN_POINT('Ctrl Pts',(-6.36689066081281,-2.9036077548181,85.1825466074266));
#55781=CARTESIAN_POINT('Ctrl Pts',(-1.00052076260523,-6.92583517593222,
85.4609158831571));
#55782=CARTESIAN_POINT('Ctrl Pts',(5.28480530277132,-4.5868363380858,85.7392851588871));
#55783=CARTESIAN_POINT('Ctrl Pts',(6.71615471240727,1.96507011569431,86.0176544346176));
#55784=CARTESIAN_POINT('Ctrl Pts',(1.97886472613705,6.71210317830676,86.2960237103478));
#55785=CARTESIAN_POINT('Ctrl Pts',(-4.57596869555562,5.29421808937629,86.574392986078));
#55786=CARTESIAN_POINT('Ctrl Pts',(-6.92787619034991,-0.98628909137584,
86.8527622618084));
#55787=CARTESIAN_POINT('Ctrl Pts',(-2.91668279963266,-6.36091157986905,
87.1311315375386));
#55788=CARTESIAN_POINT('Ctrl Pts',(3.77341916207662,-5.89317762398675,87.4095008132688));
#55789=CARTESIAN_POINT('Ctrl Pts',(6.99771917353418,-0.0126905057570474,
87.6878700889991));
#55790=CARTESIAN_POINT('Ctrl Pts',(3.79476906587156,5.87945256102033,87.9662393647294));
#55791=CARTESIAN_POINT('Ctrl Pts',(-2.89359240595405,6.37144863188822,88.2446086404596));
#55792=CARTESIAN_POINT('Ctrl Pts',(-6.92425332211979,1.01141020940972,88.52297791619));
#55793=CARTESIAN_POINT('Ctrl Pts',(-4.59514087702648,-5.27758609601629,
88.8013471919202));
#55794=CARTESIAN_POINT('Ctrl Pts',(1.9545067191403,-6.71923642726015,89.0797164676505));
#55795=CARTESIAN_POINT('Ctrl Pts',(6.70898316998215,-1.98941687574033,89.3580857433807));
#55796=CARTESIAN_POINT('Ctrl Pts',(5.30140712784506,4.5676380269696,89.636455019111));
#55797=CARTESIAN_POINT('Ctrl Pts',(-0.975393978769655,6.92941853742182,
89.9148242948413));
#55798=CARTESIAN_POINT('Ctrl Pts',(-6.35631731281709,2.92668155072702,90.1931935705715));
#55799=CARTESIAN_POINT('Ctrl Pts',(-5.89910393505123,-3.76414763844981,
90.4715628463019));
#55800=CARTESIAN_POINT('Ctrl Pts',(-0.0236942094442284,-6.99769056653865,
90.749932122032));
#55801=CARTESIAN_POINT('Ctrl Pts',(5.87347812290604,-3.80400965039908,91.0283013977623));
#55802=CARTESIAN_POINT('Ctrl Pts',(6.37599084846996,2.88356990218922,91.3066706734926));
#55803=CARTESIAN_POINT('Ctrl Pts',(1.0222971553301,6.92265434690973,91.5850399492228));
#55804=CARTESIAN_POINT('Ctrl Pts',(-5.27035383952926,4.60343405369778,91.8634092249532));
#55805=CARTESIAN_POINT('Ctrl Pts',(-6.72230152765492,-1.94393848973506,
92.1417785006834));
#55806=CARTESIAN_POINT('Ctrl Pts',(-1.99996410617077,-6.7058465725524,92.4201477764137));
#55807=CARTESIAN_POINT('Ctrl Pts',(4.55929606411945,-5.30858305768019,92.6985170521439));
#55808=CARTESIAN_POINT('Ctrl Pts',(6.93094375032431,0.964496454335416,92.9768863278743));
#55809=CARTESIAN_POINT('Ctrl Pts',(2.93667306510209,6.35170732868644,93.2552556036044));
#55810=CARTESIAN_POINT('Ctrl Pts',(-3.75486680732616,5.90501565957488,93.5336248793348));
#55811=CARTESIAN_POINT('Ctrl Pts',(-6.9976446565594,0.0346978545432685,
93.811994155065));
#55812=CARTESIAN_POINT('Ctrl Pts',(-3.81324082886386,-5.86748916161511,
94.0903634307953));
#55813=CARTESIAN_POINT('Ctrl Pts',(2.87354026830597,-6.38051729932687,94.3687327065256));
#55814=CARTESIAN_POINT('Ctrl Pts',(6.92103825425605,-1.03318157344609,94.6471019822558));
#55815=CARTESIAN_POINT('Ctrl Pts',(4.61171584759291,5.26310855119335,94.9254712579861));
#55816=CARTESIAN_POINT('Ctrl Pts',(-1.93336545361025,6.72535000601245,95.2038405337164));
#55817=CARTESIAN_POINT('Ctrl Pts',(-6.70269339377315,2.01050639134894,95.4822098094466));
#55818=CARTESIAN_POINT('Ctrl Pts',(-5.31574586113814,-4.5509428276322,95.760579085177));
#55819=CARTESIAN_POINT('Ctrl Pts',(0.953596545019199,-6.93245182528603,
96.038948360907));
#55820=CARTESIAN_POINT('Ctrl Pts',(6.34708163887577,-2.94665731805215,96.3173176366376));
#55821=CARTESIAN_POINT('Ctrl Pts',(5.91091278294024,3.74557669165362,96.5956869123676));
#55822=CARTESIAN_POINT('Ctrl Pts',(0.0457014138459489,6.99758144371023,
96.8740561880982));
#55823=CARTESIAN_POINT('Ctrl Pts',(-5.86148569195634,3.82246257844015,97.152425463828));
#55824=CARTESIAN_POINT('Ctrl Pts',(-6.38502797326628,-2.86350352910403,
97.4307947395587));
#55825=CARTESIAN_POINT('Ctrl Pts',(-1.04406343684472,-6.91940504815473,
97.7091640152887));
#55826=CARTESIAN_POINT('Ctrl Pts',(5.2558502489239,-4.61998623823404,97.9875332910192));
#55827=CARTESIAN_POINT('Ctrl Pts',(6.72838185479479,1.9227876369096,98.2659025667492));
#55828=CARTESIAN_POINT('Ctrl Pts',(2.02104370520724,6.69952364144096,98.5442718424796));
#55829=CARTESIAN_POINT('Ctrl Pts',(-4.54257833816235,5.32289552050794,98.8226411182098));
#55830=CARTESIAN_POINT('Ctrl Pts',(-6.93394275857822,-0.942694277772887,
99.1010103939402));
#55831=CARTESIAN_POINT('Ctrl Pts',(-2.95663428488913,-6.34244025482325,
99.3793796696704));
#55832=CARTESIAN_POINT('Ctrl Pts',(3.73627731440385,-5.91679529056526,99.6577489454006));
#55833=CARTESIAN_POINT('Ctrl Pts',(6.99750092814722,-0.0567048601441356,
99.9361182211311));
#55834=CARTESIAN_POINT('Ctrl Pts',(3.83167487632577,5.85546772877446,100.214487496861));
#55835=CARTESIAN_POINT('Ctrl Pts',(-2.85345970940146,6.38952285913484,100.492856772592));
#55836=CARTESIAN_POINT('Ctrl Pts',(-6.91775473264401,1.0549427186182,100.771226048322));
#55837=CARTESIAN_POINT('Ctrl Pts',(-4.62824520517111,-5.24857895066806,
101.049595324052));
#55838=CARTESIAN_POINT('Ctrl Pts',(1.91220506578854,-6.73139706650542,101.327964599782));
#55839=CARTESIAN_POINT('Ctrl Pts',(6.69633732339394,-2.03157602168996,101.606333875513));
#55840=CARTESIAN_POINT('Ctrl Pts',(5.33003201811036,4.53420261639271,101.884703151243));
#55841=CARTESIAN_POINT('Ctrl Pts',(-0.931789679554102,6.93541654651411,
102.163072426973));
#55842=CARTESIAN_POINT('Ctrl Pts',(-6.33778318800533,2.96660394094364,102.441441702703));
#55843=CARTESIAN_POINT('Ctrl Pts',(-5.92266316790465,-3.72696869857125,
102.719810978434));
#55844=CARTESIAN_POINT('Ctrl Pts',(-0.0677081662298231,-6.99740311006948,
102.998180254164));
#55845=CARTESIAN_POINT('Ctrl Pts',(5.84943528694958,-3.84087769974172,103.276549529894));
#55846=CARTESIAN_POINT('Ctrl Pts',(6.39400194581841,2.84340883403278,103.554918805624));
#55847=CARTESIAN_POINT('Ctrl Pts',(1.06581939186588,6.91608731180484,103.833288081355));
#55848=CARTESIAN_POINT('Ctrl Pts',(-5.24129467440546,4.63649272798234,104.111657357085));
#55849=CARTESIAN_POINT('Ctrl Pts',(-6.73439563368848,-1.90161776641409,
104.390026632815));
#55850=CARTESIAN_POINT('Ctrl Pts',(-2.04210331475472,-6.6931344475106,104.668395908546));
#55851=CARTESIAN_POINT('Ctrl Pts',(4.52581568303376,-5.33715533629955,104.946765184276));
#55852=CARTESIAN_POINT('Ctrl Pts',(6.93687318544946,0.920882777326449,105.225134460006));
#55853=CARTESIAN_POINT('Ctrl Pts',(2.97656626156395,6.33311044993717,105.503503735736));
#55854=CARTESIAN_POINT('Ctrl Pts',(-3.71765086717258,5.92851640044929,105.781873011467));
#55855=CARTESIAN_POINT('Ctrl Pts',(-6.99728798971909,0.0787113048955276,
106.060242287197));
#55856=CARTESIAN_POINT('Ctrl Pts',(-3.85007102593217,-5.84338838139839,
106.338611562927));
#55857=CARTESIAN_POINT('Ctrl Pts',(2.83335092785082,-6.39846522224127,106.616980838657));
#55858=CARTESIAN_POINT('Ctrl Pts',(6.91440278975997,-1.07669342969335,106.895350114388));
#55859=CARTESIAN_POINT('Ctrl Pts',(4.64472878627452,5.23399743814782,107.173719390118));
#55860=CARTESIAN_POINT('Ctrl Pts',(-1.89102576496565,6.73737754892958,107.452088665848));
#55861=CARTESIAN_POINT('Ctrl Pts',(-6.68991502171053,2.0526255583705,107.730457941578));
#55862=CARTESIAN_POINT('Ctrl Pts',(-5.34426545746175,-4.51741755882344,
108.008827217309));
#55863=CARTESIAN_POINT('Ctrl Pts',(0.909973598059053,-6.93831267178273,
108.287196493039));
#55864=CARTESIAN_POINT('Ctrl Pts',(6.32842205217333,-2.98652122211621,108.565565768769));
#55865=CARTESIAN_POINT('Ctrl Pts',(5.93435497372563,3.70832384324806,108.843935044499));
#55866=CARTESIAN_POINT('Ctrl Pts',(0.0897142489341528,6.99715556738046,
109.12230432023));
#55867=CARTESIAN_POINT('Ctrl Pts',(-5.83732702707266,3.85925483216542,109.40067359596));
#55868=CARTESIAN_POINT('Ctrl Pts',(-6.40291267736745,-2.82328601572554,
109.679042871691));
#55869=CARTESIAN_POINT('Ctrl Pts',(-1.0875648052126,-6.91270117067468,109.95741214742));
#55870=CARTESIAN_POINT('Ctrl Pts',(5.22668725993863,-4.65295335968247,110.235781423151));
#55871=CARTESIAN_POINT('Ctrl Pts',(6.74034280485554,1.88042908763332,110.514150698881));
#55872=CARTESIAN_POINT('Ctrl Pts',(2.06314272651936,6.68667905395455,110.792519974612));
#55873=CARTESIAN_POINT('Ctrl Pts',(-4.50900826452764,5.35136236401588,111.070889250342));
#55874=CARTESIAN_POINT('Ctrl Pts',(-6.93973500195425,-0.899062168726521,
111.349258526072));
#55875=CARTESIAN_POINT('Ctrl Pts',(-2.99646879798562,-6.3237180063064,111.627627801802));
#55876=CARTESIAN_POINT('Ctrl Pts',(3.69898764986036,-5.94017887329715,111.905997077532));
#55877=CARTESIAN_POINT('Ctrl Pts',(6.99700584338106,-0.100716971138942,
112.184366353263));
#55878=CARTESIAN_POINT('Ctrl Pts',(3.86842909573286,5.83125123895993,112.462735628993));
#55879=CARTESIAN_POINT('Ctrl Pts',(-2.81321412254376,6.40734430020001,112.741104904723));
#55880=CARTESIAN_POINT('Ctrl Pts',(-6.91098245875672,1.09843349154236,113.019474180454));
#55881=CARTESIAN_POINT('Ctrl Pts',(-4.66116642786946,-5.21936415785361,
113.297843456184));
#55882=CARTESIAN_POINT('Ctrl Pts',(1.86982776061911,-6.74329139413405,113.576212731914));
#55883=CARTESIAN_POINT('Ctrl Pts',(6.68342655224396,-2.0736547931962,113.854582007644));
#55884=CARTESIAN_POINT('Ctrl Pts',(5.35844603841386,4.50058782093984,114.132951283375));
#55885=CARTESIAN_POINT('Ctrl Pts',(-0.888148516309729,6.94114017244725,
114.411320559105));
#55886=CARTESIAN_POINT('Ctrl Pts',(-6.31899832396796,3.00640896457457,114.689689834835));
#55887=CARTESIAN_POINT('Ctrl Pts',(-5.9459880847631,-3.68964231009464,114.968059110565));
#55888=CARTESIAN_POINT('Ctrl Pts',(-0.111719444303851,-6.99683881809132,
115.246428386296));
#55889=CARTESIAN_POINT('Ctrl Pts',(5.82516103208404,-3.87759379394926,115.524797662026));
#55890=CARTESIAN_POINT('Ctrl Pts',(6.41176007978063,2.80313527321026,115.803166937756));
#55891=CARTESIAN_POINT('Ctrl Pts',(1.109299461808,6.90924665825571,116.081536213487));
#55892=CARTESIAN_POINT('Ctrl Pts',(-5.2120281500005,4.66936797052745,116.359905489217));
#55893=CARTESIAN_POINT('Ctrl Pts',(-6.74622330947431,-1.85922181013711,
116.638274764947));
#55894=CARTESIAN_POINT('Ctrl Pts',(-2.08416173240764,-6.6801575246211,116.916644040677));
#55895=CARTESIAN_POINT('Ctrl Pts',(4.49215624888088,-5.36551646313994,117.195013316408));
#55896=CARTESIAN_POINT('Ctrl Pts',(6.94252817978723,0.877232667794093,117.473382592138));
#55897=CARTESIAN_POINT('Ctrl Pts',(3.01634169730445,6.31426301682841,117.751751867868));
#55898=CARTESIAN_POINT('Ctrl Pts',(-3.68028784705895,5.95178259375914,118.030121143598));
#55899=CARTESIAN_POINT('Ctrl Pts',(-6.99665449192391,0.122721641223584,
118.308490419329));
#55900=CARTESIAN_POINT('Ctrl Pts',(-3.88674890415396,-5.81905642150383,
118.586859695059));
#55901=CARTESIAN_POINT('Ctrl Pts',(2.79304949264689,-6.41616000519071,118.865228970789));
#55902=CARTESIAN_POINT('Ctrl Pts',(6.90749377346335,-1.12016268914174,119.143598246519));
#55903=CARTESIAN_POINT('Ctrl Pts',(4.67755796737731,5.20467925451912,119.42196752225));
#55904=CARTESIAN_POINT('Ctrl Pts',(-1.84861126241298,6.74913854362568,119.70033679798));
#55905=CARTESIAN_POINT('Ctrl Pts',(-6.67687197916712,2.0946635181759,119.97870607371));
#55906=CARTESIAN_POINT('Ctrl Pts',(-5.37257362071552,-4.48371356920345,
120.257075349441));
#55907=CARTESIAN_POINT('Ctrl Pts',(0.86631465017897,-6.94389902053411,120.535444625171));
#55908=CARTESIAN_POINT('Ctrl Pts',(6.30951209658112,-3.02626697163003,120.813813900901));
#55909=CARTESIAN_POINT('Ctrl Pts',(5.95756238598644,3.67092428391178,121.092183176631));
#55910=CARTESIAN_POINT('Ctrl Pts',(0.133723534638353,6.99645286528214,121.370552452362));
#55911=CARTESIAN_POINT('Ctrl Pts',(-5.81293742221111,3.8958944038083,121.648921728092));
#55912=CARTESIAN_POINT('Ctrl Pts',(-6.42054406574492,-2.78295680598006,
121.927291003822));
#55913=CARTESIAN_POINT('Ctrl Pts',(-1.13102314631542,-6.90572380835968,
122.205660279552));
#55914=CARTESIAN_POINT('Ctrl Pts',(5.19731748888817,-4.68573639883701,122.484029555283));
#55915=CARTESIAN_POINT('Ctrl Pts',(6.75203709068823,1.83799614494737,122.762398831013));
#55916=CARTESIAN_POINT('Ctrl Pts',(2.10516012206219,6.67356992161945,123.040768106744));
#55917=CARTESIAN_POINT('Ctrl Pts',(-4.47525979811722,5.37961749819687,123.319137382473));
#55918=CARTESIAN_POINT('Ctrl Pts',(-6.94525270010952,-0.855394498969912,
123.597506658204));
#55919=CARTESIAN_POINT('Ctrl Pts',(-3.03618474637166,-6.30474555890793,
123.875875933934));
#55920=CARTESIAN_POINT('Ctrl Pts',(3.66155161239148,-5.96332747748852,124.154245209664));
#55921=CARTESIAN_POINT('Ctrl Pts',(6.99623399798153,-0.1447250400655,124.432614485395));
#55922=CARTESIAN_POINT('Ctrl Pts',(3.90503015829615,5.80680394118188,124.710983761125));
#55923=CARTESIAN_POINT('Ctrl Pts',(-2.77285702668229,6.42491245482045,124.989353036855));
#55924=CARTESIAN_POINT('Ctrl Pts',(-6.90393716664472,1.14188042087048,125.267722312585));
#55925=CARTESIAN_POINT('Ctrl Pts',(-4.69390249067992,-5.18994214321111,
125.546091588316));
#55926=CARTESIAN_POINT('Ctrl Pts',(1.82737506027401,-6.75492031829483,125.824460864046));
#55927=CARTESIAN_POINT('Ctrl Pts',(6.67025404840435,-2.11564892221031,126.102830139776));
#55928=CARTESIAN_POINT('Ctrl Pts',(5.38664300218255,4.46679005493539,126.381199415506));
#55929=CARTESIAN_POINT('Ctrl Pts',(-0.844462656677822,6.94659847036505,
126.659568691237));
#55930=CARTESIAN_POINT('Ctrl Pts',(-6.29998151306312,3.04607752130724,126.937937966967));
#55931=CARTESIAN_POINT('Ctrl Pts',(-5.96904368230331,-3.65213685798737,
127.216307242697));
#55932=CARTESIAN_POINT('Ctrl Pts',(-0.155790653488725,-6.99606019700873,
127.494676518427));
#55933=CARTESIAN_POINT('Ctrl Pts',(5.80077782692774,-3.9140384969439,127.773045794158));
#55934=CARTESIAN_POINT('Ctrl Pts',(6.42903511182726,2.76252802932186,128.051415069888));
#55935=CARTESIAN_POINT('Ctrl Pts',(1.15316889662473,6.90255337426073,128.329784345618));
#55936=CARTESIAN_POINT('Ctrl Pts',(-5.18337373568856,4.70126361979388,128.608153621349));
#55937=CARTESIAN_POINT('Ctrl Pts',(-6.75623695130492,-1.81524767029855,
128.886522897079));
#55938=CARTESIAN_POINT('Ctrl Pts',(-2.12907532833933,-6.66978817737252,
129.164892172809));
#55939=CARTESIAN_POINT('Ctrl Pts',(4.46399912483758,-5.3879904519143,129.44326144854));
#55940=CARTESIAN_POINT('Ctrl Pts',(6.52410345000868,-0.214043852273786,
129.675235844981));
#55941=CARTESIAN_POINT('Ctrl Pts',(5.0100391049337,3.57981706251019,129.860815362135));
#55942=CARTESIAN_POINT('Ctrl Pts',(3.47055515188223,4.89229596196689,129.953605120712));
#55943=CARTESIAN_POINT('Ctrl Pts',(2.58391981634458,5.32271443393329,130.));
#55944=CARTESIAN_POINT('Ctrl Pts',(3.24375760296843,-4.54512507566758,-10.3843228291906));
#55945=CARTESIAN_POINT('Ctrl Pts',(4.00086538069068,-4.00479360637521,-10.3379279499022));
#55946=CARTESIAN_POINT('Ctrl Pts',(5.2263164302552,-2.54076122583732,-10.2451381913254));
#55947=CARTESIAN_POINT('Ctrl Pts',(6.03675826576676,1.22812655469745,-10.0595586741719));
#55948=CARTESIAN_POINT('Ctrl Pts',(3.3038612674489,5.71744161547796,-9.82758427773004));
#55949=CARTESIAN_POINT('Ctrl Pts',(-3.03299291957947,5.87028068222262,-9.54921500199974));
#55950=CARTESIAN_POINT('Ctrl Pts',(-6.57280714142195,0.623467478762871,
-9.27084572626949));
#55951=CARTESIAN_POINT('Ctrl Pts',(-4.08153023623295,-5.19191713446524,
-8.99247645053922));
#55952=CARTESIAN_POINT('Ctrl Pts',(2.1616472547184,-6.24078027128343,-8.71410717480895));
#55953=CARTESIAN_POINT('Ctrl Pts',(6.41775644389384,-1.55649378700411,-8.43573789907868));
#55954=CARTESIAN_POINT('Ctrl Pts',(4.78016848203232,4.5567989667075,-8.1573686233484));
#55955=CARTESIAN_POINT('Ctrl Pts',(-1.24835914482659,6.48508986838572,-7.87899934761815));
#55956=CARTESIAN_POINT('Ctrl Pts',(-6.13005252277504,2.45680138155627,-7.60063007188787));
#55957=CARTESIAN_POINT('Ctrl Pts',(-5.38155761977461,-3.82791583738751,
-7.3222607961576));
#55958=CARTESIAN_POINT('Ctrl Pts',(0.309847241136156,-6.59682421882921,
-7.04389152042733));
#55959=CARTESIAN_POINT('Ctrl Pts',(5.71662802486233,-3.30667067493405,-6.76552224469707));
#55960=CARTESIAN_POINT('Ctrl Pts',(5.87283174034777,3.02057345711623,-6.48715296896679));
#55961=CARTESIAN_POINT('Ctrl Pts',(0.634959370610084,6.57349474634657,-6.20878369323653));
#55962=CARTESIAN_POINT('Ctrl Pts',(-5.1861037376981,4.08880295424966,-5.93041441750626));
#55963=CARTESIAN_POINT('Ctrl Pts',(-6.24384824386448,-2.15136185560887,
-5.65204514177599));
#55964=CARTESIAN_POINT('Ctrl Pts',(-1.56675487761984,-6.41554947533565,
-5.37367586604572));
#55965=CARTESIAN_POINT('Ctrl Pts',(4.54936735322769,-4.78719640305079,-5.09530659031545));
#55966=CARTESIAN_POINT('Ctrl Pts',(6.48699682467727,1.23809027700563,-4.81693731458518));
#55967=CARTESIAN_POINT('Ctrl Pts',(2.4664631218177,6.12621860550624,-4.53856803885491));
#55968=CARTESIAN_POINT('Ctrl Pts',(-3.81946222780992,5.38755070830706,-4.26019876312464));
#55969=CARTESIAN_POINT('Ctrl Pts',(-6.59729615370307,-0.299463181352188,
-3.98182948739437));
#55970=CARTESIAN_POINT('Ctrl Pts',(-3.31565960480102,-5.71142679251214,
-3.70346021166411));
#55971=CARTESIAN_POINT('Ctrl Pts',(3.01133685894659,-5.87757134360681,-3.42509093593384));
#55972=CARTESIAN_POINT('Ctrl Pts',(6.57248710337548,-0.645296761764896,
-3.14672166020357));
#55973=CARTESIAN_POINT('Ctrl Pts',(4.09695346479151,5.17966861116296,-2.8683523844733));
#55974=CARTESIAN_POINT('Ctrl Pts',(-2.14154121484956,6.24722304987754,-2.58998310874303));
#55975=CARTESIAN_POINT('Ctrl Pts',(-6.41307770751666,1.57684144270601,-2.31161383301276));
#55976=CARTESIAN_POINT('Ctrl Pts',(-4.7943443218783,-4.54183411606296,-2.03324455728249));
#55977=CARTESIAN_POINT('Ctrl Pts',(1.2278881678272,-6.48893560313017,-1.75487528155222));
#55978=CARTESIAN_POINT('Ctrl Pts',(6.12233256318639,-2.47609341527485,-1.47650600582196));
#55979=CARTESIAN_POINT('Ctrl Pts',(5.39355005832625,3.8109857495363,-1.19813673009168));
#55980=CARTESIAN_POINT('Ctrl Pts',(-0.289088752394491,6.59775888526443,
-0.919767454361418));
#55981=CARTESIAN_POINT('Ctrl Pts',(-5.70620594500332,3.32463657084714,-0.641398178631146));
#55982=CARTESIAN_POINT('Ctrl Pts',(-5.88229932251409,-3.00209082062202,
-0.36302890290088));
#55983=CARTESIAN_POINT('Ctrl Pts',(-0.655631016724059,-6.57146426489795,
-0.0846596271706075));
#55984=CARTESIAN_POINT('Ctrl Pts',(5.17321986111141,-4.10509328560812,0.193709648559658));
#55985=CARTESIAN_POINT('Ctrl Pts',(6.25058284067101,2.13171498255206,0.472078924289931));
#55986=CARTESIAN_POINT('Ctrl Pts',(1.58692387993814,6.41059023914432,0.750448200020196));
#55987=CARTESIAN_POINT('Ctrl Pts',(-4.53428952724171,4.80148030278988,1.02881747575047));
#55988=CARTESIAN_POINT('Ctrl Pts',(-6.49085840076931,-1.21768297848549,
1.30718675148073));
#55989=CARTESIAN_POINT('Ctrl Pts',(-2.48571755217521,-6.11843140565777,
1.58555602721101));
#55990=CARTESIAN_POINT('Ctrl Pts',(3.80249982994736,-5.39953605953158,1.86392530294127));
#55991=CARTESIAN_POINT('Ctrl Pts',(6.59820531227598,0.278713602079585,2.14229457867155));
#55992=CARTESIAN_POINT('Ctrl Pts',(3.33360531111273,5.70097099138844,2.42066385440181));
#55993=CARTESIAN_POINT('Ctrl Pts',(-2.99283735644156,5.88701275459968,2.69903313013208));
#55994=CARTESIAN_POINT('Ctrl Pts',(-6.57042517877034,0.665963651494575,
2.97740240586235));
#55995=CARTESIAN_POINT('Ctrl Pts',(-4.11322295513127,-5.1667583199055,3.25577168159262));
#55996=CARTESIAN_POINT('Ctrl Pts',(2.1218834788284,-6.25392717555989,3.53414095732289));
#55997=CARTESIAN_POINT('Ctrl Pts',(6.40808691970446,-1.59700239337454,3.81251023305315));
#55998=CARTESIAN_POINT('Ctrl Pts',(4.80860441111101,4.52673372669247,4.09087950878343));
#55999=CARTESIAN_POINT('Ctrl Pts',(-1.20747477815584,6.49276514861342,4.36924878451369));
#56000=CARTESIAN_POINT('Ctrl Pts',(-6.11451511929506,2.49533554273639,4.64761806024396));
#56001=CARTESIAN_POINT('Ctrl Pts',(-5.40550870944644,-3.7940045080403,4.92598733597424));
#56002=CARTESIAN_POINT('Ctrl Pts',(0.268337762589008,-6.59863542409339,
5.20435661170449));
#56003=CARTESIAN_POINT('Ctrl Pts',(5.69572194115494,-3.34256580847368,5.48272588743478));
#56004=CARTESIAN_POINT('Ctrl Pts',(5.89171163003959,2.9835764919619,5.76109516316503));
#56005=CARTESIAN_POINT('Ctrl Pts',(0.676294639557663,6.56936984614483,6.03946443889531));
#56006=CARTESIAN_POINT('Ctrl Pts',(-5.16028400300898,4.12134245400949,6.31783371462558));
#56007=CARTESIAN_POINT('Ctrl Pts',(-6.25725604654667,-2.11204672838612,
6.59620299035585));
#56008=CARTESIAN_POINT('Ctrl Pts',(-1.60707695795029,-6.40556775517648,
6.87457226608611));
#56009=CARTESIAN_POINT('Ctrl Pts',(4.51916673302206,-4.81571662933754,7.15294154181639));
#56010=CARTESIAN_POINT('Ctrl Pts',(6.4946558419881,1.19726359213888,7.43131081754665));
#56011=CARTESIAN_POINT('Ctrl Pts',(2.50494736315481,6.11058371375067,7.70968009327693));
#56012=CARTESIAN_POINT('Ctrl Pts',(-3.78549980480989,5.41146799331898,7.98804936900718));
#56013=CARTESIAN_POINT('Ctrl Pts',(-6.5990492196591,-0.25796125958747,8.26641864473747));
#56014=CARTESIAN_POINT('Ctrl Pts',(-3.35151804077057,-5.69045880727739,
8.54478792046771));
#56015=CARTESIAN_POINT('Ctrl Pts',(2.97430825008044,-5.89639593721748,8.82315719619802));
#56016=CARTESIAN_POINT('Ctrl Pts',(6.56829826963177,-0.686623955366883,
9.10152647192824));
#56017=CARTESIAN_POINT('Ctrl Pts',(4.12945176216551,5.15379692643003,9.37989574765855));
#56018=CARTESIAN_POINT('Ctrl Pts',(-2.10220475554805,6.26056944540052,9.65826502338879));
#56019=CARTESIAN_POINT('Ctrl Pts',(-6.40303275178956,1.61714754875415,9.93663429911908));
#56020=CARTESIAN_POINT('Ctrl Pts',(-4.82281693988325,-4.51158856494102,
10.2150035748493));
#56021=CARTESIAN_POINT('Ctrl Pts',(1.18704944568345,-6.49653047621837,10.4933728505796));
#56022=CARTESIAN_POINT('Ctrl Pts',(6.10663719874576,-2.51455298966355,10.7717421263099));
#56023=CARTESIAN_POINT('Ctrl Pts',(5.41741389641379,3.77698574128553,11.0501114020401));
#56024=CARTESIAN_POINT('Ctrl Pts',(-0.247584118732828,6.59944669794996,
11.3284806777704));
#56025=CARTESIAN_POINT('Ctrl Pts',(-5.68518160276977,3.36046198586736,11.6068499535007));
#56026=CARTESIAN_POINT('Ctrl Pts',(-5.9010656645506,-2.96503265371453,11.885219229231));
#56027=CARTESIAN_POINT('Ctrl Pts',(-0.696951573381226,-6.56721045188083,
12.1635885049612));
#56028=CARTESIAN_POINT('Ctrl Pts',(5.14729710620909,-4.13755085954758,12.4419577806915));
#56029=CARTESIAN_POINT('Ctrl Pts',(6.26386736392848,2.09235758465016,12.7203270564218));
#56030=CARTESIAN_POINT('Ctrl Pts',(1.62721414088477,6.40048191581196,12.998696332152));
#56031=CARTESIAN_POINT('Ctrl Pts',(-4.5039992411877,4.82990532519139,13.2770656078823));
#56032=CARTESIAN_POINT('Ctrl Pts',(-6.49838904666884,-1.17683236404584,
13.5554348836125));
#56033=CARTESIAN_POINT('Ctrl Pts',(-2.5241523985111,-6.1026755840387,13.8338041593428));
#56034=CARTESIAN_POINT('Ctrl Pts',(3.76846233851968,-5.42334640402861,14.1121734350731));
#56035=CARTESIAN_POINT('Ctrl Pts',(6.59982785798315,0.237206365684181,14.3905427108034));
#56036=CARTESIAN_POINT('Ctrl Pts',(3.36939762164865,5.67989034068083,14.6689119865337));
#56037=CARTESIAN_POINT('Ctrl Pts',(-2.95574972579951,5.90572080049231,14.9472812622639));
#56038=CARTESIAN_POINT('Ctrl Pts',(-6.56610639558182,0.707277468064,15.2256505379942));
#56039=CARTESIAN_POINT('Ctrl Pts',(-4.14563972612946,-5.14078455841797,
15.5040198137245));
#56040=CARTESIAN_POINT('Ctrl Pts',(2.08250524004114,-6.26714979397594,15.7823890894547));
#56041=CARTESIAN_POINT('Ctrl Pts',(6.39791525355102,-1.63727670945095,16.060758365185));
#56042=CARTESIAN_POINT('Ctrl Pts',(4.83698176773478,4.49639878052789,16.3391276409153));
#56043=CARTESIAN_POINT('Ctrl Pts',(-1.16661237248937,6.50023154874395,16.6174969166455));
#56044=CARTESIAN_POINT('Ctrl Pts',(-6.09869887942524,2.53374556596133,16.8958661923758));
#56045=CARTESIAN_POINT('Ctrl Pts',(-5.42926550149442,-3.7599296175878,17.1742354681061));
#56046=CARTESIAN_POINT('Ctrl Pts',(0.226828026102262,-6.60019269881615,
17.4526047438363));
#56047=CARTESIAN_POINT('Ctrl Pts',(5.6745850340942,-3.37832492601962,17.7309740195666));
#56048=CARTESIAN_POINT('Ctrl Pts',(5.91036133353191,2.94645948928919,18.0093432952969));
#56049=CARTESIAN_POINT('Ctrl Pts',(0.717601613882474,6.5649861034647,18.2877125710271));
#56050=CARTESIAN_POINT('Ctrl Pts',(-5.13425929916017,4.1537183419099,18.5660818467574));
#56051=CARTESIAN_POINT('Ctrl Pts',(-6.27041672742644,-2.0726477460828,18.8444511224877));
#56052=CARTESIAN_POINT('Ctrl Pts',(-1.64733522957113,-6.39533277135328,
19.1228203982179));
#56053=CARTESIAN_POINT('Ctrl Pts',(4.4887872017552,-4.84404625001559,19.4011896739482));
#56054=CARTESIAN_POINT('Ctrl Pts',(6.50205797788772,1.15638949628489,19.6795589496785));
#56055=CARTESIAN_POINT('Ctrl Pts',(2.54333246829336,6.09470709473853,19.9579282254088));
#56056=CARTESIAN_POINT('Ctrl Pts',(-3.75138759958863,5.43517117417511,20.236297501139));
#56057=CARTESIAN_POINT('Ctrl Pts',(-6.60054121954685,-0.216449125649467,
20.5146667768693));
#56058=CARTESIAN_POINT('Ctrl Pts',(-3.3872438769059,-5.6692656961281,20.7930360525995));
#56059=CARTESIAN_POINT('Ctrl Pts',(2.9371619671552,-5.91498725219492,21.0714053283298));
#56060=CARTESIAN_POINT('Ctrl Pts',(6.5638495782996,-0.727923985308585,21.3497746040601));
#56061=CARTESIAN_POINT('Ctrl Pts',(4.1617866869132,5.12772134457041,21.6281438797904));
#56062=CARTESIAN_POINT('Ctrl Pts',(-2.06278512714925,6.27366815620202,21.9065131555207));
#56063=CARTESIAN_POINT('Ctrl Pts',(-6.39273447560434,1.65738967637402,22.1848824312509));
#56064=CARTESIAN_POINT('Ctrl Pts',(-4.85109875456583,-4.48116452369038,
22.4632517069812));
#56065=CARTESIAN_POINT('Ctrl Pts',(1.14616376071003,-6.50386832958405,22.7416209827114));
#56066=CARTESIAN_POINT('Ctrl Pts',(6.09070023984887,-2.55291308180212,23.0199902584417));
#56067=CARTESIAN_POINT('Ctrl Pts',(5.44106340746798,3.74283630564365,23.298359534172));
#56068=CARTESIAN_POINT('Ctrl Pts',(-0.20606968998917,6.60087341931348,23.5767288099022));
#56069=CARTESIAN_POINT('Ctrl Pts',(-5.66393233993547,3.39615445225397,23.8550980856326));
#56070=CARTESIAN_POINT('Ctrl Pts',(-5.91959854504302,-2.92785718238713,
24.1334673613628));
#56071=CARTESIAN_POINT('Ctrl Pts',(-0.738244556818558,-6.56269682289676,
24.4118366370931));
#56072=CARTESIAN_POINT('Ctrl Pts',(5.12117071081501,-4.16984474118904,24.6902059128233));
#56073=CARTESIAN_POINT('Ctrl Pts',(6.27690407226291,2.05291740762767,24.9685751885536));
#56074=CARTESIAN_POINT('Ctrl Pts',(1.66744002499811,6.39012037272897,25.2469444642839));
#56075=CARTESIAN_POINT('Ctrl Pts',(-4.47353076518193,4.85813926394686,25.5253137400141));
#56076=CARTESIAN_POINT('Ctrl Pts',(-6.50566259935649,-1.13593519104989,
25.8036830157444));
#56077=CARTESIAN_POINT('Ctrl Pts',(-2.56248738279775,-6.08667832466393,
26.0820522914747));
#56078=CARTESIAN_POINT('Ctrl Pts',(3.73427575689756,-5.4469421868034,26.360421567205));
#56079=CARTESIAN_POINT('Ctrl Pts',(6.6011892972946,0.195689744786494,26.6387908429352));
#56080=CARTESIAN_POINT('Ctrl Pts',(3.40505663003075,5.65858497870404,26.9171601186655));
#56081=CARTESIAN_POINT('Ctrl Pts',(-2.91854515799281,5.92419520067394,27.1955293943957));
#56082=CARTESIAN_POINT('Ctrl Pts',(-6.56152784010658,0.748563302892809,
27.4738986701261));
#56083=CARTESIAN_POINT('Ctrl Pts',(-4.17789248481245,-5.11460741409143,
27.7522679458563));
#56084=CARTESIAN_POINT('Ctrl Pts',(2.04304461191766,-6.28012446760776,28.0306372215866));
#56085=CARTESIAN_POINT('Ctrl Pts',(6.38749046919093,-1.67748625059234,28.3090064973168));
#56086=CARTESIAN_POINT('Ctrl Pts',(4.86516776074983,4.46588594510562,28.5873757730471));
#56087=CARTESIAN_POINT('Ctrl Pts',(-1.12570381259618,6.50744078276843,28.8657450487773));
#56088=CARTESIAN_POINT('Ctrl Pts',(-6.0826413591286,2.57205534760617,29.1441143245077));
#56089=CARTESIAN_POINT('Ctrl Pts',(-5.45280749764514,-3.72570597451763,
29.4224836002379));
#56090=CARTESIAN_POINT('Ctrl Pts',(0.185309315707581,-6.60148885270917,
29.7008528759682));
#56091=CARTESIAN_POINT('Ctrl Pts',(5.653223625656,-3.41395038822422,29.9792221516984));
#56092=CARTESIAN_POINT('Ctrl Pts',(5.92877720772165,2.90922591699779,30.2575914274287));
#56093=CARTESIAN_POINT('Ctrl Pts',(0.758880198016653,6.56034263281954,30.535960703159));
#56094=CARTESIAN_POINT('Ctrl Pts',(-5.10803147062861,4.18592989788399,30.8143299788893));
#56095=CARTESIAN_POINT('Ctrl Pts',(-6.28332933427362,-2.03316676443131,
31.0926992546195));
#56096=CARTESIAN_POINT('Ctrl Pts',(-1.68752832831564,-6.38484477149316,
31.3710685303498));
#56097=CARTESIAN_POINT('Ctrl Pts',(4.45823008236447,-4.87218422759566,31.6494378060801));
#56098=CARTESIAN_POINT('Ctrl Pts',(6.50920287542301,1.11546965064781,31.9278070818103));
#56099=CARTESIAN_POINT('Ctrl Pts',(2.58161695256905,6.07858935322493,32.2061763575406));
#56100=CARTESIAN_POINT('Ctrl Pts',(-3.71712697969412,5.45865932549019,32.4845456332708));
#56101=CARTESIAN_POINT('Ctrl Pts',(-6.60177208481647,-0.174928428419658,
32.7629149090012));
#56102=CARTESIAN_POINT('Ctrl Pts',(-3.42283570484306,-5.64784829404818,
33.0412841847314));
#56103=CARTESIAN_POINT('Ctrl Pts',(2.89989948244532,-5.93334455485646,33.3196534604617));
#56104=CARTESIAN_POINT('Ctrl Pts',(6.55914120396629,-0.769195216679829,
33.5980227361919));
#56105=CARTESIAN_POINT('Ctrl Pts',(4.1939569605299,5.1014428966866,33.8763920119222));
#56106=CARTESIAN_POINT('Ctrl Pts',(-2.02328388959324,6.28651866433592,34.1547612876525));
#56107=CARTESIAN_POINT('Ctrl Pts',(-6.38218328617755,1.6975662333374,34.4331305633827));
#56108=CARTESIAN_POINT('Ctrl Pts',(-4.87918864713492,-4.45056319588893,
34.711499839113));
#56109=CARTESIAN_POINT('Ctrl Pts',(1.10523273051034,-6.51094887296314,34.9898691148433));
#56110=CARTESIAN_POINT('Ctrl Pts',(6.07452231697217,-2.59117217404372,35.2682383905736));
#56111=CARTESIAN_POINT('Ctrl Pts',(5.46449765586899,3.70853879364014,35.5466076663039));
#56112=CARTESIAN_POINT('Ctrl Pts',(-0.164547108591434,6.60203899291617,
35.8249769420341));
#56113=CARTESIAN_POINT('Ctrl Pts',(-5.64245899717211,3.43171255791666,36.1033462177644));
#56114=CARTESIAN_POINT('Ctrl Pts',(-5.9378972307847,-2.8905658773968,36.3817154934946));
#56115=CARTESIAN_POINT('Ctrl Pts',(-0.779508333376514,-6.55792355651757,
36.6600847692249));
#56116=CARTESIAN_POINT('Ctrl Pts',(5.09484170855686,-4.2019736529018,36.9384540449552));
#56117=CARTESIAN_POINT('Ctrl Pts',(6.28969244990843,2.01339601184075,37.2168233206854));
#56118=CARTESIAN_POINT('Ctrl Pts',(1.70759994083701,6.37950601982511,37.4951925964157));
#56119=CARTESIAN_POINT('Ctrl Pts',(-4.44288530463679,4.88618100204791,37.773561872146));
#56120=CARTESIAN_POINT('Ctrl Pts',(-6.51267877107156,-1.09499307749649,
38.0519311478762));
#56121=CARTESIAN_POINT('Ctrl Pts',(-2.60072098840308,-6.07044026042684,
38.3303004236065));
#56122=CARTESIAN_POINT('Ctrl Pts',(3.69994143759137,-5.47032247434516,38.6086696993368));
#56123=CARTESIAN_POINT('Ctrl Pts',(6.60228957634829,0.154165381892458,38.887038975067));
#56124=CARTESIAN_POINT('Ctrl Pts',(3.44058092549562,5.63705574835366,39.1654082507973));
#56125=CARTESIAN_POINT('Ctrl Pts',(-2.88122512493104,5.94243522424916,39.4437775265276));
#56126=CARTESIAN_POINT('Ctrl Pts',(-6.55668969348419,0.789819522605984,
39.7221468022579));
#56127=CARTESIAN_POINT('Ctrl Pts',(-4.20997995517711,-5.08822792256188,
40.0005160779881));
#56128=CARTESIAN_POINT('Ctrl Pts',(2.00350315562306,-6.29285068314352,40.2788853537184));
#56129=CARTESIAN_POINT('Ctrl Pts',(6.37681297905581,-1.71762942600455,40.5572546294486));
#56130=CARTESIAN_POINT('Ctrl Pts',(4.89316127504496,4.43519642759279,40.835623905179));
#56131=CARTESIAN_POINT('Ctrl Pts',(-1.0847507169254,6.5143925654708,41.1139931809092));
#56132=CARTESIAN_POINT('Ctrl Pts',(-6.06634319368244,2.61026337203627,41.3923624566395));
#56133=CARTESIAN_POINT('Ctrl Pts',(-5.47613376651594,-3.69133493280621,
41.6707317323698));
#56134=CARTESIAN_POINT('Ctrl Pts',(0.143783273993165,-6.60252383449323,
41.9491010081));
#56135=CARTESIAN_POINT('Ctrl Pts',(5.63163856095328,-3.44944078565142,42.2274702838303));
#56136=CARTESIAN_POINT('Ctrl Pts',(5.94695852402892,2.87187724814471,42.5058395595606));
#56137=CARTESIAN_POINT('Ctrl Pts',(0.800128758871884,6.55543961791714,42.7842088352908));
#56138=CARTESIAN_POINT('Ctrl Pts',(-5.08160155505548,4.21797584755876,43.0625781110211));
#56139=CARTESIAN_POINT('Ctrl Pts',(-6.29599335623184,-1.99360534540212,
43.3409473867513));
#56140=CARTESIAN_POINT('Ctrl Pts',(-1.72765466404024,-6.37410417052871,
43.6193166624817));
#56141=CARTESIAN_POINT('Ctrl Pts',(4.42749658376913,-4.90012944886603,43.8976859382118));
#56142=CARTESIAN_POINT('Ctrl Pts',(6.51609025192318,1.07450567412324,44.1760552139422));
#56143=CARTESIAN_POINT('Ctrl Pts',(2.61979930134795,6.06223112686972,44.4544244896724));
#56144=CARTESIAN_POINT('Ctrl Pts',(-3.68271930056586,5.4819315180118,44.7327937654027));
#56145=CARTESIAN_POINT('Ctrl Pts',(-6.60274176677173,-0.133400810565267,
45.011163041133));
#56146=CARTESIAN_POINT('Ctrl Pts',(-3.45829211647637,-5.62620744836598,
45.2895323168632));
#56147=CARTESIAN_POINT('Ctrl Pts',(2.86252227015201,-5.95146711893926,45.5679015925936));
#56148=CARTESIAN_POINT('Ctrl Pts',(6.5541733329074,-0.810436016682913,45.8462708683237));
#56149=CARTESIAN_POINT('Ctrl Pts',(4.22596131027567,5.07496262242242,46.1246401440542));
#56150=CARTESIAN_POINT('Ctrl Pts',(-1.98370260565189,6.2991204614026,46.4030094197842));
#56151=CARTESIAN_POINT('Ctrl Pts',(-6.37137960094171,1.73767563015518,46.6813786955147));
#56152=CARTESIAN_POINT('Ctrl Pts',(-4.90708550628124,-4.41978579220487,
46.9597479712447));
#56153=CARTESIAN_POINT('Ctrl Pts',(1.06425797442239,-6.51777182623093,47.2381172469752));
#56154=CARTESIAN_POINT('Ctrl Pts',(6.05810407015644,-2.62932875275904,47.5164865227053));
#56155=CARTESIAN_POINT('Ctrl Pts',(5.48771571449694,3.67409456217375,47.7948557984358));
#56156=CARTESIAN_POINT('Ctrl Pts',(-0.123018017281035,6.60294337264493,
48.0732250741659));
#56157=CARTESIAN_POINT('Ctrl Pts',(-5.62076242402099,3.46713489608425,48.3515943498962));
#56158=CARTESIAN_POINT('Ctrl Pts',(-5.95596099783199,-2.85316021408464,
48.6299636256265));
#56159=CARTESIAN_POINT('Ctrl Pts',(-0.820741270552748,-6.55289084158609,
48.9083329013567));
#56160=CARTESIAN_POINT('Ctrl Pts',(5.06831114107852,-4.23393632358243,49.186702177087));
#56161=CARTESIAN_POINT('Ctrl Pts',(6.30223199092358,1.9737949608586,49.4650714528173));
#56162=CARTESIAN_POINT('Ctrl Pts',(1.74769229957064,6.36863927703186,49.7434407285475));
#56163=CARTESIAN_POINT('Ctrl Pts',(-4.41206407196639,4.91402943009041,50.0218100042778));
#56164=CARTESIAN_POINT('Ctrl Pts',(-6.51943728423605,-1.05400764316224,
50.3001792800081));
#56165=CARTESIAN_POINT('Ctrl Pts',(-2.63885170270617,-6.05396203374749,
50.5785485557384));
#56166=CARTESIAN_POINT('Ctrl Pts',(3.66546073895617,-5.49348634166886,50.8569178314686));
#56167=CARTESIAN_POINT('Ctrl Pts',(6.60312865161432,0.112634919813896,51.1352871071989));
#56168=CARTESIAN_POINT('Ctrl Pts',(3.47596910260962,5.61530350138215,51.4136563829291));
#56169=CARTESIAN_POINT('Ctrl Pts',(-2.84379110309206,5.96044014959515,51.6920256586594));
#56170=CARTESIAN_POINT('Ctrl Pts',(-6.5515921471244,0.831044494999726,51.9703949343897));
#56171=CARTESIAN_POINT('Ctrl Pts',(-4.24190086775932,-5.06164712747087,
52.24876421012));
#56172=CARTESIAN_POINT('Ctrl Pts',(1.96388243552059,-6.3053279371009,52.5271334858502));
#56173=CARTESIAN_POINT('Ctrl Pts',(6.36588320557505,-1.75770464751873,52.8055027615806));
#56174=CARTESIAN_POINT('Ctrl Pts',(4.92096120312361,4.40433144214688,53.0838720373107));
#56175=CARTESIAN_POINT('Ctrl Pts',(-1.04375470568844,6.52108662182038,53.3622413130411));
#56176=CARTESIAN_POINT('Ctrl Pts',(-6.04980502788473,2.64836812764239,53.6406105887712));
#56177=CARTESIAN_POINT('Ctrl Pts',(-5.4992433852587,-3.65681785226164,53.9189798645017));
#56178=CARTESIAN_POINT('Ctrl Pts',(0.102251543837575,-6.60329760322176,
54.1973491402318));
#56179=CARTESIAN_POINT('Ctrl Pts',(5.60983069394753,-3.48479471420852,54.4757184159621));
#56180=CARTESIAN_POINT('Ctrl Pts',(5.96490456315336,2.83441496034078,54.7540876916924));
#56181=CARTESIAN_POINT('Ctrl Pts',(0.8413456645475,6.55027725273354,55.0324569674226));
#56182=CARTESIAN_POINT('Ctrl Pts',(-5.05497059807721,4.24985492311284,55.310826243153));
#56183=CARTESIAN_POINT('Ctrl Pts',(-6.30840829227937,-1.95396505414819,
55.5891955188831));
#56184=CARTESIAN_POINT('Ctrl Pts',(-1.76771264924237,-6.36311139338609,
55.8675647946135));
#56185=CARTESIAN_POINT('Ctrl Pts',(4.39658792186652,-4.92788080824088,56.1459340703437));
#56186=CARTESIAN_POINT('Ctrl Pts',(6.52271983490569,1.03349918735298,56.424303346074));
#56187=CARTESIAN_POINT('Ctrl Pts',(2.65787800403672,6.04563306284703,56.7026726218042));
#56188=CARTESIAN_POINT('Ctrl Pts',(-3.64816592346122,5.50498683103127,56.9810418975345));
#56189=CARTESIAN_POINT('Ctrl Pts',(-6.60345022704949,-0.091867915026958,
57.2594111732648));
#56190=CARTESIAN_POINT('Ctrl Pts',(-3.49361170905798,-5.60434401524959,
57.537780448995));
#56191=CARTESIAN_POINT('Ctrl Pts',(2.82503180901495,-5.96935422746755,57.8161497247253));
#56192=CARTESIAN_POINT('Ctrl Pts',(6.54894616166488,-0.851644753724631,
58.0945190004557));
#56193=CARTESIAN_POINT('Ctrl Pts',(4.25779846997512,5.04828156940651,58.3728882761858));
#56194=CARTESIAN_POINT('Ctrl Pts',(-1.94404284126394,6.3114730488422,58.6512575519163));
#56195=CARTESIAN_POINT('Ctrl Pts',(-6.36032384731875,1.777716279995,58.9296268276463));
#56196=CARTESIAN_POINT('Ctrl Pts',(-4.9347882283323,-4.38883353027258,59.2079961033768));
#56197=CARTESIAN_POINT('Ctrl Pts',(1.02324111351451,-6.52433691945361,59.4863653791069));
#56198=CARTESIAN_POINT('Ctrl Pts',(6.04144614895033,-2.66738130837423,59.7647346548373));
#56199=CARTESIAN_POINT('Ctrl Pts',(5.51071666478489,3.63950497394812,60.0431039305674));
#56200=CARTESIAN_POINT('Ctrl Pts',(-0.0814840590571557,6.60358652272017,
60.3214732062978));
#56201=CARTESIAN_POINT('Ctrl Pts',(-5.59884347885518,3.5024200653566,60.599842482028));
#56202=CARTESIAN_POINT('Ctrl Pts',(-5.97378913153509,-2.81564167231632,
60.8782117577583));
#56203=CARTESIAN_POINT('Ctrl Pts',(-0.861941737064719,-6.54759887720963,
61.1565810334886));
#56204=CARTESIAN_POINT('Ctrl Pts',(5.04158005799836,-4.26573148870439,61.4349503092188));
#56205=CARTESIAN_POINT('Ctrl Pts',(6.31452219921142,1.93411582140191,61.7133195849491));
#56206=CARTESIAN_POINT('Ctrl Pts',(1.78771551504092,6.35752057426587,61.9916888606794));
#56207=CARTESIAN_POINT('Ctrl Pts',(-4.38106828653906,4.94168344631802,62.2700581364097));
#56208=CARTESIAN_POINT('Ctrl Pts',(-6.5259378714655,-1.01298050953772,62.5484274121399));
#56209=CARTESIAN_POINT('Ctrl Pts',(-2.67687801715671,-6.03724429654741,
62.8267966878701));
#56210=CARTESIAN_POINT('Ctrl Pts',(3.6308350251382,-5.51643287235161,63.1051659636005));
#56211=CARTESIAN_POINT('Ctrl Pts',(6.6037064898967,0.0711000016040934,63.3835352393307));
#56212=CARTESIAN_POINT('Ctrl Pts',(3.51121976132422,5.59332909836506,63.661904515061));
#56213=CARTESIAN_POINT('Ctrl Pts',(-2.80624457346302,5.97820926439015,63.9402737907912));
#56214=CARTESIAN_POINT('Ctrl Pts',(-6.54623540269939,0.872236589107022,
64.2186430665216));
#56215=CARTESIAN_POINT('Ctrl Pts',(-4.2736539596849,-5.03486608042374,64.4970123422518));
#56216=CARTESIAN_POINT('Ctrl Pts',(1.92418401910897,-6.31755573584725,64.775381617982));
#56217=CARTESIAN_POINT('Ctrl Pts',(6.35470158115881,-1.79771032965511,65.0537508937123));
#56218=CARTESIAN_POINT('Ctrl Pts',(4.94856644514845,4.37329220986693,65.3321201694426));
#56219=CARTESIAN_POINT('Ctrl Pts',(-1.00271740079401,6.52752268698292,65.6104894451728));
#56220=CARTESIAN_POINT('Ctrl Pts',(-6.03302751602829,2.68636810690132,65.8888587209031));
#56221=CARTESIAN_POINT('Ctrl Pts',(-5.52213543959689,-3.62215609846939,
66.1672279966334));
#56222=CARTESIAN_POINT('Ctrl Pts',(0.0607157683442206,-6.60381012828248,
66.4455972723636));
#56223=CARTESIAN_POINT('Ctrl Pts',(5.58780088741481,-3.520010775202,66.723966548094));
#56224=CARTESIAN_POINT('Ctrl Pts',(5.9826146151029,2.79684053569169,67.0023358238242));
#56225=CARTESIAN_POINT('Ctrl Pts',(0.882529284395388,6.54485574150535,67.2807050995545));
#56226=CARTESIAN_POINT('Ctrl Pts',(-5.02813965328381,4.28156586332698,67.5590743752847));
#56227=CARTESIAN_POINT('Ctrl Pts',(-6.320573651249,-1.91424745894271,67.8374436510151));
#56228=CARTESIAN_POINT('Ctrl Pts',(-1.80770069912375,-6.35186687496823,
68.1158129267453));
#56229=CARTESIAN_POINT('Ctrl Pts',(4.36550531948381,-4.95543720780412,68.3941822024755));
#56230=CARTESIAN_POINT('Ctrl Pts',(6.52909136208694,0.992451812660304,68.6725514782058));
#56231=CARTESIAN_POINT('Ctrl Pts',(2.69585155414282,6.02879581781948,68.9509207539361));
#56232=CARTESIAN_POINT('Ctrl Pts',(-3.61346821540184,5.52782435242044,69.2292900296664));
#56233=CARTESIAN_POINT('Ctrl Pts',(-6.60389743762118,-0.0503313849543038,
69.5076593053966));
#56234=CARTESIAN_POINT('Ctrl Pts',(-3.52879308525274,-5.58225885967351,
69.786028581127));
#56235=CARTESIAN_POINT('Ctrl Pts',(2.78742958225481,-5.98700517278068,70.0643978568572));
#56236=CARTESIAN_POINT('Ctrl Pts',(6.54345989703921,-0.892819797479564,
70.3427671325874));
#56237=CARTESIAN_POINT('Ctrl Pts',(4.28946718006704,5.02140079321086,70.6211364083178));
#56238=CARTESIAN_POINT('Ctrl Pts',(-1.9043061654729,6.32357593795416,70.8995056840479));
#56239=CARTESIAN_POINT('Ctrl Pts',(-6.34901646270328,1.81768659874434,71.1778749597783));
#56240=CARTESIAN_POINT('Ctrl Pts',(-4.96229571729612,-4.3577076346442,71.4562442355084));
#56241=CARTESIAN_POINT('Ctrl Pts',(0.982183770520482,-6.53064389289886,
71.7346135112389));
#56242=CARTESIAN_POINT('Ctrl Pts',(6.02454921238457,-2.7053283354313,72.0129827869689));
#56243=CARTESIAN_POINT('Ctrl Pts',(5.53349959675533,3.60477139741766,72.2913520626995));
#56244=CARTESIAN_POINT('Ctrl Pts',(-0.0399468771114501,6.60396841769711,
72.5697213384295));
#56245=CARTESIAN_POINT('Ctrl Pts',(-5.57670302884517,3.53756666976046,72.84809061416));
#56246=CARTESIAN_POINT('Ctrl Pts',(-5.99138092656673,-2.77801173642291,
73.12645988989));
#56247=CARTESIAN_POINT('Ctrl Pts',(-0.903108102914542,-6.54204787275223,
73.4048291656205));
#56248=CARTESIAN_POINT('Ctrl Pts',(5.01464951686801,-4.2973578903679,73.6831984413506));
#56249=CARTESIAN_POINT('Ctrl Pts',(6.32656258853912,1.89436016328156,73.961567717081));
#56250=CARTESIAN_POINT('Ctrl Pts',(1.82766800382458,6.34615035141201,74.2399369928112));
#56251=CARTESIAN_POINT('Ctrl Pts',(-4.34989917462906,4.96914195666549,74.5183062685415));
#56252=CARTESIAN_POINT('Ctrl Pts',(-6.53218027557985,-0.971913299763653,
74.7966755442717));
#56253=CARTESIAN_POINT('Ctrl Pts',(-2.71479842733392,-6.02028771022417,
75.0750448200021));
#56254=CARTESIAN_POINT('Ctrl Pts',(3.59606566602131,-5.53916115856847,75.3534140957322));
#56255=CARTESIAN_POINT('Ctrl Pts',(6.60402306833451,0.029562270492965,75.6317833714626));
#56256=CARTESIAN_POINT('Ctrl Pts',(3.54633150703141,5.57113340866723,75.9101526471928));
#56257=CARTESIAN_POINT('Ctrl Pts',(-2.76858702148319,5.99574186564154,76.1885219229231));
#56258=CARTESIAN_POINT('Ctrl Pts',(-6.54061967213588,0.913394175260629,
76.4668911986534));
#56259=CARTESIAN_POINT('Ctrl Pts',(-4.30523797471837,-5.00788584094864,
76.7452604743836));
#56260=CARTESIAN_POINT('Ctrl Pts',(1.88440947696132,-6.32953359561905,77.0236297501139));
#56261=CARTESIAN_POINT('Ctrl Pts',(6.34326854818163,-1.83764488968394,77.3019990258441));
#56262=CARTESIAN_POINT('Ctrl Pts',(4.97597590898363,4.34207995874622,77.5803683015745));
#56263=CARTESIAN_POINT('Ctrl Pts',(-0.961640425785212,6.53370050633074,
77.8587375773046));
#56264=CARTESIAN_POINT('Ctrl Pts',(-6.01601132187544,2.72426180643463,78.1371068530351));
#56265=CARTESIAN_POINT('Ctrl Pts',(-5.54480902386091,-3.58735104273928,
78.4154761287652));
#56266=CARTESIAN_POINT('Ctrl Pts',(0.0191775907770066,-6.60406138939841,
78.6938454044956));
#56267=CARTESIAN_POINT('Ctrl Pts',(5.56555001291159,-3.55508757539258,78.9722146802257));
#56268=CARTESIAN_POINT('Ctrl Pts',(6.00008797922182,2.75915546073972,79.2505839559561));
#56269=CARTESIAN_POINT('Ctrl Pts',(0.923677989083838,6.53917529872184,79.5289532316863));
#56270=CARTESIAN_POINT('Ctrl Pts',(-5.00110978217752,4.3131074136334,79.8073225074166));
#56271=CARTESIAN_POINT('Ctrl Pts',(-6.3324889518473,-1.87445413111732,80.0856917831468));
#56272=CARTESIAN_POINT('Ctrl Pts',(-1.84761723165289,-6.34037106013766,
80.3640610588772));
#56273=CARTESIAN_POINT('Ctrl Pts',(4.33425000633009,-4.98279755735265,80.6424303346073));
#56274=CARTESIAN_POINT('Ctrl Pts',(6.53520458139265,0.95136517398707,80.9207996103378));
#56275=CARTESIAN_POINT('Ctrl Pts',(2.73371844933311,6.01172005791245,81.1991688860678));
#56276=CARTESIAN_POINT('Ctrl Pts',(-3.57862754911977,5.55044317866717,81.4775381617983));
#56277=CARTESIAN_POINT('Ctrl Pts',(-6.6040833807941,-0.00879286364105391,
81.7559074375284));
#56278=CARTESIAN_POINT('Ctrl Pts',(-3.56383485319324,-5.55995285538431,
82.0342767132588));
#56279=CARTESIAN_POINT('Ctrl Pts',(2.74971707751372,-6.00441925656099,82.3126459889889));
#56280=CARTESIAN_POINT('Ctrl Pts',(6.53771475608128,-0.933959518955791,
82.5910152647193));
#56281=CARTESIAN_POINT('Ctrl Pts',(4.32096618765487,4.99432135730924,82.8693845404496));
#56282=CARTESIAN_POINT('Ctrl Pts',(-1.86449415036578,6.33542864991657,83.1477538161797));
#56283=CARTESIAN_POINT('Ctrl Pts',(-6.33745789444466,1.85758500507299,83.4261230919102));
#56284=CARTESIAN_POINT('Ctrl Pts',(-4.98960688490476,-4.32640933674127,
83.7044923676402));
#56285=CARTESIAN_POINT('Ctrl Pts',(0.941087569775988,-6.53669249704657,
83.9828616433708));
#56286=CARTESIAN_POINT('Ctrl Pts',(6.00741392894626,-2.74316833264646,84.2612309191007));
#56287=CARTESIAN_POINT('Ctrl Pts',(5.5560636090558,3.56989520673322,84.5396001948314));
#56288=CARTESIAN_POINT('Ctrl Pts',(0.00159188523690413,6.60408904246697,
84.8179694705613));
#56289=CARTESIAN_POINT('Ctrl Pts',(-5.55434194992508,3.57257331880457,85.0963387462919));
#56290=CARTESIAN_POINT('Ctrl Pts',(-6.00873568694944,-2.74027189514327,
85.3747080220218));
#56291=CARTESIAN_POINT('Ctrl Pts',(-0.944238739453256,-6.53623804782589,
85.6530772977524));
#56292=CARTESIAN_POINT('Ctrl Pts',(4.98752058312948,-4.32881427735017,85.9314465734823));
#56293=CARTESIAN_POINT('Ctrl Pts',(6.33835268255775,1.85452955933434,86.2098158492128));
#56294=CARTESIAN_POINT('Ctrl Pts',(1.86754818529735,6.33452905830612,86.4881851249431));
#56295=CARTESIAN_POINT('Ctrl Pts',(-4.31855796936763,4.99640387480258,86.7665544006733));
#56296=CARTESIAN_POINT('Ctrl Pts',(-6.53816424961312,-0.930807638565494,
87.0449236764036));
#56297=CARTESIAN_POINT('Ctrl Pts',(-2.7526114330082,-6.00309294562432,87.3232929521339));
#56298=CARTESIAN_POINT('Ctrl Pts',(3.56115403717188,-5.56167030112953,87.6016622278641));
#56299=CARTESIAN_POINT('Ctrl Pts',(6.60407837440324,-0.0119766301783775,
87.8800315035943));
#56300=CARTESIAN_POINT('Ctrl Pts',(3.58130295061876,5.5487173104079,88.1584007793249));
#56301=CARTESIAN_POINT('Ctrl Pts',(-2.73081993698305,6.01303725971391,88.4367700550547));
#56302=CARTESIAN_POINT('Ctrl Pts',(-6.53474517760702,0.954515625159502,
88.7151393307855));
#56303=CARTESIAN_POINT('Ctrl Pts',(-4.33665166331373,-4.98070747645445,
88.9935086065153));
#56304=CARTESIAN_POINT('Ctrl Pts',(1.84456038266226,-6.34126104254065,89.2718778822459));
#56305=CARTESIAN_POINT('Ctrl Pts',(6.33158455896374,-1.87750674769037,89.5502471579759));
#56306=CARTESIAN_POINT('Ctrl Pts',(5.00318851023979,4.31069592362259,89.8286164337064));
#56307=CARTESIAN_POINT('Ctrl Pts',(-0.92052540577437,6.53961983545342,90.1069857094364));
#56308=CARTESIAN_POINT('Ctrl Pts',(-5.99875711863103,2.76204772706856,90.385354985167));
#56309=CARTESIAN_POINT('Ctrl Pts',(-5.56726324102471,-3.55240406204953,
90.6637242608969));
#56310=CARTESIAN_POINT('Ctrl Pts',(-0.0223613455058675,-6.60405137662928,
90.9420935366275));
#56311=CARTESIAN_POINT('Ctrl Pts',(5.54307895074079,-3.59002372705058,91.2204628123576));
#56312=CARTESIAN_POINT('Ctrl Pts',(6.01732396421797,2.72136122640474,91.4988320880879));
#56313=CARTESIAN_POINT('Ctrl Pts',(0.964790150663175,6.53323614911586,91.7772013638182));
#56314=CARTESIAN_POINT('Ctrl Pts',(-4.97388205413045,4.34447832616656,92.0555706395484));
#56315=CARTESIAN_POINT('Ctrl Pts',(-6.34415372267409,-1.83458664500002,
92.3339399152788));
#56316=CARTESIAN_POINT('Ctrl Pts',(-1.88746066762744,-6.32862440369867,
92.6123091910088));
#56317=CARTESIAN_POINT('Ctrl Pts',(4.30282321894659,-5.00996077443976,92.8906784667394));
#56318=CARTESIAN_POINT('Ctrl Pts',(6.5410592509681,0.910240896827098,93.1690477424694));
#56319=CARTESIAN_POINT('Ctrl Pts',(2.77147719149483,5.99440645868761,93.4474170181999));
#56320=CARTESIAN_POINT('Ctrl Pts',(-3.54364530300244,5.57284241491177,93.7257862939299));
#56321=CARTESIAN_POINT('Ctrl Pts',(-6.60400804921164,0.0327460055409614,
94.0041555696604));
#56322=CARTESIAN_POINT('Ctrl Pts',(-3.59873562653636,-5.53742688486538,
94.2825248453905));
#56323=CARTESIAN_POINT('Ctrl Pts',(2.71189578679664,-6.02159578986222,94.560894121121));
#56324=CARTESIAN_POINT('Ctrl Pts',(6.531710966084,-0.975062290558369,94.839263396851));
#56325=CARTESIAN_POINT('Ctrl Pts',(4.35229424655544,4.96704433303463,95.1176326725814));
#56326=CARTESIAN_POINT('Ctrl Pts',(-1.82460837100929,6.3470307158052,95.3960019483117));
#56327=CARTESIAN_POINT('Ctrl Pts',(-6.32564859983025,1.89740992049619,95.674371224042));
#56328=CARTESIAN_POINT('Ctrl Pts',(-5.01672065065709,-4.29493987480636,
95.9527404997721));
#56329=CARTESIAN_POINT('Ctrl Pts',(0.899954137153977,-6.54248249259793,
96.2311097755025));
#56330=CARTESIAN_POINT('Ctrl Pts',(5.99004097655152,-2.78089980297108,96.5094790512327));
#56331=CARTESIAN_POINT('Ctrl Pts',(5.57840780899557,3.53487778168767,96.7878483269631));
#56332=CARTESIAN_POINT('Ctrl Pts',(0.0431305846059591,6.60394839225773,
97.0662176026933));
#56333=CARTESIAN_POINT('Ctrl Pts',(-5.53176112675738,3.60743862753435,97.3445868784233));
#56334=CARTESIAN_POINT('Ctrl Pts',(-6.02585272608368,-2.70242364156341,
97.622956154154));
#56335=CARTESIAN_POINT('Ctrl Pts',(-0.985332019446007,-6.53016963228263,
97.9013254298839));
#56336=CARTESIAN_POINT('Ctrl Pts',(4.96019433007453,-4.36009940515447,98.1796947056146));
#56337=CARTESIAN_POINT('Ctrl Pts',(6.34989201482012,1.81462558536316,98.4580639813445));
#56338=CARTESIAN_POINT('Ctrl Pts',(1.90735448169537,6.32265715471649,98.7364332570749));
#56339=CARTESIAN_POINT('Ctrl Pts',(-4.28704591069449,5.0234681221771,99.0148025328052));
#56340=CARTESIAN_POINT('Ctrl Pts',(-6.54388955682393,-0.889665152190753,
99.2931718085354));
#56341=CARTESIAN_POINT('Ctrl Pts',(-2.79031553819798,-5.98566068301753,
99.5715410842657));
#56342=CARTESIAN_POINT('Ctrl Pts',(3.52610151978467,-5.58395940951429,99.849910359996));
#56343=CARTESIAN_POINT('Ctrl Pts',(6.60387240591485,-0.0535150570232872,
100.128279635726));
#56344=CARTESIAN_POINT('Ctrl Pts',(3.61613270852506,5.5260816904265,100.406648911456));
#56345=CARTESIAN_POINT('Ctrl Pts',(-2.69294481412704,6.03009476235633,100.685018187187));
#56346=CARTESIAN_POINT('Ctrl Pts',(-6.52861215152283,0.995599311931976,
100.963387462917));
#56347=CARTESIAN_POINT('Ctrl Pts',(-4.36789378266397,-4.95333206218776,
101.241756738647));
#56348=CARTESIAN_POINT('Ctrl Pts',(1.80463831274576,-6.35273761264401,101.520126014377));
#56349=CARTESIAN_POINT('Ctrl Pts',(6.31965007575454,-1.91729432663498,101.798495290108));
#56350=CARTESIAN_POINT('Ctrl Pts',(5.03020317231507,4.27914134613035,102.076864565838));
#56351=CARTESIAN_POINT('Ctrl Pts',(-0.879373967378626,6.54528044016669,
102.355233841568));
#56352=CARTESIAN_POINT('Ctrl Pts',(-5.98126558891647,2.79972437389389,102.633603117299));
#56353=CARTESIAN_POINT('Ctrl Pts',(-5.58949720274087,-3.51731653899433,
102.911972393029));
#56354=CARTESIAN_POINT('Ctrl Pts',(-0.0638993971154535,-6.60378009037091,
103.190341668759));
#56355=CARTESIAN_POINT('Ctrl Pts',(5.52038858991582,-3.62481784801088,103.468710944489));
#56356=CARTESIAN_POINT('Ctrl Pts',(6.03432188819125,2.68345932792503,103.74708022022));
#56357=CARTESIAN_POINT('Ctrl Pts',(1.00586414262883,6.52703852765597,104.02544949595));
#56358=CARTESIAN_POINT('Ctrl Pts',(-4.94645754634252,4.37567735981095,104.30381877168));
#56359=CARTESIAN_POINT('Ctrl Pts',(-6.35556750224043,-1.79464657785212,
104.58218804741));
#56360=CARTESIAN_POINT('Ctrl Pts',(-1.9272294307376,-6.31662737037975,104.860557323141));
#56361=CARTESIAN_POINT('Ctrl Pts',(4.2712262006594,-5.03692578441776,105.138926598871));
#56362=CARTESIAN_POINT('Ctrl Pts',(6.54665513918701,0.869080608164411,105.417295874602));
#56363=CARTESIAN_POINT('Ctrl Pts',(2.80912628679378,5.97685570511578,105.695665150331));
#56364=CARTESIAN_POINT('Ctrl Pts',(-3.50852286103865,5.59502117498236,105.974034426062));
#56365=CARTESIAN_POINT('Ctrl Pts',(-6.60367144585437,0.0742835792054609,
106.252403701792));
#56366=CARTESIAN_POINT('Ctrl Pts',(-3.63349402451605,-5.51468183930289,
106.530772977523));
#56367=CARTESIAN_POINT('Ctrl Pts',(2.67396720641217,-6.03853409313579,106.809142253253));
#56368=CARTESIAN_POINT('Ctrl Pts',(6.52544876457291,-1.01612648615505,107.087511528983));
#56369=CARTESIAN_POINT('Ctrl Pts',(4.38345011734935,4.93957079953733,107.365880804713));
#56370=CARTESIAN_POINT('Ctrl Pts',(-1.78465040538896,6.35838167661206,107.644250080444));
#56371=CARTESIAN_POINT('Ctrl Pts',(-6.31358904606623,1.93715976943654,107.922619356174));
#56372=CARTESIAN_POINT('Ctrl Pts',(-5.04363594186223,-4.26330049385302,
108.200988631904));
#56373=CARTESIAN_POINT('Ctrl Pts',(0.858785100000153,-6.54801365048589,
108.479357907634));
#56374=CARTESIAN_POINT('Ctrl Pts',(5.97243104252002,-2.81852125364953,108.757727183365));
#56375=CARTESIAN_POINT('Ctrl Pts',(5.60053131257941,3.49972050766179,109.036096459095));
#56376=CARTESIAN_POINT('Ctrl Pts',(0.0846675776166999,6.60354647263366,
109.314465734825));
#56377=CARTESIAN_POINT('Ctrl Pts',(-5.50896145269841,3.64216121658758,109.592835010555));
#56378=CARTESIAN_POINT('Ctrl Pts',(-6.04273136677475,-2.66446847305942,
109.871204286286));
#56379=CARTESIAN_POINT('Ctrl Pts',(-1.02638631713515,-6.52384286620461,
110.149573562016));
#56380=CARTESIAN_POINT('Ctrl Pts',(4.93267183880067,-4.3912120360596,110.427942837746));
#56381=CARTESIAN_POINT('Ctrl Pts',(6.36118012880049,1.77464982007316,110.706312113476));
#56382=CARTESIAN_POINT('Ctrl Pts',(1.9470853181774,6.31053511032693,110.984681389207));
#56383=CARTESIAN_POINT('Ctrl Pts',(-4.25536424530892,5.05033362805641,111.263050664937));
#56384=CARTESIAN_POINT('Ctrl Pts',(-6.54935597070397,-0.848487468343064,
111.541419940667));
#56385=CARTESIAN_POINT('Ctrl Pts',(-2.82790925123099,-5.96799161206968,
111.819789216398));
#56386=CARTESIAN_POINT('Ctrl Pts',(3.49090950062908,-5.60602760190756,112.098158492128));
#56387=CARTESIAN_POINT('Ctrl Pts',(6.6034051710178,-0.095051366672858,112.376527767858));
#56388=CARTESIAN_POINT('Ctrl Pts',(3.6508194027943,5.50322744424684,112.654897043588));
#56389=CARTESIAN_POINT('Ctrl Pts',(-2.65496315135363,6.04691369872981,112.933266319319));
#56390=CARTESIAN_POINT('Ctrl Pts',(-6.52222083652212,1.03664361020002,113.211635595049));
#56391=CARTESIAN_POINT('Ctrl Pts',(-4.39896309674896,-4.92576068119147,
113.490004870779));
#56392=CARTESIAN_POINT('Ctrl Pts',(1.76464484663277,-6.36396285188586,113.768374146509));
#56393=CARTESIAN_POINT('Ctrl Pts',(6.30746557071311,-1.95700605241798,114.04674342224));
#56394=CARTESIAN_POINT('Ctrl Pts',(5.05701882643932,4.24741747465094,114.32511269797));
#56395=CARTESIAN_POINT('Ctrl Pts',(-0.838187738656269,6.55068209652226,
114.603481973701));
#56396=CARTESIAN_POINT('Ctrl Pts',(-5.963537424742,2.83729025632424,114.88185124943));
#56397=CARTESIAN_POINT('Ctrl Pts',(-5.61151002937618,-3.48208986172708,
115.160220525161));
#56398=CARTESIAN_POINT('Ctrl Pts',(-0.105434920698308,-6.60324754135638,
115.438589800891));
#56399=CARTESIAN_POINT('Ctrl Pts',(5.49747982812689,-3.65946856172709,115.716959076621));
#56400=CARTESIAN_POINT('Ctrl Pts',(6.05108107865909,2.64545126479867,115.995328352351));
#56401=CARTESIAN_POINT('Ctrl Pts',(1.04689833998677,6.520582679536,116.273697628082));
#56402=CARTESIAN_POINT('Ctrl Pts',(-4.91883734379885,4.40670328025178,116.552066903812));
#56403=CARTESIAN_POINT('Ctrl Pts',(-6.36672983898753,-1.75463550980728,
116.830436179542));
#56404=CARTESIAN_POINT('Ctrl Pts',(-1.96692194762707,-6.30438043481466,
117.108805455273));
#56405=CARTESIAN_POINT('Ctrl Pts',(4.23946020152865,-5.06369152048054,117.387174731003));
#56406=CARTESIAN_POINT('Ctrl Pts',(6.55199202466173,0.827885936407187,117.665544006733));
#56407=CARTESIAN_POINT('Ctrl Pts',(2.84666424573328,5.95906849155092,117.943913282464));
#56408=CARTESIAN_POINT('Ctrl Pts',(-3.47326161276393,5.61697858142893,118.222282558194));
#56409=CARTESIAN_POINT('Ctrl Pts',(-6.60307358403887,0.115818214018131,
118.500651833924));
#56410=CARTESIAN_POINT('Ctrl Pts',(-3.66810867199999,-5.49171861855029,
118.779021109654));
#56411=CARTESIAN_POINT('Ctrl Pts',(2.63593283691441,-6.05523349625818,119.057390385385));
#56412=CARTESIAN_POINT('Ctrl Pts',(6.51892839929654,-1.05715048113904,119.335759661115));
#56413=CARTESIAN_POINT('Ctrl Pts',(4.41443256742969,4.91190184374221,119.614128936845));
#56414=CARTESIAN_POINT('Ctrl Pts',(-1.74462183434705,6.36948108326269,119.892498212575));
#56415=CARTESIAN_POINT('Ctrl Pts',(-6.3012797102582,1.97683297928823,120.170867488306));
#56416=CARTESIAN_POINT('Ctrl Pts',(-5.07035169368467,-4.23149244562176,
120.449236764036));
#56417=CARTESIAN_POINT('Ctrl Pts',(0.817582087076372,-6.55328575187579,
120.727606039766));
#56418=CARTESIAN_POINT('Ctrl Pts',(5.95458482353203,-2.85603119629362,121.005975315497));
#56419=CARTESIAN_POINT('Ctrl Pts',(5.62243324457135,3.4644247755954,121.284344591226));
#56420=CARTESIAN_POINT('Ctrl Pts',(0.126201220905966,6.60288329944592,121.562713866957));
#56421=CARTESIAN_POINT('Ctrl Pts',(-5.48594382966552,3.67673971234222,121.841083142687));
#56422=CARTESIAN_POINT('Ctrl Pts',(-6.05937094144284,-2.62640789141387,
122.119452418417));
#56423=CARTESIAN_POINT('Ctrl Pts',(-1.0674000079603,-6.5172579995599,122.397821694148));
#56424=CARTESIAN_POINT('Ctrl Pts',(4.90495419751704,-4.4221509398022,122.676190969878));
#56425=CARTESIAN_POINT('Ctrl Pts',(6.37221657914332,1.73460384620578,122.954560245608));
#56426=CARTESIAN_POINT('Ctrl Pts',(1.98673912056242,6.29816340245835,123.232929521338));
#56427=CARTESIAN_POINT('Ctrl Pts',(-4.22351422222807,5.07699933383612,123.511298797069));
#56428=CARTESIAN_POINT('Ctrl Pts',(-6.55456328328112,-0.80727622417212,
123.789668072799));
#56429=CARTESIAN_POINT('Ctrl Pts',(-2.86539106914205,-5.95008641661004,
124.068037348529));
#56430=CARTESIAN_POINT('Ctrl Pts',(3.45557934242459,-5.62787403394446,124.34640662426));
#56431=CARTESIAN_POINT('Ctrl Pts',(6.60267674402822,-0.136583861631543,
124.62477589999));
#56432=CARTESIAN_POINT('Ctrl Pts',(3.68536155571016,5.48015537368143,124.90314517572));
#56433=CARTESIAN_POINT('Ctrl Pts',(-2.61687625226222,6.06349359671225,125.18151445145));
#56434=CARTESIAN_POINT('Ctrl Pts',(-6.51557186131684,1.07764653119394,125.459883727181));
#56435=CARTESIAN_POINT('Ctrl Pts',(-4.42985766669503,-4.89799373516042,
125.738253002911));
#56436=CARTESIAN_POINT('Ctrl Pts',(1.72458022652849,-6.37493761732919,126.016622278641));
#56437=CARTESIAN_POINT('Ctrl Pts',(6.29503405616005,-1.99663789708001,126.294991554372));
#56438=CARTESIAN_POINT('Ctrl Pts',(5.08362963405118,4.21552092521275,126.573360830102));
#56439=CARTESIAN_POINT('Ctrl Pts',(-0.796959327840158,6.55583335028739,
126.851730105832));
#56440=CARTESIAN_POINT('Ctrl Pts',(-5.94559036134429,2.87472734849176,127.130099381562));
#56441=CARTESIAN_POINT('Ctrl Pts',(-5.63326868663984,-3.44669419364702,
127.408468657293));
#56442=CARTESIAN_POINT('Ctrl Pts',(-0.14702700410348,-6.60251271983441,
127.686837933023));
#56443=CARTESIAN_POINT('Ctrl Pts',(5.47446824479836,-3.69386315072671,127.965207208753));
#56444=CARTESIAN_POINT('Ctrl Pts',(6.06738434301238,2.60712828918945,128.243576484483));
#56445=CARTESIAN_POINT('Ctrl Pts',(1.08829999938262,6.51426591103059,128.521945760214));
#56446=CARTESIAN_POINT('Ctrl Pts',(-4.89179481848511,4.43680471220902,128.800315035944));
#56447=CARTESIAN_POINT('Ctrl Pts',(-6.37618018613959,-1.7131350353328,129.078684311674));
#56448=CARTESIAN_POINT('Ctrl Pts',(-2.00930903122581,-6.29459439164505,
129.357053587405));
#56449=CARTESIAN_POINT('Ctrl Pts',(4.21288699254892,-5.08490128605854,129.635422863135));
#56450=CARTESIAN_POINT('Ctrl Pts',(6.15710482774512,-0.202003301493498,
129.867397259577));
#56451=CARTESIAN_POINT('Ctrl Pts',(4.72821073371232,3.37844258401427,130.05297677673));
#56452=CARTESIAN_POINT('Ctrl Pts',(3.27532695401748,4.61709096383853,130.145766535307));
#56453=CARTESIAN_POINT('Ctrl Pts',(2.43856727558522,5.02329722221597,130.192161414595));
#56454=CARTESIAN_POINT('Ctrl Pts',(3.05041111877606,-4.274209655604,-10.1921614145953));
#56455=CARTESIAN_POINT('Ctrl Pts',(3.76239094771356,-3.76608502870656,-10.1457665353069));
#56456=CARTESIAN_POINT('Ctrl Pts',(4.9147981139233,-2.38931734182567,-10.0529767767301));
#56457=CARTESIAN_POINT('Ctrl Pts',(5.67693298611737,1.15492319595148,-9.86739725957665));
#56458=CARTESIAN_POINT('Ctrl Pts',(3.10693226149187,5.3766494323891,-9.63542286313474));
#56459=CARTESIAN_POINT('Ctrl Pts',(-2.85220921458105,5.52037841761172,-9.35705358740447));
#56460=CARTESIAN_POINT('Ctrl Pts',(-6.18103028642409,0.586305255261647,
-9.0786843116742));
#56461=CARTESIAN_POINT('Ctrl Pts',(-3.83824771704109,-4.88244921267984,
-8.80031503594394));
#56462=CARTESIAN_POINT('Ctrl Pts',(2.03280072920052,-5.86879411456106,-8.52194576021367));
#56463=CARTESIAN_POINT('Ctrl Pts',(6.03522149624778,-1.46371786530544,-8.24357648448339));
#56464=CARTESIAN_POINT('Ctrl Pts',(4.49524313218507,4.28518771604633,-7.96520720875314));
#56465=CARTESIAN_POINT('Ctrl Pts',(-1.17394980812342,6.09854146397534,-7.68683793302285));
#56466=CARTESIAN_POINT('Ctrl Pts',(-5.7646663724329,2.31036198391266,-7.4084686572926));
#56467=CARTESIAN_POINT('Ctrl Pts',(-5.06078604168037,-3.59975018522352,
-7.13009938156231));
#56468=CARTESIAN_POINT('Ctrl Pts',(0.291378575457491,-6.20361580881232,
-6.85173010583206));
#56469=CARTESIAN_POINT('Ctrl Pts',(5.37588433642207,-3.10957421224122,-6.57336083010178));
#56470=CARTESIAN_POINT('Ctrl Pts',(5.52277741809884,2.84053002303097,-6.29499155437152));
#56471=CARTESIAN_POINT('Ctrl Pts',(0.597112164703471,6.18167690616701,-6.01662227864124));
#56472=CARTESIAN_POINT('Ctrl Pts',(-4.876982327571,3.84508693951616,-5.73825300291099));
#56473=CARTESIAN_POINT('Ctrl Pts',(-5.87167921844947,-2.02312839863673,
-5.45988372718071));
#56474=CARTESIAN_POINT('Ctrl Pts',(-1.47336733630053,-6.03314607562369,
-5.18151445145044));
#56475=CARTESIAN_POINT('Ctrl Pts',(4.2781990691855,-4.50185214896148,-4.90314517572017));
#56476=CARTESIAN_POINT('Ctrl Pts',(6.10033475477778,1.16429302348895,-4.62477589998991));
#56477=CARTESIAN_POINT('Ctrl Pts',(2.31944782925857,5.76106097853586,-4.34640662425962));
#56478=CARTESIAN_POINT('Ctrl Pts',(-3.59180045907085,5.06642190789875,-4.06803734852937));
#56479=CARTESIAN_POINT('Ctrl Pts',(-6.2040596136716,-0.281613464959076,
-3.78966807279909));
#56480=CARTESIAN_POINT('Ctrl Pts',(-3.11802735053584,-5.37099312723374,
-3.51129879706883));
#56481=CARTESIAN_POINT('Ctrl Pts',(2.83184397887941,-5.52723451392706,-3.23292952133855));
#56482=CARTESIAN_POINT('Ctrl Pts',(6.1807293244735,-0.60683338828964,-2.95456024560829));
#56483=CARTESIAN_POINT('Ctrl Pts',(3.85275163306719,4.87093077134018,-2.67619096987801));
#56484=CARTESIAN_POINT('Ctrl Pts',(-2.01389312417038,5.87485286674442,-2.39782169414775));
#56485=CARTESIAN_POINT('Ctrl Pts',(-6.03082163928753,1.48285268448469,-2.11945241841748));
#56486=CARTESIAN_POINT('Ctrl Pts',(-4.50857401099197,-4.27111485599194,
-1.84108314268722));
#56487=CARTESIAN_POINT('Ctrl Pts',(1.15469901830053,-6.10215797095896,-1.56271386695694));
#56488=CARTESIAN_POINT('Ctrl Pts',(5.7574065665386,-2.32850410220939,-1.28434459122668));
#56489=CARTESIAN_POINT('Ctrl Pts',(5.07206366238349,3.58382922732706,-1.0059753154964));
#56490=CARTESIAN_POINT('Ctrl Pts',(-0.271857411234665,6.2044947637884,-0.727606039766137));
#56491=CARTESIAN_POINT('Ctrl Pts',(-5.3660834720623,3.12646923812167,-0.449236764035865));
#56492=CARTESIAN_POINT('Ctrl Pts',(-5.53168067828129,-2.82314905726007,
-0.170867488305599));
#56493=CARTESIAN_POINT('Ctrl Pts',(-0.616551662615334,-6.17976745301254,
0.107501787424673));
#56494=CARTESIAN_POINT('Ctrl Pts',(4.86486640363235,-3.86040627406166,0.385871063154939));
#56495=CARTESIAN_POINT('Ctrl Pts',(5.87801239481268,2.00465259145346,0.664240338885211));
#56496=CARTESIAN_POINT('Ctrl Pts',(1.49233415085848,6.02848243824067,0.942609614615477));
#56497=CARTESIAN_POINT('Ctrl Pts',(-4.26401996776543,4.51528464667454,1.22097889034575));
#56498=CARTESIAN_POINT('Ctrl Pts',(-6.10396615887418,-1.14510211654415,
1.49934816607602));
#56499=CARTESIAN_POINT('Ctrl Pts',(-2.33755458556937,-5.75373794028536,
1.77771744180629));
#56500=CARTESIAN_POINT('Ctrl Pts',(3.57584911702428,-5.07769286371995,2.05608671753656));
#56501=CARTESIAN_POINT('Ctrl Pts',(6.2049145811997,0.262100679150067,2.33445599326682));
#56502=CARTESIAN_POINT('Ctrl Pts',(3.13490339023048,5.36116055158928,2.61282526899709));
#56503=CARTESIAN_POINT('Ctrl Pts',(-2.8144471524083,5.53611316288752,2.89119454472736));
#56504=CARTESIAN_POINT('Ctrl Pts',(-6.17879030235427,0.626268413324878,
3.16956382045763));
#56505=CARTESIAN_POINT('Ctrl Pts',(-3.86805136883776,-4.85879000719604,
3.44793309618789));
#56506=CARTESIAN_POINT('Ctrl Pts',(1.9954071015175,-5.88115738823654,3.72630237191817));
#56507=CARTESIAN_POINT('Ctrl Pts',(6.02612833094048,-1.50181192731717,4.00467164764843));
#56508=CARTESIAN_POINT('Ctrl Pts',(4.52198411744087,4.25691453609398,4.28304092337871));
#56509=CARTESIAN_POINT('Ctrl Pts',(-1.13550238327193,6.10575925365384,4.56141019910898));
#56510=CARTESIAN_POINT('Ctrl Pts',(-5.75005508696296,2.3465992889471,4.83977947483924));
#56511=CARTESIAN_POINT('Ctrl Pts',(-5.0833095095791,-3.56786016483527,5.11814875056952));
#56512=CARTESIAN_POINT('Ctrl Pts',(0.252343298968592,-6.20531905589563,
5.39651802629978));
#56513=CARTESIAN_POINT('Ctrl Pts',(5.35622437473667,-3.14332979075887,5.67488730203006));
#56514=CARTESIAN_POINT('Ctrl Pts',(5.5405319585073,2.80573828835742,5.95325657776032));
#56515=CARTESIAN_POINT('Ctrl Pts',(0.635983615480163,6.17779787358219,6.23162585349059));
#56516=CARTESIAN_POINT('Ctrl Pts',(-4.85270159657326,3.87568689919748,6.50999512922086));
#56517=CARTESIAN_POINT('Ctrl Pts',(-5.88428783949522,-1.98615667759732,
6.78836440495113));
#56518=CARTESIAN_POINT('Ctrl Pts',(-1.51128599028987,-6.02375932300995,
7.06673368068139));
#56519=CARTESIAN_POINT('Ctrl Pts',(4.24979857847531,-4.52867240683016,7.34510295641167));
#56520=CARTESIAN_POINT('Ctrl Pts',(6.10753725090218,1.12589984227641,7.62347223214193));
#56521=CARTESIAN_POINT('Ctrl Pts',(2.35563818995783,5.74635801564849,7.9018415078722));
#56522=CARTESIAN_POINT('Ctrl Pts',(-3.55986239050335,5.08891358608843,8.18021078360247));
#56523=CARTESIAN_POINT('Ctrl Pts',(-6.20570818688168,-0.242585294825209,
8.45858005933274));
#56524=CARTESIAN_POINT('Ctrl Pts',(-3.15174841886823,-5.35127495370563,
8.73694933506301));
#56525=CARTESIAN_POINT('Ctrl Pts',(2.79702248664004,-5.54493705421672,9.01531861079328));
#56526=CARTESIAN_POINT('Ctrl Pts',(6.17679016915104,-0.645697245057467,
9.29368788652355));
#56527=CARTESIAN_POINT('Ctrl Pts',(3.88331284626025,4.84660118681802,9.57205716225382));
#56528=CARTESIAN_POINT('Ctrl Pts',(-1.97690134256598,5.88740374084846,9.85042643798408));
#56529=CARTESIAN_POINT('Ctrl Pts',(-6.02137542030695,1.52075631635018,10.1287957137144));
#56530=CARTESIAN_POINT('Ctrl Pts',(-4.53534949830443,-4.24267211250473,
10.4071649894446));
#56531=CARTESIAN_POINT('Ctrl Pts',(1.11629451730146,-6.10930014622284,10.6855342651749));
#56532=CARTESIAN_POINT('Ctrl Pts',(5.74264673548367,-2.36467126625128,10.9639035409052));
#56533=CARTESIAN_POINT('Ctrl Pts',(5.09450507939081,3.55185581380451,11.2422728166354));
#56534=CARTESIAN_POINT('Ctrl Pts',(-0.232826690848401,6.20608197319566,
11.5206420923657));
#56535=CARTESIAN_POINT('Ctrl Pts',(-5.34631230073448,3.16015925374197,11.799011368096));
#56536=CARTESIAN_POINT('Ctrl Pts',(-5.54932843912339,-2.78829976880751,
12.0773806438262));
#56537=CARTESIAN_POINT('Ctrl Pts',(-0.655409278038173,-6.17576719155257,
12.3557499195565));
#56538=CARTESIAN_POINT('Ctrl Pts',(4.84048879301466,-3.89092919116954,12.6341191952868));
#56539=CARTESIAN_POINT('Ctrl Pts',(5.89050508459169,1.96764111930887,12.912488471017));
#56540=CARTESIAN_POINT('Ctrl Pts',(1.53022288208102,6.01897662872612,13.1908577467473));
#56541=CARTESIAN_POINT('Ctrl Pts',(-4.23553515580366,4.54201537535343,13.4692270224776));
#56542=CARTESIAN_POINT('Ctrl Pts',(-6.11104793525676,-1.10668643209798,
13.7475962982079));
#56543=CARTESIAN_POINT('Ctrl Pts',(-2.37369849549166,-5.7389212556452,14.0259655739381));
#56544=CARTESIAN_POINT('Ctrl Pts',(3.54384045453631,-5.10008397566036,14.3043348496684));
#56545=CARTESIAN_POINT('Ctrl Pts',(6.20644041391337,0.223067511167865,14.5827041253987));
#56546=CARTESIAN_POINT('Ctrl Pts',(3.16856227458287,5.34133642809414,14.8610734011289));
#56547=CARTESIAN_POINT('Ctrl Pts',(-2.77957015642807,5.55370610236895,15.1394426768592));
#56548=CARTESIAN_POINT('Ctrl Pts',(-6.17472894331627,0.665119690407707,
15.4178119525895));
#56549=CARTESIAN_POINT('Ctrl Pts',(-3.89853591509276,-4.834364430277,15.6961812283197));
#56550=CARTESIAN_POINT('Ctrl Pts',(1.95837603072338,-5.89359186305633,15.97455050405));
#56551=CARTESIAN_POINT('Ctrl Pts',(6.01656295419885,-1.53968566407487,16.2529197797802));
#56552=CARTESIAN_POINT('Ctrl Pts',(4.54867002149468,4.22838772601937,16.5312890555106));
#56553=CARTESIAN_POINT('Ctrl Pts',(-1.0970756104234,6.11278061368228,16.8096583312408));
#56554=CARTESIAN_POINT('Ctrl Pts',(-5.73518158534497,2.38271985535767,17.0880276069711));
#56555=CARTESIAN_POINT('Ctrl Pts',(-5.10565026110237,-3.53581633251799,
17.3663968827013));
#56556=CARTESIAN_POINT('Ctrl Pts',(0.213307779914776,-6.20678350814845,
17.6447661584316));
#56557=CARTESIAN_POINT('Ctrl Pts',(5.33634734808843,-3.1769574606131,17.9231354341619));
#56558=CARTESIAN_POINT('Ctrl Pts',(5.55807003312879,2.77083367108736,18.2015047098922));
#56559=CARTESIAN_POINT('Ctrl Pts',(0.674828458155247,6.17367542700939,18.4798739856224));
#56560=CARTESIAN_POINT('Ctrl Pts',(-4.8282281137487,3.90613299922089,18.7582432613527));
#56561=CARTESIAN_POINT('Ctrl Pts',(-5.89666406860973,-1.9491060997192,19.0366125370829));
#56562=CARTESIAN_POINT('Ctrl Pts',(-1.5491446389332,-6.01413440269339,19.3149818128132));
#56563=CARTESIAN_POINT('Ctrl Pts',(4.22122984082524,-4.55531342027332,19.5933510885435));
#56564=CARTESIAN_POINT('Ctrl Pts',(6.11449817721499,1.08746207604232,19.8717203642738));
#56565=CARTESIAN_POINT('Ctrl Pts',(2.39173532354231,5.73142773382999,20.150089640004));
#56566=CARTESIAN_POINT('Ctrl Pts',(-3.52778346759073,5.11120392195315,20.4284589157343));
#56567=CARTESIAN_POINT('Ctrl Pts',(-6.20711125505255,-0.20354752122192,
20.7068281914646));
#56568=CARTESIAN_POINT('Ctrl Pts',(-3.18534479107406,-5.33134507305361,
20.9851974671948));
#56569=CARTESIAN_POINT('Ctrl Pts',(2.76209033438777,-5.56242022061237,21.2635667429251));
#56570=CARTESIAN_POINT('Ctrl Pts',(6.1726066452369,-0.684535557274347,21.5419360186554));
#56571=CARTESIAN_POINT('Ctrl Pts',(3.91372042476886,4.82207985860276,21.8203052943857));
#56572=CARTESIAN_POINT('Ctrl Pts',(-1.93983134921762,5.89972169365541,22.0986745701159));
#56573=CARTESIAN_POINT('Ctrl Pts',(-6.01169098021472,1.55859978326723,22.3770438458462));
#56574=CARTESIAN_POINT('Ctrl Pts',(-4.56194555526257,-4.21406151792019,
22.6554131215764));
#56575=CARTESIAN_POINT('Ctrl Pts',(1.07784585272568,-6.11620062160797,22.9337823973067));
#56576=CARTESIAN_POINT('Ctrl Pts',(5.72765971038225,-2.40074487775348,23.212151673037));
#56577=CARTESIAN_POINT('Ctrl Pts',(5.11674494448041,3.51974187961701,23.4905209487673));
#56578=CARTESIAN_POINT('Ctrl Pts',(-0.193786759222999,6.20742365381528,
23.7688902244975));
#56579=CARTESIAN_POINT('Ctrl Pts',(-5.32632961535865,3.19372424522674,24.0472595002278));
#56580=CARTESIAN_POINT('Ctrl Pts',(-5.56675665406317,-2.75334016794859,
24.3256287759581));
#56581=CARTESIAN_POINT('Ctrl Pts',(-0.694240963762592,-6.17152260064156,
24.6039980516883));
#56582=CARTESIAN_POINT('Ctrl Pts',(4.81591968004187,-3.92129817297552,24.8823673274186));
#56583=CARTESIAN_POINT('Ctrl Pts',(5.9027647306328,1.93055180215219,25.1607366031489));
#56584=CARTESIAN_POINT('Ctrl Pts',(1.56805107369734,6.00923269280466,25.4391058788792));
#56585=CARTESIAN_POINT('Ctrl Pts',(-4.20688277502926,4.56856641006321,25.7174751546094));
#56586=CARTESIAN_POINT('Ctrl Pts',(-6.1178879426516,-1.06822696425142,25.9958444303397));
#56587=CARTESIAN_POINT('Ctrl Pts',(-2.40974849571335,-5.72387752431889,
26.27421370607));
#56588=CARTESIAN_POINT('Ctrl Pts',(3.51169158848119,-5.12227331498293,26.5525829818002));
#56589=CARTESIAN_POINT('Ctrl Pts',(6.20772070366418,0.18402551805332,26.8309522575305));
#56590=CARTESIAN_POINT('Ctrl Pts',(3.20209580235133,5.32130098740521,27.1093215332608));
#56591=CARTESIAN_POINT('Ctrl Pts',(-2.74458319340624,5.57107932275853,27.387690808991));
#56592=CARTESIAN_POINT('Ctrl Pts',(-6.17042329590389,0.703944653621518,
27.6660600847213));
#56593=CARTESIAN_POINT('Ctrl Pts',(-3.92886622510352,-4.80974759329806,
27.9444293604515));
#56594=CARTESIAN_POINT('Ctrl Pts',(1.92126748146815,-5.90579317201751,28.2227986361818));
#56595=CARTESIAN_POINT('Ctrl Pts',(6.00675954654171,-1.57749848685371,28.5011679119121));
#56596=CARTESIAN_POINT('Ctrl Pts',(4.57517596830407,4.19969362990309,28.7795371876424));
#56597=CARTESIAN_POINT('Ctrl Pts',(-1.05860543440373,6.11956013617373,29.0579064633726));
#56598=CARTESIAN_POINT('Ctrl Pts',(-5.72008118499199,2.41874615515898,29.3362757391029));
#56599=CARTESIAN_POINT('Ctrl Pts',(-5.12778901979094,-3.50363261408887,
29.6146450148332));
#56600=CARTESIAN_POINT('Ctrl Pts',(0.1742638218492,-6.20800240386472,29.8930142905635));
#56601=CARTESIAN_POINT('Ctrl Pts',(5.31625920162736,-3.21045944174788,30.1713835662937));
#56602=CARTESIAN_POINT('Ctrl Pts',(5.57538821600995,2.73581943241381,30.449752842024));
#56603=CARTESIAN_POINT('Ctrl Pts',(0.713646602857252,6.16930873374205,30.7281221177543));
#56604=CARTESIAN_POINT('Ctrl Pts',(-4.80356361363291,3.93642456243958,31.0064913934845));
#56605=CARTESIAN_POINT('Ctrl Pts',(-5.90880701032121,-1.91197841012251,
31.2848606692148));
#56606=CARTESIAN_POINT('Ctrl Pts',(-1.58694199937596,-6.00427154754116,
31.563229944945));
#56607=CARTESIAN_POINT('Ctrl Pts',(4.19249410031801,-4.58177421364196,31.8415992206754));
#56608=CARTESIAN_POINT('Ctrl Pts',(6.12121719803953,1.04898128697357,32.1199684964056));
#56609=CARTESIAN_POINT('Ctrl Pts',(2.42773783384219,5.71627070178861,32.3983377721359));
#56610=CARTESIAN_POINT('Ctrl Pts',(-3.49556497636723,5.1332920452659,32.6767070478661));
#56611=CARTESIAN_POINT('Ctrl Pts',(-6.20826875372037,-0.164501694747944,
32.9550763235964));
#56612=CARTESIAN_POINT('Ctrl Pts',(-3.21881514273589,-5.31120427049176,
33.2334455993267));
#56613=CARTESIAN_POINT('Ctrl Pts',(2.72704890664107,-5.57968332316301,33.511814875057));
#56614=CARTESIAN_POINT('Ctrl Pts',(6.16817891691201,-0.723346787480091,
33.7901841507872));
#56615=CARTESIAN_POINT('Ctrl Pts',(3.94397316629452,4.79736775633728,34.0685534265175));
#56616=CARTESIAN_POINT('Ctrl Pts',(-1.90268461108404,5.91180623809167,34.3469227022477));
#56617=CARTESIAN_POINT('Ctrl Pts',(-6.00176870195498,1.59638158791352,34.6252919779781));
#56618=CARTESIAN_POINT('Ctrl Pts',(-4.58836112976159,-4.18528420407607,
34.9036612537083));
#56619=CARTESIAN_POINT('Ctrl Pts',(1.03935454575815,-6.12285912415169,35.1820305294386));
#56620=CARTESIAN_POINT('Ctrl Pts',(5.71244608413083,-2.43672350952955,35.4603998051688));
#56621=CARTESIAN_POINT('Ctrl Pts',(5.13878237780069,3.48748869526495,35.7387690808992));
#56622=CARTESIAN_POINT('Ctrl Pts',(-0.15473916088826,6.20851975257254,36.0171383566293));
#56623=CARTESIAN_POINT('Ctrl Pts',(-5.30613620649767,3.22716288465429,36.2955076323597));
#56624=CARTESIAN_POINT('Ctrl Pts',(-5.58396463359725,-2.71827163777478,
36.5738769080898));
#56625=CARTESIAN_POINT('Ctrl Pts',(-0.733045183504503,-6.16703384820746,
36.8522461838203));
#56626=CARTESIAN_POINT('Ctrl Pts',(4.79116003673157,-3.95151201800298,37.1306154595503));
#56627=CARTESIAN_POINT('Ctrl Pts',(5.91479084791276,1.89338610733341,37.4089847352808));
#56628=CARTESIAN_POINT('Ctrl Pts',(1.60581722912522,5.99925101597193,37.6873540110109));
#56629=CARTESIAN_POINT('Ctrl Pts',(-4.17806395900508,4.59493670037558,37.9657232867413));
#56630=CARTESIAN_POINT('Ctrl Pts',(-6.12448591045022,-1.02972523456137,
38.2440925624714));
#56631=CARTESIAN_POINT('Ctrl Pts',(-2.44570316000227,-5.70860734147573,
38.5224618382019));
#56632=CARTESIAN_POINT('Ctrl Pts',(3.47940379075197,-5.14426000381944,38.800831113932));
#56633=CARTESIAN_POINT('Ctrl Pts',(6.20875539980056,0.144976244409641,39.0792003896624));
#56634=CARTESIAN_POINT('Ctrl Pts',(3.23550264686201,5.30105502217667,39.3575696653926));
#56635=CARTESIAN_POINT('Ctrl Pts',(-2.70948764751817,5.58823213672641,39.6359389411229));
#56636=CARTESIAN_POINT('Ctrl Pts',(-6.16587353045974,0.74274176694977,39.9143082168531));
#56637=CARTESIAN_POINT('Ctrl Pts',(-3.95904109892399,-4.78494047016537,
40.1926774925834));
#56638=CARTESIAN_POINT('Ctrl Pts',(1.88408292186256,-5.91776083240456,40.4710467683136));
#56639=CARTESIAN_POINT('Ctrl Pts',(5.99671849581738,-1.61524889967998,40.7494160440439));
#56640=CARTESIAN_POINT('Ctrl Pts',(4.60150090922485,4.1708333829582,41.0277853197742));
#56641=CARTESIAN_POINT('Ctrl Pts',(-1.02009337719325,6.12609755291264,41.3061545955045));
#56642=CARTESIAN_POINT('Ctrl Pts',(-5.70475448331516,2.45467676305686,41.5845238712348));
#56643=CARTESIAN_POINT('Ctrl Pts',(-5.14972490977789,-3.47131028281956,
41.862893146965));
#56644=CARTESIAN_POINT('Ctrl Pts',(0.135212969452428,-6.20897569482178,
42.1412624226953));
#56645=CARTESIAN_POINT('Ctrl Pts',(5.29596073009285,-3.2438344087376,42.4196316984255));
#56646=CARTESIAN_POINT('Ctrl Pts',(5.59248582199842,2.70069695759119,42.6980009741559));
#56647=CARTESIAN_POINT('Ctrl Pts',(0.752436513839245,6.16469796653795,42.9763702498861));
#56648=CARTESIAN_POINT('Ctrl Pts',(-4.77870907201771,3.96656039044047,43.2547395256164));
#56649=CARTESIAN_POINT('Ctrl Pts',(-5.92071618422324,-1.87477507767536,
43.5331088013466));
#56650=CARTESIAN_POINT('Ctrl Pts',(-1.6246765762562,-5.99417114775347,43.8114780770769));
#56651=CARTESIAN_POINT('Ctrl Pts',(4.16359249381437,-4.60805374007816,44.0898473528071));
#56652=CARTESIAN_POINT('Ctrl Pts',(6.12769404755385,1.01045899747034,44.3682166285375));
#56653=CARTESIAN_POINT('Ctrl Pts',(2.46364429650437,5.70088751917604,44.6465859042677));
#56654=CARTESIAN_POINT('Ctrl Pts',(-3.46320819148043,5.15517708216299,44.9249551799981));
#56655=CARTESIAN_POINT('Ctrl Pts',(-6.20918063709147,-0.12544936015814,
45.2033244557282));
#56656=CARTESIAN_POINT('Ctrl Pts',(-3.25215814967919,-5.29085334284281,
45.4816937314586));
#56657=CARTESIAN_POINT('Ctrl Pts',(2.69189958973031,-5.59672567889524,45.7600630071887));
#56658=CARTESIAN_POINT('Ctrl Pts',(6.16350715934888,-0.762129400201062,
46.0384322829191));
#56659=CARTESIAN_POINT('Ctrl Pts',(3.97406987395981,4.7724658576967,46.3168015586493));
#56660=CARTESIAN_POINT('Ctrl Pts',(-1.86546259778696,5.92365689606119,46.5951708343796));
#56661=CARTESIAN_POINT('Ctrl Pts',(-5.99160897807888,1.63410023554255,46.8735401101098));
#56662=CARTESIAN_POINT('Ctrl Pts',(-4.6145951767326,-4.15634130947783,47.1519093858402));
#56663=CARTESIAN_POINT('Ctrl Pts',(1.0008221192151,-6.12927539042631,47.4302786615703));
#56664=CARTESIAN_POINT('Ctrl Pts',(5.69700645862006,-2.47260573817116,47.7086479373007));
#56665=CARTESIAN_POINT('Ctrl Pts',(5.16061650749346,3.4550975367682,47.9870172130309));
#56666=CARTESIAN_POINT('Ctrl Pts',(-0.115685440668852,6.20937022610289,
48.2653864887612));
#56667=CARTESIAN_POINT('Ctrl Pts',(-5.28573287305531,3.26047384910508,48.5437557644915));
#56668=CARTESIAN_POINT('Ctrl Pts',(-5.60095169693318,-2.68309556568845,
48.8221250402218));
#56669=CARTESIAN_POINT('Ctrl Pts',(-0.771820402068029,-6.16230111183698,
49.100494315952));
#56670=CARTESIAN_POINT('Ctrl Pts',(4.76621084263973,-3.98156953091355,49.3788635916823));
#56671=CARTESIAN_POINT('Ctrl Pts',(5.92658296064706,1.8561455052241,49.6572328674126));
#56672=CARTESIAN_POINT('Ctrl Pts',(1.64351985423726,5.98903199312908,49.9356021431428));
#56673=CARTESIAN_POINT('Ctrl Pts',(-4.1490798478785,4.62112520301324,50.2139714188731));
#56674=CARTESIAN_POINT('Ctrl Pts',(-6.13084157761981,-0.991182766256508,
50.4923406946034));
#56675=CARTESIAN_POINT('Ctrl Pts',(-2.4815610658984,-5.69311131124387,50.7707099703336));
#56676=CARTESIAN_POINT('Ctrl Pts',(3.44697833873802,-5.16604317231927,51.0490792460639));
#56677=CARTESIAN_POINT('Ctrl Pts',(6.20954446138722,0.105921235127679,51.3274485217941));
#56678=CARTESIAN_POINT('Ctrl Pts',(3.26878148645317,5.28059933339168,51.6058177975245));
#56679=CARTESIAN_POINT('Ctrl Pts',(-2.67428490723522,5.60516386566259,51.8841870732547));
#56680=CARTESIAN_POINT('Ctrl Pts',(-6.16107982698442,0.78150949547734,52.162556348985));
#56681=CARTESIAN_POINT('Ctrl Pts',(-3.98905934275737,-4.75994404231351,
52.4409256247152));
#56682=CARTESIAN_POINT('Ctrl Pts',(1.84682382302487,-5.92949437074557,52.7192949004455));
#56683=CARTESIAN_POINT('Ctrl Pts',(5.98644019927607,-1.65293540904875,52.9976641761758));
#56684=CARTESIAN_POINT('Ctrl Pts',(4.62764380277359,4.14180812697147,53.2760334519061));
#56685=CARTESIAN_POINT('Ctrl Pts',(-0.981540962429502,6.13239260526172,
53.5544027276362));
#56686=CARTESIAN_POINT('Ctrl Pts',(-5.68920208667882,2.49051025754264,53.8327720033667));
#56687=CARTESIAN_POINT('Ctrl Pts',(-5.17145706322212,-3.43885061746587,
54.1111412790968));
#56688=CARTESIAN_POINT('Ctrl Pts',(0.0961567676780714,-6.20970334251366,
54.3895105548272));
#56689=CARTESIAN_POINT('Ctrl Pts',(5.27545273654541,-3.2770810411815,54.6678798305573));
#56690=CARTESIAN_POINT('Ctrl Pts',(5.60936217466827,2.66546763615629,54.9462491062877));
#56691=CARTESIAN_POINT('Ctrl Pts',(0.791196656471176,6.15984330781104,55.2246183820179));
#56692=CARTESIAN_POINT('Ctrl Pts',(-4.75366547221362,3.9965392909716,55.5029876577482));
#56693=CARTESIAN_POINT('Ctrl Pts',(-5.93239111915783,-1.83749757423864,
55.7813569334784));
#56694=CARTESIAN_POINT('Ctrl Pts',(-1.66234687669558,-5.98383360292849,
56.0597262092088));
#56695=CARTESIAN_POINT('Ctrl Pts',(4.13452616473729,-4.6341509598953,56.338095484939));
#56696=CARTESIAN_POINT('Ctrl Pts',(6.13392846951687,0.971896731574924,56.6164647606693));
#56697=CARTESIAN_POINT('Ctrl Pts',(2.4994532909755,5.68527879459112,56.8948340363995));
#56698=CARTESIAN_POINT('Ctrl Pts',(-3.43071439304901,5.17685816681528,57.1732033121299));
#56699=CARTESIAN_POINT('Ctrl Pts',(-6.20984686908935,-0.0863920624645414,
57.4515725878601));
#56700=CARTESIAN_POINT('Ctrl Pts',(-3.2853724927679,-5.27029309524236,57.7299418635904));
#56701=CARTESIAN_POINT('Ctrl Pts',(2.65664377425388,-5.61354661356913,58.0083111393206));
#56702=CARTESIAN_POINT('Ctrl Pts',(6.15859155737437,-0.800881861096334,
58.2866804150509));
#56703=CARTESIAN_POINT('Ctrl Pts',(4.00400935706071,4.74737514786502,58.5650496907811));
#56704=CARTESIAN_POINT('Ctrl Pts',(-1.82816678192627,5.93527319872107,58.8434189665115));
#56705=CARTESIAN_POINT('Ctrl Pts',(-5.98121221053155,1.67175423390625,59.1217882422417));
#56706=CARTESIAN_POINT('Ctrl Pts',(-4.64064665828831,-4.1272339791819,59.400157517972));
#56707=CARTESIAN_POINT('Ctrl Pts',(0.962250097539924,-6.1354491665876,59.6785267937022));
#56708=CARTESIAN_POINT('Ctrl Pts',(5.6813414446818,-2.50839014408368,59.9568960694325));
#56709=CARTESIAN_POINT('Ctrl Pts',(5.18224646974358,3.42256968560548,60.2352653451627));
#56710=CARTESIAN_POINT('Ctrl Pts',(-0.0766271436318026,6.20997504075942,
60.5136346208931));
#56711=CARTESIAN_POINT('Ctrl Pts',(-5.26512042224072,3.29365582071042,60.7920038966233));
#56712=CARTESIAN_POINT('Ctrl Pts',(-5.61771717201837,-2.6478133433468,61.0703731723536));
#56713=CARTESIAN_POINT('Ctrl Pts',(-0.810565085404379,-6.15732457876948,
61.3487424480839));
#56714=CARTESIAN_POINT('Ctrl Pts',(4.74107308482143,-4.01146952255369,61.627111723814));
#56715=CARTESIAN_POINT('Ctrl Pts',(5.93814060230899,1.81883146915945,61.9054809995444));
#56716=CARTESIAN_POINT('Ctrl Pts',(1.68115745741945,5.97857602856726,62.1838502752747));
#56717=CARTESIAN_POINT('Ctrl Pts',(-4.11993158833646,4.64713088189084,62.4622195510049));
#56718=CARTESIAN_POINT('Ctrl Pts',(-6.1369546927136,-0.952601084177306,
62.7405888267352));
#56719=CARTESIAN_POINT('Ctrl Pts',(-2.51732079476958,-5.67739004668659,
63.0189581024655));
#56720=CARTESIAN_POINT('Ctrl Pts',(3.41441651527462,-5.18762195868357,63.2973273781957));
#56721=CARTESIAN_POINT('Ctrl Pts',(6.21008785720687,0.0668620353253585,
63.575696653926));
#56722=CARTESIAN_POINT('Ctrl Pts',(3.30193100452715,5.25993473033056,63.8540659296562));
#56723=CARTESIAN_POINT('Ctrl Pts',(-2.63897636526924,5.62187383970377,64.1324352053865));
#56724=CARTESIAN_POINT('Ctrl Pts',(-6.15604237512935,0.820246305452156,
64.4108044811168));
#56725=CARTESIAN_POINT('Ctrl Pts',(-4.01891976900398,-4.7347592986661,64.6891737568471));
#56726=CARTESIAN_POINT('Ctrl Pts',(1.80949165902193,-5.94099332283124,64.9675430325774));
#56727=CARTESIAN_POINT('Ctrl Pts',(5.97592506355382,-1.69055652398388,65.2459123083075));
#56728=CARTESIAN_POINT('Ctrl Pts',(4.65360361466952,4.11261901025744,65.524281584038));
#56729=CARTESIAN_POINT('Ctrl Pts',(-0.942949715346173,6.1384450441724,65.802650859768));
#56730=CARTESIAN_POINT('Ctrl Pts',(-5.67342461037618,2.52624522095008,66.0810201354985));
#56731=CARTESIAN_POINT('Ctrl Pts',(-5.1929846203432,-3.40625490221655,66.3593894112286));
#56732=CARTESIAN_POINT('Ctrl Pts',(0.0570967616911944,-6.21018531815279,
66.6377586869591));
#56733=CARTESIAN_POINT('Ctrl Pts',(5.25473603233471,-3.31019802375619,66.9161279626891));
#56734=CARTESIAN_POINT('Ctrl Pts',(5.62601660634699,2.6301328618728,67.1944972384196));
#56735=CARTESIAN_POINT('Ctrl Pts',(0.829925497300859,6.15474494962425,67.4728665141497));
#56736=CARTESIAN_POINT('Ctrl Pts',(-4.72843380501069,4.02636007798958,67.7512357898801));
#56737=CARTESIAN_POINT('Ctrl Pts',(-5.94383135323418,-1.80014737460753,
68.0296050656102));
#56738=CARTESIAN_POINT('Ctrl Pts',(-1.69995141035886,-5.9732593220464,68.3079743413406));
#56739=CARTESIAN_POINT('Ctrl Pts',(4.10529626302638,-4.66006484061938,68.5863436170708));
#56740=CARTESIAN_POINT('Ctrl Pts',(6.13992021727863,0.933296014910856,68.8647128928011));
#56741=CARTESIAN_POINT('Ctrl Pts',(2.53516340055861,5.66944514555562,69.1430821685314));
#56742=CARTESIAN_POINT('Ctrl Pts',(-3.39808486661228,5.19833444146264,69.4214514442617));
#56743=CARTESIAN_POINT('Ctrl Pts',(-6.21026742335611,-0.047331346875596,
69.6998207199918));
#56744=CARTESIAN_POINT('Ctrl Pts',(-3.31845685795602,-5.24952434110749,
69.9781899957223));
#56745=CARTESIAN_POINT('Ctrl Pts',(2.621282855024,-5.63014546170463,70.2565592714524));
#56746=CARTESIAN_POINT('Ctrl Pts',(6.15343230546253,-0.839602637017208,
70.5349285471828));
#56747=CARTESIAN_POINT('Ctrl Pts',(4.03379043111301,4.72209661949609,70.813297822913));
#56748=CARTESIAN_POINT('Ctrl Pts',(-1.79079863902149,5.94665468650014,71.0916670986432));
#56749=CARTESIAN_POINT('Ctrl Pts',(-5.97057881063638,1.70934209331426,71.3700363743736));
#56750=CARTESIAN_POINT('Ctrl Pts',(-4.66651454376411,-4.09796336475011,
71.6484056501037));
#56751=CARTESIAN_POINT('Ctrl Pts',(0.923640006742209,-6.1413802083848,71.9267749258341));
#56752=CARTESIAN_POINT('Ctrl Pts',(5.66545166206479,-2.544075311543,72.2051442015643));
#56753=CARTESIAN_POINT('Ctrl Pts',(5.20367140881343,3.38990642866345,72.4835134772947));
#56754=CARTESIAN_POINT('Ctrl Pts',(-0.0375658150251663,6.21033417261403,
72.7618827530248));
#56755=CARTESIAN_POINT('Ctrl Pts',(-5.24429966953607,3.32670748670501,73.0402520287552));
#56756=CARTESIAN_POINT('Ctrl Pts',(-5.63426039556707,-2.61242636660629,
73.3186213044854));
#56757=CARTESIAN_POINT('Ctrl Pts',(-0.849277700672862,-6.15210444588971,
73.5969905802157));
#56758=CARTESIAN_POINT('Ctrl Pts',(4.71574775779221,-4.0412108100016,73.8753598559459));
#56759=CARTESIAN_POINT('Ctrl Pts',(5.94946331564799,1.78144547538063,74.1537291316763));
#56760=CARTESIAN_POINT('Ctrl Pts',(1.71872854962958,5.96788353595171,74.4320984074064));
#56761=CARTESIAN_POINT('Ctrl Pts',(-4.09062033356033,4.67295270815561,74.7104676831368));
#56762=CARTESIAN_POINT('Ctrl Pts',(-6.1428250138809,-0.913981714715994,
74.9888369588671));
#56763=CARTESIAN_POINT('Ctrl Pts',(-2.55298093186715,-5.66144416977842,
75.2672062345973));
#56764=CARTESIAN_POINT('Ctrl Pts',(3.38171960859274,-5.20899550919893,75.5455755103276));
#56765=CARTESIAN_POINT('Ctrl Pts',(6.21038556576122,0.0278001902866955,
75.8239447860578));
#56766=CARTESIAN_POINT('Ctrl Pts',(3.33494988960255,5.23906203053906,76.1023140617882));
#56767=CARTESIAN_POINT('Ctrl Pts',(-2.60356341851882,5.6383613977597,76.3806833375183));
#56768=CARTESIAN_POINT('Ctrl Pts',(-6.15076137418917,0.858950664344476,
76.6590526132487));
#56769=CARTESIAN_POINT('Ctrl Pts',(-4.04862119630716,-4.7093872355974,76.9374218889788));
#56770=CARTESIAN_POINT('Ctrl Pts',(1.77208790681172,-5.95225723373308,77.2157911647093));
#56771=CARTESIAN_POINT('Ctrl Pts',(5.96517350465712,-1.72811075609542,77.4941604404393));
#56772=CARTESIAN_POINT('Ctrl Pts',(4.67937931787436,4.08326718761399,77.7725297161699));
#56773=CARTESIAN_POINT('Ctrl Pts',(-0.904321162713915,6.14425463019421,
78.0508989918999));
#56774=CARTESIAN_POINT('Ctrl Pts',(-5.65742267860557,2.56188023951072,78.3292682676303));
#56775=CARTESIAN_POINT('Ctrl Pts',(-5.21430672945461,-3.37352442664352,
78.6076375433605));
#56776=CARTESIAN_POINT('Ctrl Pts',(0.0180344968077807,-6.2104216026708,
78.8860068190908));
#56777=CARTESIAN_POINT('Ctrl Pts',(5.23381143706748,-3.34318404626741,79.164376094821));
#56778=CARTESIAN_POINT('Ctrl Pts',(5.64244845814195,2.59469403267662,79.4427453705514));
#56779=CARTESIAN_POINT('Ctrl Pts',(0.868621504114074,6.14940309368207,79.7211146462815));
#56780=CARTESIAN_POINT('Ctrl Pts',(-4.70301506863955,4.05602157170603,79.999483922012));
#56781=CARTESIAN_POINT('Ctrl Pts',(-5.95503643384666,-1.76272595645327,
80.277853197742));
#56782=CARTESIAN_POINT('Ctrl Pts',(-1.73748868951266,-5.96244872345345,
80.5562224734725));
#56783=CARTESIAN_POINT('Ctrl Pts',(4.0759039450931,-4.68579435702962,80.8345917492026));
#56784=CARTESIAN_POINT('Ctrl Pts',(6.1456690537899,0.894658374623772,81.112961024933));
#56785=CARTESIAN_POINT('Ctrl Pts',(2.5707732124682,5.65338719849006,81.3913303006631));
#56786=CARTESIAN_POINT('Ctrl Pts',(-3.36532090307962,5.21960505644742,81.6696995763936));
#56787=CARTESIAN_POINT('Ctrl Pts',(-6.21044228325367,-0.00826875873537722,
81.9480688521236));
#56788=CARTESIAN_POINT('Ctrl Pts',(-3.35140993633938,-5.22854790210446,
82.2264381278542));
#56789=CARTESIAN_POINT('Ctrl Pts',(2.58581823101083,-5.64652156660783,82.5048074035842));
#56790=CARTESIAN_POINT('Ctrl Pts',(6.14802960772673,-0.878290196068972,
82.7831766793146));
#56791=CARTESIAN_POINT('Ctrl Pts',(4.06341191789994,4.69663127267458,83.0615459550448));
#56792=CARTESIAN_POINT('Ctrl Pts',(-1.75335964745426,5.95780090911698,83.3399152307751));
#56793=CARTESIAN_POINT('Ctrl Pts',(-5.95970919907819,1.74686232669266,83.6182845065053));
#56794=CARTESIAN_POINT('Ctrl Pts',(-4.69219780975906,-4.06853062420423,
83.8966537822357));
#56795=CARTESIAN_POINT('Ctrl Pts',(0.884993374337941,-6.14706828117063,
84.1750230579659));
#56796=CARTESIAN_POINT('Ctrl Pts',(5.64933773941046,-2.57965982875044,84.4533923336961));
#56797=CARTESIAN_POINT('Ctrl Pts',(5.22489047707629,3.35710905818575,84.7317616094266));
#56798=CARTESIAN_POINT('Ctrl Pts',(0.00149699978309382,6.2104476074585,
85.0101308851566));
#56799=CARTESIAN_POINT('Ctrl Pts',(-5.2232714386648,3.35962753947885,85.288500160887));
#56800=CARTESIAN_POINT('Ctrl Pts',(-5.65058071308607,-2.57693603546843,
85.5668694366171));
#56801=CARTESIAN_POINT('Ctrl Pts',(-0.887956716301287,-6.14664091971955,
85.8452387123476));
#56802=CARTESIAN_POINT('Ctrl Pts',(4.69023586348765,-4.07079221661454,86.1236079880777));
#56803=CARTESIAN_POINT('Ctrl Pts',(5.96055065270824,1.74398900297437,86.4019772638081));
#56804=CARTESIAN_POINT('Ctrl Pts',(1.75623164445764,5.95695493830545,86.6803465395383));
#56805=CARTESIAN_POINT('Ctrl Pts',(-4.06114724317963,4.69858966022888,86.9587158152687));
#56806=CARTESIAN_POINT('Ctrl Pts',(-6.14845230887633,-0.87532618575515,
87.2370850909987));
#56807=CARTESIAN_POINT('Ctrl Pts',(-2.58854006638374,-5.64527431137958,
87.5154543667293));
#56808=CARTESIAN_POINT('Ctrl Pts',(3.34888891226714,-5.23016297827231,87.7938236424592));
#56809=CARTESIAN_POINT('Ctrl Pts',(6.2104375752723,-0.0112627545997063,
88.0721929181899));
#56810=CARTESIAN_POINT('Ctrl Pts',(3.36783683536597,5.21798205979547,88.3505621939197));
#56811=CARTESIAN_POINT('Ctrl Pts',(-2.56804746801205,5.6546258875396,88.6289314696503));
#56812=CARTESIAN_POINT('Ctrl Pts',(-6.14523703309425,0.897621040909271,
88.9073007453804));
#56813=CARTESIAN_POINT('Ctrl Pts',(-4.07816244960097,-4.6838288568926,89.1856700211108));
#56814=CARTESIAN_POINT('Ctrl Pts',(1.73461404618421,-5.96328565782118,89.464039296841));
#56815=CARTESIAN_POINT('Ctrl Pts',(5.95418594794534,-1.7655966196404,89.7424085725712));
#56816=CARTESIAN_POINT('Ctrl Pts',(4.70496989263451,4.05375382027557,90.0207778483016));
#56817=CARTESIAN_POINT('Ctrl Pts',(-0.865656832779086,6.14982113348502,
90.2991471240318));
#56818=CARTESIAN_POINT('Ctrl Pts',(-5.64119692444495,2.5974139034101,90.5775163997621));
#56819=CARTESIAN_POINT('Ctrl Pts',(-5.23542254699819,-3.34066048564925,
90.8558856754923));
#56820=CARTESIAN_POINT('Ctrl Pts',(-0.0210284815675073,-6.2104121867199,
91.1342549512226));
#56821=CARTESIAN_POINT('Ctrl Pts',(5.21267977857556,-3.37603780370208,91.4126242269529));
#56822=CARTESIAN_POINT('Ctrl Pts',(5.65865707996597,2.55915255062027,91.6909935026832));
#56823=CARTESIAN_POINT('Ctrl Pts',(0.907283145996256,6.14381795132199,91.9693627784133));
#56824=CARTESIAN_POINT('Ctrl Pts',(-4.67741026873163,4.08552259863533,92.2477320541438));
#56825=CARTESIAN_POINT('Ctrl Pts',(-5.96600591769324,-1.72523480026497,
92.5261013298739));
#56826=CARTESIAN_POINT('Ctrl Pts',(-1.77495722908411,-5.95140223484494,
92.8044706056043));
#56827=CARTESIAN_POINT('Ctrl Pts',(4.04635037377374,-4.71133849119933,93.0828398813344));
#56828=CARTESIAN_POINT('Ctrl Pts',(6.15117475161187,0.855985339318785,93.3612091570649));
#56829=CARTESIAN_POINT('Ctrl Pts',(2.60628131788759,5.63710558868877,93.6395784327949));
#56830=CARTESIAN_POINT('Ctrl Pts',(-3.33242379867873,5.24066917024868,93.9179477085254));
#56831=CARTESIAN_POINT('Ctrl Pts',(-6.21037144186387,0.0307941565386455,
94.1963169842555));
#56832=CARTESIAN_POINT('Ctrl Pts',(-3.38423042420886,-5.20736460811563,
94.4746862599858));
#56833=CARTESIAN_POINT('Ctrl Pts',(2.55025130528732,-5.6626742803976,94.7530555357162));
#56834=CARTESIAN_POINT('Ctrl Pts',(6.14238367791196,-0.91694300767064,95.0314248114463));
#56835=CARTESIAN_POINT('Ctrl Pts',(4.09287264551796,4.6709801148759,95.3097940871767));
#56836=CARTESIAN_POINT('Ctrl Pts',(-1.71585128840834,5.96871142559795,95.5881633629069));
#56837=CARTESIAN_POINT('Ctrl Pts',(-5.94860380588736,1.78431344964343,95.8665326386373));
#56838=CARTESIAN_POINT('Ctrl Pts',(-4.71769544017605,-4.03893692198051,
96.1449019143674));
#56839=CARTESIAN_POINT('Ctrl Pts',(0.84631172928875,-6.15251315990983,96.4232711900978));
#56840=CARTESIAN_POINT('Ctrl Pts',(5.63300031422728,-2.61514228789002,96.7016404658279));
#56841=CARTESIAN_POINT('Ctrl Pts',(5.24590283505089,3.32417887172173,96.9800097415584));
#56842=CARTESIAN_POINT('Ctrl Pts',(0.0405597553659755,6.21031534080523,
97.2583790172885));
#56843=CARTESIAN_POINT('Ctrl Pts',(-5.20203656155841,3.39241467662855,97.5367482930187));
#56844=CARTESIAN_POINT('Ctrl Pts',(-5.66667747890107,-2.54134375402281,
97.8151175687492));
#56845=CARTESIAN_POINT('Ctrl Pts',(-0.9266006020473,-6.14093421641053,98.0934868444793));
#56846=CARTESIAN_POINT('Ctrl Pts',(4.66453841122517,-4.1002125720749,98.3718561202097));
#56847=CARTESIAN_POINT('Ctrl Pts',(5.97140217484545,1.70646353381673,98.6502253959399));
#56848=CARTESIAN_POINT('Ctrl Pts',(1.79366525818349,5.945790667992,98.9285946716701));
#56849=CARTESIAN_POINT('Ctrl Pts',(-4.03151348322664,4.72404072384627,99.2069639474005));
#56850=CARTESIAN_POINT('Ctrl Pts',(-6.15383635506962,-0.836636026608615,
99.4853332231307));
#56851=CARTESIAN_POINT('Ctrl Pts',(-2.62399679150684,-5.62888111121181,
99.7637024988609));
#56852=CARTESIAN_POINT('Ctrl Pts',(3.31592572516549,-5.25112352846331,100.042071774591));
#56853=CARTESIAN_POINT('Ctrl Pts',(6.21024388368248,-0.0503252539024463,
100.320441050321));
#56854=CARTESIAN_POINT('Ctrl Pts',(3.40059054072436,5.19669565207855,100.598810326052));
#56855=CARTESIAN_POINT('Ctrl Pts',(-2.53242991885262,5.67066666557781,100.877179601782));
#56856=CARTESIAN_POINT('Ctrl Pts',(-6.13946957040164,0.936255905245747,
101.155548877512));
#56857=CARTESIAN_POINT('Ctrl Pts',(-4.10754236015684,-4.65808517370746,
101.433918153243));
#56858=CARTESIAN_POINT('Ctrl Pts',(1.69707155970298,-5.97407815878261,101.712287428973));
#56859=CARTESIAN_POINT('Ctrl Pts',(5.94296282811514,-1.80301263158,101.990656704703));
#56860=CARTESIAN_POINT('Ctrl Pts',(4.73037432651978,4.024080075868,102.269025980433));
#56861=CARTESIAN_POINT('Ctrl Pts',(-0.826958255203146,6.15514433381927,
102.547395256164));
#56862=CARTESIAN_POINT('Ctrl Pts',(-5.62474798982763,2.63284480684413,102.825764531894));
#56863=CARTESIAN_POINT('Ctrl Pts',(-5.25633123757708,-3.3076643794174,103.104133807624));
#56864=CARTESIAN_POINT('Ctrl Pts',(-0.0600906280010852,-6.21015707067235,
103.382503083354));
#56865=CARTESIAN_POINT('Ctrl Pts',(5.19134189288205,-3.40875799628004,103.660872359085));
#56866=CARTESIAN_POINT('Ctrl Pts',(5.67464183056409,2.52350982181727,103.939241634815));
#56867=CARTESIAN_POINT('Ctrl Pts',(0.945908893391775,6.13798974350711,104.217610910545));
#56868=CARTESIAN_POINT('Ctrl Pts',(-4.65162041827958,4.11486199163955,104.495980186275));
#56869=CARTESIAN_POINT('Ctrl Pts',(-5.97673937079238,-1.68767538929013,
104.774349462006));
#56870=CARTESIAN_POINT('Ctrl Pts',(-1.81235554672049,-5.94012029324891,
105.052718737736));
#56871=CARTESIAN_POINT('Ctrl Pts',(4.01663671828505,-4.73669623253596,105.331088013466));
#56872=CARTESIAN_POINT('Ctrl Pts',(6.15643709292455,0.817278439002367,105.609457289197));
#56873=CARTESIAN_POINT('Ctrl Pts',(2.64168631202361,5.6206009602944,105.887826564927));
#56874=CARTESIAN_POINT('Ctrl Pts',(-3.29939485490473,5.26152594951544,106.166195840657));
#56875=CARTESIAN_POINT('Ctrl Pts',(-6.21005490198965,0.0698558535153989,
106.444565116388));
#56876=CARTESIAN_POINT('Ctrl Pts',(-3.41691702309993,-5.18597529720738,
106.722934392118));
#56877=CARTESIAN_POINT('Ctrl Pts',(2.51458348497352,-5.67860296403031,107.001303667848));
#56878=CARTESIAN_POINT('Ctrl Pts',(6.13649473938585,-0.955559542616737,
107.279672943578));
#56879=CARTESIAN_POINT('Ctrl Pts',(4.12217144842418,4.64514416092682,107.558042219308));
#56880=CARTESIAN_POINT('Ctrl Pts',(-1.67827504581228,5.97938580429455,107.836411495039));
#56881=CARTESIAN_POINT('Ctrl Pts',(-5.93726307042192,1.82169398050257,108.114780770769));
#56882=CARTESIAN_POINT('Ctrl Pts',(-4.74300642626271,-4.00918342888258,
108.3931500465));
#56883=CARTESIAN_POINT('Ctrl Pts',(0.807596601941249,-6.15771462918907,
108.671519322229));
#56884=CARTESIAN_POINT('Ctrl Pts',(5.61644003286672,-2.65052128518285,108.94988859796));
#56885=CARTESIAN_POINT('Ctrl Pts',(5.26670765143319,3.29111717207553,109.22825787369));
#56886=CARTESIAN_POINT('Ctrl Pts',(0.079620906299245,6.20993737788685,109.506627149421));
#56887=CARTESIAN_POINT('Ctrl Pts',(-5.18059587832416,3.42506760100976,109.78499642515));
#56888=CARTESIAN_POINT('Ctrl Pts',(-5.68255005618204,-2.50565093039329,
110.063365700881));
#56889=CARTESIAN_POINT('Ctrl Pts',(-0.965207829057699,-6.13498456173453,
110.341734976611));
#56890=CARTESIAN_POINT('Ctrl Pts',(4.6386564176627,-4.12947071243673,110.620104252342));
#56891=CARTESIAN_POINT('Ctrl Pts',(5.98201745274544,1.668870552513,110.898473528072));
#56892=CARTESIAN_POINT('Ctrl Pts',(1.83102790983545,5.93439116669932,111.176842803802));
#56893=CARTESIAN_POINT('Ctrl Pts',(-4.0017202260902,4.74930489209694,111.455212079532));
#56894=CARTESIAN_POINT('Ctrl Pts',(-6.15897693945369,-0.797912767959604,
111.733581355263));
#56895=CARTESIAN_POINT('Ctrl Pts',(-2.65934970447637,-5.61226521783295,
112.011950630993));
#56896=CARTESIAN_POINT('Ctrl Pts',(3.28283135139781,-5.27187633051798,112.290319906723));
#56897=CARTESIAN_POINT('Ctrl Pts',(6.20980449865453,-0.089385762206777,
112.568689182453));
#56898=CARTESIAN_POINT('Ctrl Pts',(3.43320970985575,5.17520364953375,112.847058458183));
#56899=CARTESIAN_POINT('Ctrl Pts',(-2.49671218016352,5.6864830972596,113.125427733914));
#56900=CARTESIAN_POINT('Ctrl Pts',(-6.13345921428751,0.974853728857669,
113.403797009644));
#56901=CARTESIAN_POINT('Ctrl Pts',(-4.13675976562846,-4.63215720452932,
113.682166285374));
#56902=CARTESIAN_POINT('Ctrl Pts',(1.65946193264643,-5.9846343096377,113.960535561105));
#56903=CARTESIAN_POINT('Ctrl Pts',(5.93150458918226,-1.84035731163975,114.238904836835));
#56904=CARTESIAN_POINT('Ctrl Pts',(4.75559161446478,3.99424712836203,114.517274112565));
#56905=CARTESIAN_POINT('Ctrl Pts',(-0.788226961002809,6.16022402059727,
114.795643388296));
#56906=CARTESIAN_POINT('Ctrl Pts',(-5.60807652551605,2.66817154807391,115.074012664026));
#56907=CARTESIAN_POINT('Ctrl Pts',(-5.27703197398926,-3.2745374133595,115.352381939756));
#56908=CARTESIAN_POINT('Ctrl Pts',(-0.0991503970927691,-6.20965626462145,
115.630751215486));
#56909=CARTESIAN_POINT('Ctrl Pts',(5.16979862416974,-3.44134332950492,115.909120491217));
#56910=CARTESIAN_POINT('Ctrl Pts',(5.69040207753754,2.48776725638707,116.187489766947));
#56911=CARTESIAN_POINT('Ctrl Pts',(0.984497218165544,6.13191870081628,116.465859042677));
#56912=CARTESIAN_POINT('Ctrl Pts',(-4.62564653759719,4.14403858997612,116.744228318407));
#56913=CARTESIAN_POINT('Ctrl Pts',(-5.98723636850076,-1.65004920947743,
117.022597594138));
#56914=CARTESIAN_POINT('Ctrl Pts',(-1.8496821628465,-5.92860334500824,117.300966869868));
#56915=CARTESIAN_POINT('Ctrl Pts',(3.98676415417643,-4.76186657782114,117.579336145598));
#56916=CARTESIAN_POINT('Ctrl Pts',(6.16145586953622,0.778539205020277,117.857705421328));
#56917=CARTESIAN_POINT('Ctrl Pts',(2.67698679416211,5.60387396627344,118.136074697059));
#56918=CARTESIAN_POINT('Ctrl Pts',(-3.2662353784689,5.28217456909872,118.414443972789));
#56919=CARTESIAN_POINT('Ctrl Pts',(-6.20949267615386,0.108914786812677,
118.692813248519));
#56920=CARTESIAN_POINT('Ctrl Pts',(-3.44946843984602,-5.16438081559675,
118.97118252425));
#56921=CARTESIAN_POINT('Ctrl Pts',(2.47881618118194,-5.69430698732565,119.24955179998));
#56922=CARTESIAN_POINT('Ctrl Pts',(6.13036302512973,-0.994138273136335,
119.52792107571));
#56923=CARTESIAN_POINT('Ctrl Pts',(4.15130716748207,4.6191244329653,119.80629035144));
#56924=CARTESIAN_POINT('Ctrl Pts',(-1.64063240628113,5.98982362289971,120.084659627171));
#56925=CARTESIAN_POINT('Ctrl Pts',(-5.92568744134926,1.85900244040056,120.363028902901));
#56926=CARTESIAN_POINT('Ctrl Pts',(-4.76812976665383,-3.97927132204007,
120.641398178631));
#56927=CARTESIAN_POINT('Ctrl Pts',(0.768849523973782,-6.16267248321747,
120.919767454361));
#56928=CARTESIAN_POINT('Ctrl Pts',(5.59965755048293,-2.6857954209572,121.198136730092));
#56929=CARTESIAN_POINT('Ctrl Pts',(5.28730410315625,3.25792526727902,121.476506005822));
#56930=CARTESIAN_POINT('Ctrl Pts',(0.118678907173586,6.20931373360969,121.754875281552));
#56931=CARTESIAN_POINT('Ctrl Pts',(-5.15895023711994,3.45758502087614,122.033244557282));
#56932=CARTESIAN_POINT('Ctrl Pts',(-5.69819781714075,-2.46985897684768,
122.311613833013));
#56933=CARTESIAN_POINT('Ctrl Pts',(-1.00377686960519,-6.1287921907601,122.589983108743));
#56934=CARTESIAN_POINT('Ctrl Pts',(4.61259090614592,-4.15856548076738,122.868352384473));
#56935=CARTESIAN_POINT('Ctrl Pts',(5.9923960675984,1.63121154746421,123.146721660204));
#56936=CARTESIAN_POINT('Ctrl Pts',(1.86831811906265,5.92275688329723,123.425090935934));
#56937=CARTESIAN_POINT('Ctrl Pts',(-3.97176864633893,4.77438116947538,123.703460211664));
#56938=CARTESIAN_POINT('Ctrl Pts',(-6.16387386645271,-0.759157949374332,
123.981829487395));
#56939=CARTESIAN_POINT('Ctrl Pts',(-2.69459739191245,-5.59542727431215,
124.260198763124));
#56940=CARTESIAN_POINT('Ctrl Pts',(3.2496070724577,-5.29242059040039,124.538568038855));
#56941=CARTESIAN_POINT('Ctrl Pts',(6.20911949007491,-0.128442683197594,
124.816937314585));
#56942=CARTESIAN_POINT('Ctrl Pts',(3.46569295312417,5.153506806181,125.095306590315));
#56943=CARTESIAN_POINT('Ctrl Pts',(-2.46089547784216,5.70207473860405,125.373675866046));
#56944=CARTESIAN_POINT('Ctrl Pts',(-6.12720655598897,1.01341264151739,125.652045141776));
#56945=CARTESIAN_POINT('Ctrl Pts',(-4.16581284271013,-4.60604532710973,
125.930414417506));
#56946=CARTESIAN_POINT('Ctrl Pts',(1.62178539278297,-5.99495491636355,126.208783693237));
#56947=CARTESIAN_POINT('Ctrl Pts',(5.91981406391576,-1.8776268719497,126.487152968967));
#56948=CARTESIAN_POINT('Ctrl Pts',(4.78061626591979,3.96425179549011,126.765522244697));
#56949=CARTESIAN_POINT('Ctrl Pts',(-0.749455999002484,6.16506823020972,
127.043891520427));
#56950=CARTESIAN_POINT('Ctrl Pts',(-5.59119920962547,2.70337717567628,127.322260796158));
#56951=CARTESIAN_POINT('Ctrl Pts',(-5.29749369097637,-3.24125152930667,
127.600630071888));
#56952=CARTESIAN_POINT('Ctrl Pts',(-0.13826335471824,-6.2089652426601,127.878999347618));
#56953=CARTESIAN_POINT('Ctrl Pts',(5.14815866266899,-3.47368780450951,128.157368623348));
#56954=CARTESIAN_POINT('Ctrl Pts',(5.7057335741975,2.45172854905703,128.435737899079));
#56955=CARTESIAN_POINT('Ctrl Pts',(1.02343110214051,6.12597844780046,128.714107174809));
#56956=CARTESIAN_POINT('Ctrl Pts',(-4.60021590128167,4.17234580462416,128.992476450539));
#56957=CARTESIAN_POINT('Ctrl Pts',(-5.99612342097425,-1.61102240036703,
129.270845726269));
#56958=CARTESIAN_POINT('Ctrl Pts',(-1.88954273411231,-5.91940060591759,
129.549215002));
#56959=CARTESIAN_POINT('Ctrl Pts',(3.96177486026028,-4.78181212020278,129.82758427773));
#56960=CARTESIAN_POINT('Ctrl Pts',(5.79010620548154,-0.189962750713211,
130.059558674172));
#56961=CARTESIAN_POINT('Ctrl Pts',(4.44638236249096,3.17706810551834,130.245138191326));
#56962=CARTESIAN_POINT('Ctrl Pts',(3.08009875615274,4.34188596571016,130.337927949902));
#56963=CARTESIAN_POINT('Ctrl Pts',(2.29321473482586,4.72388001049864,130.384322829191));
#56964=CARTESIAN_POINT('Ctrl Pts',(2.85706463458369,-4.00329423554042,-10.));
#56965=CARTESIAN_POINT('Ctrl Pts',(3.52391651473643,-3.52737645103792,-9.95360512071162));
#56966=CARTESIAN_POINT('Ctrl Pts',(4.6032797975914,-2.23787345781402,-9.86081536213486));
#56967=CARTESIAN_POINT('Ctrl Pts',(5.31710770646798,1.0817198372055,-9.67523584498136));
#56968=CARTESIAN_POINT('Ctrl Pts',(2.91000325553484,5.03585724930024,-9.44326144853946));
#56969=CARTESIAN_POINT('Ctrl Pts',(-2.67142550958262,5.17047615300083,-9.16489217280919));
#56970=CARTESIAN_POINT('Ctrl Pts',(-5.78925343142622,0.549143031760425,
-8.88652289707893));
#56971=CARTESIAN_POINT('Ctrl Pts',(-3.59496519784923,-4.57298129089445,
-8.60815362134865));
#56972=CARTESIAN_POINT('Ctrl Pts',(1.90395420368265,-5.4968079578387,-8.32978434561839));
#56973=CARTESIAN_POINT('Ctrl Pts',(5.65268654860171,-1.37094194360677,-8.05141506988812));
#56974=CARTESIAN_POINT('Ctrl Pts',(4.21031778233782,4.01357646538516,-7.77304579415784));
#56975=CARTESIAN_POINT('Ctrl Pts',(-1.09954047142025,5.71199305956496,-7.49467651842759));
#56976=CARTESIAN_POINT('Ctrl Pts',(-5.39928022209077,2.16392258626905,-7.21630724269731));
#56977=CARTESIAN_POINT('Ctrl Pts',(-4.74001446358611,-3.37158453305954,
-6.93793796696704));
#56978=CARTESIAN_POINT('Ctrl Pts',(0.272909909778823,-5.81040739879541,
-6.65956869123677));
#56979=CARTESIAN_POINT('Ctrl Pts',(5.03514064798181,-2.9124777495484,-6.38119941550651));
#56980=CARTESIAN_POINT('Ctrl Pts',(5.17272309584991,2.66048658894571,-6.10283013977622));
#56981=CARTESIAN_POINT('Ctrl Pts',(0.559264958796863,5.78985906598745,-5.82446086404598));
#56982=CARTESIAN_POINT('Ctrl Pts',(-4.56786091744391,3.60137092478267,-5.54609158831568));
#56983=CARTESIAN_POINT('Ctrl Pts',(-5.49951019303444,-1.89489494166458,
-5.26772231258544));
#56984=CARTESIAN_POINT('Ctrl Pts',(-1.37997979498124,-5.65074267591175,
-4.98935303685515));
#56985=CARTESIAN_POINT('Ctrl Pts',(4.00703078514331,-4.21650789487217,-4.7109837611249));
#56986=CARTESIAN_POINT('Ctrl Pts',(5.71367268487829,1.09049576997227,-4.43261448539462));
#56987=CARTESIAN_POINT('Ctrl Pts',(2.17243253669944,5.39590335156548,-4.15424520966435));
#56988=CARTESIAN_POINT('Ctrl Pts',(-3.36413869033177,4.74529310749045,-3.87587593393408));
#56989=CARTESIAN_POINT('Ctrl Pts',(-5.81082307364013,-0.263763748565971,
-3.59750665820381));
#56990=CARTESIAN_POINT('Ctrl Pts',(-2.92039509627066,-5.03055946195533,
-3.31913738247355));
#56991=CARTESIAN_POINT('Ctrl Pts',(2.65235109881223,-5.17689768424732,-3.04076810674327));
#56992=CARTESIAN_POINT('Ctrl Pts',(5.78897154557153,-0.568370014814376,
-2.76239883101301));
#56993=CARTESIAN_POINT('Ctrl Pts',(3.60854980134286,4.56219293151739,-2.48402955528274));
#56994=CARTESIAN_POINT('Ctrl Pts',(-1.8862450334912,5.50248268361132,-2.20566027955247));
#56995=CARTESIAN_POINT('Ctrl Pts',(-5.6485655710584,1.38886392626336,-1.9272910038222));
#56996=CARTESIAN_POINT('Ctrl Pts',(-4.22280370010565,-4.00039559592092,
-1.64892172809193));
#56997=CARTESIAN_POINT('Ctrl Pts',(1.08150986877385,-5.71538033878776,-1.37055245236166));
#56998=CARTESIAN_POINT('Ctrl Pts',(5.39248056989081,-2.18091478914392,-1.0921831766314));
#56999=CARTESIAN_POINT('Ctrl Pts',(4.75057726644074,3.35667270511782,-0.813813900901123));
#57000=CARTESIAN_POINT('Ctrl Pts',(-0.254626070074851,5.81123064231236,
-0.535444625170857));
#57001=CARTESIAN_POINT('Ctrl Pts',(-5.02596099912126,2.9283019053962,-0.257075349440584));
#57002=CARTESIAN_POINT('Ctrl Pts',(-5.18106203404851,-2.64420729389814,
0.0212939262896814));
#57003=CARTESIAN_POINT('Ctrl Pts',(-0.577472308506603,-5.78807064112712,
0.299663202019953));
#57004=CARTESIAN_POINT('Ctrl Pts',(4.5565129461533,-3.61571926251521,0.578032477750221));
#57005=CARTESIAN_POINT('Ctrl Pts',(5.50544194895434,1.87759020035487,0.856401753480491));
#57006=CARTESIAN_POINT('Ctrl Pts',(1.3977444217788,5.64637463733703,1.13477102921076));
#57007=CARTESIAN_POINT('Ctrl Pts',(-3.99375040828915,4.2290889905592,1.41314030494103));
#57008=CARTESIAN_POINT('Ctrl Pts',(-5.71707391697906,-1.07252125460282,
1.6915095806713));
#57009=CARTESIAN_POINT('Ctrl Pts',(-2.18939161896353,-5.38904447491294,
1.96987885640157));
#57010=CARTESIAN_POINT('Ctrl Pts',(3.34919840410121,-4.75584966790831,2.24824813213183));
#57011=CARTESIAN_POINT('Ctrl Pts',(5.81162385012341,0.245487756220548,2.5266174078621));
#57012=CARTESIAN_POINT('Ctrl Pts',(2.93620146934825,5.02135011179013,2.80498668359237));
#57013=CARTESIAN_POINT('Ctrl Pts',(-2.63605694837504,5.18521357117537,3.08335595932264));
#57014=CARTESIAN_POINT('Ctrl Pts',(-5.7871554259382,0.586573175155174,3.36172523505291));
#57015=CARTESIAN_POINT('Ctrl Pts',(-3.62287978254425,-4.55082169448657,
3.64009451078318));
#57016=CARTESIAN_POINT('Ctrl Pts',(1.86893072420659,-5.50838760091319,3.91846378651344));
#57017=CARTESIAN_POINT('Ctrl Pts',(5.64416974217652,-1.40662146125979,4.19683306224373));
#57018=CARTESIAN_POINT('Ctrl Pts',(4.23536382377072,3.98709534549548,4.47520233797398));
#57019=CARTESIAN_POINT('Ctrl Pts',(-1.06352998838801,5.71875335869428,4.75357161370427));
#57020=CARTESIAN_POINT('Ctrl Pts',(-5.38559505463087,2.1978630351578,5.03194088943452));
#57021=CARTESIAN_POINT('Ctrl Pts',(-4.76111030971177,-3.34171582163024,
5.3103101651648));
#57022=CARTESIAN_POINT('Ctrl Pts',(0.236348835348182,-5.81200268769786,
5.58867944089506));
#57023=CARTESIAN_POINT('Ctrl Pts',(5.01672680831839,-2.94409377304407,5.86704871662534));
#57024=CARTESIAN_POINT('Ctrl Pts',(5.18935228697503,2.62790008475296,6.1454179923556));
#57025=CARTESIAN_POINT('Ctrl Pts',(0.59567259140266,5.78622590101952,6.42378726808587));
#57026=CARTESIAN_POINT('Ctrl Pts',(-4.54511919013754,3.63003134438547,6.70215654381614));
#57027=CARTESIAN_POINT('Ctrl Pts',(-5.51131963244376,-1.86026662680852,
6.9805258195464));
#57028=CARTESIAN_POINT('Ctrl Pts',(-1.41549502262945,-5.64195089084342,
7.25889509527668));
#57029=CARTESIAN_POINT('Ctrl Pts',(3.98043042392857,-4.24162818432278,7.53726437100694));
#57030=CARTESIAN_POINT('Ctrl Pts',(5.72041865981625,1.05453609241393,7.81563364673722));
#57031=CARTESIAN_POINT('Ctrl Pts',(2.20632901676084,5.38213231754632,8.09400292246748));
#57032=CARTESIAN_POINT('Ctrl Pts',(-3.33422497619683,4.76635917885788,8.37237219819775));
#57033=CARTESIAN_POINT('Ctrl Pts',(-5.81236715410425,-0.227209330062944,
8.65074147392803));
#57034=CARTESIAN_POINT('Ctrl Pts',(-2.9519787969659,-5.01209110013389,8.92911074965828));
#57035=CARTESIAN_POINT('Ctrl Pts',(2.61973672319965,-5.19347817121596,9.20748002538857));
#57036=CARTESIAN_POINT('Ctrl Pts',(5.7852820686703,-0.60477053474805,9.48584930111882));
#57037=CARTESIAN_POINT('Ctrl Pts',(3.63717393035499,4.53940544720601,9.7642185768491));
#57038=CARTESIAN_POINT('Ctrl Pts',(-1.8515979295839,5.51423803629642,10.0425878525794));
#57039=CARTESIAN_POINT('Ctrl Pts',(-5.63971808882434,1.42436508394621,10.3209571283096));
#57040=CARTESIAN_POINT('Ctrl Pts',(-4.24788205672562,-3.97375566006845,
10.5993264040399));
#57041=CARTESIAN_POINT('Ctrl Pts',(1.04553958891947,-5.72206981622731,10.8776956797702));
#57042=CARTESIAN_POINT('Ctrl Pts',(5.37865627222158,-2.214789542839,11.1560649555005));
#57043=CARTESIAN_POINT('Ctrl Pts',(4.77159626236785,3.32672588632348,11.4344342312307));
#57044=CARTESIAN_POINT('Ctrl Pts',(-0.218069262963983,5.81271724844138,
11.712803506961));
#57045=CARTESIAN_POINT('Ctrl Pts',(-5.00744299869918,2.95985652161657,11.9911727826912));
#57046=CARTESIAN_POINT('Ctrl Pts',(-5.19759121369619,-2.61156688390049,
12.2695420584215));
#57047=CARTESIAN_POINT('Ctrl Pts',(-0.613866982695112,-5.78432393122432,
12.5479113341518));
#57048=CARTESIAN_POINT('Ctrl Pts',(4.53368047982022,-3.64430752279149,12.8262806098821));
#57049=CARTESIAN_POINT('Ctrl Pts',(5.51714280525491,1.84292465396758,13.1046498856123));
#57050=CARTESIAN_POINT('Ctrl Pts',(1.43323162327729,5.63747134164028,13.3830191613426));
#57051=CARTESIAN_POINT('Ctrl Pts',(-3.96707107041965,4.25412542551546,13.6613884370729));
#57052=CARTESIAN_POINT('Ctrl Pts',(-5.72370682384467,-1.0365405001501,13.9397577128031));
#57053=CARTESIAN_POINT('Ctrl Pts',(-2.22324459247222,-5.3751669272517,14.2181269885334));
#57054=CARTESIAN_POINT('Ctrl Pts',(3.31921857055293,-4.77682154729211,14.4964962642637));
#57055=CARTESIAN_POINT('Ctrl Pts',(5.81305296984359,0.208928656651545,14.774865539994));
#57056=CARTESIAN_POINT('Ctrl Pts',(2.96772692751709,5.00278251550746,15.0532348157242));
#57057=CARTESIAN_POINT('Ctrl Pts',(-2.60339058705663,5.2016914042456,15.3316040914545));
#57058=CARTESIAN_POINT('Ctrl Pts',(-5.78335149105072,0.62296191275141,15.6099733671847));
#57059=CARTESIAN_POINT('Ctrl Pts',(-3.65143210405607,-4.52794430213603,
15.888342642915));
#57060=CARTESIAN_POINT('Ctrl Pts',(1.83424682140562,-5.52003393213674,16.1667119186453));
#57061=CARTESIAN_POINT('Ctrl Pts',(5.63521065484668,-1.44209461869877,16.4450811943755));
#57062=CARTESIAN_POINT('Ctrl Pts',(4.26035827525457,3.96037667151086,16.7234504701058));
#57063=CARTESIAN_POINT('Ctrl Pts',(-1.02753884835743,5.7253296786206,17.0018197458361));
#57064=CARTESIAN_POINT('Ctrl Pts',(-5.37166429126469,2.23169414475401,17.2801890215664));
#57065=CARTESIAN_POINT('Ctrl Pts',(-4.78203502071031,-3.31170304744819,
17.5585582972966));
#57066=CARTESIAN_POINT('Ctrl Pts',(0.199787533727289,-5.81337431748075,
17.8369275730269));
#57067=CARTESIAN_POINT('Ctrl Pts',(4.99810966208265,-2.97558999520659,18.1152968487571));
#57068=CARTESIAN_POINT('Ctrl Pts',(5.20577873272567,2.59520785288553,18.3936661244875));
#57069=CARTESIAN_POINT('Ctrl Pts',(0.632055302428017,5.78236475055406,18.6720354002177));
#57070=CARTESIAN_POINT('Ctrl Pts',(-4.52219692833723,3.65854765653187,18.950404675948));
#57071=CARTESIAN_POINT('Ctrl Pts',(-5.52291140979303,-1.8255644533556,19.2287739516782));
#57072=CARTESIAN_POINT('Ctrl Pts',(-1.45095404829527,-5.63293603403351,
19.5071432274085));
#57073=CARTESIAN_POINT('Ctrl Pts',(3.95367247989527,-4.26658059053105,19.7855125031388));
#57074=CARTESIAN_POINT('Ctrl Pts',(5.72693837654226,1.01853465579974,20.063881778869));
#57075=CARTESIAN_POINT('Ctrl Pts',(2.24013817879126,5.36814837292146,20.3422510545993));
#57076=CARTESIAN_POINT('Ctrl Pts',(-3.30417933559282,4.78723666973118,20.6206203303296));
#57077=CARTESIAN_POINT('Ctrl Pts',(-5.81368129055826,-0.190645916794373,
20.8989896060598));
#57078=CARTESIAN_POINT('Ctrl Pts',(-2.98344570524222,-4.99342444997913,
21.1773588817902));
#57079=CARTESIAN_POINT('Ctrl Pts',(2.58701870162035,-5.20985318902981,21.4557281575204));
#57080=CARTESIAN_POINT('Ctrl Pts',(5.7813637121742,-0.641147129240114,21.7340974332507));
#57081=CARTESIAN_POINT('Ctrl Pts',(3.66565416262452,4.51643837263511,22.0124667089809));
#57082=CARTESIAN_POINT('Ctrl Pts',(-1.81687757128598,5.5257752311088,22.2908359847112));
#57083=CARTESIAN_POINT('Ctrl Pts',(-5.6306474848251,1.45980989016045,22.5692052604415));
#57084=CARTESIAN_POINT('Ctrl Pts',(-4.2727923559593,-3.94695851215,22.8475745361717));
#57085=CARTESIAN_POINT('Ctrl Pts',(1.00952794474132,-5.72853291363189,23.1259438119021));
#57086=CARTESIAN_POINT('Ctrl Pts',(5.36461918091565,-2.24857667370483,23.4043130876322));
#57087=CARTESIAN_POINT('Ctrl Pts',(4.79242648149282,3.29664745359036,23.6826823633626));
#57088=CARTESIAN_POINT('Ctrl Pts',(-0.181503828456812,5.8139738883171,23.9610516390928));
#57089=CARTESIAN_POINT('Ctrl Pts',(-4.98872689078183,2.99129403819949,24.2394209148231));
#57090=CARTESIAN_POINT('Ctrl Pts',(-5.2139147630833,-2.57882315351005,24.5177901905534));
#57091=CARTESIAN_POINT('Ctrl Pts',(-0.650237370706631,-5.78034837838638,
24.7961594662836));
#57092=CARTESIAN_POINT('Ctrl Pts',(4.51066864926873,-3.67275160476199,25.0745287420139));
#57093=CARTESIAN_POINT('Ctrl Pts',(5.52862538900271,1.8081861966767,25.3528980177442));
#57094=CARTESIAN_POINT('Ctrl Pts',(1.46866212239656,5.62834501288036,25.6312672934744));
#57095=CARTESIAN_POINT('Ctrl Pts',(-3.94023478487658,4.27899355617956,25.9096365692047));
#57096=CARTESIAN_POINT('Ctrl Pts',(-5.73011328594672,-1.00051873745295,
26.1880058449349));
#57097=CARTESIAN_POINT('Ctrl Pts',(-2.25700960862895,-5.36107672397384,
26.4663751206653));
#57098=CARTESIAN_POINT('Ctrl Pts',(3.28910742006482,-4.79760444316246,26.7447443963955));
#57099=CARTESIAN_POINT('Ctrl Pts',(5.81425211003376,0.17236129132015,27.0231136721258));
#57100=CARTESIAN_POINT('Ctrl Pts',(2.99913497467191,4.98401699610638,27.3014829478561));
#57101=CARTESIAN_POINT('Ctrl Pts',(-2.57062122881967,5.21796344484313,27.5798522235863));
#57102=CARTESIAN_POINT('Ctrl Pts',(-5.7793187517012,0.659326004350221,27.8582214993166));
#57103=CARTESIAN_POINT('Ctrl Pts',(-3.6798399653946,-4.50488777250468,28.1365907750468));
#57104=CARTESIAN_POINT('Ctrl Pts',(1.79949035101865,-5.53146187642727,28.4149600507771));
#57105=CARTESIAN_POINT('Ctrl Pts',(5.62602862389248,-1.47751072311508,28.6933293265074));
#57106=CARTESIAN_POINT('Ctrl Pts',(4.28518417585832,3.93350131470056,28.9716986022376));
#57107=CARTESIAN_POINT('Ctrl Pts',(-0.991507056211286,5.73167948957902,
29.250067877968));
#57108=CARTESIAN_POINT('Ctrl Pts',(-5.35752101085537,2.26543696271178,29.5284371536982));
#57109=CARTESIAN_POINT('Ctrl Pts',(-4.80277054193674,-3.2815592536601,29.8068064294285));
#57110=CARTESIAN_POINT('Ctrl Pts',(0.163218327990816,-5.81451595502028,
30.0851757051587));
#57111=CARTESIAN_POINT('Ctrl Pts',(4.97929477759872,-3.00696849527155,30.363544980889));
#57112=CARTESIAN_POINT('Ctrl Pts',(5.22199922429825,2.56241294782984,30.6419142566192));
#57113=CARTESIAN_POINT('Ctrl Pts',(0.668413007697845,5.77827483466457,30.9202835323496));
#57114=CARTESIAN_POINT('Ctrl Pts',(-4.4990957566372,3.68691922699517,31.1986528080798));
#57115=CARTESIAN_POINT('Ctrl Pts',(-5.53428468636881,-1.79079005581371,
31.4770220838101));
#57116=CARTESIAN_POINT('Ctrl Pts',(-1.48635567043628,-5.62369832358916,
31.7553913595403));
#57117=CARTESIAN_POINT('Ctrl Pts',(3.92675811827154,-4.29136419968826,32.0337606352706));
#57118=CARTESIAN_POINT('Ctrl Pts',(5.73323152065607,0.982492923299337,32.3121299110009));
#57119=CARTESIAN_POINT('Ctrl Pts',(2.27385871511533,5.35395205035231,32.5904991867312));
#57120=CARTESIAN_POINT('Ctrl Pts',(-3.27400297304034,4.80792476504159,32.8688684624614));
#57121=CARTESIAN_POINT('Ctrl Pts',(-5.81476542262427,-0.154074961076227,
33.1472377381917));
#57122=CARTESIAN_POINT('Ctrl Pts',(-3.01479458062872,-4.97456024693533,
33.425607013922));
#57123=CARTESIAN_POINT('Ctrl Pts',(2.55419833083681,-5.22602209146957,33.7039762896522));
#57124=CARTESIAN_POINT('Ctrl Pts',(5.77721662985775,-0.677498358280351,
33.9823455653825));
#57125=CARTESIAN_POINT('Ctrl Pts',(3.69398937205911,4.49329261598795,34.2607148411128));
#57126=CARTESIAN_POINT('Ctrl Pts',(-1.78208533257483,5.53709381184744,34.539084116843));
#57127=CARTESIAN_POINT('Ctrl Pts',(-5.62135411773242,1.49519694248963,34.8174533925734));
#57128=CARTESIAN_POINT('Ctrl Pts',(-4.29753361238825,-3.92000521226321,
35.0958226683035));
#57129=CARTESIAN_POINT('Ctrl Pts',(0.973476361005944,-5.73476937534023,
35.3741919440339));
#57130=CARTESIAN_POINT('Ctrl Pts',(5.3503698512895,-2.28227484501538,35.6525612197641));
#57131=CARTESIAN_POINT('Ctrl Pts',(4.81306709973239,3.26643859688978,35.9309304954944));
#57132=CARTESIAN_POINT('Ctrl Pts',(-0.144931213185082,5.81500051222889,
36.2092997712246));
#57133=CARTESIAN_POINT('Ctrl Pts',(-4.96981341582323,3.02261321139193,36.4876690469549));
#57134=CARTESIAN_POINT('Ctrl Pts',(-5.23003203640979,-2.54597739815277,
36.7660383226852));
#57135=CARTESIAN_POINT('Ctrl Pts',(-0.6865820336325,-5.77614413989737,37.0444075984155));
#57136=CARTESIAN_POINT('Ctrl Pts',(4.48747836490629,-3.70105038310417,37.3227768741457));
#57137=CARTESIAN_POINT('Ctrl Pts',(5.53988924591708,1.77337620282608,37.601146149876));
#57138=CARTESIAN_POINT('Ctrl Pts',(1.50403451741344,5.61899601211875,37.8795154256062));
#57139=CARTESIAN_POINT('Ctrl Pts',(-3.91324261337339,4.30369239870326,38.1578847013366));
#57140=CARTESIAN_POINT('Ctrl Pts',(-5.73629304982887,-0.964457391626264,
38.4362539770668));
#57141=CARTESIAN_POINT('Ctrl Pts',(-2.29068533160149,-5.3467744225246,38.7146232527971));
#57142=CARTESIAN_POINT('Ctrl Pts',(3.25886614391259,-4.81819753329374,38.9929925285273));
#57143=CARTESIAN_POINT('Ctrl Pts',(5.81522122325282,0.135787106926827,39.2713618042576));
#57144=CARTESIAN_POINT('Ctrl Pts',(3.03042436822842,4.96505429599969,39.5497310799879));
#57145=CARTESIAN_POINT('Ctrl Pts',(-2.53775017010531,5.23402904920365,39.8281003557182));
#57146=CARTESIAN_POINT('Ctrl Pts',(-5.77505736743528,0.695664011293557,
40.1064696314484));
#57147=CARTESIAN_POINT('Ctrl Pts',(-3.70810224267088,-4.48165301776886,
40.3848389071787));
#57148=CARTESIAN_POINT('Ctrl Pts',(1.76466268810206,-5.5426709816656,40.663208182909));
#57149=CARTESIAN_POINT('Ctrl Pts',(5.61662401257895,-1.5128683733554,40.9415774586392));
#57150=CARTESIAN_POINT('Ctrl Pts',(4.30984054340475,3.90647033832362,41.2199467343696));
#57151=CARTESIAN_POINT('Ctrl Pts',(-0.955436037461097,5.73780254035447,
41.4983160100997));
#57152=CARTESIAN_POINT('Ctrl Pts',(-5.34316577294787,2.29909015407745,41.7766852858301));
#57153=CARTESIAN_POINT('Ctrl Pts',(-4.82331605303984,-3.25128563283292,
42.0550545615603));
#57154=CARTESIAN_POINT('Ctrl Pts',(0.126642664911688,-5.81542755515032,
42.3334238372905));
#57155=CARTESIAN_POINT('Ctrl Pts',(4.96028289923243,-3.03822803182378,42.6117931130208));
#57156=CARTESIAN_POINT('Ctrl Pts',(5.23801311996793,2.52951666703768,42.8901623887511));
#57157=CARTESIAN_POINT('Ctrl Pts',(0.704744268806608,5.77395631515876,43.1685316644814));
#57158=CARTESIAN_POINT('Ctrl Pts',(-4.47581658897993,3.7151449333222,43.4469009402115));
#57159=CARTESIAN_POINT('Ctrl Pts',(-5.54543901221464,-1.7559448099486,43.725270215942));
#57160=CARTESIAN_POINT('Ctrl Pts',(-1.52169848847216,-5.61423812497824,
44.0036394916721));
#57161=CARTESIAN_POINT('Ctrl Pts',(3.89968840385962,-4.31597803129028,44.2820087674025));
#57162=CARTESIAN_POINT('Ctrl Pts',(5.73929784318452,0.946412320817448,44.5603780431327));
#57163=CARTESIAN_POINT('Ctrl Pts',(2.30748929166079,5.33954391148237,44.838747318863));
#57164=CARTESIAN_POINT('Ctrl Pts',(-3.24369708239501,4.82842264631418,45.1171165945933));
#57165=CARTESIAN_POINT('Ctrl Pts',(-5.8156195074112,-0.117497909751016,
45.3954858703235));
#57166=CARTESIAN_POINT('Ctrl Pts',(-3.046024182882,-4.95549923731964,45.6738551460538));
#57167=CARTESIAN_POINT('Ctrl Pts',(2.52127690930862,-5.24198423885123,45.9522244217841));
#57168=CARTESIAN_POINT('Ctrl Pts',(5.77284098579036,-0.713822783719208,
46.2305936975144));
#57169=CARTESIAN_POINT('Ctrl Pts',(3.72217843764396,4.46996909297098,46.5089629732446));
#57170=CARTESIAN_POINT('Ctrl Pts',(-1.74722258992204,5.54819333071977,46.7873322489749));
#57171=CARTESIAN_POINT('Ctrl Pts',(-5.61183835521605,1.53052484092992,47.0657015247051));
#57172=CARTESIAN_POINT('Ctrl Pts',(-4.32210484718396,-3.89289682675079,
47.3440708004355));
#57173=CARTESIAN_POINT('Ctrl Pts',(0.937386264007801,-5.74077895462167,
47.6224400761656));
#57174=CARTESIAN_POINT('Ctrl Pts',(5.33590884708369,-2.31588272358329,47.900809351896));
#57175=CARTESIAN_POINT('Ctrl Pts',(4.83351730048996,3.23610051136267,48.1791786276262));
#57176=CARTESIAN_POINT('Ctrl Pts',(-0.108352864056654,5.81579707956082,
48.4575479033566));
#57177=CARTESIAN_POINT('Ctrl Pts',(-4.95070332208964,3.05381280212593,48.7359171790867));
#57178=CARTESIAN_POINT('Ctrl Pts',(-5.24594239603436,-2.51303091729227,
49.0142864548171));
#57179=CARTESIAN_POINT('Ctrl Pts',(-0.722899533583313,-5.77171138208786,
49.2926557305472));
#57180=CARTESIAN_POINT('Ctrl Pts',(4.46411054420093,-3.72920273824468,49.5710250062776));
#57181=CARTESIAN_POINT('Ctrl Pts',(5.55093393037054,1.73849604958962,49.8493942820078));
#57182=CARTESIAN_POINT('Ctrl Pts',(1.53934740890388,5.60942470922629,50.1277635577381));
#57183=CARTESIAN_POINT('Ctrl Pts',(-3.88609562379059,4.32822097593609,50.4061328334684));
#57184=CARTESIAN_POINT('Ctrl Pts',(-5.74224587100358,-0.92835788935079,
50.6845021091986));
#57185=CARTESIAN_POINT('Ctrl Pts',(-2.32427042909063,-5.33226058874023,
50.962871384929));
#57186=CARTESIAN_POINT('Ctrl Pts',(3.22849593851986,-4.8386000029697,51.2412406606591));
#57187=CARTESIAN_POINT('Ctrl Pts',(5.81596027116012,0.0992075504414687,
51.5196099363895));
#57188=CARTESIAN_POINT('Ctrl Pts',(3.06159387029672,4.94589516540121,51.7979792121197));
#57189=CARTESIAN_POINT('Ctrl Pts',(-2.50477871137838,5.24988758173003,52.07634848785));
#57190=CARTESIAN_POINT('Ctrl Pts',(-5.77056750684446,0.731974495954949,
52.3547177635803));
#57191=CARTESIAN_POINT('Ctrl Pts',(-3.73621781775542,-4.45824095715614,
52.6330870393105));
#57192=CARTESIAN_POINT('Ctrl Pts',(1.72976521052916,-5.55366080439025,52.9114563150408));
#57193=CARTESIAN_POINT('Ctrl Pts',(5.6069971929771,-1.54816617057876,53.1898255907711));
#57194=CARTESIAN_POINT('Ctrl Pts',(4.33432640242356,3.87928481179605,53.4681948665013));
#57195=CARTESIAN_POINT('Ctrl Pts',(-0.919327219170563,5.74369858870307,
53.7465641422317));
#57196=CARTESIAN_POINT('Ctrl Pts',(-5.3285991454729,2.33265238744289,54.0249334179618));
#57197=CARTESIAN_POINT('Ctrl Pts',(-4.84367074118554,-3.2208833826701,54.3033026936922));
#57198=CARTESIAN_POINT('Ctrl Pts',(0.0900619915185718,-5.81610908180557,
54.5816719694224));
#57199=CARTESIAN_POINT('Ctrl Pts',(4.94107477914329,-3.06936736815449,54.8600412451526));
#57200=CARTESIAN_POINT('Ctrl Pts',(5.25381978618318,2.49652031197179,55.138410520883));
#57201=CARTESIAN_POINT('Ctrl Pts',(0.741047648394848,5.76940936288854,55.4167797966132));
#57202=CARTESIAN_POINT('Ctrl Pts',(-4.45236034635004,3.74322365883036,55.6951490723435));
#57203=CARTESIAN_POINT('Ctrl Pts',(-5.55637394603631,-1.7210300943291,55.9735183480737));
#57204=CARTESIAN_POINT('Ctrl Pts',(-1.55698110414879,-5.60455581247088,
56.2518876238041));
#57205=CARTESIAN_POINT('Ctrl Pts',(3.87246440760804,-4.34042111154972,56.5302568995343));
#57206=CARTESIAN_POINT('Ctrl Pts',(5.74513710412806,0.910294275796876,56.8086261752646));
#57207=CARTESIAN_POINT('Ctrl Pts',(2.34102857791428,5.3249245263352,57.0869954509948));
#57208=CARTESIAN_POINT('Ctrl Pts',(-3.21326286263679,4.8487295025993,57.3653647267251));
#57209=CARTESIAN_POINT('Ctrl Pts',(-5.81624351112921,-0.0809162099021229,
57.6437340024553));
#57210=CARTESIAN_POINT('Ctrl Pts',(-3.0771332764778,-4.93624217523513,57.9221032781857));
#57211=CARTESIAN_POINT('Ctrl Pts',(2.4882557394928,-5.25773899967072,58.2004725539159));
#57212=CARTESIAN_POINT('Ctrl Pts',(5.76823695308387,-0.750118968468039,
58.4788418296462));
#57213=CARTESIAN_POINT('Ctrl Pts',(3.7502202441463,4.44646872632352,58.7572111053764));
#57214=CARTESIAN_POINT('Ctrl Pts',(-1.7122907225886,5.55907334859995,59.0355803811067));
#57215=CARTESIAN_POINT('Ctrl Pts',(-5.60210057374436,1.5657921878175,59.313949656837));
#57216=CARTESIAN_POINT('Ctrl Pts',(-4.34650508824432,-3.86563442809122,
59.5923189325673));
#57217=CARTESIAN_POINT('Ctrl Pts',(0.901259081565336,-5.74656141372159,
59.8706882082974));
#57218=CARTESIAN_POINT('Ctrl Pts',(5.32123674041329,-2.34939897979313,60.1490574840279));
#57219=CARTESIAN_POINT('Ctrl Pts',(4.85377627470227,3.20563439726283,60.4274267597579));
#57220=CARTESIAN_POINT('Ctrl Pts',(-0.0717702282064447,5.81636355879867,
60.7057960354884));
#57221=CARTESIAN_POINT('Ctrl Pts',(-4.93139736562627,3.08489157606423,60.9841653112185));
#57222=CARTESIAN_POINT('Ctrl Pts',(-5.26164521250164,-2.47998501437728,
61.2625345869489));
#57223=CARTESIAN_POINT('Ctrl Pts',(-0.75918843374404,-5.76705028032932,
61.5409038626791));
#57224=CARTESIAN_POINT('Ctrl Pts',(4.4405661116445,-3.75720755640298,61.8192731384095));
#57225=CARTESIAN_POINT('Ctrl Pts',(5.56175900540656,1.703547116917,62.0976424141395));
#57226=CARTESIAN_POINT('Ctrl Pts',(1.57459939979797,5.59963148286865,62.3760116898701));
#57227=CARTESIAN_POINT('Ctrl Pts',(-3.85879489013386,4.35257831746365,62.6543809656001));
#57228=CARTESIAN_POINT('Ctrl Pts',(-5.74797151396171,-0.89222165881688,
62.9327502413306));
#57229=CARTESIAN_POINT('Ctrl Pts',(-2.35776357238246,-5.31753579682578,
63.2111195170607));
#57230=CARTESIAN_POINT('Ctrl Pts',(3.19799800541104,-4.85881104501553,63.489488792791));
#57231=CARTESIAN_POINT('Ctrl Pts',(5.81646922451705,0.0626240690466223,
63.7678580685212));
#57232=CARTESIAN_POINT('Ctrl Pts',(3.09264224773008,4.92654036229607,64.0462273442516));
#57233=CARTESIAN_POINT('Ctrl Pts',(-2.47170815707546,5.26553841501739,64.3245966199818));
#57234=CARTESIAN_POINT('Ctrl Pts',(-5.76584934755931,0.768256021797297,
64.6029658957121));
#57235=CARTESIAN_POINT('Ctrl Pts',(-3.76418557832305,-4.43465251690848,
64.8813351714424));
#57236=CARTESIAN_POINT('Ctrl Pts',(1.69479929893489,-5.56443090981521,65.1597044471726));
#57237=CARTESIAN_POINT('Ctrl Pts',(5.59714854594884,-1.58340271831267,65.4380737229028));
#57238=CARTESIAN_POINT('Ctrl Pts',(4.3586407841906,3.85194581064795,65.7164429986333));
#57239=CARTESIAN_POINT('Ctrl Pts',(-0.883182029898331,5.74936740136187,
65.9948122743633));
#57240=CARTESIAN_POINT('Ctrl Pts',(-5.31382170472409,2.36612233499885,66.2731815500938));
#57241=CARTESIAN_POINT('Ctrl Pts',(-4.8638338010895,-3.19035370596371,66.5515508258239));
#57242=CARTESIAN_POINT('Ctrl Pts',(0.0534777550381669,-5.8165605080231,
66.8299201015543));
#57243=CARTESIAN_POINT('Ctrl Pts',(4.92167117725461,-3.10038527231038,67.1082893772844));
#57244=CARTESIAN_POINT('Ctrl Pts',(5.26941859759108,2.46342518805391,67.3866586530149));
#57245=CARTESIAN_POINT('Ctrl Pts',(0.777321710206332,5.76463415774316,67.665027928745));
#57246=CARTESIAN_POINT('Ctrl Pts',(-4.42872795673757,3.77115429265218,67.9433972044754));
#57247=CARTESIAN_POINT('Ctrl Pts',(-5.56708905521936,-1.68604729027233,
68.2217664802056));
#57248=CARTESIAN_POINT('Ctrl Pts',(-1.59220212159397,-5.59465176912459,
68.5001357559359));
#57249=CARTESIAN_POINT('Ctrl Pts',(3.84508720656895,-4.36469247343464,68.7785050316661));
#57250=CARTESIAN_POINT('Ctrl Pts',(5.75074907247032,0.874140217161407,69.0568743073964));
#57251=CARTESIAN_POINT('Ctrl Pts',(2.37447524697441,5.31009447329176,69.3352435831267));
#57252=CARTESIAN_POINT('Ctrl Pts',(-3.18270151782271,4.86884453050484,69.6136128588569));
#57253=CARTESIAN_POINT('Ctrl Pts',(-5.81663740909106,-0.0443313087968929,
69.8919821345872));
#57254=CARTESIAN_POINT('Ctrl Pts',(-3.10812063065928,-4.91678982254146,
70.1703514103174));
#57255=CARTESIAN_POINT('Ctrl Pts',(2.45513612779318,-5.2732857506286,70.4487206860478));
#57256=CARTESIAN_POINT('Ctrl Pts',(5.76340471388584,-0.786385476554853,
70.7270899617779));
#57257=CARTESIAN_POINT('Ctrl Pts',(3.77811368215897,4.42279244578133,71.0054592375083));
#57258=CARTESIAN_POINT('Ctrl Pts',(-1.67729111257008,5.56973343504611,71.2838285132385));
#57259=CARTESIAN_POINT('Ctrl Pts',(-5.5921411585695,1.60099758788418,71.5621977889689));
#57260=CARTESIAN_POINT('Ctrl Pts',(-4.3707333702321,-3.83821909485602,71.840567064699));
#57261=CARTESIAN_POINT('Ctrl Pts',(0.865096242963933,-5.75211652387075,
72.1189363404294));
#57262=CARTESIAN_POINT('Ctrl Pts',(5.30635411174501,-2.38282228765471,72.3973056161595));
#57263=CARTESIAN_POINT('Ctrl Pts',(4.87384322087152,3.17504145990924,72.67567489189));
#57264=CARTESIAN_POINT('Ctrl Pts',(-0.0351847529388852,5.81669992753095,
72.95404416762));
#57265=CARTESIAN_POINT('Ctrl Pts',(-4.91189631022696,3.11584830364957,73.2324134433506));
#57266=CARTESIAN_POINT('Ctrl Pts',(-5.27713986456742,-2.44684099678966,
73.5107827190805));
#57267=CARTESIAN_POINT('Ctrl Pts',(-0.795447298431173,-5.7621610190272,
73.7891519948111));
#57268=CARTESIAN_POINT('Ctrl Pts',(4.41684599871641,-3.78506372963529,74.0675212705412));
#57269=CARTESIAN_POINT('Ctrl Pts',(5.57236404275686,1.66853078747969,74.3458905462716));
#57270=CARTESIAN_POINT('Ctrl Pts',(1.60978909543459,5.58961672049141,74.6242598220017));
#57271=CARTESIAN_POINT('Ctrl Pts',(-3.83134149249159,4.37676345964574,74.9026290977321));
#57272=CARTESIAN_POINT('Ctrl Pts',(-5.75346975218196,-0.856050129668336,
75.1809983734624));
#57273=CARTESIAN_POINT('Ctrl Pts',(-2.39116343640037,-5.30260062933267,
75.4593676491925));
#57274=CARTESIAN_POINT('Ctrl Pts',(3.16737355116417,-4.87882985982939,75.7377369249229));
#57275=CARTESIAN_POINT('Ctrl Pts',(5.81674806318794,0.0260381100804274,
76.016106200653));
#57276=CARTESIAN_POINT('Ctrl Pts',(3.12356827217368,4.90699065241089,76.2944754763835));
#57277=CARTESIAN_POINT('Ctrl Pts',(-2.43853981555445,5.28098092987785,76.5728447521136));
#57278=CARTESIAN_POINT('Ctrl Pts',(-5.76090307624246,0.80450715342832,76.851214027844));
#57279=CARTESIAN_POINT('Ctrl Pts',(-3.79200441789593,-4.41088863024617,
77.1295833035741));
#57280=CARTESIAN_POINT('Ctrl Pts',(1.65976633666211,-5.5749808718471,77.4079525793045));
#57281=CARTESIAN_POINT('Ctrl Pts',(5.58707846113262,-1.61857662250689,77.6863218550347));
#57282=CARTESIAN_POINT('Ctrl Pts',(4.38278272676508,3.82445441648177,77.964691130765));
#57283=CARTESIAN_POINT('Ctrl Pts',(-0.847001899642621,5.75480875405768,
78.2430604064953));
#57284=CARTESIAN_POINT('Ctrl Pts',(-5.2988340353357,2.39949867258681,78.5214296822255));
#57285=CARTESIAN_POINT('Ctrl Pts',(-4.88380443504831,-3.15969781054777,
78.7997989579558));
#57286=CARTESIAN_POINT('Ctrl Pts',(0.0168914028385561,-5.81678181594319,
79.0781682336861));
#57287=CARTESIAN_POINT('Ctrl Pts',(4.90207286122337,-3.13128051714223,79.3565375094163));
#57288=CARTESIAN_POINT('Ctrl Pts',(5.28480893706208,2.43023260461352,79.6349067851467));
#57289=CARTESIAN_POINT('Ctrl Pts',(0.813565019144324,5.75963088864231,79.9132760608768));
#57290=CARTESIAN_POINT('Ctrl Pts',(-4.40492035510159,3.79893572977866,80.1916453366072));
#57291=CARTESIAN_POINT('Ctrl Pts',(-5.57758391584602,-1.65099778178922,
80.4700146123374));
#57292=CARTESIAN_POINT('Ctrl Pts',(-1.62736014737243,-5.58452638676924,
80.7483838880677));
#57293=CARTESIAN_POINT('Ctrl Pts',(3.81755788385611,-4.3887911567066,81.0267531637979));
#57294=CARTESIAN_POINT('Ctrl Pts',(5.75613352618714,0.837951575260477,81.3051224395282));
#57295=CARTESIAN_POINT('Ctrl Pts',(2.40782797560329,5.29505433906766,81.5834917152585));
#57296=CARTESIAN_POINT('Ctrl Pts',(-3.15201425703949,4.88876693422767,81.8618609909888));
#57297=CARTESIAN_POINT('Ctrl Pts',(-5.81680118571323,-0.00774465382969917,
82.1402302667191));
#57298=CARTESIAN_POINT('Ctrl Pts',(-3.13898501948552,-4.89714294882462,
82.4185995424493));
#57299=CARTESIAN_POINT('Ctrl Pts',(2.42191938450794,-5.28862387665468,82.6969688181796));
#57300=CARTESIAN_POINT('Ctrl Pts',(5.75834445937218,-0.822620873182145,
82.9753380939098));
#57301=CARTESIAN_POINT('Ctrl Pts',(3.805857648145,4.39894118803992,83.2537073696402));
#57302=CARTESIAN_POINT('Ctrl Pts',(-1.64222514454274,5.5801731683174,83.5320766453704));
#57303=CARTESIAN_POINT('Ctrl Pts',(-5.58196050371171,1.63613964831234,83.8104459211006));
#57304=CARTESIAN_POINT('Ctrl Pts',(-4.39478873461335,-3.81065191166719,
84.0888151968309));
#57305=CARTESIAN_POINT('Ctrl Pts',(0.828899178899882,-5.75744406529468,
84.3671844725612));
#57306=CARTESIAN_POINT('Ctrl Pts',(5.29126154987468,-2.41615132485442,84.6455537482915));
#57307=CARTESIAN_POINT('Ctrl Pts',(4.89371734509677,3.14432290963829,84.9239230240216));
#57308=CARTESIAN_POINT('Ctrl Pts',(0.00140211432928147,5.81680617245002,
85.2022922997521));
#57309=CARTESIAN_POINT('Ctrl Pts',(-4.8922009274045,3.14668176015314,85.4806615754822));
#57310=CARTESIAN_POINT('Ctrl Pts',(-5.29242573922271,-2.41360017579359,
85.7590308512126));
#57311=CARTESIAN_POINT('Ctrl Pts',(-0.831674693149312,-5.75704379161321,
86.0374001269427));
#57312=CARTESIAN_POINT('Ctrl Pts',(4.39295114384581,-3.81277015587892,86.3157694026731));
#57313=CARTESIAN_POINT('Ctrl Pts',(5.58274862285872,1.6334484466144,86.5941386784033));
#57314=CARTESIAN_POINT('Ctrl Pts',(1.64491510361793,5.5793808183048,86.8725079541337));
#57315=CARTESIAN_POINT('Ctrl Pts',(-3.80373651699164,4.40077544565517,87.1508772298638));
#57316=CARTESIAN_POINT('Ctrl Pts',(-5.75874036813954,-0.819844732944801,
87.4292465055942));
#57317=CARTESIAN_POINT('Ctrl Pts',(-2.42446869975928,-5.28745567713485,
87.7076157813245));
#57318=CARTESIAN_POINT('Ctrl Pts',(3.1366237873624,-4.89865565541509,87.9859850570546));
#57319=CARTESIAN_POINT('Ctrl Pts',(5.81679677614137,-0.0105488790210397,
88.2643543327851));
#57320=CARTESIAN_POINT('Ctrl Pts',(3.15437072011317,4.88724680918305,88.5427236085151));
#57321=CARTESIAN_POINT('Ctrl Pts',(-2.40527499904105,5.29621451536529,88.8210928842456));
#57322=CARTESIAN_POINT('Ctrl Pts',(-5.75572888858148,0.840726456659049,
89.0994621599757));
#57323=CARTESIAN_POINT('Ctrl Pts',(-3.81967323588822,-4.38695023733077,
89.3778314357061));
#57324=CARTESIAN_POINT('Ctrl Pts',(1.62466770970617,-5.58531027310169,89.6562007114362));
#57325=CARTESIAN_POINT('Ctrl Pts',(5.57678733692693,-1.65368649159043,89.9345699871666));
#57326=CARTESIAN_POINT('Ctrl Pts',(4.40675127502924,3.79681171692856,90.2129392628969));
#57327=CARTESIAN_POINT('Ctrl Pts',(-0.810788259783799,5.76002243151662,
90.4913085386271));
#57328=CARTESIAN_POINT('Ctrl Pts',(-5.28363673025889,2.43278007975165,90.7696778143574));
#57329=CARTESIAN_POINT('Ctrl Pts',(-4.90358185297166,-3.12891690924898,
91.0480470900876));
#57330=CARTESIAN_POINT('Ctrl Pts',(-0.0196956176291403,-5.81677299681053,
91.3264163658181));
#57331=CARTESIAN_POINT('Ctrl Pts',(4.88228060641031,-3.16205188035358,91.6047856415481));
#57332=CARTESIAN_POINT('Ctrl Pts',(5.29999019571399,2.3969438748358,91.8831549172785));
#57333=CARTESIAN_POINT('Ctrl Pts',(0.849776141329328,5.75439975352813,92.1615241930086));
#57334=CARTESIAN_POINT('Ctrl Pts',(-4.38093848333281,3.82656687110411,92.4398934687391));
#57335=CARTESIAN_POINT('Ctrl Pts',(-5.5878581127124,-1.61588295552992,92.7182627444692));
#57336=CARTESIAN_POINT('Ctrl Pts',(-1.66245379054078,-5.57418006599121,
92.9966320201996));
#57337=CARTESIAN_POINT('Ctrl Pts',(3.78987752860088,-4.41271620795891,93.2750012959297));
#57338=CARTESIAN_POINT('Ctrl Pts',(5.76129025225566,0.801729781810469,93.5533705716601));
#57339=CARTESIAN_POINT('Ctrl Pts',(2.44108544428034,5.27980471868994,93.8317398473903));
#57340=CARTESIAN_POINT('Ctrl Pts',(-3.12120229435501,4.90849592558558,94.1101091231206));
#57341=CARTESIAN_POINT('Ctrl Pts',(-5.81673483451611,0.0288423075363337,
94.3884783988509));
#57342=CARTESIAN_POINT('Ctrl Pts',(-3.16972522188136,-4.87730233136589,
94.6668476745812));
#57343=CARTESIAN_POINT('Ctrl Pts',(2.38860682377799,-5.30375277093297,94.9452169503114));
#57344=CARTESIAN_POINT('Ctrl Pts',(5.75305638973991,-0.858823724782912,
95.2235862260417));
#57345=CARTESIAN_POINT('Ctrl Pts',(3.83345104448049,4.37491589671717,95.5019555017719));
#57346=CARTESIAN_POINT('Ctrl Pts',(-1.60709420580738,5.59039213539071,95.7803247775023));
#57347=CARTESIAN_POINT('Ctrl Pts',(-5.57155901194447,1.67121697879068,96.0586940532323));
#57348=CARTESIAN_POINT('Ctrl Pts',(-4.41867022969501,-3.78293396915468,
96.3370633289629));
#57349=CARTESIAN_POINT('Ctrl Pts',(0.792669321423524,-5.76254382722172,
96.6154326046929));
#57350=CARTESIAN_POINT('Ctrl Pts',(5.27595965190304,-2.44938477280896,96.8938018804233));
#57351=CARTESIAN_POINT('Ctrl Pts',(4.91339786110621,3.11347996175579,97.1721711561536));
#57352=CARTESIAN_POINT('Ctrl Pts',(0.0379889261259919,5.81668228935273,
97.4505404318838));
#57353=CARTESIAN_POINT('Ctrl Pts',(-4.87231199635946,3.17739072572275,97.7289097076141));
#57354=CARTESIAN_POINT('Ctrl Pts',(-5.30750223171846,-2.38026386648219,
98.0072789833443));
#57355=CARTESIAN_POINT('Ctrl Pts',(-0.867869184648594,-5.75169880053843,
98.2856482590747));
#57356=CARTESIAN_POINT('Ctrl Pts',(4.36888249237581,-3.84032573899534,98.5640175348048));
#57357=CARTESIAN_POINT('Ctrl Pts',(5.59291233487078,1.5983014822703,98.8423868105353));
#57358=CARTESIAN_POINT('Ctrl Pts',(1.67997603467162,5.56892418126753,99.1207560862653));
#57359=CARTESIAN_POINT('Ctrl Pts',(-3.77598105575879,4.42461332551543,99.3991253619959));
#57360=CARTESIAN_POINT('Ctrl Pts',(-5.76378315331532,-0.783606901026482,
99.6774946377258));
#57361=CARTESIAN_POINT('Ctrl Pts',(-2.4576780448157,-5.27210153940609,99.9558639134564));
#57362=CARTESIAN_POINT('Ctrl Pts',(3.10574993054631,-4.91828764741234,100.234233189186));
#57363=CARTESIAN_POINT('Ctrl Pts',(5.81661536145012,-0.0471354507815979,
100.512602464917));
#57364=CARTESIAN_POINT('Ctrl Pts',(3.18504837292365,4.8673096137306,100.790971740647));
#57365=CARTESIAN_POINT('Ctrl Pts',(-2.3719150235782,5.3112385687993,101.069341016377));
#57366=CARTESIAN_POINT('Ctrl Pts',(-5.75032698928046,0.876912498559519,
101.347710292108));
#57367=CARTESIAN_POINT('Ctrl Pts',(-3.8471909376497,-4.36283828522717,101.626079567838));
#57368=CARTESIAN_POINT('Ctrl Pts',(1.58950480666019,-5.5954187049212,101.904448843568));
#57369=CARTESIAN_POINT('Ctrl Pts',(5.56627558047574,-1.68873093652502,102.182818119298));
#57370=CARTESIAN_POINT('Ctrl Pts',(4.43054548072448,3.76901880560565,102.461187395029));
#57371=CARTESIAN_POINT('Ctrl Pts',(-0.774542543027661,5.76500822747185,
102.739556670759));
#57372=CARTESIAN_POINT('Ctrl Pts',(-5.26823039073879,2.46596523979438,103.017925946489));
#57373=CARTESIAN_POINT('Ctrl Pts',(-4.92316527241329,-3.09801221984049,
103.296295222219));
#57374=CARTESIAN_POINT('Ctrl Pts',(-0.0562818588867149,-5.81653405097377,
103.57466449795));
#57375=CARTESIAN_POINT('Ctrl Pts',(4.86229519584828,-3.19269814454921,103.85303377368));
#57376=CARTESIAN_POINT('Ctrl Pts',(5.31496177293694,2.36356031570952,104.13140304941));
#57377=CARTESIAN_POINT('Ctrl Pts',(0.885953644154715,5.74894095935824,104.409772325141));
#57378=CARTESIAN_POINT('Ctrl Pts',(-4.35678329021663,3.85404662346816,104.688141600871));
#57379=CARTESIAN_POINT('Ctrl Pts',(-5.59791123934433,-1.58070420072815,
104.966510876601));
#57380=CARTESIAN_POINT('Ctrl Pts',(-1.69748166270338,-5.56361321611808,
105.244880152331));
#57381=CARTESIAN_POINT('Ctrl Pts',(3.76204723591069,-4.43646668065416,105.523249428062));
#57382=CARTESIAN_POINT('Ctrl Pts',(5.76621904666208,0.765476269840323,105.801618703792));
#57383=CARTESIAN_POINT('Ctrl Pts',(2.47424633725344,5.26434621547303,106.079987979522));
#57384=CARTESIAN_POINT('Ctrl Pts',(-3.0902668487708,4.92803072404851,106.358357255252));
#57385=CARTESIAN_POINT('Ctrl Pts',(-5.81643835812494,0.0654281278253369,
106.636726530983));
#57386=CARTESIAN_POINT('Ctrl Pts',(-3.20034002168381,-4.85726875511187,
106.915095806713));
#57387=CARTESIAN_POINT('Ctrl Pts',(2.35519976353486,-5.31867183492482,107.193465082443));
#57388=CARTESIAN_POINT('Ctrl Pts',(5.74754071419879,-0.894992599078435,
107.471834358174));
#57389=CARTESIAN_POINT('Ctrl Pts',(3.860892779499,4.35071752231632,107.750203633904));
#57390=CARTESIAN_POINT('Ctrl Pts',(-1.57189968623559,5.60038993197703,108.028572909634));
#57391=CARTESIAN_POINT('Ctrl Pts',(-5.56093709477762,1.7062281915686,108.306942185364));
#57392=CARTESIAN_POINT('Ctrl Pts',(-4.44237691066319,-3.75506636391214,
108.585311461095));
#57393=CARTESIAN_POINT('Ctrl Pts',(0.756408103882341,-5.76741560789225,
108.863680736825));
#57394=CARTESIAN_POINT('Ctrl Pts',(5.26044902321342,-2.48252131671617,109.142050012555));
#57395=CARTESIAN_POINT('Ctrl Pts',(4.93288399028696,3.08251383648926,109.420419288285));
#57396=CARTESIAN_POINT('Ctrl Pts',(0.0745742349817975,5.81632828314004,
109.698788564016));
#57397=CARTESIAN_POINT('Ctrl Pts',(-4.85223030394992,3.20797398543193,109.977157839746));
#57398=CARTESIAN_POINT('Ctrl Pts',(-5.32236874558934,-2.34683338772717,
110.255527115476));
#57399=CARTESIAN_POINT('Ctrl Pts',(-0.904029340980253,-5.74612625726445,
110.533896391206));
#57400=CARTESIAN_POINT('Ctrl Pts',(4.34464099652475,-3.86772938881385,110.812265666937));
#57401=CARTESIAN_POINT('Ctrl Pts',(5.60285477669039,1.56309128495284,111.090634942667));
#57402=CARTESIAN_POINT('Ctrl Pts',(1.71497050149349,5.55824722307171,111.369004218397));
#57403=CARTESIAN_POINT('Ctrl Pts',(-3.74807620687148,4.44827615613746,111.647373494127));
#57404=CARTESIAN_POINT('Ctrl Pts',(-5.7685979082034,-0.747338067576144,
111.925742769858));
#57405=CARTESIAN_POINT('Ctrl Pts',(-2.49079015772174,-5.25653882359623,
112.204112045588));
#57406=CARTESIAN_POINT('Ctrl Pts',(3.07475320216653,-4.9377250591284,112.482481321318));
#57407=CARTESIAN_POINT('Ctrl Pts',(5.81620382629126,-0.0837201577406925,
112.760850597049));
#57408=CARTESIAN_POINT('Ctrl Pts',(3.21560001691721,4.84717985482067,113.039219872779));
#57409=CARTESIAN_POINT('Ctrl Pts',(-2.3384612089734,5.3260524957894,113.317589148509));
#57410=CARTESIAN_POINT('Ctrl Pts',(-5.7446975920529,0.913063847515321,113.595958424239));
#57411=CARTESIAN_POINT('Ctrl Pts',(-3.87455643450797,-4.33855372786718,
113.87432769997));
#57412=CARTESIAN_POINT('Ctrl Pts',(1.55427901866009,-5.60530576738952,114.1526969757));
#57413=CARTESIAN_POINT('Ctrl Pts',(5.55554360765141,-1.72370857086153,114.43106625143));
#57414=CARTESIAN_POINT('Ctrl Pts',(4.45416440249025,3.74107678207312,114.70943552716));
#57415=CARTESIAN_POINT('Ctrl Pts',(-0.738266183349346,5.76976594467228,
114.987804802891));
#57416=CARTESIAN_POINT('Ctrl Pts',(-5.2526156262901,2.49905283982359,115.266174078621));
#57417=CARTESIAN_POINT('Ctrl Pts',(-4.94255391860234,-3.06698496499194,
115.544543354351));
#57418=CARTESIAN_POINT('Ctrl Pts',(-0.0928658734872262,-5.81606498788651,
115.822912630082));
#57419=CARTESIAN_POINT('Ctrl Pts',(4.84211742021259,-3.22321809728275,116.101281905812));
#57420=CARTESIAN_POINT('Ctrl Pts',(5.329723076416,2.33008324797548,116.379651181542));
#57421=CARTESIAN_POINT('Ctrl Pts',(0.922096096344309,5.74325472209657,116.658020457272));
#57422=CARTESIAN_POINT('Ctrl Pts',(-4.33245573139553,3.88137389970045,116.936389733003));
#57423=CARTESIAN_POINT('Ctrl Pts',(-5.60774289801398,-1.54546290914759,
117.214759008733));
#57424=CARTESIAN_POINT('Ctrl Pts',(-1.73244237806593,-5.5528262552018,117.493128284463));
#57425=CARTESIAN_POINT('Ctrl Pts',(3.7340681068242,-4.46004163516174,117.771497560194));
#57426=CARTESIAN_POINT('Ctrl Pts',(5.77091971441071,0.72919247363337,118.049866835924));
#57427=CARTESIAN_POINT('Ctrl Pts',(2.50730934259094,5.24867944099596,118.328236111654));
#57428=CARTESIAN_POINT('Ctrl Pts',(-3.05920914417388,4.94737055676852,118.606605387384));
#57429=CARTESIAN_POINT('Ctrl Pts',(-5.81591176826883,0.102011359607224,
118.884974663115));
#57430=CARTESIAN_POINT('Ctrl Pts',(-3.23082820769206,-4.83704301264321,
119.163343938845));
#57431=CARTESIAN_POINT('Ctrl Pts',(2.32169952544947,-5.33338047839311,119.441713214575));
#57432=CARTESIAN_POINT('Ctrl Pts',(5.74179765096292,-0.931126065133631,
119.720082490305));
#57433=CARTESIAN_POINT('Ctrl Pts',(3.88818176753445,4.3263470221884,119.998451766036));
#57434=CARTESIAN_POINT('Ctrl Pts',(-1.53664297821521,5.61016616253672,120.276821041766));
#57435=CARTESIAN_POINT('Ctrl Pts',(-5.55009517244032,1.74117190151289,120.555190317496));
#57436=CARTESIAN_POINT('Ctrl Pts',(-4.46590783962299,-3.72705019845838,
120.833559593227));
#57437=CARTESIAN_POINT('Ctrl Pts',(0.720116960871199,-5.77205921455916,
121.111928868956));
#57438=CARTESIAN_POINT('Ctrl Pts',(5.24473027743382,-2.51555964562078,121.390298144687));
#57439=CARTESIAN_POINT('Ctrl Pts',(4.95217496174117,3.05142575896264,121.668667420417));
#57440=CARTESIAN_POINT('Ctrl Pts',(0.111156593441196,5.81574416777347,121.947036696148));
#57441=CARTESIAN_POINT('Ctrl Pts',(-4.83195664457435,3.23843032941005,122.225405971878));
#57442=CARTESIAN_POINT('Ctrl Pts',(-5.33702469283866,-2.31331006228149,
122.503775247608));
#57443=CARTESIAN_POINT('Ctrl Pts',(-0.940153731250069,-5.74032638196031,
122.782144523338));
#57444=CARTESIAN_POINT('Ctrl Pts',(4.3202276147748,-3.89498002173257,123.060513799069));
#57445=CARTESIAN_POINT('Ctrl Pts',(5.61257555605349,1.52781924872262,123.338883074799));
#57446=CARTESIAN_POINT('Ctrl Pts',(1.74989711756287,5.54735036413612,123.617252350529));
#57447=CARTESIAN_POINT('Ctrl Pts',(-3.72002307044978,4.47176300511463,123.895621626259));
#57448=CARTESIAN_POINT('Ctrl Pts',(-5.77318444962431,-0.711039674576537,
124.17399090199));
#57449=CARTESIAN_POINT('Ctrl Pts',(-2.52380371468285,-5.24076813201426,
124.45236017772));
#57450=CARTESIAN_POINT('Ctrl Pts',(3.04363480249081,-4.95696714685634,124.73072945345));
#57451=CARTESIAN_POINT('Ctrl Pts',(5.8155622361216,-0.120301504763635,125.00909872918));
#57452=CARTESIAN_POINT('Ctrl Pts',(3.24602435053818,4.82685823868056,125.287468004911));
#57453=CARTESIAN_POINT('Ctrl Pts',(-2.30491470342209,5.34065588049586,125.565837280641));
#57454=CARTESIAN_POINT('Ctrl Pts',(-5.7388412506611,0.94917875184084,125.844206556371));
#57455=CARTESIAN_POINT('Ctrl Pts',(-3.90176801872524,-4.31409691905904,
126.122575832102));
#57456=CARTESIAN_POINT('Ctrl Pts',(1.51899055903744,-5.61497221539792,126.400945107832));
#57457=CARTESIAN_POINT('Ctrl Pts',(5.54459407167148,-1.75861584681939,126.679314383562));
#57458=CARTESIAN_POINT('Ctrl Pts',(4.4776028977884,3.71298266576747,126.957683659292));
#57459=CARTESIAN_POINT('Ctrl Pts',(-0.701952670164813,5.77430311013206,
127.236052935023));
#57460=CARTESIAN_POINT('Ctrl Pts',(-5.23680805790664,2.5320270028608,127.514422210753));
#57461=CARTESIAN_POINT('Ctrl Pts',(-4.96171869531289,-3.03580886496632,
127.792791486483));
#57462=CARTESIAN_POINT('Ctrl Pts',(-0.129499705332998,-5.81541776548578,
128.071160762213));
#57463=CARTESIAN_POINT('Ctrl Pts',(4.82184908053961,-3.25351245829232,128.349530037944));
#57464=CARTESIAN_POINT('Ctrl Pts',(5.34408280538262,2.29632880892462,128.627899313674));
#57465=CARTESIAN_POINT('Ctrl Pts',(0.958562204898396,5.73769098457033,128.906268589404));
#57466=CARTESIAN_POINT('Ctrl Pts',(-4.30863698407822,3.9078868970393,129.184637865134));
#57467=CARTESIAN_POINT('Ctrl Pts',(-5.61606665580893,-1.50890976540128,
129.463007140865));
#57468=CARTESIAN_POINT('Ctrl Pts',(-1.7697764369988,-5.54420682019011,129.741376416595));
#57469=CARTESIAN_POINT('Ctrl Pts',(3.71066272797163,-4.47872295434702,130.019745692325));
#57470=CARTESIAN_POINT('Ctrl Pts',(5.42310758321798,-0.17792219993292,130.251720088767));
#57471=CARTESIAN_POINT('Ctrl Pts',(4.16455399126958,2.97569362702242,130.437299605921));
#57472=CARTESIAN_POINT('Ctrl Pts',(2.88487055828799,4.0666809675818,130.530089364497));
#57473=CARTESIAN_POINT('Ctrl Pts',(2.14786219406649,4.42446279878132,130.576484243786));
#57474=CARTESIAN_POINT('Ctrl Pts',(-5.91448192755925,-0.0049507822674949,
128.813375192205));
#57475=CARTESIAN_POINT('Ctrl Pts',(-5.90159134039941,1.44883428144936,128.744968001919));
#57476=CARTESIAN_POINT('Ctrl Pts',(-5.3612661550492,2.91089247196232,128.676560811634));
#57477=CARTESIAN_POINT('Ctrl Pts',(-4.38942716623899,3.98206003052305,128.608153621349));
#57478=CARTESIAN_POINT('Ctrl Pts',(-3.07119285825066,5.43502687128293,128.515363862772));
#57479=CARTESIAN_POINT('Ctrl Pts',(-0.959011980812732,6.16879012277187,
128.422574104195));
#57480=CARTESIAN_POINT('Ctrl Pts',(0.976389493773268,5.84566752435974,128.329784345618));
#57481=CARTESIAN_POINT('Ctrl Pts',(2.91179096835905,5.52254492594765,128.236994587042));
#57482=CARTESIAN_POINT('Ctrl Pts',(4.67041304009307,4.14253647763474,128.144204828465));
#57483=CARTESIAN_POINT('Ctrl Pts',(5.44501452847686,2.33977116576748,128.051415069888));
#57484=CARTESIAN_POINT('Ctrl Pts',(6.21961601686079,0.537005853899908,127.958625311311));
#57485=CARTESIAN_POINT('Ctrl Pts',(6.01019692189429,-1.68851632152195,127.865835552735));
#57486=CARTESIAN_POINT('Ctrl Pts',(4.91272596100818,-3.31494769257717,127.773045794158));
#57487=CARTESIAN_POINT('Ctrl Pts',(3.81525500012219,-4.94137906363219,127.680256035581));
#57488=CARTESIAN_POINT('Ctrl Pts',(1.8297321733167,-5.96871963032048,127.587466277004));
#57489=CARTESIAN_POINT('Ctrl Pts',(-0.131904744888432,-5.92506935716104,
127.494676518428));
#57490=CARTESIAN_POINT('Ctrl Pts',(-2.09354166309357,-5.88141908400161,
127.401886759851));
#57491=CARTESIAN_POINT('Ctrl Pts',(-4.03129267269846,-4.76677797099448,
127.309097001274));
#57492=CARTESIAN_POINT('Ctrl Pts',(-5.05532448262752,-3.09308835127519,
127.216307242697));
#57493=CARTESIAN_POINT('Ctrl Pts',(-5.6179127354129,-2.17358750205046,127.165329892533));
#57494=CARTESIAN_POINT('Ctrl Pts',(-5.90471818937535,-1.08535214236168,
127.114352542369));
#57495=CARTESIAN_POINT('Ctrl Pts',(-5.90733548964813,0.0015994485885984,
127.063375192205));
#57496=CARTESIAN_POINT('Origin',(0.,0.,-10.));
#57497=CARTESIAN_POINT('Origin',(-9.00000000000001,-15.5884572681199,169.));
#57498=CARTESIAN_POINT('',(-12.,-15.5884572681199,174.));
#57499=CARTESIAN_POINT('Origin',(-9.00000000000001,-15.5884572681199,174.));
#57500=CARTESIAN_POINT('',(-12.,-15.5884572681199,164.));
#57501=CARTESIAN_POINT('',(-12.,-15.5884572681199,169.));
#57502=CARTESIAN_POINT('Origin',(-9.00000000000001,-15.5884572681199,164.));
#57503=CARTESIAN_POINT('Origin',(-9.,15.5884572681199,169.));
#57504=CARTESIAN_POINT('',(-12.,15.5884572681199,174.));
#57505=CARTESIAN_POINT('Origin',(-9.,15.5884572681199,174.));
#57506=CARTESIAN_POINT('',(-12.,15.5884572681199,164.));
#57507=CARTESIAN_POINT('',(-12.,15.5884572681199,169.));
#57508=CARTESIAN_POINT('Origin',(-9.,15.5884572681199,164.));
#57509=CARTESIAN_POINT('Origin',(18.,0.,169.));
#57510=CARTESIAN_POINT('',(15.,3.67394039744206E-16,174.));
#57511=CARTESIAN_POINT('Origin',(18.,0.,174.));
#57512=CARTESIAN_POINT('',(15.,3.67394039744206E-16,164.));
#57513=CARTESIAN_POINT('',(15.,3.67394039744206E-16,169.));
#57514=CARTESIAN_POINT('Origin',(18.,0.,164.));
#57515=CARTESIAN_POINT('Origin',(9.,15.5884572681199,169.));
#57516=CARTESIAN_POINT('',(6.,15.5884572681199,174.));
#57517=CARTESIAN_POINT('Origin',(9.,15.5884572681199,174.));
#57518=CARTESIAN_POINT('',(6.,15.5884572681199,164.));
#57519=CARTESIAN_POINT('',(6.,15.5884572681199,169.));
#57520=CARTESIAN_POINT('Origin',(9.,15.5884572681199,164.));
#57521=CARTESIAN_POINT('Origin',(-18.,2.20436423846524E-15,169.));
#57522=CARTESIAN_POINT('',(-21.,2.57175827820944E-15,174.));
#57523=CARTESIAN_POINT('Origin',(-18.,2.20436423846524E-15,174.));
#57524=CARTESIAN_POINT('',(-21.,2.57175827820944E-15,164.));
#57525=CARTESIAN_POINT('',(-21.,2.57175827820944E-15,169.));
#57526=CARTESIAN_POINT('Origin',(-18.,2.20436423846524E-15,164.));
#57527=CARTESIAN_POINT('Origin',(9.,-15.5884572681199,169.));
#57528=CARTESIAN_POINT('',(6.,-15.5884572681199,174.));
#57529=CARTESIAN_POINT('Origin',(9.,-15.5884572681199,174.));
#57530=CARTESIAN_POINT('',(6.,-15.5884572681199,164.));
#57531=CARTESIAN_POINT('',(6.,-15.5884572681199,169.));
#57532=CARTESIAN_POINT('Origin',(9.,-15.5884572681199,164.));
#57533=CARTESIAN_POINT('Origin',(0.,0.,164.));
#57534=CARTESIAN_POINT('',(-25.,-3.06161699786838E-15,164.));
#57535=CARTESIAN_POINT('Origin',(0.,0.,164.));
#57536=CARTESIAN_POINT('',(-12.,-1.46957615897682E-15,164.));
#57537=CARTESIAN_POINT('Origin',(0.,0.,164.));
#57538=CARTESIAN_POINT('Origin',(0.,0.,164.));
#57539=CARTESIAN_POINT('',(-25.,-3.06161699786838E-15,174.));
#57540=CARTESIAN_POINT('Origin',(0.,0.,174.));
#57541=CARTESIAN_POINT('',(-25.,-3.06161699786838E-15,164.));
#57542=CARTESIAN_POINT('Origin',(0.,0.,174.));
#57543=CARTESIAN_POINT('Origin',(0.,0.,162.));
#57544=CARTESIAN_POINT('',(-12.,-1.46957615897682E-15,162.));
#57545=CARTESIAN_POINT('Origin',(0.,0.,162.));
#57546=CARTESIAN_POINT('Origin',(0.,0.,162.));
#57547=CARTESIAN_POINT('',(-12.,-1.46957615897682E-15,162.));
#63867=UNCERTAINTY_MEASURE_WITH_UNIT(LENGTH_MEASURE(0.01),#63899,
'DISTANCE_ACCURACY_VALUE',
'Maximum model space distance between geometric entities at asserted c
onnectivities');
#63878=UNCERTAINTY_MEASURE_WITH_UNIT(LENGTH_MEASURE(0.01),#63899,
'DISTANCE_ACCURACY_VALUE',
'Maximum model space distance between geometric entities at asserted c
onnectivities');
#63887=(
GEOMETRIC_REPRESENTATION_CONTEXT(3)
GLOBAL_UNCERTAINTY_ASSIGNED_CONTEXT((#63867))
GLOBAL_UNIT_ASSIGNED_CONTEXT((#63899,#63901,#63902))
REPRESENTATION_CONTEXT('','3D')
);
#63898=(
GEOMETRIC_REPRESENTATION_CONTEXT(3)
GLOBAL_UNCERTAINTY_ASSIGNED_CONTEXT((#63878))
GLOBAL_UNIT_ASSIGNED_CONTEXT((#63899,#63901,#63902))
REPRESENTATION_CONTEXT('','3D')
);
#63899=(
LENGTH_UNIT()
NAMED_UNIT(*)
SI_UNIT(.MILLI.,.METRE.)
);
#63901=(
NAMED_UNIT(*)
PLANE_ANGLE_UNIT()
SI_UNIT($,.RADIAN.)
);
#63902=(
NAMED_UNIT(*)
SI_UNIT($,.STERADIAN.)
SOLID_ANGLE_UNIT()
);
#63911=SHAPE_DEFINITION_REPRESENTATION(#63930,#64002);
#63930=PRODUCT_DEFINITION_SHAPE('',$,#64022);
#64002=SHAPE_REPRESENTATION('',(#16304),#63887);
#64013=PRODUCT_DEFINITION_CONTEXT('part definition',#64072,'design');
#64022=PRODUCT_DEFINITION('Feed screw','Feed screw',#64041,#64013);
#64041=PRODUCT_DEFINITION_FORMATION('',$,#64082);
#64072=APPLICATION_CONTEXT(
'Core Data for Automotive Mechanical Design Process');
#64073=PRODUCT_CONTEXT('part definition',#64072,'mechanical');
#64082=PRODUCT('Feed screw','Feed screw','Feed screw',(#64073));
#64098=PRESENTATION_STYLE_ASSIGNMENT((#64111));
#64111=SURFACE_STYLE_USAGE(.BOTH.,#64124);
#64124=SURFACE_SIDE_STYLE('',(#64137));
#64137=SURFACE_STYLE_FILL_AREA(#64150);
#64150=FILL_AREA_STYLE('Gray',(#64163));
#64163=FILL_AREA_STYLE_COLOUR('Gray',#64176);
#64176=COLOUR_RGB('Gray',0.407843137254902,0.447058823529412,0.498039215686275);
ENDSEC;
END-ISO-10303-21;
